ISO-10303-21;
HEADER;
FILE_DESCRIPTION (('STEP AP214'),
    '1' );
FILE_NAME ('Injection Molded Chain Links 15.step',
    '2026-10-08T22:59:04',
    ( '' ),
    ( '' ),
    'SwSTEP 2.0',
    'SolidWorks 2020',
    '' );
FILE_SCHEMA (( 'AUTOMOTIVE_DESIGN' ));
ENDSEC;

DATA;
#11=ORIENTED_EDGE ( 'NONE', *, *, #97972, .T. ) ;
#23=EDGE_CURVE ( 'NONE', #151382, #73251, #20149, .T. ) ;
#30=EDGE_CURVE ( 'NONE', #21530, #216178, #199211, .T. ) ;
#66=LINE ( 'NONE', #97860, #134130 ) ;
#75=CARTESIAN_POINT ( 'NONE',  ( 20.94999999999999574, 65.57661458509869590, -62.03105556065429482 ) ) ;
#93=EDGE_LOOP ( 'NONE', ( #41790, #120721, #253364, #8024, #101724, #76712, #208119, #163090, #81602, #93473, #199890, #120447, #37635, #170547, #25122, #143467, #230838, #110010, #37319, #108527, #200762, #188074, #74749, #27804, #95098, #214920, #223956 ) ) ;
#97=ORIENTED_EDGE ( 'NONE', *, *, #227198, .T. ) ;
#98=ADVANCED_FACE ( 'NONE', ( #186389 ), #170715, .F. ) ;
#124=ORIENTED_EDGE ( 'NONE', *, *, #248251, .T. ) ;
#137=ORIENTED_EDGE ( 'NONE', *, *, #203695, .F. ) ;
#148=ORIENTED_EDGE ( 'NONE', *, *, #102799, .T. ) ;
#169=VECTOR ( 'NONE', #156157, 1000.000000000000000 ) ;
#172=AXIS2_PLACEMENT_3D ( 'NONE', #68198, #90308, #107312 ) ;
#200=VERTEX_POINT ( 'NONE', #187678 ) ;
#204=DIRECTION ( 'NONE',  ( -1.000000000000000000, -0.000000000000000000, -0.000000000000000000 ) ) ;
#206=DIRECTION ( 'NONE',  ( 2.694716079187273439E-16, 1.000000000000000000, 6.467318590049456648E-15 ) ) ;
#266=AXIS2_PLACEMENT_3D ( 'NONE', #27213, #123720, #224080 ) ;
#276=CARTESIAN_POINT ( 'NONE',  ( 23.25000000000000000, 85.60000000001159037, -59.62913836187181005 ) ) ;
#290=DIRECTION ( 'NONE',  ( 1.000000000000000000, 0.000000000000000000, 0.000000000000000000 ) ) ;
#311=CARTESIAN_POINT ( 'NONE',  ( 23.14999999999998437, 76.00000000001165290, -69.52310748452431710 ) ) ;
#327=DIRECTION ( 'NONE',  ( -1.000000000000000000, -0.000000000000000000, -0.000000000000000000 ) ) ;
#335=EDGE_CURVE ( 'NONE', #34147, #83134, #97503, .T. ) ;
#338=CIRCLE ( 'NONE', #33524, 0.5000000000000004441 ) ;
#346=DIRECTION ( 'NONE',  ( 0.000000000000000000, -7.272083257015735086E-15, 1.000000000000000000 ) ) ;
#368=CARTESIAN_POINT ( 'NONE',  ( -23.15000000000000213, 71.75000000001151079, -48.27310748452435263 ) ) ;
#382=AXIS2_PLACEMENT_3D ( 'NONE', #149587, #227805, #71331 ) ;
#452=DIRECTION ( 'NONE',  ( 1.000000000000000000, 0.000000000000000000, 0.000000000000000000 ) ) ;
#471=ADVANCED_FACE ( 'NONE', ( #161377 ), #240905, .T. ) ;
#496=FACE_OUTER_BOUND ( 'NONE', #17360, .T. ) ;
#498=EDGE_CURVE ( 'NONE', #61807, #44661, #190075, .T. ) ;
#546=DIRECTION ( 'NONE',  ( 1.000000000000000000, 0.000000000000000000, 0.000000000000000000 ) ) ;
#549=DIRECTION ( 'NONE',  ( 0.000000000000000000, 0.000000000000000000, 1.000000000000000000 ) ) ;
#550=CARTESIAN_POINT ( 'NONE',  ( -20.94999999999999929, 74.25000000001156764, -57.85359592662268824 ) ) ;
#561=EDGE_CURVE ( 'NONE', #167581, #177661, #248601, .T. ) ;
#567=AXIS2_PLACEMENT_3D ( 'NONE', #191071, #17524, #234014 ) ;
#614=ORIENTED_EDGE ( 'NONE', *, *, #241541, .T. ) ;
#629=EDGE_CURVE ( 'NONE', #170828, #113349, #13847, .T. ) ;
#638=EDGE_CURVE ( 'NONE', #245148, #85564, #76363, .T. ) ;
#644=CARTESIAN_POINT ( 'NONE',  ( 23.15000000000000213, 85.00000000001149658, -45.91707660717670336 ) ) ;
#655=ORIENTED_EDGE ( 'NONE', *, *, #91877, .T. ) ;
#656=CARTESIAN_POINT ( 'NONE',  ( -21.44999999999999929, 68.75000000001151079, -48.27310748452437394 ) ) ;
#659=DIRECTION ( 'NONE',  ( 0.000000000000000000, -0.9876197685951263461, 0.1568667991644794590 ) ) ;
#680=EDGE_LOOP ( 'NONE', ( #34192, #227915, #87333 ) ) ;
#699=EDGE_LOOP ( 'NONE', ( #15772, #45586, #89651 ) ) ;
#729=VERTEX_POINT ( 'NONE', #162357 ) ;
#752=DIRECTION ( 'NONE',  ( 0.000000000000000000, 0.000000000000000000, 1.000000000000000000 ) ) ;
#773=CARTESIAN_POINT ( 'NONE',  ( 20.94999999999999929, 71.00000000001151079, -48.42837350343745584 ) ) ;
#791=TOROIDAL_SURFACE ( 'NONE', #108965, 0.4000000000000003553, 0.1000000000000000056 ) ;
#842=ORIENTED_EDGE ( 'NONE', *, *, #95761, .F. ) ;
#865=ORIENTED_EDGE ( 'NONE', *, *, #57052, .T. ) ;
#884=CARTESIAN_POINT ( 'NONE',  ( 20.22516295850462598, 66.10063570456274817, -61.61304177243275149 ) ) ;
#943=CARTESIAN_POINT ( 'NONE',  ( 23.14999999999999503, 64.35000000001173248, -81.27310748452440237 ) ) ;
#946=CIRCLE ( 'NONE', #104987, 0.1999999999999987899 ) ;
#980=CARTESIAN_POINT ( 'NONE',  ( 18.52928932188133970, 65.72071067813013201, -44.87310748452439668 ) ) ;
#993=CARTESIAN_POINT ( 'NONE',  ( -18.52309608778508476, 85.64247632006660638, -29.30851114335468921 ) ) ;
#1031=EDGE_CURVE ( 'NONE', #108484, #237026, #66, .T. ) ;
#1042=CARTESIAN_POINT ( 'NONE',  ( 19.99999999999998934, 64.25000000001151079, -48.17310748452440805 ) ) ;
#1067=VECTOR ( 'NONE', #103802, 1000.000000000000000 ) ;
#1074=VERTEX_POINT ( 'NONE', #134427 ) ;
#1076=ORIENTED_EDGE ( 'NONE', *, *, #254807, .T. ) ;
#1105=FACE_OUTER_BOUND ( 'NONE', #33158, .T. ) ;
#1125=DIRECTION ( 'NONE',  ( 0.000000000000000000, 6.982962677686266711E-15, -1.000000000000000000 ) ) ;
#1131=AXIS2_PLACEMENT_3D ( 'NONE', #155849, #153298, #136228 ) ;
#1135=CIRCLE ( 'NONE', #230280, 0.1000000000000028644 ) ;
#1136=EDGE_LOOP ( 'NONE', ( #176857, #128273, #32056, #181394 ) ) ;
#1143=CARTESIAN_POINT ( 'NONE',  ( -22.57848426163147693, 76.00426432929484122, -81.27316579141465525 ) ) ;
#1153=CARTESIAN_POINT ( 'NONE',  ( -23.24999999999999645, 85.60000000001137721, -29.32291809330221355 ) ) ;
#1154=ADVANCED_FACE ( 'NONE', ( #82149 ), #61338, .F. ) ;
#1163=DIRECTION ( 'NONE',  ( 1.000000000000000000, 0.000000000000000000, 0.000000000000000000 ) ) ;
#1170=FACE_OUTER_BOUND ( 'NONE', #239611, .T. ) ;
#1172=ADVANCED_FACE ( 'NONE', ( #241277 ), #63904, .F. ) ;
#1213=AXIS2_PLACEMENT_3D ( 'NONE', #17555, #99643, #159659 ) ;
#1237=CIRCLE ( 'NONE', #88726, 0.5000000000000004441 ) ;
#1239=FACE_OUTER_BOUND ( 'NONE', #129427, .T. ) ;
#1266=CARTESIAN_POINT ( 'NONE',  ( 18.44206774312972996, 85.49102735755145943, -29.39687997982606404 ) ) ;
#1283=EDGE_LOOP ( 'NONE', ( #201603, #71956, #89397 ) ) ;
#1289=VERTEX_POINT ( 'NONE', #29937 ) ;
#1336=ORIENTED_EDGE ( 'NONE', *, *, #63720, .F. ) ;
#1342=ORIENTED_EDGE ( 'NONE', *, *, #193622, .T. ) ;
#1372=ADVANCED_FACE ( 'NONE', ( #75483 ), #194142, .F. ) ;
#1373=EDGE_CURVE ( 'NONE', #62686, #5270, #114584, .T. ) ;
#1382=SPHERICAL_SURFACE ( 'NONE', #206436, 0.1000000000000000056 ) ;
#1412=CARTESIAN_POINT ( 'NONE',  ( -21.05000000000000071, 74.83729825007360148, -61.52310748452433131 ) ) ;
#1503=ORIENTED_EDGE ( 'NONE', *, *, #31993, .T. ) ;
#1529=DIRECTION ( 'NONE',  ( 0.000000000000000000, 0.9915357197604892647, -0.1298341882519715440 ) ) ;
#1545=DIRECTION ( 'NONE',  ( -1.000000000000000000, -0.000000000000000000, -0.000000000000000000 ) ) ;
#1598=ORIENTED_EDGE ( 'NONE', *, *, #104966, .F. ) ;
#1614=DIRECTION ( 'NONE',  ( 1.000000000000000000, 0.000000000000000000, 0.000000000000000000 ) ) ;
#1627=CARTESIAN_POINT ( 'NONE',  ( 21.14999999999999503, 76.00000000001165290, -69.52310748452431710 ) ) ;
#1666=EDGE_CURVE ( 'NONE', #136766, #153767, #80300, .T. ) ;
#1705=CARTESIAN_POINT ( 'NONE',  ( 22.39999999999999503, 75.90000000001170122, -75.77310748452431710 ) ) ;
#1706=DIRECTION ( 'NONE',  ( 0.000000000000000000, 0.000000000000000000, -1.000000000000000000 ) ) ;
#1712=CARTESIAN_POINT ( 'NONE',  ( 21.14999999999999858, 76.00000000001173817, -81.17267829206912211 ) ) ;
#1718=ORIENTED_EDGE ( 'NONE', *, *, #113383, .T. ) ;
#1723=ORIENTED_EDGE ( 'NONE', *, *, #2166, .F. ) ;
#1732=ADVANCED_FACE ( 'NONE', ( #95967 ), #218051, .T. ) ;
#1756=AXIS2_PLACEMENT_3D ( 'NONE', #224993, #141630, #165050 ) ;
#1763=ORIENTED_EDGE ( 'NONE', *, *, #132664, .T. ) ;
#1775=DIRECTION ( 'NONE',  ( 1.000000000000000000, 0.000000000000000000, 0.000000000000000000 ) ) ;
#1832=AXIS2_PLACEMENT_3D ( 'NONE', #135364, #212370, #33764 ) ;
#1869=ORIENTED_EDGE ( 'NONE', *, *, #233397, .T. ) ;
#1880=AXIS2_PLACEMENT_3D ( 'NONE', #236031, #155251, #232209 ) ;
#1896=EDGE_CURVE ( 'NONE', #52627, #85480, #251193, .T. ) ;
#1911=DIRECTION ( 'NONE',  ( 0.000000000000000000, -1.000000000000000000, -6.982962677686265922E-15 ) ) ;
#1944=LINE ( 'NONE', #161050, #230414 ) ;
#1966=ORIENTED_EDGE ( 'NONE', *, *, #252403, .T. ) ;
#1973=CIRCLE ( 'NONE', #35361, 0.09999999999999939493 ) ;
#1992=CARTESIAN_POINT ( 'NONE',  ( -20.99749315643149217, 64.25000000001148237, -43.03791325328343476 ) ) ;
#2004=VERTEX_POINT ( 'NONE', #113950 ) ;
#2006=DIRECTION ( 'NONE',  ( -1.836970198721029934E-16, -1.000000000000000000, -6.982962677686266711E-15 ) ) ;
#2040=EDGE_CURVE ( 'NONE', #95482, #64016, #240281, .T. ) ;
#2049=CYLINDRICAL_SURFACE ( 'NONE', #165163, 0.09999999999999976963 ) ;
#2090=CYLINDRICAL_SURFACE ( 'NONE', #228963, 0.1000000000000028644 ) ;
#2111=CIRCLE ( 'NONE', #114562, 0.09999999999999939493 ) ;
#2136=ORIENTED_EDGE ( 'NONE', *, *, #172077, .F. ) ;
#2140=DIRECTION ( 'NONE',  ( 0.000000000000000000, -7.056502275159894776E-15, 1.000000000000000000 ) ) ;
#2141=CARTESIAN_POINT ( 'NONE',  ( 19.75857864376268935, 64.25000000001148237, -44.77310748452440237 ) ) ;
#2151=DIRECTION ( 'NONE',  ( 1.000000000000000000, 0.000000000000000000, -0.000000000000000000 ) ) ;
#2164=CARTESIAN_POINT ( 'NONE',  ( 23.14999999999998437, 71.95000000001165574, -69.52310748452434552 ) ) ;
#2166=EDGE_CURVE ( 'NONE', #91133, #131663, #9782, .T. ) ;
#2170=CARTESIAN_POINT ( 'NONE',  ( 21.05000000000000071, 87.48912529308749697, -39.02310748452423894 ) ) ;
#2180=CARTESIAN_POINT ( 'NONE',  ( 20.41140022480506389, 65.58956915760997219, -61.90810618088980277 ) ) ;
#2202=CARTESIAN_POINT ( 'NONE',  ( -21.04999999999999716, 76.01771943332057901, -75.96419217299552429 ) ) ;
#2210=CARTESIAN_POINT ( 'NONE',  ( 21.05000000000000071, 87.65000000001163016, -66.62310748452424036 ) ) ;
#2249=DIRECTION ( 'NONE',  ( 0.000000000000000000, -1.000000000000000000, -6.860497997771531562E-15 ) ) ;
#2252=DIRECTION ( 'NONE',  ( -1.000000000000000000, 0.000000000000000000, 0.000000000000000000 ) ) ;
#2281=CARTESIAN_POINT ( 'NONE',  ( -23.15000000000000213, 76.00000000001142553, -36.02310748452432421 ) ) ;
#2324=ORIENTED_EDGE ( 'NONE', *, *, #82387, .T. ) ;
#2353=CARTESIAN_POINT ( 'NONE',  ( -20.92356734117541706, 65.68026841930851845, -30.47257401318895376 ) ) ;
#2385=CYLINDRICAL_SURFACE ( 'NONE', #18571, 0.1000000000000028644 ) ;
#2421=VERTEX_POINT ( 'NONE', #86353 ) ;
#2425=AXIS2_PLACEMENT_3D ( 'NONE', #153513, #135160, #16531 ) ;
#2431=CARTESIAN_POINT ( 'NONE',  ( 21.05000000000000071, 71.00000000001151079, -48.42837350343745584 ) ) ;
#2445=DIRECTION ( 'NONE',  ( 1.000000000000000000, 0.000000000000000000, 0.000000000000000000 ) ) ;
#2453=AXIS2_PLACEMENT_3D ( 'NONE', #52385, #167250, #207647 ) ;
#2484=CARTESIAN_POINT ( 'NONE',  ( -20.94999999999999929, 87.48912529308749697, -39.12310748452424747 ) ) ;
#2496=ORIENTED_EDGE ( 'NONE', *, *, #130595, .F. ) ;
#2499=DIRECTION ( 'NONE',  ( -1.000000000000000000, 0.000000000000000000, 0.000000000000000000 ) ) ;
#2515=ORIENTED_EDGE ( 'NONE', *, *, #16126, .T. ) ;
#2553=AXIS2_PLACEMENT_3D ( 'NONE', #217952, #178894, #254505 ) ;
#2557=CARTESIAN_POINT ( 'NONE',  ( 21.05000000000000071, 69.35000000001159037, -59.67928539484125139 ) ) ;
#2560=CARTESIAN_POINT ( 'NONE',  ( -22.00411653962182967, 68.74655713164163728, -69.62214559032503303 ) ) ;
#2580=CARTESIAN_POINT ( 'NONE',  ( -18.59999999999999787, 85.32100840337290037, -62.28716923544637751 ) ) ;
#2604=CARTESIAN_POINT ( 'NONE',  ( -20.94999999999999929, 76.00000000001142553, -36.02310748452432421 ) ) ;
#2642=TOROIDAL_SURFACE ( 'NONE', #31902, 4.149999999999999467, 0.1000000000000000056 ) ;
#2701=CARTESIAN_POINT ( 'NONE',  ( -18.59999999999999787, 64.35000000001150511, -48.17310748452440095 ) ) ;
#2725=FACE_OUTER_BOUND ( 'NONE', #118331, .T. ) ;
#2731=CARTESIAN_POINT ( 'NONE',  ( -22.50000000000000000, 76.00000000001169553, -75.77310748452431710 ) ) ;
#2785=CARTESIAN_POINT ( 'NONE',  ( -18.52643265882458579, 65.68026841930851845, -30.47257401318894310 ) ) ;
#2790=EDGE_CURVE ( 'NONE', #26749, #121900, #118323, .T. ) ;
#2802=DIRECTION ( 'NONE',  ( 0.000000000000000000, -0.9908441862701605762, -0.1350103645451835310 ) ) ;
#2817=VECTOR ( 'NONE', #17607, 1000.000000000000000 ) ;
#2898=AXIS2_PLACEMENT_3D ( 'NONE', #38094, #215425, #113750 ) ;
#2901=AXIS2_PLACEMENT_3D ( 'NONE', #193611, #108922, #89350 ) ;
#2927=ORIENTED_EDGE ( 'NONE', *, *, #160399, .F. ) ;
#2960=VERTEX_POINT ( 'NONE', #205416 ) ;
#2976=CARTESIAN_POINT ( 'NONE',  ( 18.59999999999999076, 64.35000000001147669, -44.67310748452440095 ) ) ;
#2986=CARTESIAN_POINT ( 'NONE',  ( -2.995603634470891112E-16, 87.75000000001148237, -44.77310748452423894 ) ) ;
#2994=ORIENTED_EDGE ( 'NONE', *, *, #42913, .T. ) ;
#2998=ORIENTED_EDGE ( 'NONE', *, *, #111549, .F. ) ;
#3005=CARTESIAN_POINT ( 'NONE',  ( -23.24999999999999645, 85.60000000001137721, -29.42291809330221142 ) ) ;
#3033=CIRCLE ( 'NONE', #61328, 0.1000000000000028644 ) ;
#3041=FACE_OUTER_BOUND ( 'NONE', #99103, .T. ) ;
#3060=ORIENTED_EDGE ( 'NONE', *, *, #212807, .F. ) ;
#3081=EDGE_LOOP ( 'NONE', ( #130287, #144768, #249114, #198906 ) ) ;
#3095=FACE_OUTER_BOUND ( 'NONE', #60148, .T. ) ;
#3100=CARTESIAN_POINT ( 'NONE',  ( 20.95420533658165141, 65.45413552525202761, -61.95560146383115807 ) ) ;
#3111=CARTESIAN_POINT ( 'NONE',  ( 22.47071067811864964, 75.90090754530910999, -77.24318222902236641 ) ) ;
#3122=ORIENTED_EDGE ( 'NONE', *, *, #54019, .T. ) ;
#3145=CARTESIAN_POINT ( 'NONE',  ( -21.05000000000000071, 74.83729825007360148, -61.42310748452432989 ) ) ;
#3183=CARTESIAN_POINT ( 'NONE',  ( 22.57320508075687115, 64.25000000001165290, -69.52310748452440237 ) ) ;
#3209=AXIS2_PLACEMENT_3D ( 'NONE', #140254, #135122, #215946 ) ;
#3212=AXIS2_PLACEMENT_3D ( 'NONE', #200042, #21426, #136171 ) ;
#3213=CIRCLE ( 'NONE', #119782, 0.09999999999999938105 ) ;
#3217=ORIENTED_EDGE ( 'NONE', *, *, #114180, .F. ) ;
#3227=AXIS2_PLACEMENT_3D ( 'NONE', #114821, #96517, #75710 ) ;
#3237=EDGE_CURVE ( 'NONE', #175273, #231640, #180435, .T. ) ;
#3239=DIRECTION ( 'NONE',  ( -1.000000000000000000, 0.000000000000000000, -0.000000000000000000 ) ) ;
#3242=DIRECTION ( 'NONE',  ( 1.000000000000000000, -2.952720810173289112E-16, -2.061873921506763405E-30 ) ) ;
#3267=EDGE_LOOP ( 'NONE', ( #217053, #59577, #2324, #33032 ) ) ;
#3269=DIRECTION ( 'NONE',  ( 0.000000000000000000, -1.000000000000000000, -7.272083257015735086E-15 ) ) ;
#3300=EDGE_LOOP ( 'NONE', ( #4920, #124689, #155253, #176443 ) ) ;
#3334=CIRCLE ( 'NONE', #82440, 0.09999999999999939493 ) ;
#3337=ORIENTED_EDGE ( 'NONE', *, *, #7308, .T. ) ;
#3350=AXIS2_PLACEMENT_3D ( 'NONE', #60232, #155528, #40721 ) ;
#3357=EDGE_CURVE ( 'NONE', #79018, #152525, #99576, .T. ) ;
#3366=ORIENTED_EDGE ( 'NONE', *, *, #228409, .F. ) ;
#3389=DIRECTION ( 'NONE',  ( -2.252264143451594314E-15, 0.1298341882520054891, 0.9915357197604850459 ) ) ;
#3410=LINE ( 'NONE', #221177, #99736 ) ;
#3422=CARTESIAN_POINT ( 'NONE',  ( 19.81427058490522697, 64.33143601962973435, -44.77310748452440947 ) ) ;
#3476=FACE_OUTER_BOUND ( 'NONE', #56653, .T. ) ;
#3497=DIRECTION ( 'NONE',  ( 1.000000000000000000, 0.000000000000000000, 0.000000000000000000 ) ) ;
#3521=DIRECTION ( 'NONE',  ( 0.000000000000000000, -6.982962677686266711E-15, 1.000000000000000000 ) ) ;
#3527=EDGE_CURVE ( 'NONE', #108916, #13565, #239493, .T. ) ;
#3544=DIRECTION ( 'NONE',  ( 0.000000000000000000, -6.982962677686266711E-15, 1.000000000000000000 ) ) ;
#3550=ORIENTED_EDGE ( 'NONE', *, *, #73181, .T. ) ;
#3576=CARTESIAN_POINT ( 'NONE',  ( 18.49999999999999289, 65.74999999739246448, -44.83593553489160399 ) ) ;
#3596=CARTESIAN_POINT ( 'NONE',  ( 21.30000000000002558, 76.00000000001165290, -69.52310748452431710 ) ) ;
#3604=CARTESIAN_POINT ( 'NONE',  ( -20.64999999999999858, 71.65000000001151648, -48.37310748452434694 ) ) ;
#3677=VERTEX_POINT ( 'NONE', #183674 ) ;
#3681=ORIENTED_EDGE ( 'NONE', *, *, #123545, .F. ) ;
#3686=DIRECTION ( 'NONE',  ( 0.000000000000000000, -7.026728003956686545E-15, 1.000000000000000000 ) ) ;
#3691=ORIENTED_EDGE ( 'NONE', *, *, #87920, .F. ) ;
#3716=EDGE_CURVE ( 'NONE', #81112, #156105, #220238, .T. ) ;
#3760=DIRECTION ( 'NONE',  ( 1.000000000000000000, 0.000000000000000000, 0.000000000000000000 ) ) ;
#3793=DIRECTION ( 'NONE',  ( 0.000000000000000000, -0.008583690987135041833, 0.9999631594459055250 ) ) ;
#3853=ORIENTED_EDGE ( 'NONE', *, *, #166112, .T. ) ;
#3879=CARTESIAN_POINT ( 'NONE',  ( 20.12500000000000000, 66.25000000001161027, -61.41133620241011215 ) ) ;
#3885=DIRECTION ( 'NONE',  ( 0.000000000000000000, 0.000000000000000000, 1.000000000000000000 ) ) ;
#3916=DIRECTION ( 'NONE',  ( 0.000000000000000000, 0.000000000000000000, 1.000000000000000000 ) ) ;
#3920=CIRCLE ( 'NONE', #78718, 11.65000000000000036 ) ;
#3931=DIRECTION ( 'NONE',  ( 0.000000000000000000, 6.982962677686267499E-15, -1.000000000000000000 ) ) ;
#3938=AXIS2_PLACEMENT_3D ( 'NONE', #43164, #19759, #137124 ) ;
#3953=ORIENTED_EDGE ( 'NONE', *, *, #123060, .F. ) ;
#3966=EDGE_CURVE ( 'NONE', #102057, #206913, #135597, .T. ) ;
#3969=AXIS2_PLACEMENT_3D ( 'NONE', #198040, #199350, #145435 ) ;
#3983=ORIENTED_EDGE ( 'NONE', *, *, #184256, .T. ) ;
#4008=AXIS2_PLACEMENT_3D ( 'NONE', #177996, #118002, #136252 ) ;
#4024=PLANE ( 'NONE',  #89798 ) ;
#4029=AXIS2_PLACEMENT_3D ( 'NONE', #147918, #173619, #116173 ) ;
#4050=ORIENTED_EDGE ( 'NONE', *, *, #162882, .T. ) ;
#4084=ADVANCED_FACE ( 'NONE', ( #201627 ), #252299, .F. ) ;
#4095=CIRCLE ( 'NONE', #29082, 0.09999999999999766020 ) ;
#4099=DIRECTION ( 'NONE',  ( 0.000000000000000000, 0.000000000000000000, 1.000000000000000000 ) ) ;
#4117=B_SPLINE_CURVE_WITH_KNOTS ( 'NONE', 3,
 ( #131527, #152407, #188942, #250195, #230642, #71580, #228073, #51971, #151102, #247625, #128972, #10318, #109381, #208520, #231934, #29891 ),
 .UNSPECIFIED., .F., .F.,
 ( 4, 3, 3, 3, 3, 4 ),
 ( 0.000000000000000000, 2.209833635978096787E-05, 5.595056164119028614E-05, 8.979992002654958564E-05, 0.0001236482757198868287, 0.0001574984039362969566 ),
 .UNSPECIFIED. ) ;
#4118=CARTESIAN_POINT ( 'NONE',  ( 22.45463910399149299, 76.00000000001263345, -81.17267829470745255 ) ) ;
#4132=ORIENTED_EDGE ( 'NONE', *, *, #31243, .T. ) ;
#4138=ORIENTED_EDGE ( 'NONE', *, *, #21133, .F. ) ;
#4158=ORIENTED_EDGE ( 'NONE', *, *, #56990, .T. ) ;
#4185=VECTOR ( 'NONE', #99583, 1000.000000000000000 ) ;
#4196=DIRECTION ( 'NONE',  ( 1.000000000000000000, 0.000000000000000000, 0.000000000000000000 ) ) ;
#4202=EDGE_CURVE ( 'NONE', #193535, #175419, #29454, .T. ) ;
#4238=ORIENTED_EDGE ( 'NONE', *, *, #139069, .F. ) ;
#4242=VERTEX_POINT ( 'NONE', #184631 ) ;
#4250=DIRECTION ( 'NONE',  ( 0.000000000000000000, -7.429790795770647916E-15, 1.000000000000000000 ) ) ;
#4279=CARTESIAN_POINT ( 'NONE',  ( 20.95512820512820440, 67.12384868372348024, -60.96447848938343839 ) ) ;
#4325=EDGE_LOOP ( 'NONE', ( #243895, #125884, #223275, #245663 ) ) ;
#4340=CARTESIAN_POINT ( 'NONE',  ( 21.93642651522410603, 68.67283376068586165, -69.52310748452435973 ) ) ;
#4348=ORIENTED_EDGE ( 'NONE', *, *, #256323, .T. ) ;
#4358=CARTESIAN_POINT ( 'NONE',  ( -22.50000000000000000, 76.00000000001165290, -69.52310748452431710 ) ) ;
#4360=EDGE_CURVE ( 'NONE', #175273, #226817, #46659, .T. ) ;
#4372=ORIENTED_EDGE ( 'NONE', *, *, #23, .F. ) ;
#4383=EDGE_CURVE ( 'NONE', #211078, #144573, #72330, .T. ) ;
#4385=DIRECTION ( 'NONE',  ( 0.000000000000000000, -6.938893903907229955E-15, 1.000000000000000000 ) ) ;
#4386=CARTESIAN_POINT ( 'NONE',  ( 23.14999999999999858, 76.00000000001142553, -36.02310748452432421 ) ) ;
#4388=DIRECTION ( 'NONE',  ( 0.000000000000000000, -7.086529944415894657E-15, 1.000000000000000000 ) ) ;
#4393=CARTESIAN_POINT ( 'NONE',  ( -23.15000000000000213, 76.00000000001142553, -36.02310748452432421 ) ) ;
#4405=VECTOR ( 'NONE', #221213, 1000.000000000000000 ) ;
#4406=CYLINDRICAL_SURFACE ( 'NONE', #232860, 0.1000000000000028644 ) ;
#4428=EDGE_LOOP ( 'NONE', ( #21008, #208272, #77657, #210809 ) ) ;
#4441=DIRECTION ( 'NONE',  ( 1.000000000000000000, 0.000000000000000000, 0.000000000000000000 ) ) ;
#4459=CARTESIAN_POINT ( 'NONE',  ( 21.05000000000000071, 67.22371710471912820, -60.96447848938343839 ) ) ;
#4461=ORIENTED_EDGE ( 'NONE', *, *, #125617, .F. ) ;
#4472=EDGE_LOOP ( 'NONE', ( #138854, #61855, #52121, #154961 ) ) ;
#4517=DIRECTION ( 'NONE',  ( -1.000000000000000000, -0.000000000000000000, -0.000000000000000000 ) ) ;
#4567=EDGE_CURVE ( 'NONE', #210362, #230778, #17452, .T. ) ;
#4573=CARTESIAN_POINT ( 'NONE',  ( -20.85000000000000142, 77.83585931145498193, -24.51866831572578675 ) ) ;
#4578=VECTOR ( 'NONE', #143083, 1000.000000000000000 ) ;
#4595=CARTESIAN_POINT ( 'NONE',  ( -18.59999999999999787, 77.26178616857662007, -61.43660852097883662 ) ) ;
#4606=CARTESIAN_POINT ( 'NONE',  ( 20.85000000000000142, 76.00000000001142553, -36.02310748452432421 ) ) ;
#4623=CIRCLE ( 'NONE', #250355, 0.1000000000000028644 ) ;
#4626=VERTEX_POINT ( 'NONE', #150350 ) ;
#4639=CARTESIAN_POINT ( 'NONE',  ( 19.97071067811864609, 64.27928932189283273, -44.87310748452440379 ) ) ;
#4658=EDGE_CURVE ( 'NONE', #120086, #62040, #214166, .T. ) ;
#4662=ORIENTED_EDGE ( 'NONE', *, *, #157310, .T. ) ;
#4727=DIRECTION ( 'NONE',  ( -0.000000000000000000, 0.1350103645451945777, -0.9908441862701590219 ) ) ;
#4771=DIRECTION ( 'NONE',  ( 0.000000000000000000, -7.116814260417668513E-15, 1.000000000000000000 ) ) ;
#4825=AXIS2_PLACEMENT_3D ( 'NONE', #135112, #256290, #235506 ) ;
#4852=ORIENTED_EDGE ( 'NONE', *, *, #206248, .F. ) ;
#4860=EDGE_CURVE ( 'NONE', #147579, #46909, #26030, .T. ) ;
#4868=ADVANCED_FACE ( 'NONE', ( #86176 ), #204851, .T. ) ;
#4920=ORIENTED_EDGE ( 'NONE', *, *, #52238, .T. ) ;
#4931=ORIENTED_EDGE ( 'NONE', *, *, #197138, .T. ) ;
#4933=AXIS2_PLACEMENT_3D ( 'NONE', #107040, #189166, #66654 ) ;
#4946=DIRECTION ( 'NONE',  ( -1.000000000000000000, 2.952720810173289112E-16, 2.061873921506763405E-30 ) ) ;
#4962=ORIENTED_EDGE ( 'NONE', *, *, #99767, .F. ) ;
#4966=DIRECTION ( 'NONE',  ( 0.000000000000000000, -1.000000000000000000, -6.982962677686265922E-15 ) ) ;
#4983=ORIENTED_EDGE ( 'NONE', *, *, #169940, .F. ) ;
#4985=VECTOR ( 'NONE', #115695, 1000.000000000000000 ) ;
#4999=ORIENTED_EDGE ( 'NONE', *, *, #252051, .F. ) ;
#5008=EDGE_CURVE ( 'NONE', #91161, #71888, #195606, .T. ) ;
#5047=EDGE_LOOP ( 'NONE', ( #159442, #30952, #98191, #241110 ) ) ;
#5064=ORIENTED_EDGE ( 'NONE', *, *, #209922, .F. ) ;
#5078=DIRECTION ( 'NONE',  ( 0.000000000000000000, 0.000000000000000000, -1.000000000000000000 ) ) ;
#5105=CARTESIAN_POINT ( 'NONE',  ( -21.07094088545304444, 69.67983277809517517, -69.62200118707659158 ) ) ;
#5120=CARTESIAN_POINT ( 'NONE',  ( -23.25000000000000000, 76.00000000001139711, -32.12310748452431852 ) ) ;
#5155=ADVANCED_FACE ( 'NONE', ( #136886 ), #234711, .T. ) ;
#5158=CARTESIAN_POINT ( 'NONE',  ( 18.51565452909320086, 85.35285933884857457, -62.32819816329048024 ) ) ;
#5172=EDGE_CURVE ( 'NONE', #224378, #167778, #163580, .T. ) ;
#5179=FACE_OUTER_BOUND ( 'NONE', #4325, .T. ) ;
#5183=ORIENTED_EDGE ( 'NONE', *, *, #51226, .F. ) ;
#5191=EDGE_CURVE ( 'NONE', #218147, #21197, #117774, .T. ) ;
#5196=DIRECTION ( 'NONE',  ( 0.000000000000000000, 6.982962677686266711E-15, -1.000000000000000000 ) ) ;
#5210=CARTESIAN_POINT ( 'NONE',  ( 21.14999999999999503, 76.10085836911045476, -81.27267460801371612 ) ) ;
#5215=EDGE_CURVE ( 'NONE', #221285, #43098, #101150, .T. ) ;
#5249=EDGE_LOOP ( 'NONE', ( #237507, #58905, #168146, #41404 ) ) ;
#5261=ORIENTED_EDGE ( 'NONE', *, *, #145268, .T. ) ;
#5264=CYLINDRICAL_SURFACE ( 'NONE', #95320, 11.79999999999999716 ) ;
#5270=VERTEX_POINT ( 'NONE', #205849 ) ;
#5273=ORIENTED_EDGE ( 'NONE', *, *, #158998, .T. ) ;
#5277=DIRECTION ( 'NONE',  ( 0.000000000000000000, -0.9875055080513754913, 0.1575844902526733482 ) ) ;
#5281=DIRECTION ( 'NONE',  ( -0.000000000000000000, 6.982962677686266711E-15, -1.000000000000000000 ) ) ;
#5327=CARTESIAN_POINT ( 'NONE',  ( 18.59999999999999076, 69.35000000001151932, -48.37310748452436826 ) ) ;
#5329=CARTESIAN_POINT ( 'NONE',  ( 22.48660254037844197, 64.35000000001164722, -69.57310748452439952 ) ) ;
#5377=CARTESIAN_POINT ( 'NONE',  ( 22.45380639572249493, 75.99999985734224595, -81.27354037563121381 ) ) ;
#5433=CARTESIAN_POINT ( 'NONE',  ( 18.57071067811864040, 65.82071067813016896, -48.27310748452439526 ) ) ;
#5482=CARTESIAN_POINT ( 'NONE',  ( 21.06086055315975258, 67.22529248505534838, -57.32078532937043747 ) ) ;
#5483=ORIENTED_EDGE ( 'NONE', *, *, #91685, .F. ) ;
#5498=FACE_OUTER_BOUND ( 'NONE', #139366, .T. ) ;
#5512=DIRECTION ( 'NONE',  ( 0.000000000000000000, 0.000000000000000000, 1.000000000000000000 ) ) ;
#5514=EDGE_CURVE ( 'NONE', #172081, #182847, #137408, .T. ) ;
#5528=CYLINDRICAL_SURFACE ( 'NONE', #168096, 0.09999999999999939493 ) ;
#5539=CIRCLE ( 'NONE', #151333, 0.09999999999999939493 ) ;
#5550=CARTESIAN_POINT ( 'NONE',  ( -23.15000000000000213, 70.05000000001149374, -46.32880978955918039 ) ) ;
#5567=CARTESIAN_POINT ( 'NONE',  ( -23.15000000000000213, 76.00000000001142553, -36.02310748452432421 ) ) ;
#5574=DIRECTION ( 'NONE',  ( -0.4999999999999799050, -6.047423072554995242E-15, 0.8660254037844502539 ) ) ;
#5591=FACE_OUTER_BOUND ( 'NONE', #69074, .T. ) ;
#5599=DIRECTION ( 'NONE',  ( 1.000000000000000000, 0.000000000000000000, 0.000000000000000000 ) ) ;
#5611=CARTESIAN_POINT ( 'NONE',  ( 21.05000000000000071, 65.27628289530407812, -61.85819391543678591 ) ) ;
#5622=ORIENTED_EDGE ( 'NONE', *, *, #200586, .F. ) ;
#5629=DIRECTION ( 'NONE',  ( -0.000000000000000000, -6.982962677686266711E-15, 1.000000000000000000 ) ) ;
#5636=ORIENTED_EDGE ( 'NONE', *, *, #236832, .T. ) ;
#5648=CARTESIAN_POINT ( 'NONE',  ( -18.59999999999999787, 66.65000000001157332, -57.37310748452438247 ) ) ;
#5653=DIRECTION ( 'NONE',  ( 1.000000000000000000, -0.000000000000000000, 0.000000000000000000 ) ) ;
#5663=CARTESIAN_POINT ( 'NONE',  ( -21.00023020733502932, 76.00000000001170974, -75.91397672979267952 ) ) ;
#5676=AXIS2_PLACEMENT_3D ( 'NONE', #169481, #209857, #11663 ) ;
#5688=CARTESIAN_POINT ( 'NONE',  ( 23.24999999999999289, 64.35000000001150511, -48.17310748452440095 ) ) ;
#5689=DIRECTION ( 'NONE',  ( 1.000000000000000000, 0.000000000000000000, 0.000000000000000000 ) ) ;
#5700=CARTESIAN_POINT ( 'NONE',  ( 20.94999999999999929, 68.87972903831379767, -32.36354444268504693 ) ) ;
#5701=CARTESIAN_POINT ( 'NONE',  ( -21.08376601933334271, 75.93622398908182447, -75.86505475580005964 ) ) ;
#5740=EDGE_LOOP ( 'NONE', ( #98996, #255463, #253948, #152510 ) ) ;
#5748=EDGE_CURVE ( 'NONE', #87766, #92561, #231862, .T. ) ;
#5795=FACE_OUTER_BOUND ( 'NONE', #237734, .T. ) ;
#5798=AXIS2_PLACEMENT_3D ( 'NONE', #147551, #105827, #48441 ) ;
#5881=AXIS2_PLACEMENT_3D ( 'NONE', #7189, #104978, #240678 ) ;
#5886=CIRCLE ( 'NONE', #155782, 0.1000000000000028644 ) ;
#5895=CARTESIAN_POINT ( 'NONE',  ( -22.49510344025093644, 75.93287232181748436, -81.17307758963858078 ) ) ;
#5915=FACE_OUTER_BOUND ( 'NONE', #191720, .T. ) ;
#5917=ORIENTED_EDGE ( 'NONE', *, *, #233349, .T. ) ;
#5943=ORIENTED_EDGE ( 'NONE', *, *, #46844, .T. ) ;
#5957=AXIS2_PLACEMENT_3D ( 'NONE', #230984, #186715, #206266 ) ;
#6013=DIRECTION ( 'NONE',  ( 0.000000000000000000, 1.000000000000000000, 7.116814260417668513E-15 ) ) ;
#6026=VERTEX_POINT ( 'NONE', #174688 ) ;
#6036=ORIENTED_EDGE ( 'NONE', *, *, #19436, .T. ) ;
#6050=LINE ( 'NONE', #105119, #217304 ) ;
#6059=CARTESIAN_POINT ( 'NONE',  ( -21.04999999999999716, 75.98514436511781867, -75.86746652656786694 ) ) ;
#6075=CARTESIAN_POINT ( 'NONE',  ( -23.15000000000000213, 87.75000000001143974, -39.12310748452424747 ) ) ;
#6080=DIRECTION ( 'NONE',  ( -1.000000000000000000, -0.000000000000000000, 0.000000000000000000 ) ) ;
#6131=FACE_OUTER_BOUND ( 'NONE', #134886, .T. ) ;
#6147=ORIENTED_EDGE ( 'NONE', *, *, #257612, .T. ) ;
#6161=ORIENTED_EDGE ( 'NONE', *, *, #235307, .T. ) ;
#6183=CARTESIAN_POINT ( 'NONE',  ( 18.59999999999999787, 77.36242903720467723, -28.13422623660311217 ) ) ;
#6208=CARTESIAN_POINT ( 'NONE',  ( 21.05000000000000071, 85.00000000001149658, -45.91707660717670336 ) ) ;
#6226=DIRECTION ( 'NONE',  ( 0.000000000000000000, 6.982962677686266711E-15, -1.000000000000000000 ) ) ;
#6230=ORIENTED_EDGE ( 'NONE', *, *, #55941, .F. ) ;
#6232=DIRECTION ( 'NONE',  ( -1.000000000000000000, -0.000000000000000000, -0.000000000000000000 ) ) ;
#6238=VERTEX_POINT ( 'NONE', #211210 ) ;
#6251=CARTESIAN_POINT ( 'NONE',  ( 20.85000000000000142, 77.83585931145498193, -24.51866831572578320 ) ) ;
#6258=DIRECTION ( 'NONE',  ( 0.000000000000000000, 1.000000000000000000, 0.000000000000000000 ) ) ;
#6275=ORIENTED_EDGE ( 'NONE', *, *, #14358, .T. ) ;
#6290=CARTESIAN_POINT ( 'NONE',  ( 21.95218792049437795, 68.79849243876499543, -69.62213592432428300 ) ) ;
#6347=VECTOR ( 'NONE', #108233, 1000.000000000000000 ) ;
#6351=VERTEX_POINT ( 'NONE', #14324 ) ;
#6369=CARTESIAN_POINT ( 'NONE',  ( 21.14999999999999503, 76.10000000001174669, -81.17267829206912211 ) ) ;
#6381=CARTESIAN_POINT ( 'NONE',  ( -18.59999999999999787, 76.00000000001165290, -69.52310748452431710 ) ) ;
#6382=AXIS2_PLACEMENT_3D ( 'NONE', #245737, #226131, #228753 ) ;
#6402=DIRECTION ( 'NONE',  ( -1.000000000000000000, 0.000000000000000000, 0.000000000000000000 ) ) ;
#6409=ORIENTED_EDGE ( 'NONE', *, *, #168690, .F. ) ;
#6418=DIRECTION ( 'NONE',  ( 1.000000000000000000, 0.000000000000000000, 0.000000000000000000 ) ) ;
#6432=CARTESIAN_POINT ( 'NONE',  ( -18.59999999999999787, 77.26327546522863088, -28.12124281777790813 ) ) ;
#6443=ORIENTED_EDGE ( 'NONE', *, *, #104986, .F. ) ;
#6448=ORIENTED_EDGE ( 'NONE', *, *, #85791, .T. ) ;
#6454=CARTESIAN_POINT ( 'NONE',  ( -23.15000000000000213, 76.00000000001165290, -69.52310748452431710 ) ) ;
#6456=CARTESIAN_POINT ( 'NONE',  ( 18.59999999999999076, 65.50857864377418593, -44.77310748452440237 ) ) ;
#6466=FACE_OUTER_BOUND ( 'NONE', #42091, .T. ) ;
#6470=CARTESIAN_POINT ( 'NONE',  ( 23.14999999999999858, 79.90000000001141700, -36.02310748452429578 ) ) ;
#6497=DIRECTION ( 'NONE',  ( 0.000000000000000000, 0.9999631594459055250, 0.008583690987131395445 ) ) ;
#6537=DIRECTION ( 'NONE',  ( -1.000000000000000000, 0.000000000000000000, -0.000000000000000000 ) ) ;
#6553=AXIS2_PLACEMENT_3D ( 'NONE', #44071, #45349, #123609 ) ;
#6578=ORIENTED_EDGE ( 'NONE', *, *, #233545, .T. ) ;
#6580=ADVANCED_FACE ( 'NONE', ( #183648 ), #102783, .T. ) ;
#6582=ORIENTED_EDGE ( 'NONE', *, *, #197667, .F. ) ;
#6585=ORIENTED_EDGE ( 'NONE', *, *, #29050, .F. ) ;
#6606=CARTESIAN_POINT ( 'NONE',  ( 23.15000000000000213, 85.60000000001149090, -45.91707660717669626 ) ) ;
#6607=CIRCLE ( 'NONE', #56478, 0.5000000000000004441 ) ;
#6626=CIRCLE ( 'NONE', #52402, 0.09999999999999739653 ) ;
#6642=AXIS2_PLACEMENT_3D ( 'NONE', #102787, #25865, #126223 ) ;
#6692=B_SPLINE_CURVE_WITH_KNOTS ( 'NONE', 3,
 ( #35298, #258102, #215173, #16992, #176079, #159081, #238588, #160369, #61236, #100334, #114792, #255528, #18259, #194358, #97762, #177367, #59926, #256808, #139473 ),
 .UNSPECIFIED., .F., .F.,
 ( 4, 3, 3, 3, 3, 3, 4 ),
 ( -2.000416914655991116E-06, 0.000000000000000000, 4.714008503746756575E-05, 9.979203887778493915E-05, 0.0001372215519229563188, 0.0001635031576221042350, 0.0001900083748504183658 ),
 .UNSPECIFIED. ) ;
#6732=( BOUNDED_SURFACE ( )  B_SPLINE_SURFACE ( 3, 2, ( 
 ( #135536, #18173, #76853 ),
 ( #71747, #156440, #74337 ),
 ( #134250, #151283, #230826 ),
 ( #52148, #238501, #256730 ) ),
 .UNSPECIFIED., .F., .F., .F. ) 
 B_SPLINE_SURFACE_WITH_KNOTS ( ( 4, 4 ),
 ( 3, 3 ),
 ( 0.04058434257139476031, 0.04256401539001599538 ),
 ( 0.000000000000000000, 1.000000000000000000 ),
 .UNSPECIFIED. ) 
 GEOMETRIC_REPRESENTATION_ITEM ( )  RATIONAL_B_SPLINE_SURFACE ( (
 ( 1.000000000000000000, 0.7103081912008298859, 1.000000000000000000),
 ( 1.000000000000000000, 0.7104998333555424539, 1.000000000000000000),
 ( 1.000000000000000000, 0.7107238315755094460, 1.000000000000000000),
 ( 1.000000000000000000, 0.7110073749539290722, 1.000000000000000000) ) ) 
 REPRESENTATION_ITEM ( '' )  SURFACE ( )  );
#6756=ORIENTED_EDGE ( 'NONE', *, *, #62043, .F. ) ;
#6772=DIRECTION ( 'NONE',  ( 0.000000000000000000, 7.086529944415894657E-15, -1.000000000000000000 ) ) ;
#6790=PLANE ( 'NONE',  #118645 ) ;
#6817=FACE_OUTER_BOUND ( 'NONE', #122980, .T. ) ;
#6825=EDGE_LOOP ( 'NONE', ( #13573, #220731, #21013, #48177 ) ) ;
#6838=ORIENTED_EDGE ( 'NONE', *, *, #118794, .F. ) ;
#6870=CARTESIAN_POINT ( 'NONE',  ( -21.45000000000000284, 68.29142135624888965, -57.17310748452437963 ) ) ;
#6871=VERTEX_POINT ( 'NONE', #206417 ) ;
#6895=DIRECTION ( 'NONE',  ( -0.000000000000000000, -0.9876197685951290106, 0.1568667991644625281 ) ) ;
#6914=CARTESIAN_POINT ( 'NONE',  ( -20.64999999999999858, 85.50000000001149658, -45.91707660717669626 ) ) ;
#6923=ADVANCED_FACE ( 'NONE', ( #121767 ), #166035, .T. ) ;
#6933=CYLINDRICAL_SURFACE ( 'NONE', #178184, 0.09999999999999867328 ) ;
#6940=EDGE_CURVE ( 'NONE', #131784, #210362, #256715, .T. ) ;
#6945=FACE_OUTER_BOUND ( 'NONE', #196661, .T. ) ;
#6957=TOROIDAL_SURFACE ( 'NONE', #65217, 11.90000000000000391, 0.1000000000000000056 ) ;
#6972=CARTESIAN_POINT ( 'NONE',  ( -22.00411653889206320, 75.90096189422482098, -76.77655035216469059 ) ) ;
#6980=CIRCLE ( 'NONE', #219359, 0.1000000000000028644 ) ;
#6995=CARTESIAN_POINT ( 'NONE',  ( -20.54999999999999716, 84.73084112150681335, -45.62118220350859588 ) ) ;
#7026=CIRCLE ( 'NONE', #73514, 4.150000000000001243 ) ;
#7032=CIRCLE ( 'NONE', #169587, 0.09999999999999976963 ) ;
#7038=CARTESIAN_POINT ( 'NONE',  ( -20.54999999999999716, 85.00000000001159606, -59.62913836187181715 ) ) ;
#7076=ORIENTED_EDGE ( 'NONE', *, *, #210416, .T. ) ;
#7091=DIRECTION ( 'NONE',  ( 0.000000000000000000, 0.000000000000000000, 1.000000000000000000 ) ) ;
#7106=FACE_BOUND ( 'NONE', #163423, .T. ) ;
#7127=EDGE_LOOP ( 'NONE', ( #144785, #97628, #100600, #155503 ) ) ;
#7135=ORIENTED_EDGE ( 'NONE', *, *, #213017, .T. ) ;
#7160=ORIENTED_EDGE ( 'NONE', *, *, #198394, .T. ) ;
#7165=ORIENTED_EDGE ( 'NONE', *, *, #233097, .T. ) ;
#7189=CARTESIAN_POINT ( 'NONE',  ( -21.14999999999999858, 64.35000000001160458, -62.73924182154625129 ) ) ;
#7191=EDGE_LOOP ( 'NONE', ( #70922, #171395, #104279, #39728 ) ) ;
#7219=EDGE_CURVE ( 'NONE', #156105, #99760, #132046, .T. ) ;
#7242=EDGE_LOOP ( 'NONE', ( #166260, #234593, #62337 ) ) ;
#7243=CARTESIAN_POINT ( 'NONE',  ( 20.94999999999999574, 77.34908441863862549, -61.53660852097883804 ) ) ;
#7259=DIRECTION ( 'NONE',  ( -0.000000000000000000, 6.982962677686266711E-15, -1.000000000000000000 ) ) ;
#7263=DIRECTION ( 'NONE',  ( 0.000000000000000000, 1.000000000000000000, 6.982962677686266711E-15 ) ) ;
#7271=ORIENTED_EDGE ( 'NONE', *, *, #144629, .F. ) ;
#7286=LINE ( 'NONE', #43862, #1067 ) ;
#7288=VECTOR ( 'NONE', #159658, 1000.000000000000000 ) ;
#7293=ADVANCED_FACE ( 'NONE', ( #214130 ), #137153, .F. ) ;
#7301=FACE_OUTER_BOUND ( 'NONE', #204662, .T. ) ;
#7308=EDGE_CURVE ( 'NONE', #193539, #85480, #44490, .T. ) ;
#7353=ADVANCED_FACE ( 'NONE', ( #66614 ), #90336, .T. ) ;
#7355=CARTESIAN_POINT ( 'NONE',  ( -18.59999999999999787, 76.00000000001142553, -36.02310748452432421 ) ) ;
#7369=ORIENTED_EDGE ( 'NONE', *, *, #104750, .F. ) ;
#7372=EDGE_CURVE ( 'NONE', #156337, #14506, #115466, .T. ) ;
#7386=ORIENTED_EDGE ( 'NONE', *, *, #155654, .F. ) ;
#7389=CARTESIAN_POINT ( 'NONE',  ( -23.25000000000000000, 77.83585931145498193, -24.51866831572578675 ) ) ;
#7427=AXIS2_PLACEMENT_3D ( 'NONE', #54105, #193630, #15007 ) ;
#7476=DIRECTION ( 'NONE',  ( 0.000000000000000000, -6.982962677686266711E-15, 1.000000000000000000 ) ) ;
#7525=DIRECTION ( 'NONE',  ( 0.000000000000000000, 1.000000000000000000, 0.000000000000000000 ) ) ;
#7550=DIRECTION ( 'NONE',  ( 0.000000000000000000, -1.000000000000000000, -6.982962677686265922E-15 ) ) ;
#7596=ORIENTED_EDGE ( 'NONE', *, *, #142375, .F. ) ;
#7637=EDGE_CURVE ( 'NONE', #122601, #136730, #217643, .T. ) ;
#7686=CYLINDRICAL_SURFACE ( 'NONE', #40353, 2.000000000000001776 ) ;
#7716=CIRCLE ( 'NONE', #45111, 0.09999999999999520384 ) ;
#7719=FACE_OUTER_BOUND ( 'NONE', #237363, .T. ) ;
#7757=ORIENTED_EDGE ( 'NONE', *, *, #158998, .F. ) ;
#7758=CARTESIAN_POINT ( 'NONE',  ( 18.52928932188134326, 65.72071067813014622, -44.81452884076170307 ) ) ;
#7765=VERTEX_POINT ( 'NONE', #141976 ) ;
#7769=AXIS2_PLACEMENT_3D ( 'NONE', #196791, #158995, #78125 ) ;
#7772=CARTESIAN_POINT ( 'NONE',  ( 18.42595409746860469, 85.49999981257654724, -62.52374513277740675 ) ) ;
#7820=CIRCLE ( 'NONE', #132725, 0.09999999999999766020 ) ;
#7850=AXIS2_PLACEMENT_3D ( 'NONE', #185540, #190706, #125561 ) ;
#7859=CARTESIAN_POINT ( 'NONE',  ( -21.05000000000000071, 87.48912529308749697, -38.92310748452424463 ) ) ;
#7870=ADVANCED_FACE ( 'NONE', ( #51844 ), #169293, .F. ) ;
#7883=DIRECTION ( 'NONE',  ( 0.000000000000000000, -1.000000000000000000, 6.938893903907030216E-14 ) ) ;
#7920=AXIS2_PLACEMENT_3D ( 'NONE', #119347, #120650, #179337 ) ;
#7932=CARTESIAN_POINT ( 'NONE',  ( 21.05000000000000071, 64.35000000001156195, -57.37310748452439668 ) ) ;
#7944=AXIS2_PLACEMENT_3D ( 'NONE', #254463, #253203, #96667 ) ;
#7952=ADVANCED_FACE ( 'NONE', ( #49299 ), #66305, .T. ) ;
#7976=ADVANCED_FACE ( 'NONE', ( #191415 ), #12768, .T. ) ;
#7986=DIRECTION ( 'NONE',  ( 0.000000000000000000, 0.000000000000000000, 1.000000000000000000 ) ) ;
#8002=DIRECTION ( 'NONE',  ( 0.000000000000000000, 6.938893903907234689E-15, -1.000000000000000000 ) ) ;
#8024=ORIENTED_EDGE ( 'NONE', *, *, #16502, .F. ) ;
#8025=DIRECTION ( 'NONE',  ( 1.000000000000000000, 0.000000000000000000, 0.000000000000000000 ) ) ;
#8042=ORIENTED_EDGE ( 'NONE', *, *, #205024, .T. ) ;
#8048=VERTEX_POINT ( 'NONE', #17865 ) ;
#8055=CARTESIAN_POINT ( 'NONE',  ( 20.94999999999999929, 71.00000000001158185, -57.11784146561126363 ) ) ;
#8069=DIRECTION ( 'NONE',  ( 1.000000000000000000, 0.000000000000000000, 0.000000000000000000 ) ) ;
#8070=ORIENTED_EDGE ( 'NONE', *, *, #171045, .T. ) ;
#8079=VECTOR ( 'NONE', #6537, 1000.000000000000000 ) ;
#8088=DIRECTION ( 'NONE',  ( 2.952720810173289112E-16, 1.000000000000000000, 7.086529944415894657E-15 ) ) ;
#8119=AXIS2_PLACEMENT_3D ( 'NONE', #19524, #117328, #255499 ) ;
#8133=DIRECTION ( 'NONE',  ( 1.000000000000000000, 0.000000000000000000, 0.000000000000000000 ) ) ;
#8164=EDGE_CURVE ( 'NONE', #121991, #208753, #103349, .T. ) ;
#8207=AXIS2_PLACEMENT_3D ( 'NONE', #72693, #68826, #152230 ) ;
#8219=CARTESIAN_POINT ( 'NONE',  ( 20.95512820512820795, 67.12384868372345181, -57.32293462539563222 ) ) ;
#8226=CARTESIAN_POINT ( 'NONE',  ( 21.04999999999975557, 65.49746832288597886, -61.96427766744952237 ) ) ;
#8227=FACE_OUTER_BOUND ( 'NONE', #199362, .T. ) ;
#8253=CARTESIAN_POINT ( 'NONE',  ( 20.94999999999999929, 65.27628289530409234, -61.85819391543678591 ) ) ;
#8259=AXIS2_PLACEMENT_3D ( 'NONE', #155077, #115924, #95063 ) ;
#8270=LINE ( 'NONE', #68234, #108337 ) ;
#8281=CARTESIAN_POINT ( 'NONE',  ( -23.15000000000000213, 76.00000000001168132, -73.57310748452432847 ) ) ;
#8283=CARTESIAN_POINT ( 'NONE',  ( -18.50000000000000000, 76.00000000001165290, -69.52310748452431710 ) ) ;
#8303=CIRCLE ( 'NONE', #74952, 0.1000000000000028644 ) ;
#8312=DIRECTION ( 'NONE',  ( 0.000000000000000000, -1.000000000000000000, -6.982962677686265922E-15 ) ) ;
#8398=CARTESIAN_POINT ( 'NONE',  ( 21.05000000000000071, 87.65000000001164437, -69.52310748452424605 ) ) ;
#8409=EDGE_CURVE ( 'NONE', #127854, #253340, #161849, .T. ) ;
#8434=ORIENTED_EDGE ( 'NONE', *, *, #81700, .T. ) ;
#8463=CARTESIAN_POINT ( 'NONE',  ( -20.94999999999999929, 76.00000000001165290, -69.52310748452431710 ) ) ;
#8480=DIRECTION ( 'NONE',  ( 1.000000000000000000, 0.000000000000000000, 0.000000000000000000 ) ) ;
#8488=VECTOR ( 'NONE', #210655, 1000.000000000000000 ) ;
#8506=ORIENTED_EDGE ( 'NONE', *, *, #128820, .T. ) ;
#8529=DIRECTION ( 'NONE',  ( 1.000000000000000000, -1.836970198721029934E-16, -1.282749433769087582E-30 ) ) ;
#8549=CARTESIAN_POINT ( 'NONE',  ( 23.14999999999999503, 64.35000000001146248, -43.03791325517834565 ) ) ;
#8550=FACE_OUTER_BOUND ( 'NONE', #57139, .T. ) ;
#8560=VECTOR ( 'NONE', #171268, 1000.000000000000000 ) ;
#8565=DIRECTION ( 'NONE',  ( 2.952720810173289112E-16, 1.000000000000000000, 6.308085367188367561E-15 ) ) ;
#8576=CARTESIAN_POINT ( 'NONE',  ( 20.94999999999999574, 69.65000000001158753, -59.67928539484123718 ) ) ;
#8597=FACE_OUTER_BOUND ( 'NONE', #119207, .T. ) ;
#8608=ORIENTED_EDGE ( 'NONE', *, *, #561, .F. ) ;
#8641=CARTESIAN_POINT ( 'NONE',  ( -18.39999999999999858, 85.51932773110404185, -62.55013110796492271 ) ) ;
#8655=DIRECTION ( 'NONE',  ( 1.000000000000000000, 7.304098846218105085E-16, 4.217023435051676515E-16 ) ) ;
#8690=LINE ( 'NONE', #69968, #162667 ) ;
#8696=ORIENTED_EDGE ( 'NONE', *, *, #638, .F. ) ;
#8708=CARTESIAN_POINT ( 'NONE',  ( 21.30000000000002558, 76.00000000001165290, -69.52310748452431710 ) ) ;
#8719=DIRECTION ( 'NONE',  ( -0.000000000000000000, -6.982962677686266711E-15, 1.000000000000000000 ) ) ;
#8723=VECTOR ( 'NONE', #103285, 1000.000000000000000 ) ;
#8728=ORIENTED_EDGE ( 'NONE', *, *, #159407, .F. ) ;
#8730=LINE ( 'NONE', #102659, #4578 ) ;
#8749=DIRECTION ( 'NONE',  ( 1.000000000000000000, -0.000000000000000000, -0.000000000000000000 ) ) ;
#8751=ADVANCED_FACE ( 'NONE', ( #188202 ), #49963, .T. ) ;
#8752=DIRECTION ( 'NONE',  ( 1.000000000000000000, 0.000000000000000000, 0.000000000000000000 ) ) ;
#8755=ADVANCED_FACE ( 'NONE', ( #9549 ), #86494, .F. ) ;
#8822=ORIENTED_EDGE ( 'NONE', *, *, #192687, .T. ) ;
#8856=ORIENTED_EDGE ( 'NONE', *, *, #3237, .F. ) ;
#8896=DIRECTION ( 'NONE',  ( 0.000000000000000000, -0.9908441862701605762, -0.1350103645451835310 ) ) ;
#8900=VERTEX_POINT ( 'NONE', #159054 ) ;
#8927=FACE_OUTER_BOUND ( 'NONE', #1283, .T. ) ;
#8946=DIRECTION ( 'NONE',  ( -0.000000000000000000, -6.982962677686266711E-15, 1.000000000000000000 ) ) ;
#8982=ADVANCED_FACE ( 'NONE', ( #244976 ), #104166, .T. ) ;
#8995=FACE_OUTER_BOUND ( 'NONE', #238193, .T. ) ;
#9012=DIRECTION ( 'NONE',  ( 1.000000000000000000, 0.000000000000000000, 0.000000000000000000 ) ) ;
#9013=DIRECTION ( 'NONE',  ( 0.000000000000000000, 1.000000000000000000, 6.982962677686266711E-15 ) ) ;
#9025=AXIS2_PLACEMENT_3D ( 'NONE', #19185, #139091, #115721 ) ;
#9035=CARTESIAN_POINT ( 'NONE',  ( -21.05000000000000071, 87.39257802171711376, -39.09705706435617856 ) ) ;
#9043=CARTESIAN_POINT ( 'NONE',  ( 18.52165635395192211, 85.48115071129370790, -62.49826990166167207 ) ) ;
#9047=DIRECTION ( 'NONE',  ( 0.000000000000000000, 6.982962677686266711E-15, -1.000000000000000000 ) ) ;
#9072=AXIS2_PLACEMENT_3D ( 'NONE', #86178, #187893, #225682 ) ;
#9109=LINE ( 'NONE', #247715, #165948 ) ;
#9112=AXIS2_PLACEMENT_3D ( 'NONE', #221239, #23086, #142976 ) ;
#9118=VERTEX_POINT ( 'NONE', #127606 ) ;
#9134=ORIENTED_EDGE ( 'NONE', *, *, #153128, .F. ) ;
#9152=CARTESIAN_POINT ( 'NONE',  ( 18.49999999999999289, 69.55000000001159322, -59.50608031408435039 ) ) ;
#9184=ORIENTED_EDGE ( 'NONE', *, *, #68451, .F. ) ;
#9252=CIRCLE ( 'NONE', #59099, 0.09999999999999939493 ) ;
#9256=CARTESIAN_POINT ( 'NONE',  ( 22.59999954896768770, 76.00882823225424545, -81.27361615859231847 ) ) ;
#9273=ORIENTED_EDGE ( 'NONE', *, *, #14604, .F. ) ;
#9295=DIRECTION ( 'NONE',  ( 0.000000000000000000, 0.000000000000000000, -1.000000000000000000 ) ) ;
#9299=EDGE_CURVE ( 'NONE', #97104, #223391, #157952, .T. ) ;
#9311=DIRECTION ( 'NONE',  ( 1.000000000000000000, -1.836970198721029934E-16, -1.601412966608202925E-30 ) ) ;
#9317=DIRECTION ( 'NONE',  ( 0.000000000000000000, -7.026728003956686545E-15, 1.000000000000000000 ) ) ;
#9328=EDGE_LOOP ( 'NONE', ( #42578, #202523 ) ) ;
#9333=ORIENTED_EDGE ( 'NONE', *, *, #192121, .F. ) ;
#9339=CARTESIAN_POINT ( 'NONE',  ( -20.94999999999999929, 76.00000000001165290, -69.52310748452431710 ) ) ;
#9343=ORIENTED_EDGE ( 'NONE', *, *, #33030, .T. ) ;
#9354=DIRECTION ( 'NONE',  ( 1.000000000000000000, -2.952720810173289112E-16, -2.061873921506763405E-30 ) ) ;
#9368=AXIS2_PLACEMENT_3D ( 'NONE', #122579, #109398, #69027 ) ;
#9398=ORIENTED_EDGE ( 'NONE', *, *, #204945, .T. ) ;
#9408=AXIS2_PLACEMENT_3D ( 'NONE', #213095, #18747, #239090 ) ;
#9431=ORIENTED_EDGE ( 'NONE', *, *, #244263, .T. ) ;
#9441=DIRECTION ( 'NONE',  ( 1.000000000000000000, 0.000000000000000000, 0.000000000000000000 ) ) ;
#9488=DIRECTION ( 'NONE',  ( -4.701977403289178058E-30, -2.433019743745433765E-14, 1.000000000000000000 ) ) ;
#9528=ADVANCED_FACE ( 'NONE', ( #194989 ), #77555, .F. ) ;
#9549=FACE_OUTER_BOUND ( 'NONE', #129348, .T. ) ;
#9556=AXIS2_PLACEMENT_3D ( 'NONE', #250747, #72137, #211643 ) ;
#9558=AXIS2_PLACEMENT_3D ( 'NONE', #183773, #82067, #62545 ) ;
#9570=DIRECTION ( 'NONE',  ( 2.952720810173289112E-16, 1.000000000000000000, 6.982962677686266711E-15 ) ) ;
#9634=CARTESIAN_POINT ( 'NONE',  ( -20.64999999999999858, 76.00000000001142553, -36.02310748452432421 ) ) ;
#9658=ORIENTED_EDGE ( 'NONE', *, *, #249757, .T. ) ;
#9659=DIRECTION ( 'NONE',  ( 2.952720810173289112E-16, 1.000000000000000000, 6.982962677686266711E-15 ) ) ;
#9672=DIRECTION ( 'NONE',  ( 1.000000000000000000, -3.265361837132813093E-16, -2.280189983783949500E-30 ) ) ;
#9693=EDGE_CURVE ( 'NONE', #17664, #122621, #141505, .T. ) ;
#9781=ORIENTED_EDGE ( 'NONE', *, *, #163943, .T. ) ;
#9782=CIRCLE ( 'NONE', #168063, 0.1000000000000052097 ) ;
#9802=CARTESIAN_POINT ( 'NONE',  ( -23.15000000000000213, 70.10000000001149090, -46.24220724918073699 ) ) ;
#9815=TOROIDAL_SURFACE ( 'NONE', #155614, 11.65000000000000036, 0.1000000000000000056 ) ;
#9818=AXIS2_PLACEMENT_3D ( 'NONE', #74855, #59068, #38269 ) ;
#9819=ORIENTED_EDGE ( 'NONE', *, *, #220508, .F. ) ;
#9825=DIRECTION ( 'NONE',  ( 0.000000000000000000, -0.8660254037844343777, 0.5000000000000074385 ) ) ;
#9833=VECTOR ( 'NONE', #220998, 1000.000000000000000 ) ;
#9842=CARTESIAN_POINT ( 'NONE',  ( -18.59999999999999787, 77.85102823015243700, -57.86919421510181394 ) ) ;
#9949=DIRECTION ( 'NONE',  ( 1.387778780781405791E-13, 0.9999176327611370985, 0.01283462868040226822 ) ) ;
#9962=ADVANCED_FACE ( 'NONE', ( #124031 ), #158059, .T. ) ;
#9979=CARTESIAN_POINT ( 'NONE',  ( -22.39999999999999858, 68.20922040163824818, -69.52310748452437394 ) ) ;
#9991=AXIS2_PLACEMENT_3D ( 'NONE', #226992, #167057, #246546 ) ;
#9993=CARTESIAN_POINT ( 'NONE',  ( -18.59999999999999787, 77.83585931145498193, -24.51866831572578320 ) ) ;
#10041=DIRECTION ( 'NONE',  ( 1.000000000000000000, -0.000000000000000000, 0.000000000000000000 ) ) ;
#10057=CIRCLE ( 'NONE', #205678, 0.1000000000000028644 ) ;
#10070=ORIENTED_EDGE ( 'NONE', *, *, #51696, .F. ) ;
#10086=AXIS2_PLACEMENT_3D ( 'NONE', #146980, #25774, #230389 ) ;
#10099=TOROIDAL_SURFACE ( 'NONE', #122742, 12.97499999999999787, 0.1000000000000000056 ) ;
#10109=VECTOR ( 'NONE', #178109, 1000.000000000000000 ) ;
#10172=EDGE_CURVE ( 'NONE', #252677, #188219, #58914, .T. ) ;
#10211=CIRCLE ( 'NONE', #89463, 0.09999999999999939493 ) ;
#10240=LINE ( 'NONE', #191467, #225751 ) ;
#10242=SPHERICAL_SURFACE ( 'NONE', #150511, 0.1000000000000000056 ) ;
#10275=CARTESIAN_POINT ( 'NONE',  ( 21.97500000000000497, 66.25000000001158185, -57.17310748452438673 ) ) ;
#10280=EDGE_CURVE ( 'NONE', #223901, #101690, #11805, .T. ) ;
#10318=CARTESIAN_POINT ( 'NONE',  ( 22.49066049874202022, 75.94365674847951198, -81.17311972204143444 ) ) ;
#10355=ORIENTED_EDGE ( 'NONE', *, *, #41256, .T. ) ;
#10385=CARTESIAN_POINT ( 'NONE',  ( -20.54999999999999716, 76.00000000001142553, -36.02310748452432421 ) ) ;
#10389=EDGE_CURVE ( 'NONE', #64792, #189058, #200594, .T. ) ;
#10415=EDGE_CURVE ( 'NONE', #56261, #106243, #251666, .T. ) ;
#10429=DIRECTION ( 'NONE',  ( 1.000000000000000000, 0.000000000000000000, 0.000000000000000000 ) ) ;
#10478=AXIS2_PLACEMENT_3D ( 'NONE', #116448, #39507, #154332 ) ;
#10502=AXIS2_PLACEMENT_3D ( 'NONE', #71961, #8133, #129353 ) ;
#10513=DIRECTION ( 'NONE',  ( 0.000000000000000000, -0.9876197685951265681, -0.1568667991644790149 ) ) ;
#10530=AXIS2_PLACEMENT_3D ( 'NONE', #14551, #54916, #130617 ) ;
#10532=ORIENTED_EDGE ( 'NONE', *, *, #18022, .F. ) ;
#10577=DIRECTION ( 'NONE',  ( -0.000000000000000000, 1.000000000000000000, 6.982962677686266711E-15 ) ) ;
#10592=CARTESIAN_POINT ( 'NONE',  ( 20.94999999999999929, 61.95000000001146390, -41.53680255528533394 ) ) ;
#10594=AXIS2_PLACEMENT_3D ( 'NONE', #92345, #75385, #117054 ) ;
#10601=DIRECTION ( 'NONE',  ( 0.000000000000000000, 0.000000000000000000, -1.000000000000000000 ) ) ;
#10619=DIRECTION ( 'NONE',  ( 0.000000000000000000, 0.000000000000000000, 1.000000000000000000 ) ) ;
#10624=CARTESIAN_POINT ( 'NONE',  ( 21.05000000000000071, 76.00000000001165290, -69.52310748452431710 ) ) ;
#10629=TOROIDAL_SURFACE ( 'NONE', #131417, 0.2000000000000000111, 0.1000000000000000056 ) ;
#10642=EDGE_LOOP ( 'NONE', ( #36682, #37007, #14049, #89140 ) ) ;
#10662=VECTOR ( 'NONE', #83402, 1000.000000000000000 ) ;
#10664=CARTESIAN_POINT ( 'NONE',  ( -20.54999999999999716, 71.65000000001151648, -48.27310748452435263 ) ) ;
#10667=CARTESIAN_POINT ( 'NONE',  ( -20.05000000000000426, 66.75000000001151079, -48.37310748452438247 ) ) ;
#10670=ORIENTED_EDGE ( 'NONE', *, *, #249757, .F. ) ;
#10695=DIRECTION ( 'NONE',  ( 0.000000000000000000, 1.000000000000000000, 7.116814260417668513E-15 ) ) ;
#10713=VERTEX_POINT ( 'NONE', #203247 ) ;
#10717=AXIS2_PLACEMENT_3D ( 'NONE', #34891, #111837, #15314 ) ;
#10720=DIRECTION ( 'NONE',  ( -1.000000000000000000, 2.952720810173289112E-16, 2.061873921506763405E-30 ) ) ;
#10749=ORIENTED_EDGE ( 'NONE', *, *, #187916, .F. ) ;
#10769=ORIENTED_EDGE ( 'NONE', *, *, #3527, .F. ) ;
#10822=ORIENTED_EDGE ( 'NONE', *, *, #137517, .F. ) ;
#10860=DIRECTION ( 'NONE',  ( 0.000000000000000000, -0.01562499999999307672, 0.9998779222360100194 ) ) ;
#10886=FACE_OUTER_BOUND ( 'NONE', #22043, .T. ) ;
#10926=DIRECTION ( 'NONE',  ( 1.000000000000000000, 0.000000000000000000, 0.000000000000000000 ) ) ;
#10930=CARTESIAN_POINT ( 'NONE',  ( 20.94999999999999929, 85.00000000001149658, -45.91707660717670336 ) ) ;
#11038=DIRECTION ( 'NONE',  ( 0.000000000000000000, 0.000000000000000000, 1.000000000000000000 ) ) ;
#11042=DIRECTION ( 'NONE',  ( 0.000000000000000000, 0.000000000000000000, 1.000000000000000000 ) ) ;
#11069=AXIS2_PLACEMENT_3D ( 'NONE', #193297, #231153, #94169 ) ;
#11071=CARTESIAN_POINT ( 'NONE',  ( -18.59999999999999787, 77.83585931145498193, -24.51866831572578675 ) ) ;
#11111=DIRECTION ( 'NONE',  ( 0.000000000000000000, 1.000000000000000000, 6.982962677686266711E-15 ) ) ;
#11123=CIRCLE ( 'NONE', #106787, 0.1000000000000028644 ) ;
#11129=CARTESIAN_POINT ( 'NONE',  ( -20.54999999999999716, 68.85000000001156195, -57.17310748452437252 ) ) ;
#11152=EDGE_LOOP ( 'NONE', ( #50765, #68084, #109767, #210658 ) ) ;
#11172=ADVANCED_FACE ( 'NONE', ( #132388 ), #155212, .T. ) ;
#11211=DIRECTION ( 'NONE',  ( 0.000000000000000000, 1.000000000000000000, 6.982962677686266711E-15 ) ) ;
#11222=DIRECTION ( 'NONE',  ( 0.000000000000000000, -1.000000000000000000, -6.982962677686265922E-15 ) ) ;
#11226=DIRECTION ( 'NONE',  ( 6.938893903907224433E-15, 1.000000000000000000, 7.272083257015735086E-15 ) ) ;
#11256=FACE_OUTER_BOUND ( 'NONE', #45772, .T. ) ;
#11268=ORIENTED_EDGE ( 'NONE', *, *, #50104, .T. ) ;
#11272=VERTEX_POINT ( 'NONE', #197480 ) ;
#11343=EDGE_CURVE ( 'NONE', #22150, #56972, #80298, .T. ) ;
#11359=ORIENTED_EDGE ( 'NONE', *, *, #257859, .T. ) ;
#11367=DIRECTION ( 'NONE',  ( 2.840903330521633255E-16, 0.8700118002898357128, -0.4930308989875171188 ) ) ;
#11401=ORIENTED_EDGE ( 'NONE', *, *, #87162, .T. ) ;
#11415=ORIENTED_EDGE ( 'NONE', *, *, #190407, .F. ) ;
#11439=FACE_OUTER_BOUND ( 'NONE', #227749, .T. ) ;
#11491=VECTOR ( 'NONE', #32700, 1000.000000000000000 ) ;
#11553=CIRCLE ( 'NONE', #69812, 4.049999999999998046 ) ;
#11561=CIRCLE ( 'NONE', #169796, 11.70000000000000284 ) ;
#11651=DIRECTION ( 'NONE',  ( 0.000000000000000000, -1.000000000000000000, -1.734723475976757554E-14 ) ) ;
#11654=ORIENTED_EDGE ( 'NONE', *, *, #5008, .F. ) ;
#11663=DIRECTION ( 'NONE',  ( -1.000000000000000000, 0.000000000000000000, 0.000000000000000000 ) ) ;
#11665=EDGE_CURVE ( 'NONE', #175343, #160781, #183735, .T. ) ;
#11725=FACE_OUTER_BOUND ( 'NONE', #56959, .T. ) ;
#11728=AXIS2_PLACEMENT_3D ( 'NONE', #86225, #207507, #186656 ) ;
#11749=EDGE_LOOP ( 'NONE', ( #254561, #92901, #49364, #38719 ) ) ;
#11783=FACE_OUTER_BOUND ( 'NONE', #78743, .T. ) ;
#11805=LINE ( 'NONE', #235945, #250474 ) ;
#11829=CARTESIAN_POINT ( 'NONE',  ( 22.47071067811865319, 68.27992525551361780, -69.62219993922698791 ) ) ;
#11853=ORIENTED_EDGE ( 'NONE', *, *, #5514, .F. ) ;
#11873=DIRECTION ( 'NONE',  ( 1.836970198721029934E-16, 1.000000000000000000, 6.982962677686266711E-15 ) ) ;
#11881=FACE_OUTER_BOUND ( 'NONE', #94670, .T. ) ;
#11904=CIRCLE ( 'NONE', #49480, 0.9750000000000036415 ) ;
#11930=EDGE_LOOP ( 'NONE', ( #37031, #81659, #142316, #75237 ) ) ;
#11953=VECTOR ( 'NONE', #31341, 1000.000000000000000 ) ;
#12034=EDGE_LOOP ( 'NONE', ( #45854, #190011, #234382, #60658, #57954, #130703, #178062, #200215, #222279, #72952, #48247, #168573, #231722, #169549 ) ) ;
#12040=VERTEX_POINT ( 'NONE', #21789 ) ;
#12052=CARTESIAN_POINT ( 'NONE',  ( -20.00857864376270001, 66.85000000001156195, -57.17310748452438673 ) ) ;
#12077=( BOUNDED_SURFACE ( )  B_SPLINE_SURFACE ( 3, 2, ( 
 ( #85502, #2141, #82939 ),
 ( #3422, #45134, #26884 ),
 ( #125938, #43858, #81654 ),
 ( #103796, #141662, #144214 ),
 ( #124679, #165080, #106367 ),
 ( #219919, #185925, #86808 ) ),
 .UNSPECIFIED., .F., .F., .F. ) 
 B_SPLINE_SURFACE_WITH_KNOTS ( ( 4, 2, 4 ),
 ( 3, 3 ),
 ( 4.712388980384689674, 5.497787143782137953, 6.283185307179586232 ),
 ( 0.000000000000000000, 1.000000000000000000 ),
 .UNSPECIFIED. ) 
 GEOMETRIC_REPRESENTATION_ITEM ( )  RATIONAL_B_SPLINE_SURFACE ( (
 ( 1.000000000000000000, 0.7071067811865475727, 1.000000000000000000),
 ( 1.000000000000000000, 0.7727932973491635771, 1.000000000000000000),
 ( 1.000000000000000000, 0.8282379607649708042, 1.000000000000000000),
 ( 1.000000000000000000, 0.9038128468039490215, 1.000000000000000000),
 ( 1.000000000000000000, 0.9240297172243560064, 1.000000000000000000),
 ( 1.000000000000000000, 0.9238795325112961754, 1.000000000000000000) ) ) 
 REPRESENTATION_ITEM ( '' )  SURFACE ( )  );
#12091=VECTOR ( 'NONE', #253039, 1000.000000000000000 ) ;
#12122=LINE ( 'NONE', #212871, #123644 ) ;
#12136=CARTESIAN_POINT ( 'NONE',  ( 23.14999999999999858, 76.00000000001142553, -36.02310748452432421 ) ) ;
#12168=DIRECTION ( 'NONE',  ( 0.000000000000000000, -6.997203936713171069E-15, 1.000000000000000000 ) ) ;
#12188=DIRECTION ( 'NONE',  ( -1.000000000000000000, 0.000000000000000000, 0.000000000000000000 ) ) ;
#12201=DIRECTION ( 'NONE',  ( -1.000000000000000000, 0.000000000000000000, -0.000000000000000000 ) ) ;
#12205=EDGE_CURVE ( 'NONE', #139895, #220391, #129846, .T. ) ;
#12255=CARTESIAN_POINT ( 'NONE',  ( 20.94999999999999574, 87.48912529308769592, -66.62310748452424036 ) ) ;
#12276=DIRECTION ( 'NONE',  ( 0.000000000000000000, 0.000000000000000000, 1.000000000000000000 ) ) ;
#12293=EDGE_CURVE ( 'NONE', #176232, #95340, #131139, .T. ) ;
#12321=CARTESIAN_POINT ( 'NONE',  ( 21.14999999999999858, 65.28660755661168480, -57.27310748452440237 ) ) ;
#12326=DIRECTION ( 'NONE',  ( 0.000000000000000000, -6.982962677686267499E-15, 1.000000000000000000 ) ) ;
#12327=FACE_OUTER_BOUND ( 'NONE', #95956, .T. ) ;
#12380=DIRECTION ( 'NONE',  ( 0.000000000000000000, 0.1298341882519953583, 0.9915357197604862671 ) ) ;
#12382=ORIENTED_EDGE ( 'NONE', *, *, #241375, .F. ) ;
#12394=VERTEX_POINT ( 'NONE', #22777 ) ;
#12409=AXIS2_PLACEMENT_3D ( 'NONE', #129138, #208692, #32644 ) ;
#12432=CARTESIAN_POINT ( 'NONE',  ( -23.15000000000000213, 64.35000000001146248, -43.03791325517834565 ) ) ;
#12453=ORIENTED_EDGE ( 'NONE', *, *, #169798, .T. ) ;
#12523=DIRECTION ( 'NONE',  ( 0.000000000000000000, 1.000000000000000000, 6.853228547068871147E-15 ) ) ;
#12559=SPHERICAL_SURFACE ( 'NONE', #245241, 0.1000000000000000056 ) ;
#12600=CARTESIAN_POINT ( 'NONE',  ( 18.50000000000000000, 65.50857864377418593, -44.77310748452439526 ) ) ;
#12606=TOROIDAL_SURFACE ( 'NONE', #145849, 12.77500000000000036, 0.1000000000000000056 ) ;
#12617=ORIENTED_EDGE ( 'NONE', *, *, #125244, .T. ) ;
#12622=DIRECTION ( 'NONE',  ( 0.000000000000000000, -6.982962677686267499E-15, 1.000000000000000000 ) ) ;
#12645=ADVANCED_FACE ( 'NONE', ( #226052 ), #130958, .T. ) ;
#12663=CARTESIAN_POINT ( 'NONE',  ( 22.50000000000000000, 75.90000000001172964, -81.27310748452431710 ) ) ;
#12684=DIRECTION ( 'NONE',  ( 0.000000000000000000, 6.997203936713167125E-15, -1.000000000000000000 ) ) ;
#12722=SPHERICAL_SURFACE ( 'NONE', #103852, 0.1000000000000000056 ) ;
#12732=ORIENTED_EDGE ( 'NONE', *, *, #33193, .F. ) ;
#12734=VERTEX_POINT ( 'NONE', #212950 ) ;
#12744=ORIENTED_EDGE ( 'NONE', *, *, #162371, .T. ) ;
#12750=LINE ( 'NONE', #92244, #48829 ) ;
#12751=CARTESIAN_POINT ( 'NONE',  ( -23.25000000000000000, 76.00000000001165290, -69.52310748452431710 ) ) ;
#12768=CYLINDRICAL_SURFACE ( 'NONE', #140794, 0.1000000000000052097 ) ;
#12785=ADVANCED_FACE ( 'NONE', ( #171307 ), #230943, .T. ) ;
#12814=EDGE_CURVE ( 'NONE', #214618, #65824, #97027, .T. ) ;
#12820=VECTOR ( 'NONE', #125973, 1000.000000000000000 ) ;
#12852=EDGE_LOOP ( 'NONE', ( #218466, #149517, #9819 ) ) ;
#12873=DIRECTION ( 'NONE',  ( 0.000000000000000000, -6.982962677686266711E-15, 1.000000000000000000 ) ) ;
#12897=CARTESIAN_POINT ( 'NONE',  ( -23.15000000000000213, 85.00000000001149658, -45.31707660717669484 ) ) ;
#12948=CARTESIAN_POINT ( 'NONE',  ( -23.15000000000000213, 74.00000000001151079, -49.24772940728643533 ) ) ;
#12951=ORIENTED_EDGE ( 'NONE', *, *, #152942, .T. ) ;
#12955=ORIENTED_EDGE ( 'NONE', *, *, #222690, .T. ) ;
#13003=LINE ( 'NONE', #151218, #6347 ) ;
#13035=ORIENTED_EDGE ( 'NONE', *, *, #41844, .T. ) ;
#13038=VERTEX_POINT ( 'NONE', #65418 ) ;
#13069=DIRECTION ( 'NONE',  ( -0.000000000000000000, 1.000000000000000000, 6.982962677686266711E-15 ) ) ;
#13116=EDGE_LOOP ( 'NONE', ( #75548, #222357, #1869, #171818, #134555, #54438, #55987, #148, #18985, #180811, #151187, #125310 ) ) ;
#13142=CARTESIAN_POINT ( 'NONE',  ( -23.15000000000000213, 87.65000000001144542, -39.12310748452424747 ) ) ;
#13178=CARTESIAN_POINT ( 'NONE',  ( 18.59999999999998721, 69.15387683765879956, -32.28538121767450519 ) ) ;
#13179=ORIENTED_EDGE ( 'NONE', *, *, #51733, .F. ) ;
#13192=EDGE_CURVE ( 'NONE', #148530, #113184, #151266, .T. ) ;
#13221=DIRECTION ( 'NONE',  ( 0.000000000000000000, 1.000000000000000000, 0.000000000000000000 ) ) ;
#13276=AXIS2_PLACEMENT_3D ( 'NONE', #211867, #71074, #150598 ) ;
#13283=DIRECTION ( 'NONE',  ( -1.000000000000000000, -0.000000000000000000, -0.000000000000000000 ) ) ;
#13343=LINE ( 'NONE', #212833, #73768 ) ;
#13351=DIRECTION ( 'NONE',  ( 0.000000000000000000, 0.000000000000000000, 1.000000000000000000 ) ) ;
#13382=ORIENTED_EDGE ( 'NONE', *, *, #11343, .T. ) ;
#13388=CARTESIAN_POINT ( 'NONE',  ( -23.15000000000000213, 71.65000000001155911, -57.27310748452435263 ) ) ;
#13423=ORIENTED_EDGE ( 'NONE', *, *, #154756, .F. ) ;
#13486=CARTESIAN_POINT ( 'NONE',  ( -21.14999999999999858, 64.35000000001166143, -69.52310748452440237 ) ) ;
#13494=DIRECTION ( 'NONE',  ( 1.000000000000000000, 0.000000000000000000, 0.000000000000000000 ) ) ;
#13533=CARTESIAN_POINT ( 'NONE',  ( 23.14999999999999503, 64.35000000001150511, -48.17310748452440095 ) ) ;
#13544=AXIS2_PLACEMENT_3D ( 'NONE', #100406, #159154, #19624 ) ;
#13552=DIRECTION ( 'NONE',  ( 1.000000000000000000, 0.000000000000000000, 0.000000000000000000 ) ) ;
#13557=CIRCLE ( 'NONE', #71833, 0.3999999999999975797 ) ;
#13565=VERTEX_POINT ( 'NONE', #234987 ) ;
#13573=ORIENTED_EDGE ( 'NONE', *, *, #99699, .T. ) ;
#13574=ORIENTED_EDGE ( 'NONE', *, *, #205213, .T. ) ;
#13641=CARTESIAN_POINT ( 'NONE',  ( -23.25000000000000000, 77.25000000001136868, -28.22262673010923351 ) ) ;
#13659=DIRECTION ( 'NONE',  ( 0.000000000000000000, 7.086529944415894657E-15, -1.000000000000000000 ) ) ;
#13665=DIRECTION ( 'NONE',  ( 1.000000000000000000, 0.000000000000000000, 0.000000000000000000 ) ) ;
#13685=DIRECTION ( 'NONE',  ( 3.469446951953728416E-14, 0.8660254037844343777, -0.5000000000000074385 ) ) ;
#13720=EDGE_CURVE ( 'NONE', #90111, #138795, #47525, .T. ) ;
#13758=CONICAL_SURFACE ( 'NONE', #197090, 4.049999999999998046, 0.7853981633974604915 ) ;
#13760=ORIENTED_EDGE ( 'NONE', *, *, #218439, .T. ) ;
#13777=ORIENTED_EDGE ( 'NONE', *, *, #70749, .T. ) ;
#13798=FACE_OUTER_BOUND ( 'NONE', #96112, .T. ) ;
#13831=DIRECTION ( 'NONE',  ( 0.000000000000000000, 0.4930308989875575865, 0.8700118002898125091 ) ) ;
#13834=AXIS2_PLACEMENT_3D ( 'NONE', #82703, #46175, #162297 ) ;
#13847=LINE ( 'NONE', #175507, #184028 ) ;
#13927=AXIS2_PLACEMENT_3D ( 'NONE', #46887, #147286, #126439 ) ;
#13957=CARTESIAN_POINT ( 'NONE',  ( -18.59999999999999787, 77.83585931145498193, -24.51866831572578320 ) ) ;
#13982=VERTEX_POINT ( 'NONE', #6432 ) ;
#13984=CARTESIAN_POINT ( 'NONE',  ( 20.94999999999999929, 76.00000000001142553, -36.02310748452432421 ) ) ;
#13987=CARTESIAN_POINT ( 'NONE',  ( 23.14999999999999858, 76.00000000001156764, -56.64810748452432421 ) ) ;
#13989=CYLINDRICAL_SURFACE ( 'NONE', #184957, 0.09999999999999939493 ) ;
#14016=CIRCLE ( 'NONE', #172641, 0.09999999999999939493 ) ;
#14019=CARTESIAN_POINT ( 'NONE',  ( 20.04142135623730070, 64.35000000001150511, -48.17310748452440095 ) ) ;
#14049=ORIENTED_EDGE ( 'NONE', *, *, #10415, .F. ) ;
#14062=ORIENTED_EDGE ( 'NONE', *, *, #23509, .F. ) ;
#14063=CARTESIAN_POINT ( 'NONE',  ( -23.15000000000000213, 64.35000000001150511, -48.17310748452440095 ) ) ;
#14116=DIRECTION ( 'NONE',  ( 0.000000000000000000, 0.000000000000000000, 1.000000000000000000 ) ) ;
#14145=AXIS2_PLACEMENT_3D ( 'NONE', #96872, #38237, #255933 ) ;
#14218=CARTESIAN_POINT ( 'NONE',  ( -22.48660254037843131, 64.25000000001163869, -69.57310748452438531 ) ) ;
#14223=CARTESIAN_POINT ( 'NONE',  ( -18.59999999999999787, 64.35000000001161879, -62.50830171387039513 ) ) ;
#14229=DIRECTION ( 'NONE',  ( 1.000000000000000000, 0.000000000000000000, 0.000000000000000000 ) ) ;
#14268=ORIENTED_EDGE ( 'NONE', *, *, #223551, .T. ) ;
#14275=ADVANCED_FACE ( 'NONE', ( #93675 ), #103052, .T. ) ;
#14292=ORIENTED_EDGE ( 'NONE', *, *, #18581, .T. ) ;
#14297=FACE_OUTER_BOUND ( 'NONE', #178465, .T. ) ;
#14309=EDGE_CURVE ( 'NONE', #47209, #106650, #235744, .T. ) ;
#14324=CARTESIAN_POINT ( 'NONE',  ( 18.39999999999999858, 85.68240343348777799, -29.36626410711146562 ) ) ;
#14356=CARTESIAN_POINT ( 'NONE',  ( -21.07928932188134041, 69.67148334361296236, -69.62200263017901136 ) ) ;
#14358=EDGE_CURVE ( 'NONE', #212829, #169291, #164456, .T. ) ;
#14379=FACE_OUTER_BOUND ( 'NONE', #184773, .T. ) ;
#14406=VERTEX_POINT ( 'NONE', #201754 ) ;
#14433=CARTESIAN_POINT ( 'NONE',  ( -23.15000000000000213, 76.00000000001162448, -65.47310748452431994 ) ) ;
#14457=EDGE_LOOP ( 'NONE', ( #108721, #95228, #4348, #10355 ) ) ;
#14483=ORIENTED_EDGE ( 'NONE', *, *, #119180, .F. ) ;
#14486=DIRECTION ( 'NONE',  ( -1.000000000000000000, 0.000000000000000000, 0.000000000000000000 ) ) ;
#14497=CARTESIAN_POINT ( 'NONE',  ( 23.24999999999999289, 64.35000000001173248, -81.27310748452440237 ) ) ;
#14502=VECTOR ( 'NONE', #184870, 1000.000000000000000 ) ;
#14506=VERTEX_POINT ( 'NONE', #68677 ) ;
#14510=EDGE_CURVE ( 'NONE', #200641, #69752, #164636, .T. ) ;
#14525=CARTESIAN_POINT ( 'NONE',  ( -23.25000000000000000, 77.14957036958705316, -28.20719500002235236 ) ) ;
#14548=DIRECTION ( 'NONE',  ( -1.000000000000000000, 0.000000000000000000, -0.000000000000000000 ) ) ;
#14550=AXIS2_PLACEMENT_3D ( 'NONE', #101078, #144094, #222335 ) ;
#14551=CARTESIAN_POINT ( 'NONE',  ( 23.14999999999999858, 78.10000000001141984, -36.02310748452431000 ) ) ;
#14575=B_SPLINE_CURVE_WITH_KNOTS ( 'NONE', 3,
 ( #141301, #104697, #60462, #39664, #4340, #223385, #202556 ),
 .UNSPECIFIED., .F., .F.,
 ( 4, 3, 4 ),
 ( 0.000000000000000000, 0.0007844235214594318627, 0.001767853679404347454 ),
 .UNSPECIFIED. ) ;
#14580=ORIENTED_EDGE ( 'NONE', *, *, #39894, .T. ) ;
#14604=EDGE_CURVE ( 'NONE', #177733, #79556, #2111, .T. ) ;
#14606=VERTEX_POINT ( 'NONE', #82436 ) ;
#14609=AXIS2_PLACEMENT_3D ( 'NONE', #9993, #149530, #210759 ) ;
#14636=ORIENTED_EDGE ( 'NONE', *, *, #119180, .T. ) ;
#14653=CARTESIAN_POINT ( 'NONE',  ( 21.13461538461538325, 67.11458296203710461, -57.17310748452437963 ) ) ;
#14658=EDGE_LOOP ( 'NONE', ( #256327, #254797, #49243, #3953 ) ) ;
#14659=ORIENTED_EDGE ( 'NONE', *, *, #240347, .F. ) ;
#14666=ORIENTED_EDGE ( 'NONE', *, *, #24736, .F. ) ;
#14717=DIRECTION ( 'NONE',  ( -0.000000000000000000, 0.1350103645451807555, 0.9908441862701610203 ) ) ;
#14736=CARTESIAN_POINT ( 'NONE',  ( -23.25000000000000000, 76.00000000001142553, -36.02310748452432421 ) ) ;
#14798=FACE_OUTER_BOUND ( 'NONE', #41506, .T. ) ;
#14801=CARTESIAN_POINT ( 'NONE',  ( -23.25000000000000000, 64.25000000001173817, -81.27310748452440237 ) ) ;
#14808=CARTESIAN_POINT ( 'NONE',  ( 18.49999999999999289, 64.25000000001173817, -81.27310748452440237 ) ) ;
#14820=DIRECTION ( 'NONE',  ( 0.000000000000000000, 1.000000000000000000, 6.982962677686266711E-15 ) ) ;
#14824=CIRCLE ( 'NONE', #85659, 2.000000000000001776 ) ;
#14838=DIRECTION ( 'NONE',  ( 0.000000000000000000, 0.000000000000000000, 1.000000000000000000 ) ) ;
#14839=LINE ( 'NONE', #116484, #168601 ) ;
#14849=LINE ( 'NONE', #209161, #97324 ) ;
#14861=ORIENTED_EDGE ( 'NONE', *, *, #141473, .F. ) ;
#14867=EDGE_CURVE ( 'NONE', #101132, #179727, #148063, .T. ) ;
#14873=DIRECTION ( 'NONE',  ( -2.978066053179069723E-16, -1.000000000000000000, -7.742971738265580590E-15 ) ) ;
#14878=ORIENTED_EDGE ( 'NONE', *, *, #157064, .T. ) ;
#14883=CARTESIAN_POINT ( 'NONE',  ( 21.22070241538126467, 75.90108096947668059, -75.99305375739393753 ) ) ;
#14888=FACE_OUTER_BOUND ( 'NONE', #11749, .T. ) ;
#14919=DIRECTION ( 'NONE',  ( -1.000000000000000000, -0.000000000000000000, -0.000000000000000000 ) ) ;
#14932=VECTOR ( 'NONE', #156281, 1000.000000000000000 ) ;
#14934=DIRECTION ( 'NONE',  ( 0.000000000000000000, -7.116814260417668513E-15, 1.000000000000000000 ) ) ;
#14959=ORIENTED_EDGE ( 'NONE', *, *, #91830, .T. ) ;
#14994=DIRECTION ( 'NONE',  ( 0.000000000000000000, 0.000000000000000000, 1.000000000000000000 ) ) ;
#14999=DIRECTION ( 'NONE',  ( -0.000000000000000000, 6.982962677686266711E-15, -1.000000000000000000 ) ) ;
#15000=FACE_OUTER_BOUND ( 'NONE', #11152, .T. ) ;
#15007=DIRECTION ( 'NONE',  ( 0.000000000000000000, -6.982962677686266711E-15, 1.000000000000000000 ) ) ;
#15024=CARTESIAN_POINT ( 'NONE',  ( 23.14999999999999503, 69.35000000001151932, -48.37310748452436826 ) ) ;
#15029=EDGE_CURVE ( 'NONE', #89321, #183814, #93891, .T. ) ;
#15070=CARTESIAN_POINT ( 'NONE',  ( 18.49999999999999289, 65.79142135624879018, -44.87310748452438958 ) ) ;
#15075=DIRECTION ( 'NONE',  ( -1.000000000000000000, -0.000000000000000000, -0.000000000000000000 ) ) ;
#15081=DIRECTION ( 'NONE',  ( 0.000000000000000000, -7.056502275159890832E-15, 1.000000000000000000 ) ) ;
#15087=AXIS2_PLACEMENT_3D ( 'NONE', #96320, #138014, #175906 ) ;
#15113=DIRECTION ( 'NONE',  ( 1.000000000000000000, 0.000000000000000000, 0.000000000000000000 ) ) ;
#15114=AXIS2_PLACEMENT_3D ( 'NONE', #51973, #75439, #135365 ) ;
#15139=ORIENTED_EDGE ( 'NONE', *, *, #184429, .T. ) ;
#15148=EDGE_CURVE ( 'NONE', #44661, #134285, #183833, .T. ) ;
#15177=ADVANCED_FACE ( 'NONE', ( #168169 ), #33791, .T. ) ;
#15182=EDGE_CURVE ( 'NONE', #218877, #230655, #206510, .T. ) ;
#15203=ORIENTED_EDGE ( 'NONE', *, *, #30436, .T. ) ;
#15232=CIRCLE ( 'NONE', #65291, 0.09999999999999939493 ) ;
#15262=ADVANCED_FACE ( 'NONE', ( #131564 ), #91644, .T. ) ;
#15268=ORIENTED_EDGE ( 'NONE', *, *, #71376, .F. ) ;
#15277=EDGE_LOOP ( 'NONE', ( #143142, #47800, #150012 ) ) ;
#15286=ORIENTED_EDGE ( 'NONE', *, *, #146992, .F. ) ;
#15300=AXIS2_PLACEMENT_3D ( 'NONE', #197183, #175112, #18561 ) ;
#15314=DIRECTION ( 'NONE',  ( 0.000000000000000000, 0.000000000000000000, -1.000000000000000000 ) ) ;
#15329=LINE ( 'NONE', #190101, #4985 ) ;
#15333=VECTOR ( 'NONE', #176717, 1000.000000000000000 ) ;
#15356=FACE_OUTER_BOUND ( 'NONE', #5740, .T. ) ;
#15384=VERTEX_POINT ( 'NONE', #182247 ) ;
#15403=AXIS2_PLACEMENT_3D ( 'NONE', #249150, #27556, #48356 ) ;
#15407=CIRCLE ( 'NONE', #2901, 0.1000000000000028644 ) ;
#15429=EDGE_CURVE ( 'NONE', #237026, #33150, #180962, .T. ) ;
#15441=ORIENTED_EDGE ( 'NONE', *, *, #71368, .T. ) ;
#15481=CARTESIAN_POINT ( 'NONE',  ( -18.47140463609787986, 85.67147468523226905, -29.35034702625017999 ) ) ;
#15499=ORIENTED_EDGE ( 'NONE', *, *, #19436, .F. ) ;
#15504=VECTOR ( 'NONE', #147285, 1000.000000000000000 ) ;
#15541=EDGE_CURVE ( 'NONE', #89873, #144828, #106901, .T. ) ;
#15598=EDGE_CURVE ( 'NONE', #116437, #70665, #50399, .T. ) ;
#15665=CIRCLE ( 'NONE', #148912, 12.87499999999999822 ) ;
#15724=LINE ( 'NONE', #196886, #135280 ) ;
#15732=CARTESIAN_POINT ( 'NONE',  ( -21.05000000000000071, 87.48912529308749697, -39.12310748452424747 ) ) ;
#15737=ORIENTED_EDGE ( 'NONE', *, *, #141405, .T. ) ;
#15739=ORIENTED_EDGE ( 'NONE', *, *, #234141, .T. ) ;
#15759=CIRCLE ( 'NONE', #182332, 0.09999999999999939493 ) ;
#15772=ORIENTED_EDGE ( 'NONE', *, *, #16495, .F. ) ;
#15782=ORIENTED_EDGE ( 'NONE', *, *, #102713, .T. ) ;
#15801=VECTOR ( 'NONE', #205231, 1000.000000000000000 ) ;
#15828=EDGE_CURVE ( 'NONE', #14606, #211829, #144063, .T. ) ;
#15840=ORIENTED_EDGE ( 'NONE', *, *, #189492, .F. ) ;
#15868=CIRCLE ( 'NONE', #49149, 0.5000000000000004441 ) ;
#15879=CARTESIAN_POINT ( 'NONE',  ( 18.39999999999999858, 85.50000000001161027, -62.49103808782458458 ) ) ;
#15904=ORIENTED_EDGE ( 'NONE', *, *, #8164, .T. ) ;
#15906=DIRECTION ( 'NONE',  ( 1.000000000000000000, -0.000000000000000000, 0.000000000000000000 ) ) ;
#15925=FACE_OUTER_BOUND ( 'NONE', #48088, .T. ) ;
#16001=LINE ( 'NONE', #255819, #125089 ) ;
#16025=FACE_OUTER_BOUND ( 'NONE', #65533, .T. ) ;
#16044=EDGE_LOOP ( 'NONE', ( #112107, #166714, #210141, #176270 ) ) ;
#16061=DIRECTION ( 'NONE',  ( 0.000000000000000000, 0.000000000000000000, -1.000000000000000000 ) ) ;
#16066=DIRECTION ( 'NONE',  ( -1.000000000000000000, -0.000000000000000000, -0.000000000000000000 ) ) ;
#16069=EDGE_LOOP ( 'NONE', ( #235286, #125234, #192212, #145513 ) ) ;
#16087=TOROIDAL_SURFACE ( 'NONE', #207606, 3.899999999999999467, 0.1000000000000000056 ) ;
#16106=CARTESIAN_POINT ( 'NONE',  ( 21.05000000000000071, 67.07338541492448769, -61.05142446530125966 ) ) ;
#16108=EDGE_CURVE ( 'NONE', #85480, #152615, #78658, .T. ) ;
#16126=EDGE_CURVE ( 'NONE', #28771, #40138, #28015, .T. ) ;
#16174=DIRECTION ( 'NONE',  ( 1.000000000000000000, 0.000000000000000000, 0.000000000000000000 ) ) ;
#16206=DIRECTION ( 'NONE',  ( 1.000000000000000000, -7.304098846218134667E-16, -5.100424963727256530E-30 ) ) ;
#16217=CARTESIAN_POINT ( 'NONE',  ( -23.25000000000000000, 69.01799029515495931, -32.32695536626808774 ) ) ;
#16253=EDGE_LOOP ( 'NONE', ( #125426, #79208, #58829, #247057 ) ) ;
#16263=CARTESIAN_POINT ( 'NONE',  ( 23.14999999999999503, 64.35000000001156195, -57.37310748452439668 ) ) ;
#16279=ORIENTED_EDGE ( 'NONE', *, *, #47004, .T. ) ;
#16290=CYLINDRICAL_SURFACE ( 'NONE', #144168, 0.09999999999999939493 ) ;
#16424=ORIENTED_EDGE ( 'NONE', *, *, #102616, .T. ) ;
#16427=DIRECTION ( 'NONE',  ( 0.000000000000000000, 7.026728003956683390E-15, -1.000000000000000000 ) ) ;
#16441=ORIENTED_EDGE ( 'NONE', *, *, #217433, .F. ) ;
#16442=EDGE_CURVE ( 'NONE', #56972, #196513, #115898, .T. ) ;
#16477=ORIENTED_EDGE ( 'NONE', *, *, #52348, .T. ) ;
#16495=EDGE_CURVE ( 'NONE', #239369, #64016, #144867, .T. ) ;
#16502=EDGE_CURVE ( 'NONE', #124577, #144086, #51763, .T. ) ;
#16513=AXIS2_PLACEMENT_3D ( 'NONE', #6470, #166877, #127721 ) ;
#16531=DIRECTION ( 'NONE',  ( 1.000000000000000000, 0.000000000000000000, 0.000000000000000000 ) ) ;
#16535=ORIENTED_EDGE ( 'NONE', *, *, #166951, .F. ) ;
#16551=EDGE_CURVE ( 'NONE', #115457, #174034, #186596, .T. ) ;
#16563=DIRECTION ( 'NONE',  ( 1.000000000000000000, 0.000000000000000000, 0.000000000000000000 ) ) ;
#16635=CARTESIAN_POINT ( 'NONE',  ( -21.55000000000000071, 68.65000000001157332, -57.27310748452437394 ) ) ;
#16650=FACE_OUTER_BOUND ( 'NONE', #194230, .T. ) ;
#16709=DIRECTION ( 'NONE',  ( 0.000000000000000000, 7.109473446599835262E-15, -1.000000000000000000 ) ) ;
#16741=VERTEX_POINT ( 'NONE', #179423 ) ;
#16746=FACE_OUTER_BOUND ( 'NONE', #110335, .T. ) ;
#16757=DIRECTION ( 'NONE',  ( -1.000000000000000000, 0.000000000000000000, -0.000000000000000000 ) ) ;
#16764=EDGE_CURVE ( 'NONE', #112286, #25147, #194788, .T. ) ;
#16769=CARTESIAN_POINT ( 'NONE',  ( -18.39999999999999858, 85.50000000001138289, -29.42291809330222563 ) ) ;
#16778=TOROIDAL_SURFACE ( 'NONE', #29271, 11.65000000000000036, 0.1000000000000000056 ) ;
#16788=EDGE_LOOP ( 'NONE', ( #216731, #246363, #145209, #216619 ) ) ;
#16796=ORIENTED_EDGE ( 'NONE', *, *, #139595, .F. ) ;
#16815=ORIENTED_EDGE ( 'NONE', *, *, #30240, .T. ) ;
#16818=EDGE_LOOP ( 'NONE', ( #214245, #94111, #167259 ) ) ;
#16823=DIRECTION ( 'NONE',  ( 0.000000000000000000, 6.982962677686266711E-15, -1.000000000000000000 ) ) ;
#16857=DIRECTION ( 'NONE',  ( 0.000000000000000000, 6.982962677686267499E-15, -1.000000000000000000 ) ) ;
#16862=ORIENTED_EDGE ( 'NONE', *, *, #70304, .F. ) ;
#16877=EDGE_CURVE ( 'NONE', #112680, #53080, #236450, .T. ) ;
#16883=CARTESIAN_POINT ( 'NONE',  ( -23.25000000000000000, 77.16412189325258453, -28.10825939895270764 ) ) ;
#16887=EDGE_CURVE ( 'NONE', #29497, #84837, #244702, .T. ) ;
#16894=EDGE_LOOP ( 'NONE', ( #14878, #131398, #60078, #189232 ) ) ;
#16904=FACE_OUTER_BOUND ( 'NONE', #226858, .T. ) ;
#16921=CARTESIAN_POINT ( 'NONE',  ( -23.25000000000000000, 87.48912529308749697, -39.12310748452424747 ) ) ;
#16960=DIRECTION ( 'NONE',  ( 0.000000000000000000, 6.982962677686266711E-15, -1.000000000000000000 ) ) ;
#16972=DIRECTION ( 'NONE',  ( -1.000000000000000000, -0.000000000000000000, -0.000000000000000000 ) ) ;
#16980=ORIENTED_EDGE ( 'NONE', *, *, #68251, .F. ) ;
#16992=CARTESIAN_POINT ( 'NONE',  ( 18.50000972452444969, 65.70673848566912056, -30.56382523348295166 ) ) ;
#17003=CYLINDRICAL_SURFACE ( 'NONE', #106109, 0.1000000000000028644 ) ;
#17021=ORIENTED_EDGE ( 'NONE', *, *, #115871, .F. ) ;
#17059=CARTESIAN_POINT ( 'NONE',  ( 23.25000000000000000, 87.75000000001156764, -57.37310748452424036 ) ) ;
#17070=EDGE_CURVE ( 'NONE', #160725, #64945, #95179, .T. ) ;
#17075=EDGE_CURVE ( 'NONE', #43683, #22150, #82399, .T. ) ;
#17080=EDGE_LOOP ( 'NONE', ( #86014, #212746, #249986, #79210 ) ) ;
#17086=CARTESIAN_POINT ( 'NONE',  ( -23.25000000000000000, 64.35000000001173248, -81.27310748452440237 ) ) ;
#17108=ORIENTED_EDGE ( 'NONE', *, *, #244393, .F. ) ;
#17127=EDGE_LOOP ( 'NONE', ( #141531, #25257, #194479, #156056 ) ) ;
#17144=CIRCLE ( 'NONE', #95645, 0.1000000000000028644 ) ;
#17160=CARTESIAN_POINT ( 'NONE',  ( 23.14999999999999858, 76.00000000001142553, -36.02310748452432421 ) ) ;
#17177=TOROIDAL_SURFACE ( 'NONE', #179498, 2.100000000000002309, 0.1000000000000000056 ) ;
#17199=ADVANCED_FACE ( 'NONE', ( #64321 ), #115841, .F. ) ;
#17205=EDGE_LOOP ( 'NONE', ( #51320, #169501, #101134 ) ) ;
#17254=EDGE_CURVE ( 'NONE', #38617, #201868, #149187, .T. ) ;
#17260=ORIENTED_EDGE ( 'NONE', *, *, #138465, .F. ) ;
#17264=CARTESIAN_POINT ( 'NONE',  ( 19.88284271247461987, 64.30857864377418309, -44.77310748452440237 ) ) ;
#17320=EDGE_LOOP ( 'NONE', ( #221282, #67946, #155969, #165082, #180171, #192692 ) ) ;
#17342=DIRECTION ( 'NONE',  ( 0.000000000000000000, 1.000000000000000000, 6.853228547068871147E-15 ) ) ;
#17360=EDGE_LOOP ( 'NONE', ( #243242, #146343, #104824 ) ) ;
#17395=DIRECTION ( 'NONE',  ( 0.000000000000000000, 0.000000000000000000, -1.000000000000000000 ) ) ;
#17397=CARTESIAN_POINT ( 'NONE',  ( -18.60000000000000142, 85.32100840337290037, -62.28716923544637751 ) ) ;
#17452=CIRCLE ( 'NONE', #163213, 11.79999999999999716 ) ;
#17468=CARTESIAN_POINT ( 'NONE',  ( -21.65000000000000213, 68.25000000001158185, -57.17310748452437963 ) ) ;
#17507=CARTESIAN_POINT ( 'NONE',  ( -23.15000000000000213, 64.25000000001146816, -42.86470817442146597 ) ) ;
#17524=DIRECTION ( 'NONE',  ( 1.000000000000000000, -3.265361837132813093E-16, -2.280189983783949500E-30 ) ) ;
#17537=DIRECTION ( 'NONE',  ( -0.000000000000000000, 6.982962677686266711E-15, -1.000000000000000000 ) ) ;
#17555=CARTESIAN_POINT ( 'NONE',  ( 18.59999999999999076, 65.79142135624880439, -48.17310748452439384 ) ) ;
#17592=FACE_OUTER_BOUND ( 'NONE', #59569, .T. ) ;
#17607=DIRECTION ( 'NONE',  ( 0.000000000000000000, -1.000000000000000000, -6.982962677686266711E-15 ) ) ;
#17608=ORIENTED_EDGE ( 'NONE', *, *, #91212, .T. ) ;
#17626=AXIS2_PLACEMENT_3D ( 'NONE', #121934, #3239, #144038 ) ;
#17643=VERTEX_POINT ( 'NONE', #87419 ) ;
#17660=CARTESIAN_POINT ( 'NONE',  ( -20.94999999999999929, 87.29603075034691528, -66.47520832486038955 ) ) ;
#17664=VERTEX_POINT ( 'NONE', #49593 ) ;
#17677=DIRECTION ( 'NONE',  ( 1.000000000000000000, 0.000000000000000000, 0.000000000000000000 ) ) ;
#17722=VERTEX_POINT ( 'NONE', #191705 ) ;
#17732=FACE_OUTER_BOUND ( 'NONE', #21279, .T. ) ;
#17744=VERTEX_POINT ( 'NONE', #153881 ) ;
#17748=CARTESIAN_POINT ( 'NONE',  ( 21.05000000000000071, 67.17357026049440094, -61.10905277158068571 ) ) ;
#17764=EDGE_LOOP ( 'NONE', ( #182018, #167033, #82234, #6838 ) ) ;
#17792=ADVANCED_FACE ( 'NONE', ( #232099 ), #114698, .T. ) ;
#17799=FACE_OUTER_BOUND ( 'NONE', #68499, .T. ) ;
#17813=CARTESIAN_POINT ( 'NONE',  ( -21.05000000000000071, 77.16270174994961906, -61.42310748452431568 ) ) ;
#17828=FACE_OUTER_BOUND ( 'NONE', #86726, .T. ) ;
#17865=CARTESIAN_POINT ( 'NONE',  ( -18.39999999999999858, 85.50000000001138289, -29.42291809330221497 ) ) ;
#17888=EDGE_CURVE ( 'NONE', #171894, #244003, #169597, .T. ) ;
#17905=DIRECTION ( 'NONE',  ( 1.000000000000000000, 0.000000000000000000, 0.000000000000000000 ) ) ;
#17920=DIRECTION ( 'NONE',  ( 0.000000000000000000, -6.982962677686266711E-15, 1.000000000000000000 ) ) ;
#17934=DIRECTION ( 'NONE',  ( 1.000000000000000000, 0.000000000000000000, 0.000000000000000000 ) ) ;
#17958=ORIENTED_EDGE ( 'NONE', *, *, #73826, .T. ) ;
#17971=AXIS2_PLACEMENT_3D ( 'NONE', #21598, #101061, #68416 ) ;
#17980=CARTESIAN_POINT ( 'NONE',  ( -21.03571358705830718, 64.25000000001162448, -62.69800066246598647 ) ) ;
#18009=VECTOR ( 'NONE', #92936, 1000.000000000000000 ) ;
#18022=EDGE_CURVE ( 'NONE', #251754, #59275, #208376, .T. ) ;
#18029=CARTESIAN_POINT ( 'NONE',  ( -22.50000000000000000, 76.00000000001165290, -69.52310748452431710 ) ) ;
#18035=CARTESIAN_POINT ( 'NONE',  ( -22.57320508075686405, 64.25000000001163869, -69.52310748452435973 ) ) ;
#18060=ORIENTED_EDGE ( 'NONE', *, *, #178854, .T. ) ;
#18068=CIRCLE ( 'NONE', #76898, 0.1000000000000052097 ) ;
#18090=VERTEX_POINT ( 'NONE', #164100 ) ;
#18115=EDGE_CURVE ( 'NONE', #182718, #81112, #174414, .T. ) ;
#18151=EDGE_CURVE ( 'NONE', #193539, #22349, #145030, .T. ) ;
#18153=AXIS2_PLACEMENT_3D ( 'NONE', #84286, #79199, #120944 ) ;
#18173=CARTESIAN_POINT ( 'NONE',  ( 22.47007471830797343, 68.27928934808518591, -69.52310748452437394 ) ) ;
#18189=CARTESIAN_POINT ( 'NONE',  ( 18.39999999999999858, 85.60000000001137721, -29.32291809330221355 ) ) ;
#18219=CARTESIAN_POINT ( 'NONE',  ( -18.59999999999999787, 70.65875701002006792, -79.32975769101238939 ) ) ;
#18259=CARTESIAN_POINT ( 'NONE',  ( 18.55121869061587958, 65.67252876774480796, -30.44570419949946327 ) ) ;
#18268=CARTESIAN_POINT ( 'NONE',  ( -18.50000000000000000, 66.65000000001157332, -57.17310748452438673 ) ) ;
#18280=CARTESIAN_POINT ( 'NONE',  ( 18.31572054635712732, 85.54847543579028013, -29.17253731977572428 ) ) ;
#18281=AXIS2_PLACEMENT_3D ( 'NONE', #112052, #48204, #211137 ) ;
#18321=CARTESIAN_POINT ( 'NONE',  ( -20.94999999999999929, 87.39257802171711376, -39.09705706435617856 ) ) ;
#18336=CARTESIAN_POINT ( 'NONE',  ( 23.14999999999999858, 76.00000000001145395, -40.02310748452431710 ) ) ;
#18368=CARTESIAN_POINT ( 'NONE',  ( -18.59999999999999787, 76.00000000001165290, -69.52310748452431710 ) ) ;
#18392=ORIENTED_EDGE ( 'NONE', *, *, #26052, .T. ) ;
#18402=DIRECTION ( 'NONE',  ( 1.000000000000000000, 0.000000000000000000, 0.000000000000000000 ) ) ;
#18411=EDGE_CURVE ( 'NONE', #218484, #176547, #253184, .T. ) ;
#18417=DIRECTION ( 'NONE',  ( 0.000000000000000000, 1.000000000000000000, 6.938893903907222067E-15 ) ) ;
#18433=CARTESIAN_POINT ( 'NONE',  ( 21.98333005346336932, 76.00000000001170974, -76.89718281358098295 ) ) ;
#18438=CIRCLE ( 'NONE', #118213, 0.09999999999999939493 ) ;
#18489=AXIS2_PLACEMENT_3D ( 'NONE', #48057, #70225, #250116 ) ;
#18490=EDGE_LOOP ( 'NONE', ( #35116, #167739, #162359, #148289 ) ) ;
#18499=CARTESIAN_POINT ( 'NONE',  ( -20.54999999999999716, 74.05981308412370367, -56.69398827347101388 ) ) ;
#18530=CIRCLE ( 'NONE', #222694, 0.1000000000000028644 ) ;
#18561=DIRECTION ( 'NONE',  ( 0.000000000000000000, 1.000000000000000000, 6.608470384673536824E-15 ) ) ;
#18571=AXIS2_PLACEMENT_3D ( 'NONE', #98905, #123650, #239743 ) ;
#18575=CYLINDRICAL_SURFACE ( 'NONE', #128105, 0.09999999999999939493 ) ;
#18581=EDGE_CURVE ( 'NONE', #184441, #61365, #253377, .T. ) ;
#18592=ORIENTED_EDGE ( 'NONE', *, *, #133197, .F. ) ;
#18607=DIRECTION ( 'NONE',  ( -1.000000000000000000, -0.000000000000000000, -0.000000000000000000 ) ) ;
#18619=LINE ( 'NONE', #153033, #184692 ) ;
#18633=AXIS2_PLACEMENT_3D ( 'NONE', #179316, #77592, #39813 ) ;
#18645=CIRCLE ( 'NONE', #68719, 11.80000000000000426 ) ;
#18646=EDGE_LOOP ( 'NONE', ( #214146, #127453, #180429, #134608 ) ) ;
#18680=CARTESIAN_POINT ( 'NONE',  ( -18.46946985241262240, 85.50931722872306295, -62.53644491902446134 ) ) ;
#18700=EDGE_LOOP ( 'NONE', ( #145452, #203947, #131846, #245793 ) ) ;
#18703=ORIENTED_EDGE ( 'NONE', *, *, #169765, .T. ) ;
#18704=ADVANCED_FACE ( 'NONE', ( #50888 ), #16087, .T. ) ;
#18747=DIRECTION ( 'NONE',  ( 1.000000000000000000, -2.952720810173289112E-16, -2.061873921506763405E-30 ) ) ;
#18818=FACE_OUTER_BOUND ( 'NONE', #199780, .T. ) ;
#18827=CARTESIAN_POINT ( 'NONE',  ( -22.37643362114956957, 75.90091862633033770, -77.14889747848272350 ) ) ;
#18832=ORIENTED_EDGE ( 'NONE', *, *, #163849, .T. ) ;
#18836=AXIS2_PLACEMENT_3D ( 'NONE', #25087, #4196, #198551 ) ;
#18840=CARTESIAN_POINT ( 'NONE',  ( 22.45305468355010703, 76.10085836911147794, -81.27267460801404297 ) ) ;
#18859=DIRECTION ( 'NONE',  ( 1.000000000000000000, 0.000000000000000000, 0.000000000000000000 ) ) ;
#18874=CARTESIAN_POINT ( 'NONE',  ( -18.59999999999999787, 66.65000000001150227, -48.17310748452438673 ) ) ;
#18877=CARTESIAN_POINT ( 'NONE',  ( 18.49999999999999289, 64.35000000001173248, -81.27310748452440237 ) ) ;
#18958=CARTESIAN_POINT ( 'NONE',  ( -20.85000000000000142, 76.00000000001142553, -36.02310748452432421 ) ) ;
#18964=DIRECTION ( 'NONE',  ( 0.000000000000000000, 0.000000000000000000, 1.000000000000000000 ) ) ;
#18985=ORIENTED_EDGE ( 'NONE', *, *, #251384, .T. ) ;
#19003=ADVANCED_FACE ( 'NONE', ( #25922 ), #165435, .T. ) ;
#19012=EDGE_CURVE ( 'NONE', #202965, #57945, #24649, .T. ) ;
#19015=CARTESIAN_POINT ( 'NONE',  ( 23.15000000000000213, 84.59626168225457832, -60.07297996737398194 ) ) ;
#19025=CIRCLE ( 'NONE', #6553, 0.5000000000000004441 ) ;
#19026=AXIS2_PLACEMENT_3D ( 'NONE', #130804, #36886, #53844 ) ;
#19035=TOROIDAL_SURFACE ( 'NONE', #160736, 0.4000000000000015210, 0.1000000000000000056 ) ;
#19061=VECTOR ( 'NONE', #47831, 1000.000000000000000 ) ;
#19082=CYLINDRICAL_SURFACE ( 'NONE', #233673, 0.09999999999999939493 ) ;
#19097=ADVANCED_FACE ( 'NONE', ( #192693 ), #152305, .F. ) ;
#19106=AXIS2_PLACEMENT_3D ( 'NONE', #132661, #167960, #248758 ) ;
#19117=EDGE_CURVE ( 'NONE', #121991, #68040, #87140, .T. ) ;
#19124=AXIS2_PLACEMENT_3D ( 'NONE', #28832, #181452, #82300 ) ;
#19157=DIRECTION ( 'NONE',  ( 3.469446951953635015E-14, 6.982962677686266711E-15, -1.000000000000000000 ) ) ;
#19163=DIRECTION ( 'NONE',  ( 0.7071359030027593029, 0.7070776581709197206, 0.000000000000000000 ) ) ;
#19185=CARTESIAN_POINT ( 'NONE',  ( 20.94999999999999929, 67.22371710471909978, -57.37310748452438247 ) ) ;
#19220=CARTESIAN_POINT ( 'NONE',  ( -21.05000000000000071, 75.94867256767035713, -75.82329082079064619 ) ) ;
#19253=ORIENTED_EDGE ( 'NONE', *, *, #183217, .T. ) ;
#19274=CARTESIAN_POINT ( 'NONE',  ( -20.94999999999999929, 64.25000000001161027, -62.68150679462727481 ) ) ;
#19280=CARTESIAN_POINT ( 'NONE',  ( -21.05000000000000071, 87.39257802171731271, -66.44915790469229933 ) ) ;
#19281=EDGE_CURVE ( 'NONE', #22150, #111790, #77854, .T. ) ;
#19291=ORIENTED_EDGE ( 'NONE', *, *, #169031, .F. ) ;
#19315=CARTESIAN_POINT ( 'NONE',  ( -18.41809261886929860, 85.68240331476805238, -29.36626393443318861 ) ) ;
#19342=CARTESIAN_POINT ( 'NONE',  ( -23.15000000000000213, 74.00000000001151079, -49.24772940728643533 ) ) ;
#19353=EDGE_CURVE ( 'NONE', #161516, #233936, #107695, .T. ) ;
#19378=DIRECTION ( 'NONE',  ( 0.000000000000000000, -6.853228547068871147E-15, 1.000000000000000000 ) ) ;
#19382=CARTESIAN_POINT ( 'NONE',  ( -21.05000000000000071, 76.00000000001142553, -36.02310748452432421 ) ) ;
#19384=LINE ( 'NONE', #200580, #168188 ) ;
#19407=LINE ( 'NONE', #181060, #236200 ) ;
#19408=VECTOR ( 'NONE', #223418, 1000.000000000000000 ) ;
#19417=CARTESIAN_POINT ( 'NONE',  ( 23.15000000000000213, 84.66355140188063899, -45.54720860259157433 ) ) ;
#19436=EDGE_CURVE ( 'NONE', #227579, #170828, #46100, .T. ) ;
#19458=CARTESIAN_POINT ( 'NONE',  ( -21.05000000000000071, 87.48912529308769592, -66.62310748452424036 ) ) ;
#19461=FACE_OUTER_BOUND ( 'NONE', #45408, .T. ) ;
#19466=CYLINDRICAL_SURFACE ( 'NONE', #121755, 0.5000000000000004441 ) ;
#19499=AXIS2_PLACEMENT_3D ( 'NONE', #162204, #102166, #159616 ) ;
#19501=CIRCLE ( 'NONE', #194306, 0.1000000000000028644 ) ;
#19511=EDGE_LOOP ( 'NONE', ( #79472, #45987, #132900, #20620 ) ) ;
#19524=CARTESIAN_POINT ( 'NONE',  ( -23.15000000000000213, 76.00000000001142553, -36.02310748452432421 ) ) ;
#19552=CARTESIAN_POINT ( 'NONE',  ( 20.94403535211772294, 65.69367753730607262, -30.51892380663481674 ) ) ;
#19568=VERTEX_POINT ( 'NONE', #133678 ) ;
#19578=CARTESIAN_POINT ( 'NONE',  ( 18.39999999999999858, 85.50000000001136868, -29.42291809330220786 ) ) ;
#19613=FACE_OUTER_BOUND ( 'NONE', #178671, .T. ) ;
#19622=ORIENTED_EDGE ( 'NONE', *, *, #207522, .T. ) ;
#19624=DIRECTION ( 'NONE',  ( 0.000000000000000000, 0.000000000000000000, -1.000000000000000000 ) ) ;
#19639=CARTESIAN_POINT ( 'NONE',  ( -18.50000000000000000, 85.40000000001160174, -62.22584772486096938 ) ) ;
#19650=CARTESIAN_POINT ( 'NONE',  ( 20.94999999999999929, 70.60000000001151932, -48.42837350343745584 ) ) ;
#19759=DIRECTION ( 'NONE',  ( -0.000000000000000000, 1.000000000000000000, 6.982962677686266711E-15 ) ) ;
#19780=DIRECTION ( 'NONE',  ( 1.000000000000000000, 0.000000000000000000, 0.000000000000000000 ) ) ;
#19799=DIRECTION ( 'NONE',  ( -1.000000000000000000, 0.000000000000000000, 0.000000000000000000 ) ) ;
#19805=CARTESIAN_POINT ( 'NONE',  ( -20.54999999999999716, 87.75000000001151079, -48.37310748452424036 ) ) ;
#19861=CIRCLE ( 'NONE', #86447, 0.1000000000000028644 ) ;
#19867=ORIENTED_EDGE ( 'NONE', *, *, #44203, .T. ) ;
#19868=CARTESIAN_POINT ( 'NONE',  ( 23.14999999999999858, 72.00000000001141132, -36.02310748452435263 ) ) ;
#19875=CARTESIAN_POINT ( 'NONE',  ( -20.94999999999999929, 61.95000000001162022, -64.00941241376342816 ) ) ;
#19908=LINE ( 'NONE', #79837, #224042 ) ;
#19909=AXIS2_PLACEMENT_3D ( 'NONE', #209200, #228787, #68418 ) ;
#19923=FACE_OUTER_BOUND ( 'NONE', #58175, .T. ) ;
#19955=LINE ( 'NONE', #116476, #204122 ) ;
#19966=DIRECTION ( 'NONE',  ( 0.000000000000000000, -7.147358527629762208E-15, 1.000000000000000000 ) ) ;
#19982=CARTESIAN_POINT ( 'NONE',  ( -18.58693740092132884, 85.40643215026457824, -62.39829102802289640 ) ) ;
#19999=ORIENTED_EDGE ( 'NONE', *, *, #99913, .T. ) ;
#20001=AXIS2_PLACEMENT_3D ( 'NONE', #80381, #19157, #82946 ) ;
#20007=VECTOR ( 'NONE', #151775, 1000.000000000000000 ) ;
#20043=DIRECTION ( 'NONE',  ( 0.000000000000000000, -0.7397360091702802620, 0.6728971962616779878 ) ) ;
#20044=EDGE_LOOP ( 'NONE', ( #171747, #128100 ) ) ;
#20047=TOROIDAL_SURFACE ( 'NONE', #36639, 12.97499999999999787, 0.1000000000000000056 ) ;
#20057=DIRECTION ( 'NONE',  ( -1.000000000000000000, -0.000000000000000000, -0.000000000000000000 ) ) ;
#20066=( BOUNDED_SURFACE ( )  B_SPLINE_SURFACE ( 3, 2, ( 
 ( #76078, #100737, #21278 ),
 ( #196041, #176487, #160788 ),
 ( #61657, #159486, #18680 ),
 ( #156931, #38252, #237727 ),
 ( #198590, #136027, #199901 ),
 ( #59051, #220730, #19982 ),
 ( #99468, #116501, #42115 ),
 ( #155658, #56495, #17397 ) ),
 .UNSPECIFIED., .F., .F., .T. ) 
 B_SPLINE_SURFACE_WITH_KNOTS ( ( 4, 2, 2, 4 ),
 ( 3, 3 ),
 ( 0.0001723339234021441008, 0.0002782939632049910138, 0.0003842540030078378998, 0.0005961740826135316718 ),
 ( 0.000000000000000000, 1.000000000000000000 ),
 .UNSPECIFIED. ) 
 GEOMETRIC_REPRESENTATION_ITEM ( )  RATIONAL_B_SPLINE_SURFACE ( (
 ( 1.000000000000000000, 0.9504532311154639812, 1.000000000000000000),
 ( 1.000000000000000000, 0.9506023220709097776, 1.000000000000000000),
 ( 1.000000000000000000, 0.9395774818182517363, 1.000000000000000000),
 ( 1.000000000000000000, 0.9079328464645827212, 1.000000000000000000),
 ( 1.000000000000000000, 0.8875702416206650014, 1.000000000000000000),
 ( 1.000000000000000000, 0.8205919608037296475, 1.000000000000000000),
 ( 1.000000000000000000, 0.7666842783600821276, 1.000000000000000000),
 ( 1.000000000000000000, 0.7071067811864313324, 1.000000000000000000) ) ) 
 REPRESENTATION_ITEM ( '' )  SURFACE ( )  );
#20089=CARTESIAN_POINT ( 'NONE',  ( -21.14999999999999858, 76.00000000001165290, -69.52310748452431710 ) ) ;
#20095=DIRECTION ( 'NONE',  ( 0.000000000000000000, 6.982962677686266711E-15, -1.000000000000000000 ) ) ;
#20110=ADVANCED_FACE ( 'NONE', ( #120276 ), #18575, .T. ) ;
#20132=CARTESIAN_POINT ( 'NONE',  ( -22.47071067811865319, 75.90090754530910999, -77.24318222902238062 ) ) ;
#20137=CARTESIAN_POINT ( 'NONE',  ( -21.05000000000000071, 76.10000000001174669, -81.17310748452432279 ) ) ;
#20149=CIRCLE ( 'NONE', #165909, 0.1000000000000028644 ) ;
#20163=VECTOR ( 'NONE', #225616, 1000.000000000000000 ) ;
#20171=CARTESIAN_POINT ( 'NONE',  ( 21.05000000000000071, 67.22371710471909978, -57.37310748452438247 ) ) ;
#20179=DIRECTION ( 'NONE',  ( 0.000000000000000000, 1.000000000000000000, 6.982962677686266711E-15 ) ) ;
#20199=DIRECTION ( 'NONE',  ( 0.000000000000000000, -0.9999631594459057471, 0.008583690987121077309 ) ) ;
#20211=DIRECTION ( 'NONE',  ( 0.000000000000000000, 6.982962677686266711E-15, -1.000000000000000000 ) ) ;
#20212=PLANE ( 'NONE',  #141368 ) ;
#20226=VECTOR ( 'NONE', #239192, 1000.000000000000000 ) ;
#20251=DIRECTION ( 'NONE',  ( 0.000000000000000000, -7.429790795770647916E-15, 1.000000000000000000 ) ) ;
#20261=DIRECTION ( 'NONE',  ( 2.557131231893037478E-16, 0.8660254037844420383, -0.4999999999999943379 ) ) ;
#20321=DIRECTION ( 'NONE',  ( 0.000000000000000000, 0.1455152366551500653, 0.9893560106964507384 ) ) ;
#20329=VERTEX_POINT ( 'NONE', #127489 ) ;
#20368=CIRCLE ( 'NONE', #32481, 11.70000000000000284 ) ;
#20464=VERTEX_POINT ( 'NONE', #229165 ) ;
#20467=VERTEX_POINT ( 'NONE', #59143 ) ;
#20470=CIRCLE ( 'NONE', #157871, 11.65000000000000036 ) ;
#20507=DIRECTION ( 'NONE',  ( 0.000000000000000000, -1.000000000000000000, -6.982962677686265922E-15 ) ) ;
#20549=EDGE_CURVE ( 'NONE', #2421, #30032, #140755, .T. ) ;
#20550=ADVANCED_FACE ( 'NONE', ( #175233 ), #20066, .T. ) ;
#20566=DIRECTION ( 'NONE',  ( 0.000000000000000000, 1.000000000000000000, 0.000000000000000000 ) ) ;
#20620=ORIENTED_EDGE ( 'NONE', *, *, #63866, .T. ) ;
#20667=ADVANCED_FACE ( 'NONE', ( #6817 ), #163336, .F. ) ;
#20683=VECTOR ( 'NONE', #79181, 1000.000000000000000 ) ;
#20686=AXIS2_PLACEMENT_3D ( 'NONE', #99888, #101152, #165032 ) ;
#20694=AXIS2_PLACEMENT_3D ( 'NONE', #256368, #77778, #157372 ) ;
#20698=ORIENTED_EDGE ( 'NONE', *, *, #220569, .T. ) ;
#20702=ORIENTED_EDGE ( 'NONE', *, *, #212262, .T. ) ;
#20784=CARTESIAN_POINT ( 'NONE',  ( -20.94999999999999929, 87.65000000001143121, -36.02310748452423894 ) ) ;
#20786=ADVANCED_FACE ( 'NONE', ( #235807 ), #224131, .T. ) ;
#20842=CARTESIAN_POINT ( 'NONE',  ( 23.25000000000000000, 87.65000000001144542, -39.12310748452424747 ) ) ;
#20931=VECTOR ( 'NONE', #169193, 1000.000000000000114 ) ;
#20933=B_SPLINE_CURVE_WITH_KNOTS ( 'NONE', 3,
 ( #68033, #151442, #69332, #87577, #131856, #48462, #111012, #167172 ),
 .UNSPECIFIED., .F., .F.,
 ( 4, 2, 2, 4 ),
 ( 0.000000000000000000, 0.0001881495939909109049, 0.0002822243909863736758, 0.0003762991879818364466 ),
 .UNSPECIFIED. ) ;
#20936=VERTEX_POINT ( 'NONE', #243510 ) ;
#20977=AXIS2_PLACEMENT_3D ( 'NONE', #124028, #121480, #163157 ) ;
#20984=AXIS2_PLACEMENT_3D ( 'NONE', #142969, #238240, #41360 ) ;
#20991=ADVANCED_FACE ( 'NONE', ( #90847 ), #53004, .F. ) ;
#20998=ORIENTED_EDGE ( 'NONE', *, *, #146992, .T. ) ;
#20999=FACE_OUTER_BOUND ( 'NONE', #125011, .T. ) ;
#21006=DIRECTION ( 'NONE',  ( 1.000000000000000000, 0.000000000000000000, 0.000000000000000000 ) ) ;
#21008=ORIENTED_EDGE ( 'NONE', *, *, #220248, .T. ) ;
#21013=ORIENTED_EDGE ( 'NONE', *, *, #31993, .F. ) ;
#21050=CIRCLE ( 'NONE', #212577, 0.1000000000000052097 ) ;
#21057=EDGE_CURVE ( 'NONE', #65120, #59781, #153071, .T. ) ;
#21096=DIRECTION ( 'NONE',  ( 0.000000000000000000, -1.000000000000000000, -6.860497997771531562E-15 ) ) ;
#21103=EDGE_CURVE ( 'NONE', #44233, #6026, #234206, .T. ) ;
#21115=CARTESIAN_POINT ( 'NONE',  ( -18.55807992284872299, 65.67101464000451472, -30.44043916224794799 ) ) ;
#21128=ORIENTED_EDGE ( 'NONE', *, *, #23, .T. ) ;
#21133=EDGE_CURVE ( 'NONE', #166990, #221113, #107226, .T. ) ;
#21167=DIRECTION ( 'NONE',  ( 1.000000000000000000, 0.000000000000000000, 0.000000000000000000 ) ) ;
#21197=VERTEX_POINT ( 'NONE', #248344 ) ;
#21203=AXIS2_PLACEMENT_3D ( 'NONE', #145532, #206806, #25607 ) ;
#21236=VECTOR ( 'NONE', #59899, 1000.000000000000114 ) ;
#21245=VECTOR ( 'NONE', #148123, 1000.000000000000000 ) ;
#21260=DIRECTION ( 'NONE',  ( -0.000000000000000000, 1.000000000000000000, 6.982962677686266711E-15 ) ) ;
#21278=CARTESIAN_POINT ( 'NONE',  ( -18.40000000000000213, 85.51932773110404185, -62.55013110796492271 ) ) ;
#21279=EDGE_LOOP ( 'NONE', ( #26445, #172432, #186818, #180456, #1718, #16424, #194262, #125003, #27443, #142415, #91954, #229673, #202806, #25059, #21385, #140502, #182400, #197961 ) ) ;
#21295=CARTESIAN_POINT ( 'NONE',  ( 21.05000000000000071, 76.00000000001165290, -69.52310748452431710 ) ) ;
#21311=DIRECTION ( 'NONE',  ( 0.000000000000000000, 0.1350103645451835865, 0.9908441862701605762 ) ) ;
#21331=DIRECTION ( 'NONE',  ( 1.000000000000000000, 0.000000000000000000, 0.000000000000000000 ) ) ;
#21380=EDGE_CURVE ( 'NONE', #230778, #171007, #153650, .T. ) ;
#21385=ORIENTED_EDGE ( 'NONE', *, *, #3357, .T. ) ;
#21386=EDGE_CURVE ( 'NONE', #21500, #138858, #74534, .T. ) ;
#21387=DIRECTION ( 'NONE',  ( -4.448008912761042820E-16, -1.000000000000000000, -7.116814260417668513E-15 ) ) ;
#21390=DIRECTION ( 'NONE',  ( 0.000000000000000000, 0.000000000000000000, -1.000000000000000000 ) ) ;
#21422=AXIS2_PLACEMENT_3D ( 'NONE', #164948, #206646, #223614 ) ;
#21426=DIRECTION ( 'NONE',  ( 1.000000000000000000, 0.000000000000000000, 0.000000000000000000 ) ) ;
#21429=CARTESIAN_POINT ( 'NONE',  ( -20.54999999999999716, 76.00000000001155342, -56.54810748452432279 ) ) ;
#21448=ADVANCED_FACE ( 'NONE', ( #12327 ), #100777, .T. ) ;
#21467=CARTESIAN_POINT ( 'NONE',  ( 21.09706851349342216, 67.22415748653817502, -57.28754126812474112 ) ) ;
#21469=DIRECTION ( 'NONE',  ( 0.000000000000000000, 0.000000000000000000, 1.000000000000000000 ) ) ;
#21500=VERTEX_POINT ( 'NONE', #1712 ) ;
#21510=DIRECTION ( 'NONE',  ( 1.000000000000000000, -2.952720810173289112E-16, -2.061873921506763405E-30 ) ) ;
#21530=VERTEX_POINT ( 'NONE', #162107 ) ;
#21532=CARTESIAN_POINT ( 'NONE',  ( -20.54999999999999716, 76.00000000001142553, -36.02310748452432421 ) ) ;
#21537=LINE ( 'NONE', #243134, #40968 ) ;
#21557=DIRECTION ( 'NONE',  ( -0.000000000000000000, 1.000000000000000000, 6.982962677686266711E-15 ) ) ;
#21598=CARTESIAN_POINT ( 'NONE',  ( -21.29999999999995808, 76.00000000001165290, -69.52310748452431710 ) ) ;
#21601=DIRECTION ( 'NONE',  ( -0.000000000000000000, -6.982962677686266711E-15, 1.000000000000000000 ) ) ;
#21703=AXIS2_PLACEMENT_3D ( 'NONE', #198817, #20199, #26631 ) ;
#21729=CARTESIAN_POINT ( 'NONE',  ( -21.07946286933445279, 69.67096268100397083, -69.59979132778077826 ) ) ;
#21735=EDGE_CURVE ( 'NONE', #101690, #47640, #251560, .T. ) ;
#21781=AXIS2_PLACEMENT_3D ( 'NONE', #58571, #1163, #117289 ) ;
#21786=ADVANCED_FACE ( 'NONE', ( #54947 ), #240684, .T. ) ;
#21789=CARTESIAN_POINT ( 'NONE',  ( 23.14999999999999858, 80.00000000001142553, -36.02310748452429578 ) ) ;
#21808=LINE ( 'NONE', #160049, #108163 ) ;
#21882=DIRECTION ( 'NONE',  ( 6.938893903907222067E-15, 1.000000000000000000, 6.982962677686266711E-15 ) ) ;
#21892=AXIS2_PLACEMENT_3D ( 'NONE', #206072, #203506, #65271 ) ;
#21896=ORIENTED_EDGE ( 'NONE', *, *, #41256, .F. ) ;
#21900=DIRECTION ( 'NONE',  ( 0.000000000000000000, -1.000000000000000000, -6.982962677686266711E-15 ) ) ;
#21903=CARTESIAN_POINT ( 'NONE',  ( -21.05000000000000071, 77.83534155023598089, -57.96795619196132776 ) ) ;
#21911=AXIS2_PLACEMENT_3D ( 'NONE', #153834, #54670, #35158 ) ;
#21920=AXIS2_PLACEMENT_3D ( 'NONE', #91136, #55825, #192820 ) ;
#21939=DIRECTION ( 'NONE',  ( 0.000000000000000000, -0.9908441862701605762, 0.1350103645451835310 ) ) ;
#22027=ORIENTED_EDGE ( 'NONE', *, *, #57661, .T. ) ;
#22034=CARTESIAN_POINT ( 'NONE',  ( -18.59999999999999787, 76.00000000001165290, -69.52310748452431710 ) ) ;
#22037=FACE_OUTER_BOUND ( 'NONE', #140618, .T. ) ;
#22043=EDGE_LOOP ( 'NONE', ( #186158, #186862, #219003, #245460 ) ) ;
#22059=DIRECTION ( 'NONE',  ( 0.000000000000000000, 1.000000000000000000, 6.688090509790097607E-15 ) ) ;
#22070=EDGE_CURVE ( 'NONE', #200641, #148706, #15868, .T. ) ;
#22100=CARTESIAN_POINT ( 'NONE',  ( -20.94999999999999929, 76.00000000001142553, -36.02310748452432421 ) ) ;
#22115=CARTESIAN_POINT ( 'NONE',  ( -18.50000000000000000, 76.00000000001142553, -36.02310748452432421 ) ) ;
#22131=CARTESIAN_POINT ( 'NONE',  ( 20.94983749550516450, 65.70233904876961617, -30.54874109119683823 ) ) ;
#22150=VERTEX_POINT ( 'NONE', #216753 ) ;
#22158=CARTESIAN_POINT ( 'NONE',  ( 18.33996824403505244, 85.56963985944298656, -29.20404184700773698 ) ) ;
#22190=EDGE_LOOP ( 'NONE', ( #23055, #161444, #65161, #12617 ) ) ;
#22205=CARTESIAN_POINT ( 'NONE',  ( 20.94999999999999929, 76.00000000001142553, -36.02310748452432421 ) ) ;
#22219=VECTOR ( 'NONE', #175878, 1000.000000000000000 ) ;
#22226=CARTESIAN_POINT ( 'NONE',  ( 21.05000000000000071, 71.00000000001151079, -48.42837350343745584 ) ) ;
#22240=EDGE_CURVE ( 'NONE', #86948, #178818, #22437, .T. ) ;
#22277=DIRECTION ( 'NONE',  ( 0.000000000000000000, -6.467318590049456648E-15, 1.000000000000000000 ) ) ;
#22329=EDGE_CURVE ( 'NONE', #38617, #39343, #127939, .T. ) ;
#22349=VERTEX_POINT ( 'NONE', #14433 ) ;
#22355=ORIENTED_EDGE ( 'NONE', *, *, #52888, .F. ) ;
#22363=CIRCLE ( 'NONE', #55610, 0.4000000000000045186 ) ;
#22390=DIRECTION ( 'NONE',  ( 1.000000000000000000, 0.000000000000000000, 0.000000000000000000 ) ) ;
#22392=CARTESIAN_POINT ( 'NONE',  ( -18.50000000000000000, 65.70729864260955821, -30.56574559737245167 ) ) ;
#22407=CARTESIAN_POINT ( 'NONE',  ( -20.94999999999999929, 75.74389420791943905, -69.55800392619661920 ) ) ;
#22411=AXIS2_PLACEMENT_3D ( 'NONE', #87072, #165355, #6258 ) ;
#22417=AXIS2_PLACEMENT_3D ( 'NONE', #162003, #207539, #228382 ) ;
#22421=CARTESIAN_POINT ( 'NONE',  ( -22.57320508075687115, 64.35000000001166143, -69.52310748452435973 ) ) ;
#22437=LINE ( 'NONE', #96778, #186918 ) ;
#22455=DIRECTION ( 'NONE',  ( 0.000000000000000000, 0.000000000000000000, 1.000000000000000000 ) ) ;
#22476=DIRECTION ( 'NONE',  ( 1.000000000000000000, 0.000000000000000000, 0.000000000000000000 ) ) ;
#22508=LINE ( 'NONE', #146271, #221374 ) ;
#22537=ORIENTED_EDGE ( 'NONE', *, *, #127164, .T. ) ;
#22542=ORIENTED_EDGE ( 'NONE', *, *, #47214, .T. ) ;
#22545=EDGE_CURVE ( 'NONE', #6026, #134468, #119958, .T. ) ;
#22583=ADVANCED_FACE ( 'NONE', ( #138180 ), #258098, .F. ) ;
#22603=ORIENTED_EDGE ( 'NONE', *, *, #44203, .F. ) ;
#22650=DIRECTION ( 'NONE',  ( 0.000000000000000000, 0.000000000000000000, 1.000000000000000000 ) ) ;
#22656=AXIS2_PLACEMENT_3D ( 'NONE', #50317, #110312, #106433 ) ;
#22673=FACE_OUTER_BOUND ( 'NONE', #116157, .T. ) ;
#22696=DIRECTION ( 'NONE',  ( 0.000000000000000000, -6.982962677686266711E-15, 1.000000000000000000 ) ) ;
#22697=ORIENTED_EDGE ( 'NONE', *, *, #129500, .T. ) ;
#22717=CARTESIAN_POINT ( 'NONE',  ( 20.95378194480896639, 65.46508800846882536, -61.95805333637653689 ) ) ;
#22718=DIRECTION ( 'NONE',  ( -0.000000000000000000, 0.1298341882520054891, 0.9915357197604850459 ) ) ;
#22724=DIRECTION ( 'NONE',  ( 0.000000000000000000, 0.000000000000000000, 1.000000000000000000 ) ) ;
#22743=FACE_OUTER_BOUND ( 'NONE', #232049, .T. ) ;
#22767=AXIS2_PLACEMENT_3D ( 'NONE', #178205, #141611, #42506 ) ;
#22777=CARTESIAN_POINT ( 'NONE',  ( 23.15000000000000213, 85.00000000001149658, -45.41707660717670336 ) ) ;
#22802=AXIS2_PLACEMENT_3D ( 'NONE', #93410, #36031, #112991 ) ;
#22829=ORIENTED_EDGE ( 'NONE', *, *, #257539, .T. ) ;
#22863=ORIENTED_EDGE ( 'NONE', *, *, #235168, .F. ) ;
#22894=EDGE_CURVE ( 'NONE', #148706, #218484, #154922, .T. ) ;
#22918=DIRECTION ( 'NONE',  ( 0.000000000000000000, -6.982962677686266711E-15, 1.000000000000000000 ) ) ;
#22930=ORIENTED_EDGE ( 'NONE', *, *, #210402, .T. ) ;
#22939=CARTESIAN_POINT ( 'NONE',  ( -22.44366136229477249, 75.99065843052565583, -81.17282604199823481 ) ) ;
#22945=CARTESIAN_POINT ( 'NONE',  ( -21.05000000000000071, 77.25000000001159606, -61.52310748452431710 ) ) ;
#22984=CARTESIAN_POINT ( 'NONE',  ( -18.59999999999999787, 77.14957036958705316, -28.20719500002235236 ) ) ;
#23010=EDGE_CURVE ( 'NONE', #90665, #61807, #21808, .T. ) ;
#23020=CARTESIAN_POINT ( 'NONE',  ( -18.50000000000000000, 69.15387683765879956, -32.28538121767450519 ) ) ;
#23055=ORIENTED_EDGE ( 'NONE', *, *, #57285, .F. ) ;
#23086=DIRECTION ( 'NONE',  ( 1.000000000000000000, 0.000000000000000000, 0.000000000000000000 ) ) ;
#23101=CARTESIAN_POINT ( 'NONE',  ( -20.64999999999999858, 74.05981308412367525, -48.85222669557766295 ) ) ;
#23108=CARTESIAN_POINT ( 'NONE',  ( -21.05000000000000426, 69.52295361822181974, -69.42310748452437963 ) ) ;
#23177=CARTESIAN_POINT ( 'NONE',  ( 18.49999999999999289, 65.75000000001148237, -44.87310748452439668 ) ) ;
#23198=AXIS2_PLACEMENT_3D ( 'NONE', #103032, #143455, #125192 ) ;
#23236=CIRCLE ( 'NONE', #44057, 0.1000000000000014488 ) ;
#23237=EDGE_CURVE ( 'NONE', #192913, #45256, #110314, .T. ) ;
#23254=CARTESIAN_POINT ( 'NONE',  ( -23.25000000000000000, 70.05000000001149374, -46.32880978955918039 ) ) ;
#23262=ORIENTED_EDGE ( 'NONE', *, *, #53258, .T. ) ;
#23268=ORIENTED_EDGE ( 'NONE', *, *, #66475, .F. ) ;
#23288=DIRECTION ( 'NONE',  ( 1.000000000000000000, 0.000000000000000000, 0.000000000000000000 ) ) ;
#23323=AXIS2_PLACEMENT_3D ( 'NONE', #8463, #87960, #28048 ) ;
#23341=CIRCLE ( 'NONE', #15114, 0.1000000000000017680 ) ;
#23350=CIRCLE ( 'NONE', #2453, 6.258578643762710669 ) ;
#23411=DIRECTION ( 'NONE',  ( 0.000000000000000000, 8.896017825522085641E-15, -1.000000000000000000 ) ) ;
#23413=AXIS2_PLACEMENT_3D ( 'NONE', #229128, #203138, #24529 ) ;
#23422=DIRECTION ( 'NONE',  ( 0.000000000000000000, -0.1495327102803180597, 0.9887567792719412774 ) ) ;
#23426=DIRECTION ( 'NONE',  ( 1.000000000000000000, -0.000000000000000000, 0.000000000000000000 ) ) ;
#23443=EDGE_CURVE ( 'NONE', #69524, #101132, #37431, .T. ) ;
#23444=VERTEX_POINT ( 'NONE', #243101 ) ;
#23448=EDGE_CURVE ( 'NONE', #256296, #68040, #39804, .T. ) ;
#23477=CARTESIAN_POINT ( 'NONE',  ( 18.43565242384934066, 85.51932773110407027, -62.55013110796493692 ) ) ;
#23490=AXIS2_PLACEMENT_3D ( 'NONE', #110935, #31438, #74419 ) ;
#23509=EDGE_CURVE ( 'NONE', #98142, #92818, #58240, .T. ) ;
#23532=DIRECTION ( 'NONE',  ( 1.000000000000000000, 0.000000000000000000, 0.000000000000000000 ) ) ;
#23533=VECTOR ( 'NONE', #116591, 1000.000000000000000 ) ;
#23556=EDGE_CURVE ( 'NONE', #85964, #176232, #120830, .T. ) ;
#23562=ADVANCED_FACE ( 'NONE', ( #254316 ), #233512, .T. ) ;
#23571=CIRCLE ( 'NONE', #56805, 0.09999999999999739653 ) ;
#23594=EDGE_CURVE ( 'NONE', #83134, #156105, #87467, .T. ) ;
#23615=CARTESIAN_POINT ( 'NONE',  ( 18.59999999999999076, 74.16465844978715438, -57.96795619196135618 ) ) ;
#23642=ORIENTED_EDGE ( 'NONE', *, *, #240347, .T. ) ;
#23657=AXIS2_PLACEMENT_3D ( 'NONE', #31945, #111453, #192289 ) ;
#23678=VECTOR ( 'NONE', #115821, 1000.000000000000000 ) ;
#23692=CARTESIAN_POINT ( 'NONE',  ( 21.08489834409762054, 65.37767610527603779, -57.17310748452440805 ) ) ;
#23703=CARTESIAN_POINT ( 'NONE',  ( -23.15000000000000213, 87.48912529308749697, -39.02310748452423894 ) ) ;
#23749=FACE_OUTER_BOUND ( 'NONE', #126832, .T. ) ;
#23773=CARTESIAN_POINT ( 'NONE',  ( -23.15000000000000213, 74.00000000001156764, -56.79848556176223440 ) ) ;
#23788=EDGE_CURVE ( 'NONE', #47449, #214318, #173836, .T. ) ;
#23810=CARTESIAN_POINT ( 'NONE',  ( 18.59999999999998721, 56.14960075277809182, -67.24280442672311153 ) ) ;
#23837=CARTESIAN_POINT ( 'NONE',  ( -18.45140287520618472, 85.48607773954091726, -29.38258435783816225 ) ) ;
#23851=EDGE_CURVE ( 'NONE', #172217, #113945, #45968, .T. ) ;
#23860=EDGE_LOOP ( 'NONE', ( #140501, #95111, #198916, #131935, #123014 ) ) ;
#23877=CIRCLE ( 'NONE', #140356, 0.09999999999999939493 ) ;
#23888=DIRECTION ( 'NONE',  ( 0.000000000000000000, 0.000000000000000000, -1.000000000000000000 ) ) ;
#23942=DIRECTION ( 'NONE',  ( 0.000000000000000000, -1.000000000000000000, -6.982962677686266711E-15 ) ) ;
#23950=DIRECTION ( 'NONE',  ( 0.000000000000000000, -0.9654727137038715545, 0.2605042016806676242 ) ) ;
#24022=AXIS2_PLACEMENT_3D ( 'NONE', #170090, #252136, #12276 ) ;
#24035=CARTESIAN_POINT ( 'NONE',  ( 21.12802099929860944, 67.21944740978935329, -57.27491749959277456 ) ) ;
#24051=CIRCLE ( 'NONE', #94926, 11.65000000000000746 ) ;
#24090=ORIENTED_EDGE ( 'NONE', *, *, #142546, .T. ) ;
#24113=EDGE_LOOP ( 'NONE', ( #123098, #97470, #232666 ) ) ;
#24152=EDGE_LOOP ( 'NONE', ( #187907, #214322, #241127, #61713 ) ) ;
#24155=VECTOR ( 'NONE', #244759, 1000.000000000000000 ) ;
#24157=AXIS2_PLACEMENT_3D ( 'NONE', #180257, #103252, #78570 ) ;
#24164=AXIS2_PLACEMENT_3D ( 'NONE', #178512, #135485, #175946 ) ;
#24194=FACE_OUTER_BOUND ( 'NONE', #49728, .T. ) ;
#24205=AXIS2_PLACEMENT_3D ( 'NONE', #248574, #69964, #205580 ) ;
#24215=CARTESIAN_POINT ( 'NONE',  ( -22.43310005002225438, 75.99436305787085644, -81.17276961165872251 ) ) ;
#24227=AXIS2_PLACEMENT_3D ( 'NONE', #155103, #16857, #57223 ) ;
#24244=AXIS2_PLACEMENT_3D ( 'NONE', #207791, #227321, #52527 ) ;
#24268=FACE_OUTER_BOUND ( 'NONE', #178149, .T. ) ;
#24294=FACE_OUTER_BOUND ( 'NONE', #234149, .T. ) ;
#24321=EDGE_CURVE ( 'NONE', #102057, #156378, #95602, .T. ) ;
#24322=CARTESIAN_POINT ( 'NONE',  ( 20.94999999999999574, 77.16270174994961906, -61.52310748452431710 ) ) ;
#24334=EDGE_LOOP ( 'NONE', ( #75925, #218159, #81647, #83394 ) ) ;
#24390=MANIFOLD_SOLID_BREP ( 'Stock-MAS-200-1', #57530 ) ;
#24413=CIRCLE ( 'NONE', #186728, 0.1000000000000028644 ) ;
#24418=CARTESIAN_POINT ( 'NONE',  ( -20.54999999999999716, 71.65000000001155911, -57.17310748452435121 ) ) ;
#24458=ORIENTED_EDGE ( 'NONE', *, *, #47582, .T. ) ;
#24508=CARTESIAN_POINT ( 'NONE',  ( -20.64999999999999858, 74.00000000001156764, -56.79848556176223440 ) ) ;
#24509=CIRCLE ( 'NONE', #224211, 0.6000000000000033085 ) ;
#24513=DIRECTION ( 'NONE',  ( 0.000000000000000000, 1.000000000000000000, 6.982962677686266711E-15 ) ) ;
#24519=ORIENTED_EDGE ( 'NONE', *, *, #228726, .T. ) ;
#24529=DIRECTION ( 'NONE',  ( 0.000000000000000000, 0.000000000000000000, 1.000000000000000000 ) ) ;
#24531=EDGE_CURVE ( 'NONE', #255306, #159190, #158795, .T. ) ;
#24542=CARTESIAN_POINT ( 'NONE',  ( -22.39999999999999858, 64.25000000001165290, -69.42310748452440805 ) ) ;
#24574=CARTESIAN_POINT ( 'NONE',  ( 20.85000000000000142, 77.16412189325258453, -28.10825939895270764 ) ) ;
#24578=DIRECTION ( 'NONE',  ( 0.000000000000000000, 0.000000000000000000, 1.000000000000000000 ) ) ;
#24581=CARTESIAN_POINT ( 'NONE',  ( -23.15000000000000213, 64.40000000001147384, -42.95131071479990936 ) ) ;
#24597=VECTOR ( 'NONE', #74103, 1000.000000000000000 ) ;
#24637=EDGE_CURVE ( 'NONE', #253340, #183881, #252781, .T. ) ;
#24640=ORIENTED_EDGE ( 'NONE', *, *, #11665, .F. ) ;
#24649=CIRCLE ( 'NONE', #41198, 0.5000000000000004441 ) ;
#24662=DIRECTION ( 'NONE',  ( 1.000000000000000000, 0.000000000000000000, -0.000000000000000000 ) ) ;
#24683=EDGE_CURVE ( 'NONE', #92040, #211799, #5539, .T. ) ;
#24687=ADVANCED_FACE ( 'NONE', ( #57133 ), #117142, .T. ) ;
#24715=DIRECTION ( 'NONE',  ( 0.000000000000000000, -0.6728971962616412394, -0.7397360091703134577 ) ) ;
#24722=ADVANCED_FACE ( 'NONE', ( #100106 ), #13758, .F. ) ;
#24734=AXIS2_PLACEMENT_3D ( 'NONE', #190738, #167315, #86430 ) ;
#24735=CARTESIAN_POINT ( 'NONE',  ( 18.44208962362734638, 85.55234049691893006, -29.18093442906062407 ) ) ;
#24736=EDGE_CURVE ( 'NONE', #81658, #196598, #163788, .T. ) ;
#24741=CARTESIAN_POINT ( 'NONE',  ( 18.59999999999998721, 69.06610602788505560, -32.23746165015079868 ) ) ;
#24747=DIRECTION ( 'NONE',  ( -1.000000000000000000, 0.000000000000000000, 0.000000000000000000 ) ) ;
#24769=ORIENTED_EDGE ( 'NONE', *, *, #43636, .T. ) ;
#24779=CARTESIAN_POINT ( 'NONE',  ( -20.54999999999999716, 73.60000000001149090, -45.91707660717678152 ) ) ;
#24807=ORIENTED_EDGE ( 'NONE', *, *, #120097, .T. ) ;
#24811=CARTESIAN_POINT ( 'NONE',  ( 22.39999999999999503, 64.35000000001164722, -69.62310748452439668 ) ) ;
#24835=ORIENTED_EDGE ( 'NONE', *, *, #37352, .T. ) ;
#24847=VECTOR ( 'NONE', #18402, 1000.000000000000000 ) ;
#24848=CARTESIAN_POINT ( 'NONE',  ( -20.85000000000000142, 77.26327546522863088, -28.12124281777790813 ) ) ;
#24851=CARTESIAN_POINT ( 'NONE',  ( -18.59999999999999787, 68.87972903831379767, -32.36354444268504693 ) ) ;
#24872=ORIENTED_EDGE ( 'NONE', *, *, #248413, .T. ) ;
#24884=EDGE_LOOP ( 'NONE', ( #87712, #84736, #46534, #88040 ) ) ;
#24903=LINE ( 'NONE', #181406, #82098 ) ;
#24907=CARTESIAN_POINT ( 'NONE',  ( 21.14999999999999858, 64.25000000001156764, -57.37310748452440379 ) ) ;
#24914=ORIENTED_EDGE ( 'NONE', *, *, #140895, .T. ) ;
#24927=DIRECTION ( 'NONE',  ( 0.000000000000000000, 6.982962677686266711E-15, -1.000000000000000000 ) ) ;
#24936=AXIS2_PLACEMENT_3D ( 'NONE', #142562, #23942, #83842 ) ;
#24937=DIRECTION ( 'NONE',  ( 1.000000000000000000, 0.000000000000000000, 0.000000000000000000 ) ) ;
#24939=CARTESIAN_POINT ( 'NONE',  ( 20.95512820512820440, 67.12384868372348024, -60.96447848938343839 ) ) ;
#24952=CARTESIAN_POINT ( 'NONE',  ( 23.25000000000000000, 84.59626168225447884, -45.47323500167454569 ) ) ;
#24960=AXIS2_PLACEMENT_3D ( 'NONE', #38412, #150989, #217027 ) ;
#25020=VERTEX_POINT ( 'NONE', #176813 ) ;
#25034=AXIS2_PLACEMENT_3D ( 'NONE', #105993, #220823, #46037 ) ;
#25059=ORIENTED_EDGE ( 'NONE', *, *, #150494, .T. ) ;
#25061=FACE_OUTER_BOUND ( 'NONE', #78470, .T. ) ;
#25087=CARTESIAN_POINT ( 'NONE',  ( -20.64999999999999858, 76.00000000001142553, -36.02310748452432421 ) ) ;
#25122=ORIENTED_EDGE ( 'NONE', *, *, #122800, .F. ) ;
#25123=CARTESIAN_POINT ( 'NONE',  ( -2.995603634470891112E-16, 69.35000000001151932, -48.37310748452436826 ) ) ;
#25147=VERTEX_POINT ( 'NONE', #179383 ) ;
#25166=CARTESIAN_POINT ( 'NONE',  ( -22.39999999999999858, 68.20922040163824818, -69.62310748452438247 ) ) ;
#25209=AXIS2_PLACEMENT_3D ( 'NONE', #54099, #181460, #193624 ) ;
#25212=EDGE_LOOP ( 'NONE', ( #86945, #162648, #184139, #57728 ) ) ;
#25233=DIRECTION ( 'NONE',  ( 1.000000000000000000, 0.000000000000000000, 0.000000000000000000 ) ) ;
#25257=ORIENTED_EDGE ( 'NONE', *, *, #79567, .F. ) ;
#25258=EDGE_CURVE ( 'NONE', #233936, #189246, #222199, .T. ) ;
#25276=AXIS2_PLACEMENT_3D ( 'NONE', #160980, #243062, #202653 ) ;
#25277=CARTESIAN_POINT ( 'NONE',  ( -21.46681500597872727, 76.00000000001170974, -76.38061864395214684 ) ) ;
#25308=DIRECTION ( 'NONE',  ( 1.000000000000000000, 0.000000000000000000, 0.000000000000000000 ) ) ;
#25312=ORIENTED_EDGE ( 'NONE', *, *, #200995, .F. ) ;
#25347=CYLINDRICAL_SURFACE ( 'NONE', #183635, 0.5000000000000004441 ) ;
#25388=CIRCLE ( 'NONE', #175425, 0.1000000000000028644 ) ;
#25412=CARTESIAN_POINT ( 'NONE',  ( 23.14999999999999147, 76.00000000001165290, -69.52310748452431710 ) ) ;
#25418=CIRCLE ( 'NONE', #109151, 0.09999999999999739653 ) ;
#25420=DIRECTION ( 'NONE',  ( 0.000000000000000000, 0.000000000000000000, 1.000000000000000000 ) ) ;
#25428=DIRECTION ( 'NONE',  ( 1.000000000000000000, 0.000000000000000000, 0.000000000000000000 ) ) ;
#25601=CARTESIAN_POINT ( 'NONE',  ( -20.54999999999999716, 74.00000000001151079, -48.84772940728643675 ) ) ;
#25607=DIRECTION ( 'NONE',  ( 0.000000000000000000, 7.026728003956683390E-15, -1.000000000000000000 ) ) ;
#25609=ADVANCED_FACE ( 'NONE', ( #35979 ), #72542, .F. ) ;
#25643=DIRECTION ( 'NONE',  ( 1.000000000000000000, 0.000000000000000000, 0.000000000000000000 ) ) ;
#25662=ORIENTED_EDGE ( 'NONE', *, *, #212096, .F. ) ;
#25686=DIRECTION ( 'NONE',  ( 1.000000000000000000, 0.000000000000000000, 0.000000000000000000 ) ) ;
#25707=CIRCLE ( 'NONE', #4825, 0.1000000000000028644 ) ;
#25722=ORIENTED_EDGE ( 'NONE', *, *, #58888, .F. ) ;
#25763=CARTESIAN_POINT ( 'NONE',  ( -20.64999999999999858, 84.66355140188063899, -45.54720860259156723 ) ) ;
#25774=DIRECTION ( 'NONE',  ( -0.000000000000000000, -1.000000000000000000, -6.982962677686266711E-15 ) ) ;
#25804=LINE ( 'NONE', #105300, #64363 ) ;
#25865=DIRECTION ( 'NONE',  ( 0.000000000000000000, 6.982962677686266711E-15, -1.000000000000000000 ) ) ;
#25887=CARTESIAN_POINT ( 'NONE',  ( 22.42357213249528769, 68.32706761365174941, -69.62219444852593142 ) ) ;
#25890=ORIENTED_EDGE ( 'NONE', *, *, #255178, .F. ) ;
#25922=FACE_OUTER_BOUND ( 'NONE', #242830, .T. ) ;
#25950=CIRCLE ( 'NONE', #204980, 7.900000000000003908 ) ;
#25956=ORIENTED_EDGE ( 'NONE', *, *, #41216, .T. ) ;
#25961=EDGE_CURVE ( 'NONE', #147896, #117855, #237602, .T. ) ;
#26008=FACE_OUTER_BOUND ( 'NONE', #125155, .T. ) ;
#26025=DIRECTION ( 'NONE',  ( 0.000000000000000000, 0.000000000000000000, 1.000000000000000000 ) ) ;
#26030=CIRCLE ( 'NONE', #246580, 0.09999999999999939493 ) ;
#26036=CARTESIAN_POINT ( 'NONE',  ( -20.94999999999999929, 87.41227409416133298, -66.52310748452423184 ) ) ;
#26040=DIRECTION ( 'NONE',  ( 0.000000000000000000, 1.000000000000000000, 1.156482317317864980E-14 ) ) ;
#26052=EDGE_CURVE ( 'NONE', #187198, #85045, #80519, .T. ) ;
#26055=CARTESIAN_POINT ( 'NONE',  ( 18.59999999999999787, 85.32100840337291459, -62.28716923544639172 ) ) ;
#26061=SURFACE_STYLE_FILL_AREA ( #202122 ) ;
#26062=ORIENTED_EDGE ( 'NONE', *, *, #175817, .F. ) ;
#26098=CARTESIAN_POINT ( 'NONE',  ( 20.94999999999999929, 87.48912529308749697, -39.02310748452423894 ) ) ;
#26198=DIRECTION ( 'NONE',  ( 0.000000000000000000, -6.938893903907222067E-15, 1.000000000000000000 ) ) ;
#26200=DIRECTION ( 'NONE',  ( -1.040834085586090694E-13, 0.1568667991644355497, 0.9876197685951332295 ) ) ;
#26202=AXIS2_PLACEMENT_3D ( 'NONE', #57220, #93796, #134201 ) ;
#26228=FACE_OUTER_BOUND ( 'NONE', #209504, .T. ) ;
#26283=CARTESIAN_POINT ( 'NONE',  ( -20.85000000000000142, 87.65000000001143121, -36.02310748452423894 ) ) ;
#26304=DIRECTION ( 'NONE',  ( 0.000000000000000000, 1.000000000000000000, 6.982962677686266711E-15 ) ) ;
#26325=EDGE_LOOP ( 'NONE', ( #54399, #161812, #175639, #56904 ) ) ;
#26338=CIRCLE ( 'NONE', #255214, 4.000000000000003553 ) ;
#26356=DIRECTION ( 'NONE',  ( 0.000000000000000000, -7.056502275159890043E-15, 1.000000000000000000 ) ) ;
#26360=CARTESIAN_POINT ( 'NONE',  ( 18.59999999999999076, 64.35000000001147669, -44.67310748452440095 ) ) ;
#26368=ADVANCED_FACE ( 'NONE', ( #123441 ), #205527, .T. ) ;
#26382=PRODUCT ( 'Injection Molded Chain Links 15', 'Injection Molded Chain Links 15', '', ( #235988 ) ) ;
#26387=ORIENTED_EDGE ( 'NONE', *, *, #109691, .T. ) ;
#26412=EDGE_CURVE ( 'NONE', #1074, #243492, #82989, .T. ) ;
#26419=DIRECTION ( 'NONE',  ( -1.000000000000000000, 3.265361837132813093E-16, 2.280189983783949500E-30 ) ) ;
#26426=ORIENTED_EDGE ( 'NONE', *, *, #160132, .F. ) ;
#26438=ORIENTED_EDGE ( 'NONE', *, *, #230616, .T. ) ;
#26445=ORIENTED_EDGE ( 'NONE', *, *, #64176, .T. ) ;
#26458=VERTEX_POINT ( 'NONE', #112863 ) ;
#26468=FACE_OUTER_BOUND ( 'NONE', #172690, .T. ) ;
#26483=EDGE_CURVE ( 'NONE', #3677, #97821, #49031, .T. ) ;
#26502=CARTESIAN_POINT ( 'NONE',  ( 23.24999999999999645, 76.00000000001142553, -36.02310748452432421 ) ) ;
#26519=FACE_OUTER_BOUND ( 'NONE', #118575, .T. ) ;
#26544=AXIS2_PLACEMENT_3D ( 'NONE', #114517, #136629, #37563 ) ;
#26546=ORIENTED_EDGE ( 'NONE', *, *, #135677, .F. ) ;
#26560=CARTESIAN_POINT ( 'NONE',  ( -22.00356870070283577, 76.00000000002545164, -76.77734984626648895 ) ) ;
#26570=VECTOR ( 'NONE', #136741, 1000.000000000000114 ) ;
#26576=DIRECTION ( 'NONE',  ( 0.000000000000000000, -1.000000000000000000, -6.982962677686265922E-15 ) ) ;
#26590=AXIS2_PLACEMENT_3D ( 'NONE', #94421, #213090, #248372 ) ;
#26591=ORIENTED_EDGE ( 'NONE', *, *, #151440, .T. ) ;
#26600=CARTESIAN_POINT ( 'NONE',  ( -21.09316766718153247, 75.96073659769703568, -75.89326079699904426 ) ) ;
#26602=ADVANCED_FACE ( 'NONE', ( #17592 ), #116709, .T. ) ;
#26631=DIRECTION ( 'NONE',  ( 0.000000000000000000, -0.008583690987162452199, -0.9999631594459053030 ) ) ;
#26652=EDGE_CURVE ( 'NONE', #175343, #215740, #155785, .T. ) ;
#26693=AXIS2_PLACEMENT_3D ( 'NONE', #137574, #159737, #82723 ) ;
#26749=VERTEX_POINT ( 'NONE', #102241 ) ;
#26784=EDGE_CURVE ( 'NONE', #81112, #206635, #51669, .T. ) ;
#26785=VECTOR ( 'NONE', #212948, 1000.000000000000000 ) ;
#26786=DIRECTION ( 'NONE',  ( 0.000000000000000000, -7.086529944415893080E-15, 1.000000000000000000 ) ) ;
#26803=EDGE_CURVE ( 'NONE', #247138, #93424, #89114, .T. ) ;
#26804=AXIS2_PLACEMENT_3D ( 'NONE', #90262, #128134, #47278 ) ;
#26824=FACE_OUTER_BOUND ( 'NONE', #133687, .T. ) ;
#26865=AXIS2_PLACEMENT_3D ( 'NONE', #50440, #129984, #255021 ) ;
#26870=CARTESIAN_POINT ( 'NONE',  ( -21.07928932188134041, 69.67148334361836248, -69.62200263017875557 ) ) ;
#26874=DIRECTION ( 'NONE',  ( 1.000000000000000000, 0.000000000000000000, 0.000000000000000000 ) ) ;
#26883=VECTOR ( 'NONE', #164744, 1000.000000000000000 ) ;
#26884=CARTESIAN_POINT ( 'NONE',  ( 19.83283456528359423, 64.25000000001148237, -44.67310748510406171 ) ) ;
#26885=VECTOR ( 'NONE', #136944, 1000.000000000000000 ) ;
#26934=CARTESIAN_POINT ( 'NONE',  ( -20.54999999999999716, 85.50000000001149658, -45.91707660717669626 ) ) ;
#26945=EDGE_CURVE ( 'NONE', #188354, #52356, #56414, .T. ) ;
#26952=CARTESIAN_POINT ( 'NONE',  ( -21.14999999999999858, 76.00000000001170974, -76.06376443622556849 ) ) ;
#26968=LINE ( 'NONE', #242124, #82890 ) ;
#27028=LINE ( 'NONE', #52969, #176014 ) ;
#27041=ORIENTED_EDGE ( 'NONE', *, *, #125190, .T. ) ;
#27065=EDGE_LOOP ( 'NONE', ( #93464, #166277, #116353, #113668 ) ) ;
#27075=CIRCLE ( 'NONE', #39557, 1.900000000000005906 ) ;
#27089=DIRECTION ( 'NONE',  ( 0.000000000000000000, 6.982962677686266711E-15, -1.000000000000000000 ) ) ;
#27112=DIRECTION ( 'NONE',  ( -4.391705002472927119E-16, -1.000000000000000000, -7.026728003956683390E-15 ) ) ;
#27126=CARTESIAN_POINT ( 'NONE',  ( 23.15000000000000213, 85.00000000001149658, -45.91707660717670336 ) ) ;
#27182=ORIENTED_EDGE ( 'NONE', *, *, #213058, .T. ) ;
#27206=EDGE_LOOP ( 'NONE', ( #163321, #137463, #250823, #70220 ) ) ;
#27213=CARTESIAN_POINT ( 'NONE',  ( 21.14999999999999858, 76.00000000001165290, -69.52310748452431710 ) ) ;
#27214=CARTESIAN_POINT ( 'NONE',  ( -23.15000000000000213, 76.00000000001142553, -36.02310748452432421 ) ) ;
#27236=EDGE_CURVE ( 'NONE', #86432, #175343, #223195, .T. ) ;
#27240=DIRECTION ( 'NONE',  ( 1.000000000000000000, 0.000000000000000000, 0.000000000000000000 ) ) ;
#27309=EDGE_CURVE ( 'NONE', #159302, #249063, #218645, .T. ) ;
#27326=PLANE ( 'NONE',  #254923 ) ;
#27345=CARTESIAN_POINT ( 'NONE',  ( 23.14999999999999858, 64.35000000001146248, -43.03791325517834565 ) ) ;
#27369=CARTESIAN_POINT ( 'NONE',  ( 18.54147908293623459, 85.46326165793961138, -62.47415858776833630 ) ) ;
#27387=DIRECTION ( 'NONE',  ( 7.304098846218134667E-16, 1.000000000000000000, 6.982962677686267499E-15 ) ) ;
#27404=AXIS2_PLACEMENT_3D ( 'NONE', #112088, #31291, #168235 ) ;
#27421=VERTEX_POINT ( 'NONE', #93959 ) ;
#27436=CARTESIAN_POINT ( 'NONE',  ( -21.55000000000000071, 68.85000000001151932, -48.27310748452437394 ) ) ;
#27442=ORIENTED_EDGE ( 'NONE', *, *, #69375, .F. ) ;
#27443=ORIENTED_EDGE ( 'NONE', *, *, #133327, .T. ) ;
#27444=DIRECTION ( 'NONE',  ( 0.000000000000000000, 0.000000000000000000, 1.000000000000000000 ) ) ;
#27462=DIRECTION ( 'NONE',  ( 0.000000000000000000, -6.467318590049456648E-15, 1.000000000000000000 ) ) ;
#27465=CIRCLE ( 'NONE', #1880, 0.09999999999999799327 ) ;
#27498=LINE ( 'NONE', #69172, #11953 ) ;
#27499=ADVANCED_FACE ( 'NONE', ( #131162 ), #30814, .T. ) ;
#27506=ORIENTED_EDGE ( 'NONE', *, *, #252656, .F. ) ;
#27510=CIRCLE ( 'NONE', #198147, 0.09999999999999939493 ) ;
#27552=VECTOR ( 'NONE', #217646, 999.9999999999998863 ) ;
#27556=DIRECTION ( 'NONE',  ( 0.000000000000000000, 1.000000000000000000, 6.982962677686266711E-15 ) ) ;
#27611=ORIENTED_EDGE ( 'NONE', *, *, #136357, .F. ) ;
#27652=ADVANCED_FACE ( 'NONE', ( #73794 ), #75081, .F. ) ;
#27669=ADVANCED_FACE ( 'NONE', ( #162309 ), #43637, .F. ) ;
#27771=ORIENTED_EDGE ( 'NONE', *, *, #253489, .T. ) ;
#27772=DIRECTION ( 'NONE',  ( 1.000000000000000000, 0.000000000000000000, 0.000000000000000000 ) ) ;
#27789=AXIS2_PLACEMENT_3D ( 'NONE', #231336, #136036, #52664 ) ;
#27790=AXIS2_PLACEMENT_3D ( 'NONE', #186064, #226441, #244730 ) ;
#27804=ORIENTED_EDGE ( 'NONE', *, *, #222690, .F. ) ;
#27812=CARTESIAN_POINT ( 'NONE',  ( 21.05000000000000071, 65.37127968600724159, -61.85819391543678591 ) ) ;
#27821=ORIENTED_EDGE ( 'NONE', *, *, #128235, .T. ) ;
#27828=AXIS2_PLACEMENT_3D ( 'NONE', #22945, #102417, #185840 ) ;
#27851=CIRCLE ( 'NONE', #86237, 0.1000000000000028644 ) ;
#27859=DIRECTION ( 'NONE',  ( 0.000000000000000000, -6.982962677686266711E-15, 1.000000000000000000 ) ) ;
#27876=CARTESIAN_POINT ( 'NONE',  ( -20.54999999999999716, 74.00000000001151079, -49.24772940728643533 ) ) ;
#27923=ORIENTED_EDGE ( 'NONE', *, *, #71583, .F. ) ;
#27948=CARTESIAN_POINT ( 'NONE',  ( 21.30000000000002558, 76.00000000001162448, -65.47310748452431994 ) ) ;
#27950=DIRECTION ( 'NONE',  ( 0.000000000000000000, 0.000000000000000000, 1.000000000000000000 ) ) ;
#27968=SPHERICAL_SURFACE ( 'NONE', #139032, 0.1000000000000000056 ) ;
#27987=CARTESIAN_POINT ( 'NONE',  ( 21.13614978966381841, 76.00000000001169553, -76.02221218635807531 ) ) ;
#28000=FACE_OUTER_BOUND ( 'NONE', #160809, .T. ) ;
#28015=CIRCLE ( 'NONE', #86228, 11.64999999999999325 ) ;
#28048=DIRECTION ( 'NONE',  ( 0.000000000000000000, -7.056502275159890832E-15, 1.000000000000000000 ) ) ;
#28078=LINE ( 'NONE', #106274, #252428 ) ;
#28129=ORIENTED_EDGE ( 'NONE', *, *, #5215, .F. ) ;
#28140=ORIENTED_EDGE ( 'NONE', *, *, #26945, .T. ) ;
#28142=EDGE_CURVE ( 'NONE', #215216, #191947, #77306, .T. ) ;
#28161=DIRECTION ( 'NONE',  ( 0.000000000000000000, -6.982962677686266711E-15, 1.000000000000000000 ) ) ;
#28193=CIRCLE ( 'NONE', #144667, 0.1000000000000028644 ) ;
#28222=ORIENTED_EDGE ( 'NONE', *, *, #100002, .F. ) ;
#28223=ORIENTED_EDGE ( 'NONE', *, *, #145268, .F. ) ;
#28236=DIRECTION ( 'NONE',  ( 1.000000000000000000, 0.000000000000000000, 0.000000000000000000 ) ) ;
#28252=DIRECTION ( 'NONE',  ( 0.000000000000000000, -1.000000000000000000, 0.000000000000000000 ) ) ;
#28289=DIRECTION ( 'NONE',  ( -1.000000000000000000, -7.304098846218105085E-16, -4.217023435051676515E-16 ) ) ;
#28310=CIRCLE ( 'NONE', #90614, 0.3999999999999975797 ) ;
#28315=CIRCLE ( 'NONE', #61606, 0.1000000000000028644 ) ;
#28363=AXIS2_PLACEMENT_3D ( 'NONE', #138587, #60362, #218137 ) ;
#28370=EDGE_LOOP ( 'NONE', ( #20998, #98900, #188652, #222905 ) ) ;
#28406=ORIENTED_EDGE ( 'NONE', *, *, #59246, .T. ) ;
#28468=CIRCLE ( 'NONE', #249200, 0.09999999999999939493 ) ;
#28497=AXIS2_PLACEMENT_3D ( 'NONE', #106666, #101515, #123698 ) ;
#28498=ADVANCED_FACE ( 'NONE', ( #19613 ), #160794, .T. ) ;
#28505=CARTESIAN_POINT ( 'NONE',  ( 18.59999999999999432, 77.29973367124252093, -79.49497796165491081 ) ) ;
#28539=CARTESIAN_POINT ( 'NONE',  ( -18.50000000000000000, 74.36282728704119904, -57.94095411905231430 ) ) ;
#28556=VERTEX_POINT ( 'NONE', #82109 ) ;
#28604=LINE ( 'NONE', #32433, #113799 ) ;
#28611=CARTESIAN_POINT ( 'NONE',  ( -18.50000000000000000, 66.75000000001151079, -48.37310748452438247 ) ) ;
#28629=FACE_OUTER_BOUND ( 'NONE', #107608, .T. ) ;
#28664=DIRECTION ( 'NONE',  ( -3.469446951953515108E-14, 0.000000000000000000, -1.000000000000000000 ) ) ;
#28665=ORIENTED_EDGE ( 'NONE', *, *, #196288, .F. ) ;
#28673=DIRECTION ( 'NONE',  ( -0.000000000000000000, 1.000000000000000000, 6.982962677686266711E-15 ) ) ;
#28708=ORIENTED_EDGE ( 'NONE', *, *, #76646, .T. ) ;
#28709=EDGE_LOOP ( 'NONE', ( #212470, #49417, #71877, #67197 ) ) ;
#28771=VERTEX_POINT ( 'NONE', #214584 ) ;
#28774=EDGE_LOOP ( 'NONE', ( #22829, #39623, #147403, #143624 ) ) ;
#28797=EDGE_CURVE ( 'NONE', #116304, #78944, #123532, .T. ) ;
#28805=EDGE_CURVE ( 'NONE', #166990, #241008, #19501, .T. ) ;
#28809=ADVANCED_FACE ( 'NONE', ( #97164 ), #77623, .T. ) ;
#28832=CARTESIAN_POINT ( 'NONE',  ( 23.15000000000000213, 87.75000000001149658, -48.17310748452423752 ) ) ;
#28835=VECTOR ( 'NONE', #49597, 1000.000000000000000 ) ;
#28846=AXIS2_PLACEMENT_3D ( 'NONE', #88198, #203033, #107790 ) ;
#28852=CYLINDRICAL_SURFACE ( 'NONE', #15403, 0.1000000000000028644 ) ;
#28876=DIRECTION ( 'NONE',  ( 0.000000000000000000, -7.056502275159890832E-15, 1.000000000000000000 ) ) ;
#28920=DIRECTION ( 'NONE',  ( 1.000000000000000000, 0.000000000000000000, 0.000000000000000000 ) ) ;
#28976=CARTESIAN_POINT ( 'NONE',  ( -23.25000000000000000, 77.83585931145498193, -24.41866831572578533 ) ) ;
#28980=CARTESIAN_POINT ( 'NONE',  ( 23.14999999999999858, 71.00000000001151079, -48.42837350343745584 ) ) ;
#28994=DIRECTION ( 'NONE',  ( 1.000000000000000000, 0.000000000000000000, 0.000000000000000000 ) ) ;
#28999=AXIS2_PLACEMENT_3D ( 'NONE', #170884, #226948, #250365 ) ;
#29050=EDGE_CURVE ( 'NONE', #218543, #115457, #102648, .T. ) ;
#29057=ADVANCED_FACE ( 'NONE', ( #249585 ), #107145, .T. ) ;
#29068=DIRECTION ( 'NONE',  ( 1.000000000000000000, 0.000000000000000000, 0.000000000000000000 ) ) ;
#29082=AXIS2_PLACEMENT_3D ( 'NONE', #201582, #159920, #239445 ) ;
#29131=EDGE_CURVE ( 'NONE', #249063, #113349, #65452, .T. ) ;
#29132=EDGE_CURVE ( 'NONE', #211121, #138858, #219559, .T. ) ;
#29156=FACE_OUTER_BOUND ( 'NONE', #54619, .T. ) ;
#29159=FACE_OUTER_BOUND ( 'NONE', #119028, .T. ) ;
#29184=VECTOR ( 'NONE', #175667, 1000.000000000000000 ) ;
#29189=ORIENTED_EDGE ( 'NONE', *, *, #166328, .F. ) ;
#29230=FACE_OUTER_BOUND ( 'NONE', #125951, .T. ) ;
#29234=ORIENTED_EDGE ( 'NONE', *, *, #87920, .T. ) ;
#29271=AXIS2_PLACEMENT_3D ( 'NONE', #20089, #99581, #240415 ) ;
#29276=FACE_OUTER_BOUND ( 'NONE', #230997, .T. ) ;
#29326=LINE ( 'NONE', #128390, #203341 ) ;
#29367=AXIS2_PLACEMENT_3D ( 'NONE', #199122, #62187, #162583 ) ;
#29401=ORIENTED_EDGE ( 'NONE', *, *, #179289, .F. ) ;
#29422=EDGE_CURVE ( 'NONE', #196986, #76430, #51027, .T. ) ;
#29436=EDGE_LOOP ( 'NONE', ( #68717, #102527, #246254, #141794 ) ) ;
#29454=LINE ( 'NONE', #89367, #235548 ) ;
#29482=B_SPLINE_CURVE_WITH_KNOTS ( 'NONE', 3,
 ( #173162, #171866, #253914, #36185, #75322, #31070, #154855 ),
 .UNSPECIFIED., .F., .F.,
 ( 4, 3, 4 ),
 ( 0.000000000000000000, 1.860045280646148997E-05, 5.251155757303900822E-05 ),
 .UNSPECIFIED. ) ;
#29491=DIRECTION ( 'NONE',  ( 0.000000000000000000, -0.1495327102803180597, 0.9887567792719412774 ) ) ;
#29493=CARTESIAN_POINT ( 'NONE',  ( 18.59999999999999432, 77.83585931145498193, -24.51866831572578320 ) ) ;
#29497=VERTEX_POINT ( 'NONE', #134429 ) ;
#29500=CARTESIAN_POINT ( 'NONE',  ( 21.14999999999999503, 64.35000000001164722, -69.52310748452438816 ) ) ;
#29510=DIRECTION ( 'NONE',  ( -0.000000000000000000, 6.982962677686266711E-15, -1.000000000000000000 ) ) ;
#29548=DIRECTION ( 'NONE',  ( -1.000000000000000000, -0.000000000000000000, -0.000000000000000000 ) ) ;
#29550=DIRECTION ( 'NONE',  ( -1.000000000000000000, 0.000000000000000000, 0.000000000000000000 ) ) ;
#29558=ORIENTED_EDGE ( 'NONE', *, *, #181276, .F. ) ;
#29579=ORIENTED_EDGE ( 'NONE', *, *, #81450, .T. ) ;
#29594=ORIENTED_EDGE ( 'NONE', *, *, #168617, .T. ) ;
#29599=AXIS2_PLACEMENT_3D ( 'NONE', #62893, #104555, #6772 ) ;
#29602=CARTESIAN_POINT ( 'NONE',  ( 18.49999999999999289, 65.50857864377418593, -44.67310748452439384 ) ) ;
#29603=CARTESIAN_POINT ( 'NONE',  ( -20.94999999999999929, 68.97833521811131163, -32.18954208262707795 ) ) ;
#29614=ORIENTED_EDGE ( 'NONE', *, *, #240079, .F. ) ;
#29645=CARTESIAN_POINT ( 'NONE',  ( 18.59999999999999432, 77.16270174994961906, -61.42310748452431568 ) ) ;
#29660=TOROIDAL_SURFACE ( 'NONE', #121265, 12.77499999999999858, 0.1000000000000000056 ) ;
#29695=ORIENTED_EDGE ( 'NONE', *, *, #74740, .T. ) ;
#29698=CARTESIAN_POINT ( 'NONE',  ( -23.25000000000000000, 76.00000000001142553, -36.02310748452432421 ) ) ;
#29724=FACE_OUTER_BOUND ( 'NONE', #252978, .T. ) ;
#29745=SURFACE_SIDE_STYLE ('',( #210914 ) ) ;
#29753=DIRECTION ( 'NONE',  ( 1.000000000000000000, 0.000000000000000000, 0.000000000000000000 ) ) ;
#29865=CARTESIAN_POINT ( 'NONE',  ( 21.97500000000000497, 66.25000000001158185, -57.27310748452438816 ) ) ;
#29891=CARTESIAN_POINT ( 'NONE',  ( 22.50000000000000000, 75.90000000001172964, -81.17267829206912211 ) ) ;
#29897=AXIS2_PLACEMENT_3D ( 'NONE', #98131, #96849, #196002 ) ;
#29898=AXIS2_PLACEMENT_3D ( 'NONE', #166050, #147750, #146436 ) ;
#29935=ADVANCED_FACE ( 'NONE', ( #155019 ), #174617, .T. ) ;
#29937=CARTESIAN_POINT ( 'NONE',  ( 23.14999999999998437, 64.25000000001165290, -69.52310748452440237 ) ) ;
#29949=EDGE_LOOP ( 'NONE', ( #137739, #36410, #63039, #78673 ) ) ;
#29953=DIRECTION ( 'NONE',  ( -1.000000000000000000, 0.000000000000000000, -0.000000000000000000 ) ) ;
#29962=CYLINDRICAL_SURFACE ( 'NONE', #206341, 0.1000000000000028644 ) ;
#30009=ORIENTED_EDGE ( 'NONE', *, *, #174916, .F. ) ;
#30032=VERTEX_POINT ( 'NONE', #220101 ) ;
#30040=( BOUNDED_SURFACE ( )  B_SPLINE_SURFACE ( 3, 2, ( 
 ( #186024, #246005, #227703 ),
 ( #89474, #109040, #124778 ),
 ( #188582, #169069, #50337 ),
 ( #69950, #146871, #163900 ),
 ( #88172, #47773, #209429 ),
 ( #68654, #126035, #105151 ) ),
 .UNSPECIFIED., .F., .F., .F. ) 
 B_SPLINE_SURFACE_WITH_KNOTS ( ( 4, 2, 4 ),
 ( 3, 3 ),
 ( -1.776356839400250465E-15, 0.7853981633974468357, 1.570796326794895448 ),
 ( 0.000000000000000000, 1.000000000000000000 ),
 .UNSPECIFIED. ) 
 GEOMETRIC_REPRESENTATION_ITEM ( )  RATIONAL_B_SPLINE_SURFACE ( (
 ( 1.000000000000000000, 0.4999999999999704681, 1.000000000000000000),
 ( 1.000000000000000000, 0.4993418825335544931, 1.000000000000000000),
 ( 1.000000000000000000, 0.5278258667056193731, 1.000000000000000000),
 ( 1.000000000000000000, 0.6092287576697977824, 1.000000000000000000),
 ( 1.000000000000000000, 0.6611148371777476607, 1.000000000000000000),
 ( 1.000000000000000000, 0.7071067811865597852, 1.000000000000000000) ) ) 
 REPRESENTATION_ITEM ( '' )  SURFACE ( )  );
#30069=ADVANCED_FACE ( 'NONE', ( #238366 ), #59715, .F. ) ;
#30128=ORIENTED_EDGE ( 'NONE', *, *, #110219, .F. ) ;
#30130=CARTESIAN_POINT ( 'NONE',  ( 21.05000000000000071, 76.00000000001165290, -69.52310748452431710 ) ) ;
#30143=DIRECTION ( 'NONE',  ( -1.000000000000000000, 0.000000000000000000, -0.000000000000000000 ) ) ;
#30147=CARTESIAN_POINT ( 'NONE',  ( 20.94999999999999574, 87.75000000001162448, -66.62310748452424036 ) ) ;
#30169=FACE_OUTER_BOUND ( 'NONE', #14457, .T. ) ;
#30177=DIRECTION ( 'NONE',  ( 0.000000000000000000, -1.000000000000000000, -6.860497997771531562E-15 ) ) ;
#30189=CARTESIAN_POINT ( 'NONE',  ( 20.85000000000000142, 76.00000000001142553, -36.02310748452432421 ) ) ;
#30216=ORIENTED_EDGE ( 'NONE', *, *, #162057, .T. ) ;
#30229=CARTESIAN_POINT ( 'NONE',  ( -18.39999999999999858, 85.68240343348777799, -29.36626410711146562 ) ) ;
#30240=EDGE_CURVE ( 'NONE', #169064, #43818, #255777, .T. ) ;
#30296=DIRECTION ( 'NONE',  ( 1.000000000000000000, 0.000000000000000000, 0.000000000000000000 ) ) ;
#30299=ORIENTED_EDGE ( 'NONE', *, *, #233349, .F. ) ;
#30309=CARTESIAN_POINT ( 'NONE',  ( -23.25000000000000000, 76.00000000001136868, -28.12310748452432208 ) ) ;
#30341=ORIENTED_EDGE ( 'NONE', *, *, #110912, .F. ) ;
#30354=DIRECTION ( 'NONE',  ( -1.040834085586054343E-13, 0.9999176327611370985, 0.01283462868040226822 ) ) ;
#30384=CARTESIAN_POINT ( 'NONE',  ( 22.50000000000000000, 75.90000000001170122, -77.31388708289770761 ) ) ;
#30407=ORIENTED_EDGE ( 'NONE', *, *, #64179, .T. ) ;
#30436=EDGE_CURVE ( 'NONE', #110098, #46741, #68750, .T. ) ;
#30472=AXIS2_PLACEMENT_3D ( 'NONE', #237780, #138640, #218187 ) ;
#30486=CARTESIAN_POINT ( 'NONE',  ( 21.05000000000000071, 64.40000000001145963, -42.95131071479990936 ) ) ;
#30497=CARTESIAN_POINT ( 'NONE',  ( -22.50000000000094147, 75.90000000001182912, -81.17267829206915053 ) ) ;
#30519=ORIENTED_EDGE ( 'NONE', *, *, #76646, .F. ) ;
#30537=LINE ( 'NONE', #245712, #74297 ) ;
#30542=ADVANCED_FACE ( 'NONE', ( #112373 ), #150221, .T. ) ;
#30547=ORIENTED_EDGE ( 'NONE', *, *, #64373, .T. ) ;
#30558=CARTESIAN_POINT ( 'NONE',  ( -22.59999999999999787, 64.25043287652226809, -69.62396585362311896 ) ) ;
#30585=DIRECTION ( 'NONE',  ( 0.000000000000000000, -1.000000000000000000, 2.771150684185008344E-14 ) ) ;
#30640=CARTESIAN_POINT ( 'NONE',  ( 21.05000000000000071, 67.22371710471912820, -61.03510676294002479 ) ) ;
#30648=CARTESIAN_POINT ( 'NONE',  ( -21.52071067811865746, 68.22071067813014622, -48.37310748452437537 ) ) ;
#30678=ORIENTED_EDGE ( 'NONE', *, *, #231145, .F. ) ;
#30729=VERTEX_POINT ( 'NONE', #198307 ) ;
#30753=VECTOR ( 'NONE', #72241, 1000.000000000000000 ) ;
#30764=CARTESIAN_POINT ( 'NONE',  ( -21.05000000000000071, 76.00000000001159606, -61.62310748452431852 ) ) ;
#30773=ADVANCED_FACE ( 'NONE', ( #139597 ), #218748, .F. ) ;
#30787=DIRECTION ( 'NONE',  ( -1.000000000000000000, 1.836970198721029934E-16, 1.601412966608202925E-30 ) ) ;
#30791=CIRCLE ( 'NONE', #84893, 0.09999999999999939493 ) ;
#30793=DIRECTION ( 'NONE',  ( 0.000000000000000000, 0.000000000000000000, 1.000000000000000000 ) ) ;
#30796=AXIS2_PLACEMENT_3D ( 'NONE', #162198, #244260, #44799 ) ;
#30814=CYLINDRICAL_SURFACE ( 'NONE', #81091, 0.1000000000000028644 ) ;
#30817=ORIENTED_EDGE ( 'NONE', *, *, #66350, .F. ) ;
#30829=AXIS2_PLACEMENT_3D ( 'NONE', #94646, #218431, #116785 ) ;
#30876=ORIENTED_EDGE ( 'NONE', *, *, #12814, .T. ) ;
#30890=CARTESIAN_POINT ( 'NONE',  ( 18.49999999999928946, 65.55993210786621717, -44.75598973563730709 ) ) ;
#30906=CARTESIAN_POINT ( 'NONE',  ( 18.49999999999999289, 65.79142135624879018, -44.87310748452438958 ) ) ;
#30946=ORIENTED_EDGE ( 'NONE', *, *, #227545, .T. ) ;
#30949=LINE ( 'NONE', #32220, #137566 ) ;
#30952=ORIENTED_EDGE ( 'NONE', *, *, #156228, .T. ) ;
#30955=FACE_OUTER_BOUND ( 'NONE', #52451, .T. ) ;
#30964=AXIS2_PLACEMENT_3D ( 'NONE', #46434, #45159, #225059 ) ;
#30969=DIRECTION ( 'NONE',  ( -2.827886303505248766E-16, -0.8660254037844377084, -0.5000000000000015543 ) ) ;
#30978=CIRCLE ( 'NONE', #218362, 0.1000000000000028644 ) ;
#31020=ORIENTED_EDGE ( 'NONE', *, *, #46408, .F. ) ;
#31070=CARTESIAN_POINT ( 'NONE',  ( -22.50000000000000000, 64.35023708197972780, -69.61191746091132870 ) ) ;
#31091=DIRECTION ( 'NONE',  ( 1.000000000000000000, 0.000000000000000000, 0.000000000000000000 ) ) ;
#31122=ADVANCED_FACE ( 'NONE', ( #11881 ), #169691, .T. ) ;
#31145=AXIS2_PLACEMENT_3D ( 'NONE', #82938, #80375, #101208 ) ;
#31165=EDGE_LOOP ( 'NONE', ( #244128, #51541, #74122, #6582 ) ) ;
#31175=VECTOR ( 'NONE', #115186, 1000.000000000000000 ) ;
#31201=ORIENTED_EDGE ( 'NONE', *, *, #61826, .F. ) ;
#31204=ADVANCED_FACE ( 'NONE', ( #90089 ), #181567, .F. ) ;
#31208=EDGE_CURVE ( 'NONE', #255306, #247138, #226752, .T. ) ;
#31220=AXIS2_PLACEMENT_3D ( 'NONE', #230683, #54591, #52011 ) ;
#31240=LINE ( 'NONE', #229404, #15504 ) ;
#31243=EDGE_CURVE ( 'NONE', #218543, #47449, #27465, .T. ) ;
#31277=DIRECTION ( 'NONE',  ( 1.000000000000000000, 0.000000000000000000, 0.000000000000000000 ) ) ;
#31291=DIRECTION ( 'NONE',  ( -1.000000000000000000, -0.000000000000000000, -0.000000000000000000 ) ) ;
#31316=SPHERICAL_SURFACE ( 'NONE', #139233, 0.1000000000000000056 ) ;
#31341=DIRECTION ( 'NONE',  ( 1.000000000000000000, 0.000000000000000000, 0.000000000000000000 ) ) ;
#31360=CIRCLE ( 'NONE', #243699, 0.5000000000000004441 ) ;
#31363=DIRECTION ( 'NONE',  ( 0.000000000000000000, 6.982962677686266711E-15, -1.000000000000000000 ) ) ;
#31405=AXIS2_PLACEMENT_3D ( 'NONE', #42894, #235942, #136846 ) ;
#31419=FACE_OUTER_BOUND ( 'NONE', #114338, .T. ) ;
#31422=VERTEX_POINT ( 'NONE', #202047 ) ;
#31424=CARTESIAN_POINT ( 'NONE',  ( -23.15000000000000213, 76.00000000001156764, -56.64810748452432421 ) ) ;
#31438=DIRECTION ( 'NONE',  ( 0.000000000000000000, 0.8660254037844378194, 0.5000000000000016653 ) ) ;
#31449=CARTESIAN_POINT ( 'NONE',  ( 20.94999999999999929, 65.70729864260954400, -30.56574559737246233 ) ) ;
#31484=CIRCLE ( 'NONE', #64752, 0.1000000000000043771 ) ;
#31688=ORIENTED_EDGE ( 'NONE', *, *, #104620, .T. ) ;
#31698=VECTOR ( 'NONE', #26304, 1000.000000000000000 ) ;
#31699=ORIENTED_EDGE ( 'NONE', *, *, #187916, .T. ) ;
#31735=ORIENTED_EDGE ( 'NONE', *, *, #150494, .F. ) ;
#31772=VERTEX_POINT ( 'NONE', #149167 ) ;
#31797=DIRECTION ( 'NONE',  ( 0.000000000000000000, 6.982962677686266711E-15, -1.000000000000000000 ) ) ;
#31803=EDGE_CURVE ( 'NONE', #40625, #88995, #89158, .T. ) ;
#31815=ORIENTED_EDGE ( 'NONE', *, *, #160399, .T. ) ;
#31846=DIRECTION ( 'NONE',  ( 0.000000000000000000, -1.000000000000000000, -7.272083257015735086E-15 ) ) ;
#31850=DIRECTION ( 'NONE',  ( 0.000000000000000000, -6.982962677686266711E-15, 1.000000000000000000 ) ) ;
#31870=ORIENTED_EDGE ( 'NONE', *, *, #27236, .F. ) ;
#31889=CARTESIAN_POINT ( 'NONE',  ( 21.08804281139606829, 65.37816569817040602, -57.17310751714594375 ) ) ;
#31902=AXIS2_PLACEMENT_3D ( 'NONE', #88049, #167642, #244580 ) ;
#31903=CIRCLE ( 'NONE', #235870, 0.1000000000000011990 ) ;
#31910=ORIENTED_EDGE ( 'NONE', *, *, #26483, .F. ) ;
#31945=CARTESIAN_POINT ( 'NONE',  ( 21.05000000000000071, 71.00000000001158185, -57.11784146561126363 ) ) ;
#31956=ORIENTED_EDGE ( 'NONE', *, *, #167966, .F. ) ;
#31971=DIRECTION ( 'NONE',  ( 0.000000000000000000, -6.982962677686266711E-15, 1.000000000000000000 ) ) ;
#31993=EDGE_CURVE ( 'NONE', #196290, #196513, #64614, .T. ) ;
#31994=FACE_OUTER_BOUND ( 'NONE', #17205, .T. ) ;
#32012=DIRECTION ( 'NONE',  ( 0.000000000000000000, -7.056502275159890832E-15, 1.000000000000000000 ) ) ;
#32015=ORIENTED_EDGE ( 'NONE', *, *, #41549, .F. ) ;
#32016=EDGE_CURVE ( 'NONE', #43683, #196513, #214459, .T. ) ;
#32056=ORIENTED_EDGE ( 'NONE', *, *, #72374, .F. ) ;
#32060=CARTESIAN_POINT ( 'NONE',  ( 23.14999999999999858, 70.40000000001150227, -48.42837350343745584 ) ) ;
#32064=ORIENTED_EDGE ( 'NONE', *, *, #175334, .T. ) ;
#32096=ADVANCED_FACE ( 'NONE', ( #143695 ), #160520, .F. ) ;
#32099=DIRECTION ( 'NONE',  ( 0.000000000000000000, 0.000000000000000000, 1.000000000000000000 ) ) ;
#32159=AXIS2_PLACEMENT_3D ( 'NONE', #52642, #128353, #207903 ) ;
#32169=CARTESIAN_POINT ( 'NONE',  ( -23.15000000000000213, 71.85000000001157616, -57.17310748452435121 ) ) ;
#32181=CARTESIAN_POINT ( 'NONE',  ( -20.85000000000000142, 77.16412189325258453, -28.10825939895270764 ) ) ;
#32193=CARTESIAN_POINT ( 'NONE',  ( -20.94999999999999929, 74.63912941281955682, -61.45010955743337178 ) ) ;
#32220=CARTESIAN_POINT ( 'NONE',  ( -18.50000000000000000, 102.4393534156124730, -51.38159887701667827 ) ) ;
#32221=AXIS2_PLACEMENT_3D ( 'NONE', #29698, #188733, #143180 ) ;
#32281=AXIS2_PLACEMENT_3D ( 'NONE', #94136, #113706, #193255 ) ;
#32306=CIRCLE ( 'NONE', #132231, 0.2000000000000057288 ) ;
#32308=( LENGTH_UNIT ( ) NAMED_UNIT ( * ) SI_UNIT ( .MILLI., .METRE. ) );
#32319=CARTESIAN_POINT ( 'NONE',  ( -23.15000000000000213, 74.07476635515169505, -48.75335101765046630 ) ) ;
#32328=VERTEX_POINT ( 'NONE', #217773 ) ;
#32386=CARTESIAN_POINT ( 'NONE',  ( -21.05000000000000071, 75.74389420791943905, -69.55800392619661920 ) ) ;
#32417=AXIS2_PLACEMENT_3D ( 'NONE', #163633, #3242, #200189 ) ;
#32428=CIRCLE ( 'NONE', #73544, 0.1000000000000028644 ) ;
#32433=CARTESIAN_POINT ( 'NONE',  ( -21.05000000000000071, 74.16465844978715438, -57.86795619196135476 ) ) ;
#32458=EDGE_LOOP ( 'NONE', ( #16279, #115975, #204056, #111535 ) ) ;
#32481=AXIS2_PLACEMENT_3D ( 'NONE', #111559, #154567, #236621 ) ;
#32505=ORIENTED_EDGE ( 'NONE', *, *, #181276, .T. ) ;
#32507=CARTESIAN_POINT ( 'NONE',  ( -18.49999999999998934, 85.48068669529035901, -29.08199231576640642 ) ) ;
#32510=DIRECTION ( 'NONE',  ( -1.000000000000000000, 0.000000000000000000, -0.000000000000000000 ) ) ;
#32516=CARTESIAN_POINT ( 'NONE',  ( 21.14999999999999858, 69.45934304831041572, -69.52310748452435973 ) ) ;
#32527=AXIS2_PLACEMENT_3D ( 'NONE', #203367, #186381, #123835 ) ;
#32538=CIRCLE ( 'NONE', #144908, 0.09999999999999939493 ) ;
#32588=ORIENTED_EDGE ( 'NONE', *, *, #208917, .T. ) ;
#32598=CARTESIAN_POINT ( 'NONE',  ( 23.14999999999999858, 76.00000000001142553, -36.02310748452432421 ) ) ;
#32613=VERTEX_POINT ( 'NONE', #247627 ) ;
#32644=DIRECTION ( 'NONE',  ( 0.000000000000000000, 0.4930308989875575865, 0.8700118002898125091 ) ) ;
#32700=DIRECTION ( 'NONE',  ( 1.000000000000000000, 0.000000000000000000, 0.000000000000000000 ) ) ;
#32721=DIRECTION ( 'NONE',  ( 0.000000000000000000, -1.000000000000000000, -6.982962677686266711E-15 ) ) ;
#32728=VECTOR ( 'NONE', #81266, 1000.000000000000000 ) ;
#32747=CIRCLE ( 'NONE', #107709, 0.1000000000000028644 ) ;
#32760=CARTESIAN_POINT ( 'NONE',  ( 20.95512820512820440, 65.37615131629962661, -48.27310748452439526 ) ) ;
#32780=CARTESIAN_POINT ( 'NONE',  ( 18.49999999999998934, 65.75000000001149658, -44.87310748452439668 ) ) ;
#32791=AXIS2_PLACEMENT_3D ( 'NONE', #143412, #77328, #123866 ) ;
#32806=EDGE_CURVE ( 'NONE', #170828, #148530, #23341, .T. ) ;
#32810=CARTESIAN_POINT ( 'NONE',  ( 23.14999999999999858, 73.90000000001141700, -36.02310748452433842 ) ) ;
#32822=DIRECTION ( 'NONE',  ( 1.000000000000000000, 0.000000000000000000, 0.000000000000000000 ) ) ;
#32828=EDGE_CURVE ( 'NONE', #176547, #115707, #239983, .T. ) ;
#32865=AXIS2_PLACEMENT_3D ( 'NONE', #205171, #26576, #106063 ) ;
#32867=ORIENTED_EDGE ( 'NONE', *, *, #230628, .F. ) ;
#32930=AXIS2_PLACEMENT_3D ( 'NONE', #77386, #235200, #76114 ) ;
#32938=ORIENTED_EDGE ( 'NONE', *, *, #134717, .F. ) ;
#32968=CARTESIAN_POINT ( 'NONE',  ( -23.25000000000000000, 87.75000000001143974, -39.12310748452424747 ) ) ;
#32984=ORIENTED_EDGE ( 'NONE', *, *, #33638, .T. ) ;
#33004=VECTOR ( 'NONE', #104082, 1000.000000000000000 ) ;
#33017=ADVANCED_FACE ( 'NONE', ( #109077 ), #119165, .F. ) ;
#33019=LINE ( 'NONE', #112515, #131416 ) ;
#33030=EDGE_CURVE ( 'NONE', #34147, #45256, #106671, .T. ) ;
#33032=ORIENTED_EDGE ( 'NONE', *, *, #228377, .T. ) ;
#33077=ORIENTED_EDGE ( 'NONE', *, *, #2790, .T. ) ;
#33116=EDGE_CURVE ( 'NONE', #21197, #147150, #225158, .T. ) ;
#33132=CARTESIAN_POINT ( 'NONE',  ( 21.05563370358598263, 65.27576964416506655, -57.34001666856132573 ) ) ;
#33134=DIRECTION ( 'NONE',  ( -1.000000000000000000, 0.000000000000000000, 0.000000000000000000 ) ) ;
#33146=LINE ( 'NONE', #253420, #197132 ) ;
#33150=VERTEX_POINT ( 'NONE', #92088 ) ;
#33158=EDGE_LOOP ( 'NONE', ( #179459, #255449, #231274, #3366, #193194 ) ) ;
#33191=ORIENTED_EDGE ( 'NONE', *, *, #123735, .F. ) ;
#33193=EDGE_CURVE ( 'NONE', #47449, #174034, #165141, .T. ) ;
#33196=ORIENTED_EDGE ( 'NONE', *, *, #107991, .T. ) ;
#33216=ORIENTED_EDGE ( 'NONE', *, *, #248310, .F. ) ;
#33300=CARTESIAN_POINT ( 'NONE',  ( 20.85000000000000142, 76.00000000001142553, -36.02310748452432421 ) ) ;
#33333=EDGE_CURVE ( 'NONE', #144573, #49235, #256660, .T. ) ;
#33391=ADVANCED_FACE ( 'NONE', ( #127065 ), #140165, .T. ) ;
#33416=ORIENTED_EDGE ( 'NONE', *, *, #77916, .F. ) ;
#33431=DIRECTION ( 'NONE',  ( 0.000000000000000000, 0.000000000000000000, 1.000000000000000000 ) ) ;
#33481=CARTESIAN_POINT ( 'NONE',  ( -20.99551997958381833, 64.25000000001146816, -42.87144834683500960 ) ) ;
#33511=FACE_OUTER_BOUND ( 'NONE', #12034, .T. ) ;
#33524=AXIS2_PLACEMENT_3D ( 'NONE', #37537, #35002, #257796 ) ;
#33553=LINE ( 'NONE', #131312, #166683 ) ;
#33572=VERTEX_POINT ( 'NONE', #19650 ) ;
#33575=DIRECTION ( 'NONE',  ( 1.000000000000000000, 0.000000000000000000, 0.000000000000000000 ) ) ;
#33638=EDGE_CURVE ( 'NONE', #136422, #181531, #211116, .T. ) ;
#33643=ORIENTED_EDGE ( 'NONE', *, *, #234632, .T. ) ;
#33647=CARTESIAN_POINT ( 'NONE',  ( 20.94999999999999929, 70.15000000001148805, -46.15560470880229360 ) ) ;
#33657=DIRECTION ( 'NONE',  ( -1.000000000000000000, -0.000000000000000000, -0.000000000000000000 ) ) ;
#33674=ORIENTED_EDGE ( 'NONE', *, *, #37358, .F. ) ;
#33680=ORIENTED_EDGE ( 'NONE', *, *, #85600, .T. ) ;
#33696=ORIENTED_EDGE ( 'NONE', *, *, #191107, .F. ) ;
#33712=DIRECTION ( 'NONE',  ( 0.000000000000000000, 0.000000000000000000, 1.000000000000000000 ) ) ;
#33729=EDGE_CURVE ( 'NONE', #245148, #41808, #73767, .T. ) ;
#33755=ORIENTED_EDGE ( 'NONE', *, *, #192497, .T. ) ;
#33764=DIRECTION ( 'NONE',  ( 0.000000000000000000, 0.000000000000000000, 1.000000000000000000 ) ) ;
#33776=ORIENTED_EDGE ( 'NONE', *, *, #23556, .F. ) ;
#33790=DIRECTION ( 'NONE',  ( 0.7071067811865474617, -0.7071067811865474617, -4.937700262164531476E-15 ) ) ;
#33791=CYLINDRICAL_SURFACE ( 'NONE', #148234, 0.09999999999999939493 ) ;
#33803=EDGE_CURVE ( 'NONE', #41312, #17643, #31240, .T. ) ;
#33812=ORIENTED_EDGE ( 'NONE', *, *, #200995, .T. ) ;
#33832=ORIENTED_EDGE ( 'NONE', *, *, #62428, .T. ) ;
#33852=DIRECTION ( 'NONE',  ( 0.000000000000000000, -6.661338147750933721E-15, 1.000000000000000000 ) ) ;
#33865=EDGE_CURVE ( 'NONE', #4626, #87766, #107237, .T. ) ;
#33900=VERTEX_POINT ( 'NONE', #174614 ) ;
#33902=ADVANCED_FACE ( 'NONE', ( #117152 ), #255315, .F. ) ;
#33907=ORIENTED_EDGE ( 'NONE', *, *, #37688, .T. ) ;
#33926=STYLED_ITEM ( 'NONE', ( #85986 ), #24390 ) ;
#33971=EDGE_CURVE ( 'NONE', #174834, #116521, #95007, .T. ) ;
#33992=DIRECTION ( 'NONE',  ( -2.840903330521632269E-16, -0.8700118002898356018, 0.4930308989875170078 ) ) ;
#34020=CARTESIAN_POINT ( 'NONE',  ( 21.12757541349815682, 69.52661942876019907, -69.52826870033410955 ) ) ;
#34059=CARTESIAN_POINT ( 'NONE',  ( -20.94999999999999929, 76.00000000001149658, -47.82310748452432136 ) ) ;
#34067=ORIENTED_EDGE ( 'NONE', *, *, #154904, .T. ) ;
#34109=EDGE_CURVE ( 'NONE', #122601, #76430, #215565, .T. ) ;
#34110=CYLINDRICAL_SURFACE ( 'NONE', #34602, 0.1000000000000028644 ) ;
#34118=ADVANCED_FACE ( 'NONE', ( #162700 ), #169141, .T. ) ;
#34135=EDGE_LOOP ( 'NONE', ( #33077, #191257, #50941, #172938 ) ) ;
#34147=VERTEX_POINT ( 'NONE', #47848 ) ;
#34165=CARTESIAN_POINT ( 'NONE',  ( 18.41356215285962250, 85.50000000001165290, -62.49103808782466984 ) ) ;
#34183=CIRCLE ( 'NONE', #134087, 0.5000000000000004441 ) ;
#34184=ORIENTED_EDGE ( 'NONE', *, *, #77597, .T. ) ;
#34192=ORIENTED_EDGE ( 'NONE', *, *, #39591, .F. ) ;
#34210=ORIENTED_EDGE ( 'NONE', *, *, #179107, .F. ) ;
#34274=DIRECTION ( 'NONE',  ( 0.000000000000000000, 6.982962677686266711E-15, -1.000000000000000000 ) ) ;
#34359=CARTESIAN_POINT ( 'NONE',  ( -22.39999999999999858, 76.10085836911045476, -81.27267460801371612 ) ) ;
#34386=AXIS2_PLACEMENT_3D ( 'NONE', #66568, #185226, #88660 ) ;
#34394=ORIENTED_EDGE ( 'NONE', *, *, #66504, .F. ) ;
#34410=AXIS2_PLACEMENT_3D ( 'NONE', #208133, #214218, #209389 ) ;
#34424=AXIS2_PLACEMENT_3D ( 'NONE', #195067, #659, #97174 ) ;
#34426=ORIENTED_EDGE ( 'NONE', *, *, #33193, .T. ) ;
#34501=CIRCLE ( 'NONE', #1131, 0.1000000000000028644 ) ;
#34575=CARTESIAN_POINT ( 'NONE',  ( 20.84999999999999432, 68.97833521811131163, -32.18954208262707795 ) ) ;
#34602=AXIS2_PLACEMENT_3D ( 'NONE', #57464, #52324, #91480 ) ;
#34610=CYLINDRICAL_SURFACE ( 'NONE', #133627, 0.1000000000000028644 ) ;
#34626=EDGE_CURVE ( 'NONE', #216194, #184441, #139793, .T. ) ;
#34666=DIRECTION ( 'NONE',  ( 0.000000000000000000, -6.547589603894048205E-15, 1.000000000000000000 ) ) ;
#34673=DIRECTION ( 'NONE',  ( 0.000000000000000000, -0.4999999999999689138, 0.8660254037844565822 ) ) ;
#34698=ORIENTED_EDGE ( 'NONE', *, *, #17075, .F. ) ;
#34725=ORIENTED_EDGE ( 'NONE', *, *, #200976, .T. ) ;
#34740=CIRCLE ( 'NONE', #155567, 11.75000000000000000 ) ;
#34743=FACE_OUTER_BOUND ( 'NONE', #7127, .T. ) ;
#34748=CARTESIAN_POINT ( 'NONE',  ( -20.94999999999999929, 64.25000000001146816, -42.80697314750249660 ) ) ;
#34768=CIRCLE ( 'NONE', #184750, 3.999999999999996447 ) ;
#34779=CARTESIAN_POINT ( 'NONE',  ( 18.59999999999999076, 77.83585931145498193, -24.41866831572578533 ) ) ;
#34796=CIRCLE ( 'NONE', #93032, 12.87499999999999822 ) ;
#34811=CARTESIAN_POINT ( 'NONE',  ( 18.41416235934318379, 85.50000000001136868, -29.42291809330221497 ) ) ;
#34834=TOROIDAL_SURFACE ( 'NONE', #101391, 11.70000000000000107, 0.1000000000000000056 ) ;
#34837=EDGE_LOOP ( 'NONE', ( #228465, #107901, #111217, #222328 ) ) ;
#34854=DIRECTION ( 'NONE',  ( -1.000000000000000000, -0.000000000000000000, -0.000000000000000000 ) ) ;
#34860=ORIENTED_EDGE ( 'NONE', *, *, #190774, .F. ) ;
#34877=VERTEX_POINT ( 'NONE', #227525 ) ;
#34891=CARTESIAN_POINT ( 'NONE',  ( -18.39999999999999858, 85.60000000001160458, -62.49103808782458458 ) ) ;
#34894=ORIENTED_EDGE ( 'NONE', *, *, #231933, .T. ) ;
#34979=LINE ( 'NONE', #100006, #240837 ) ;
#34980=CARTESIAN_POINT ( 'NONE',  ( 20.94999999999999929, 85.50000000001159606, -59.62913836187181715 ) ) ;
#34981=DIRECTION ( 'NONE',  ( 0.000000000000000000, 6.938893903907222067E-15, -1.000000000000000000 ) ) ;
#34997=AXIS2_PLACEMENT_3D ( 'NONE', #207931, #189640, #166248 ) ;
#34999=VECTOR ( 'NONE', #128577, 1000.000000000000000 ) ;
#35002=DIRECTION ( 'NONE',  ( -1.000000000000000000, -0.000000000000000000, -0.000000000000000000 ) ) ;
#35015=FACE_OUTER_BOUND ( 'NONE', #215373, .T. ) ;
#35029=DIRECTION ( 'NONE',  ( -1.000000000000000000, 0.000000000000000000, -0.000000000000000000 ) ) ;
#35041=DIRECTION ( 'NONE',  ( 0.000000000000000000, 0.000000000000000000, 1.000000000000000000 ) ) ;
#35055=AXIS2_PLACEMENT_3D ( 'NONE', #17813, #16563, #179493 ) ;
#35059=DIRECTION ( 'NONE',  ( -1.000000000000000000, -0.000000000000000000, -0.000000000000000000 ) ) ;
#35081=CARTESIAN_POINT ( 'NONE',  ( -22.50000000000000000, 64.35042919246686210, -69.62310748452439668 ) ) ;
#35086=DIRECTION ( 'NONE',  ( 1.000000000000000000, 0.000000000000000000, 0.000000000000000000 ) ) ;
#35114=ORIENTED_EDGE ( 'NONE', *, *, #99913, .F. ) ;
#35116=ORIENTED_EDGE ( 'NONE', *, *, #5514, .T. ) ;
#35119=LINE ( 'NONE', #91209, #80356 ) ;
#35120=ORIENTED_EDGE ( 'NONE', *, *, #73351, .T. ) ;
#35126=FACE_OUTER_BOUND ( 'NONE', #135006, .T. ) ;
#35155=CARTESIAN_POINT ( 'NONE',  ( -21.05000000000000071, 76.00000000001142553, -36.02310748452432421 ) ) ;
#35158=DIRECTION ( 'NONE',  ( 0.000000000000000000, -7.487053152578127080E-15, 1.000000000000000000 ) ) ;
#35174=ORIENTED_EDGE ( 'NONE', *, *, #213206, .T. ) ;
#35176=AXIS2_PLACEMENT_3D ( 'NONE', #150561, #51419, #171442 ) ;
#35190=CARTESIAN_POINT ( 'NONE',  ( -23.25000000000000000, 76.10085836911045476, -81.27267460801371612 ) ) ;
#35232=CARTESIAN_POINT ( 'NONE',  ( 21.05000000000000426, 65.27628289530409234, -61.92869009291128179 ) ) ;
#35265=EDGE_CURVE ( 'NONE', #55596, #250549, #224491, .T. ) ;
#35288=AXIS2_PLACEMENT_3D ( 'NONE', #21903, #139246, #218797 ) ;
#35298=CARTESIAN_POINT ( 'NONE',  ( 18.49999999999999289, 65.70729864260954400, -30.56574559737245877 ) ) ;
#35305=CARTESIAN_POINT ( 'NONE',  ( 21.08621493067296271, 69.65070570883999324, -69.57930232400047998 ) ) ;
#35307=ADVANCED_FACE ( 'NONE', ( #175016 ), #193252, .F. ) ;
#35326=CARTESIAN_POINT ( 'NONE',  ( 18.59999999999999076, 65.79142135624880439, -48.17310748452439384 ) ) ;
#35345=DIRECTION ( 'NONE',  ( 0.000000000000000000, -6.982962677686266711E-15, 1.000000000000000000 ) ) ;
#35349=CIRCLE ( 'NONE', #222723, 0.1000000000000028644 ) ;
#35361=AXIS2_PLACEMENT_3D ( 'NONE', #13957, #251253, #190018 ) ;
#35384=LINE ( 'NONE', #14525, #251553 ) ;
#35387=CARTESIAN_POINT ( 'NONE',  ( 21.05000000000000071, 76.10000000001166143, -69.52310748452431710 ) ) ;
#35425=ORIENTED_EDGE ( 'NONE', *, *, #36559, .F. ) ;
#35426=DIRECTION ( 'NONE',  ( -0.000000000000000000, -0.1350103645451945777, 0.9908441862701590219 ) ) ;
#35430=ORIENTED_EDGE ( 'NONE', *, *, #228409, .T. ) ;
#35460=CARTESIAN_POINT ( 'NONE',  ( -20.54999999999999716, 76.00000000001143974, -37.92310748452432989 ) ) ;
#35461=ORIENTED_EDGE ( 'NONE', *, *, #109691, .F. ) ;
#35492=CARTESIAN_POINT ( 'NONE',  ( -21.78635804494510708, 68.96433851485846844, -69.62211255003204258 ) ) ;
#35500=VERTEX_POINT ( 'NONE', #224025 ) ;
#35543=ORIENTED_EDGE ( 'NONE', *, *, #83493, .F. ) ;
#35559=CARTESIAN_POINT ( 'NONE',  ( 19.75857864376268935, 64.35000000001147669, -44.77310748452440237 ) ) ;
#35599=ORIENTED_EDGE ( 'NONE', *, *, #213269, .F. ) ;
#35646=EDGE_LOOP ( 'NONE', ( #14580, #107300, #50922, #23268 ) ) ;
#35673=ADVANCED_FACE ( 'NONE', ( #29724 ), #12722, .T. ) ;
#35676=DIRECTION ( 'NONE',  ( 1.000000000000000000, 0.000000000000000000, 0.000000000000000000 ) ) ;
#35677=CIRCLE ( 'NONE', #23198, 12.87499999999999822 ) ;
#35699=DIRECTION ( 'NONE',  ( 0.000000000000000000, 0.000000000000000000, -1.000000000000000000 ) ) ;
#35711=DIRECTION ( 'NONE',  ( 0.000000000000000000, 6.982962677686266711E-15, -1.000000000000000000 ) ) ;
#35735=CARTESIAN_POINT ( 'NONE',  ( 23.15000000000000213, 87.48912529308749697, -39.02310748452423894 ) ) ;
#35776=DIRECTION ( 'NONE',  ( 0.000000000000000000, 0.000000000000000000, 1.000000000000000000 ) ) ;
#35788=DIRECTION ( 'NONE',  ( 1.000000000000000000, 0.000000000000000000, 0.000000000000000000 ) ) ;
#35790=VECTOR ( 'NONE', #60289, 1000.000000000000000 ) ;
#35845=FACE_OUTER_BOUND ( 'NONE', #100910, .T. ) ;
#35852=CARTESIAN_POINT ( 'NONE',  ( -18.59999999999999787, 64.25000000001173817, -81.27310748452440237 ) ) ;
#35863=EDGE_CURVE ( 'NONE', #155813, #130245, #183178, .T. ) ;
#35868=EDGE_CURVE ( 'NONE', #144086, #250305, #166455, .T. ) ;
#35951=ORIENTED_EDGE ( 'NONE', *, *, #141188, .F. ) ;
#35979=FACE_OUTER_BOUND ( 'NONE', #17080, .T. ) ;
#36011=CARTESIAN_POINT ( 'NONE',  ( 18.59999999999999432, 85.48068669529034480, -29.08199231576640287 ) ) ;
#36031=DIRECTION ( 'NONE',  ( -0.000000000000000000, 1.000000000000000000, 6.982962677686266711E-15 ) ) ;
#36078=VECTOR ( 'NONE', #254366, 1000.000000000000000 ) ;
#36087=CARTESIAN_POINT ( 'NONE',  ( 20.94999999999999574, 74.25000000001156764, -57.85359592662268824 ) ) ;
#36091=EDGE_CURVE ( 'NONE', #248144, #209151, #95669, .T. ) ;
#36109=DIRECTION ( 'NONE',  ( 0.000000000000000000, 6.982962677686266711E-15, -1.000000000000000000 ) ) ;
#36121=AXIS2_PLACEMENT_3D ( 'NONE', #209398, #11211, #30793 ) ;
#36144=CYLINDRICAL_SURFACE ( 'NONE', #177740, 11.75000000000000000 ) ;
#36160=ORIENTED_EDGE ( 'NONE', *, *, #235168, .T. ) ;
#36177=CIRCLE ( 'NONE', #256864, 4.150000000000001243 ) ;
#36185=CARTESIAN_POINT ( 'NONE',  ( -22.49436431346200038, 64.35004905235818740, -69.59001101424667013 ) ) ;
#36192=AXIS2_PLACEMENT_3D ( 'NONE', #158020, #39333, #195840 ) ;
#36194=EDGE_CURVE ( 'NONE', #73251, #79556, #134865, .T. ) ;
#36208=VERTEX_POINT ( 'NONE', #104715 ) ;
#36217=CARTESIAN_POINT ( 'NONE',  ( 20.72390388899089686, 65.41003688158754414, -62.01175918877954274 ) ) ;
#36238=AXIS2_PLACEMENT_3D ( 'NONE', #96766, #154256, #156809 ) ;
#36240=CARTESIAN_POINT ( 'NONE',  ( 21.14999999999999858, 65.28660755661168480, -57.17310748452439384 ) ) ;
#36260=AXIS2_PLACEMENT_3D ( 'NONE', #230004, #9672, #70971 ) ;
#36292=CARTESIAN_POINT ( 'NONE',  ( -21.14999999893415250, 64.25000000001161027, -62.67861214099805522 ) ) ;
#36298=LINE ( 'NONE', #19280, #138673 ) ;
#36317=DIRECTION ( 'NONE',  ( -1.000000000000000000, -0.000000000000000000, -0.000000000000000000 ) ) ;
#36320=CIRCLE ( 'NONE', #123604, 0.1000000000000028644 ) ;
#36333=CARTESIAN_POINT ( 'NONE',  ( -18.58744394320951798, 85.56638515455998117, -29.20025943064833740 ) ) ;
#36343=CIRCLE ( 'NONE', #144432, 12.87499999999999822 ) ;
#36344=CARTESIAN_POINT ( 'NONE',  ( -22.50014994444008209, 64.25028026811935433, -69.60618764124372149 ) ) ;
#36351=EDGE_CURVE ( 'NONE', #71888, #165845, #108352, .T. ) ;
#36355=VERTEX_POINT ( 'NONE', #186885 ) ;
#36361=DIRECTION ( 'NONE',  ( 1.000000000000000000, 0.000000000000000000, 0.000000000000000000 ) ) ;
#36410=ORIENTED_EDGE ( 'NONE', *, *, #200265, .F. ) ;
#36485=ORIENTED_EDGE ( 'NONE', *, *, #231563, .T. ) ;
#36528=CARTESIAN_POINT ( 'NONE',  ( -18.59999999999999787, 85.40000000001138858, -29.14106563635158764 ) ) ;
#36556=ORIENTED_EDGE ( 'NONE', *, *, #58218, .F. ) ;
#36559=EDGE_CURVE ( 'NONE', #39027, #122601, #118905, .T. ) ;
#36639=AXIS2_PLACEMENT_3D ( 'NONE', #63423, #43876, #244629 ) ;
#36682=ORIENTED_EDGE ( 'NONE', *, *, #38099, .F. ) ;
#36715=CIRCLE ( 'NONE', #186538, 0.1000000000000028644 ) ;
#36720=AXIS2_PLACEMENT_3D ( 'NONE', #155006, #137961, #160137 ) ;
#36746=DIRECTION ( 'NONE',  ( 2.840903330521631775E-16, 0.8700118002898354908, -0.4930308989875170078 ) ) ;
#36754=AXIS2_PLACEMENT_3D ( 'NONE', #53111, #59169, #113097 ) ;
#36755=VERTEX_POINT ( 'NONE', #84854 ) ;
#36773=AXIS2_PLACEMENT_3D ( 'NONE', #227066, #221914, #184095 ) ;
#36782=CARTESIAN_POINT ( 'NONE',  ( -21.22070241538126112, 69.53005372714204668, -69.62202651505938888 ) ) ;
#36785=CARTESIAN_POINT ( 'NONE',  ( 20.94999999999999929, 70.15000000001148805, -46.15560470880229360 ) ) ;
#36800=CARTESIAN_POINT ( 'NONE',  ( 18.59999999999999432, 77.16270174994961906, -61.42310748452431568 ) ) ;
#36806=ORIENTED_EDGE ( 'NONE', *, *, #157447, .F. ) ;
#36813=LINE ( 'NONE', #98004, #186161 ) ;
#36817=DIRECTION ( 'NONE',  ( 1.000000000000000000, 0.000000000000000000, 0.000000000000000000 ) ) ;
#36821=AXIS2_PLACEMENT_3D ( 'NONE', #168408, #10577, #167106 ) ;
#36837=DIRECTION ( 'NONE',  ( 0.000000000000000000, 6.982962677686266711E-15, -1.000000000000000000 ) ) ;
#36886=DIRECTION ( 'NONE',  ( 0.000000000000000000, -1.000000000000000000, -6.982962677686265922E-15 ) ) ;
#36890=CARTESIAN_POINT ( 'NONE',  ( 18.59999999999999076, 69.60000000001157616, -59.59268285446279378 ) ) ;
#36905=ORIENTED_EDGE ( 'NONE', *, *, #206076, .T. ) ;
#36931=ORIENTED_EDGE ( 'NONE', *, *, #51942, .F. ) ;
#36935=DIRECTION ( 'NONE',  ( 0.7071067811865475727, -0.7071067811865475727, -4.937700262164531476E-15 ) ) ;
#36953=ORIENTED_EDGE ( 'NONE', *, *, #173646, .F. ) ;
#37007=ORIENTED_EDGE ( 'NONE', *, *, #77146, .F. ) ;
#37016=ORIENTED_EDGE ( 'NONE', *, *, #17070, .T. ) ;
#37031=ORIENTED_EDGE ( 'NONE', *, *, #241781, .F. ) ;
#37057=ORIENTED_EDGE ( 'NONE', *, *, #219186, .T. ) ;
#37076=VERTEX_POINT ( 'NONE', #20784 ) ;
#37086=DIRECTION ( 'NONE',  ( 0.000000000000000000, 0.000000000000000000, 1.000000000000000000 ) ) ;
#37104=CIRCLE ( 'NONE', #103684, 0.1000000000000052097 ) ;
#37115=DIRECTION ( 'NONE',  ( 0.000000000000000000, 0.8660254037844377084, 0.5000000000000016653 ) ) ;
#37122=ORIENTED_EDGE ( 'NONE', *, *, #193622, .F. ) ;
#37136=DIRECTION ( 'NONE',  ( 1.000000000000000000, -2.952720810173289112E-16, -2.061873921506763405E-30 ) ) ;
#37181=ORIENTED_EDGE ( 'NONE', *, *, #43109, .F. ) ;
#37204=FACE_OUTER_BOUND ( 'NONE', #162075, .T. ) ;
#37229=DIRECTION ( 'NONE',  ( 1.000000000000000000, -7.304098846218134667E-16, -5.100424963727255829E-30 ) ) ;
#37262=CARTESIAN_POINT ( 'NONE',  ( 20.94999999999999929, 71.00000000001158185, -57.11784146561126363 ) ) ;
#37307=CARTESIAN_POINT ( 'NONE',  ( -21.05000000000000071, 64.25000000001146816, -42.86470817442145176 ) ) ;
#37308=CIRCLE ( 'NONE', #162213, 0.1999999999999987899 ) ;
#37319=ORIENTED_EDGE ( 'NONE', *, *, #197234, .F. ) ;
#37331=CARTESIAN_POINT ( 'NONE',  ( 23.24999999999999289, 64.35000000001164722, -69.52310748452440237 ) ) ;
#37352=EDGE_CURVE ( 'NONE', #94397, #241131, #212391, .T. ) ;
#37357=DIRECTION ( 'NONE',  ( 0.000000000000000000, -6.982962677686266711E-15, 1.000000000000000000 ) ) ;
#37358=EDGE_CURVE ( 'NONE', #176779, #88139, #185480, .T. ) ;
#37368=CIRCLE ( 'NONE', #87412, 11.79999999999999716 ) ;
#37411=EDGE_CURVE ( 'NONE', #106243, #65120, #53162, .T. ) ;
#37430=EDGE_LOOP ( 'NONE', ( #73978, #24835, #82471, #3983 ) ) ;
#37431=CIRCLE ( 'NONE', #94728, 2.000000000000001776 ) ;
#37441=DIRECTION ( 'NONE',  ( 6.484947573744954877E-15, -0.9274965247785555977, 0.3738317757009190223 ) ) ;
#37443=CYLINDRICAL_SURFACE ( 'NONE', #249735, 0.5000000000000004441 ) ;
#37476=DIRECTION ( 'NONE',  ( 0.000000000000000000, 0.000000000000000000, -1.000000000000000000 ) ) ;
#37482=LINE ( 'NONE', #16635, #173264 ) ;
#37537=CARTESIAN_POINT ( 'NONE',  ( -23.15000000000000213, 85.00000000001149658, -45.91707660717669626 ) ) ;
#37541=ORIENTED_EDGE ( 'NONE', *, *, #216869, .F. ) ;
#37546=ADVANCED_FACE ( 'NONE', ( #245603 ), #97393, .F. ) ;
#37563=DIRECTION ( 'NONE',  ( 0.000000000000000000, 0.8068669527897009974, 0.5907332058517299478 ) ) ;
#37635=ORIENTED_EDGE ( 'NONE', *, *, #237862, .T. ) ;
#37639=FACE_OUTER_BOUND ( 'NONE', #93, .T. ) ;
#37641=CARTESIAN_POINT ( 'NONE',  ( 20.94999999999999574, 77.73625713160897988, -57.95445515550681392 ) ) ;
#37649=FACE_OUTER_BOUND ( 'NONE', #93974, .T. ) ;
#37688=EDGE_CURVE ( 'NONE', #238213, #247693, #91760, .T. ) ;
#37725=TOROIDAL_SURFACE ( 'NONE', #183449, 11.70000000000000462, 0.1000000000000000056 ) ;
#37735=EDGE_CURVE ( 'NONE', #255664, #60411, #16001, .T. ) ;
#37784=CYLINDRICAL_SURFACE ( 'NONE', #195705, 0.5000000000000004441 ) ;
#37818=DIRECTION ( 'NONE',  ( 0.000000000000000000, 0.000000000000000000, 1.000000000000000000 ) ) ;
#37837=DIRECTION ( 'NONE',  ( -0.000000000000000000, -1.000000000000000000, -6.982962677686266711E-15 ) ) ;
#37845=CARTESIAN_POINT ( 'NONE',  ( 20.93975676684922504, 65.68895814178191017, -30.50265578621382190 ) ) ;
#37854=CARTESIAN_POINT ( 'NONE',  ( 21.08198257630413508, 69.66340326599659249, -69.59575080830897775 ) ) ;
#37870=CARTESIAN_POINT ( 'NONE',  ( 18.43466021071409600, 85.49419069046793140, -29.40604592439644094 ) ) ;
#37871=AXIS2_PLACEMENT_3D ( 'NONE', #58436, #36361, #74219 ) ;
#37886=ORIENTED_EDGE ( 'NONE', *, *, #199225, .F. ) ;
#37898=ORIENTED_EDGE ( 'NONE', *, *, #98231, .T. ) ;
#37937=LINE ( 'NONE', #35387, #36078 ) ;
#37959=AXIS2_PLACEMENT_3D ( 'NONE', #236280, #40697, #254532 ) ;
#37961=DIRECTION ( 'NONE',  ( 0.000000000000000000, 0.000000000000000000, -1.000000000000000000 ) ) ;
#37974=ADVANCED_FACE ( 'NONE', ( #45805 ), #185319, .T. ) ;
#37986=VERTEX_POINT ( 'NONE', #207465 ) ;
#38033=TOROIDAL_SURFACE ( 'NONE', #58651, 0.2000000000000000111, 0.1000000000000000056 ) ;
#38056=ORIENTED_EDGE ( 'NONE', *, *, #155862, .F. ) ;
#38089=DIRECTION ( 'NONE',  ( 0.000000000000000000, -5.551115123125777653E-14, 1.000000000000000000 ) ) ;
#38094=CARTESIAN_POINT ( 'NONE',  ( -20.94999999999999929, 70.15000000001163016, -59.39061026024639034 ) ) ;
#38099=EDGE_CURVE ( 'NONE', #231649, #161130, #121075, .T. ) ;
#38127=CARTESIAN_POINT ( 'NONE',  ( 18.59999999999999076, 64.25000000001173817, -81.27310748452440237 ) ) ;
#38148=CARTESIAN_POINT ( 'NONE',  ( -21.14999999999999858, 64.35000000001166143, -69.42310748452440805 ) ) ;
#38151=CARTESIAN_POINT ( 'NONE',  ( -23.15000000000000213, 76.00000000001162448, -65.37310748452432563 ) ) ;
#38202=VERTEX_POINT ( 'NONE', #49201 ) ;
#38208=ORIENTED_EDGE ( 'NONE', *, *, #93923, .T. ) ;
#38226=LINE ( 'NONE', #175206, #119542 ) ;
#38229=LINE ( 'NONE', #59022, #95730 ) ;
#38232=CARTESIAN_POINT ( 'NONE',  ( 19.99999999999998934, 64.25000000001148237, -44.67310748452440095 ) ) ;
#38237=DIRECTION ( 'NONE',  ( -0.000000000000000000, 1.000000000000000000, 6.982962677686266711E-15 ) ) ;
#38247=CARTESIAN_POINT ( 'NONE',  ( 21.05000000000000071, 65.57661458509869590, -62.03105556065429482 ) ) ;
#38252=CARTESIAN_POINT ( 'NONE',  ( -18.48550754432060472, 85.46339977857157066, -62.47431773210951178 ) ) ;
#38268=ORIENTED_EDGE ( 'NONE', *, *, #118586, .T. ) ;
#38269=DIRECTION ( 'NONE',  ( -3.469446951953515108E-14, -1.000000000000000000, 0.000000000000000000 ) ) ;
#38333=DIRECTION ( 'NONE',  ( -6.938893903907222856E-15, -1.000000000000000000, -7.272083257015735086E-15 ) ) ;
#38346=AXIS2_PLACEMENT_3D ( 'NONE', #75311, #175682, #234344 ) ;
#38369=CARTESIAN_POINT ( 'NONE',  ( 21.14999999999999858, 64.25000000001172396, -81.27310748452440237 ) ) ;
#38374=CARTESIAN_POINT ( 'NONE',  ( -23.25000000000000000, 76.00000000001145395, -39.92310748452432279 ) ) ;
#38402=LINE ( 'NONE', #175374, #229656 ) ;
#38410=DIRECTION ( 'NONE',  ( 0.000000000000000000, -1.565658005757035267E-14, 1.000000000000000000 ) ) ;
#38412=CARTESIAN_POINT ( 'NONE',  ( -21.05000000000000071, 77.16270174994961906, -61.42310748452431568 ) ) ;
#38414=CARTESIAN_POINT ( 'NONE',  ( 22.50014994444006433, 64.25028026811959592, -69.60618764124355096 ) ) ;
#38430=CARTESIAN_POINT ( 'NONE',  ( -18.59999999999999787, 64.35000000001157616, -57.37310748452440379 ) ) ;
#38503=EDGE_LOOP ( 'NONE', ( #122046, #42019, #159482, #136620 ) ) ;
#38519=ORIENTED_EDGE ( 'NONE', *, *, #108987, .F. ) ;
#38525=DIRECTION ( 'NONE',  ( -1.000000000000000000, -0.000000000000000000, -0.000000000000000000 ) ) ;
#38528=CARTESIAN_POINT ( 'NONE',  ( -23.15000000000000213, 71.75000000001156764, -57.27310748452435263 ) ) ;
#38617=VERTEX_POINT ( 'NONE', #197490 ) ;
#38620=EDGE_LOOP ( 'NONE', ( #1763, #82397, #63020, #22930 ) ) ;
#38672=CARTESIAN_POINT ( 'NONE',  ( 23.14999999999999858, 70.05000000001149374, -46.32880978955918039 ) ) ;
#38677=DIRECTION ( 'NONE',  ( 0.000000000000000000, -0.01562499999999307672, 0.9998779222360100194 ) ) ;
#38697=ADVANCED_FACE ( 'NONE', ( #22743 ), #142644, .T. ) ;
#38718=CARTESIAN_POINT ( 'NONE',  ( 21.05000000000000071, 85.00000000001159606, -59.62913836187181715 ) ) ;
#38719=ORIENTED_EDGE ( 'NONE', *, *, #7637, .F. ) ;
#38742=CARTESIAN_POINT ( 'NONE',  ( 22.39999999999999503, 68.20922040163827660, -69.62310748452438247 ) ) ;
#38755=CARTESIAN_POINT ( 'NONE',  ( 23.15000000000000213, 88.41227409416111982, -39.02310748452423894 ) ) ;
#38829=TOROIDAL_SURFACE ( 'NONE', #246913, 0.2000000000000000111, 0.1000000000000000056 ) ;
#38842=CYLINDRICAL_SURFACE ( 'NONE', #212752, 0.09999999999999939493 ) ;
#38852=CARTESIAN_POINT ( 'NONE',  ( -21.05000000000000071, 64.25000000001161027, -62.73924182154625129 ) ) ;
#38875=CARTESIAN_POINT ( 'NONE',  ( -21.05000000000000071, 76.25610579210386675, -69.55800392619661920 ) ) ;
#38880=CIRCLE ( 'NONE', #76260, 0.2000000000000057288 ) ;
#38899=VERTEX_POINT ( 'NONE', #70868 ) ;
#38901=AXIS2_PLACEMENT_3D ( 'NONE', #18029, #197943, #192835 ) ;
#38932=TOROIDAL_SURFACE ( 'NONE', #68142, 11.65000000000000036, 0.1000000000000000056 ) ;
#38933=CARTESIAN_POINT ( 'NONE',  ( 21.05000000000000071, 69.45934304831041572, -69.42310748452437963 ) ) ;
#38936=AXIS2_PLACEMENT_3D ( 'NONE', #36800, #214119, #74647 ) ;
#38938=DIRECTION ( 'NONE',  ( 0.000000000000000000, -0.1350103645451835865, -0.9908441862701605762 ) ) ;
#38947=CARTESIAN_POINT ( 'NONE',  ( -20.94403535211772294, 65.69367753730607262, -30.51892380663481674 ) ) ;
#39014=ADVANCED_FACE ( 'NONE', ( #16025 ), #155544, .F. ) ;
#39027=VERTEX_POINT ( 'NONE', #132096 ) ;
#39041=CARTESIAN_POINT ( 'NONE',  ( -23.25000000000000000, 87.75000000001173817, -81.27310748452423184 ) ) ;
#39059=DIRECTION ( 'NONE',  ( 0.000000000000000000, -1.000000000000000000, -6.860497997771532351E-15 ) ) ;
#39126=CARTESIAN_POINT ( 'NONE',  ( 20.94788355080264353, 65.69792220476271893, -30.53355541284615526 ) ) ;
#39146=EDGE_CURVE ( 'NONE', #90111, #21530, #201456, .T. ) ;
#39154=CARTESIAN_POINT ( 'NONE',  ( -18.50000000000000000, 66.85000000001150511, -48.37310748452438247 ) ) ;
#39178=ORIENTED_EDGE ( 'NONE', *, *, #26945, .F. ) ;
#39189=B_SPLINE_CURVE_WITH_KNOTS ( 'NONE', 3,
 ( #44302, #202085, #222912, #245056, #224197, #228067, #23477, #182537 ),
 .UNSPECIFIED., .F., .F.,
 ( 4, 2, 2, 4 ),
 ( 0.000000000000000000, 0.0002114466876442284862, 0.0003171700314663216010, 0.0004228933752884147970 ),
 .UNSPECIFIED. ) ;
#39203=ADVANCED_FACE ( 'NONE', ( #165805 ), #206189, .T. ) ;
#39272=ORIENTED_EDGE ( 'NONE', *, *, #179107, .T. ) ;
#39289=CARTESIAN_POINT ( 'NONE',  ( 20.94999999999999574, 74.14897176987071248, -57.86919421510183525 ) ) ;
#39297=VECTOR ( 'NONE', #232600, 999.9999999999998863 ) ;
#39333=DIRECTION ( 'NONE',  ( 1.000000000000000000, 0.000000000000000000, 0.000000000000000000 ) ) ;
#39336=DIRECTION ( 'NONE',  ( 0.000000000000000000, 1.000000000000000000, 6.982962677686266711E-15 ) ) ;
#39343=VERTEX_POINT ( 'NONE', #174816 ) ;
#39352=EDGE_LOOP ( 'NONE', ( #15904, #252138, #167191 ) ) ;
#39379=ORIENTED_EDGE ( 'NONE', *, *, #130214, .F. ) ;
#39399=EDGE_CURVE ( 'NONE', #41111, #172698, #101605, .T. ) ;
#39424=ADVANCED_FACE ( 'NONE', ( #258103 ), #117365, .F. ) ;
#39507=DIRECTION ( 'NONE',  ( 0.000000000000000000, 6.982962677686266711E-15, -1.000000000000000000 ) ) ;
#39520=ORIENTED_EDGE ( 'NONE', *, *, #82379, .T. ) ;
#39539=CARTESIAN_POINT ( 'NONE',  ( 20.95512820512820440, 67.12384868372345181, -57.37310748452438247 ) ) ;
#39557=AXIS2_PLACEMENT_3D ( 'NONE', #175756, #3497, #45202 ) ;
#39568=( BOUNDED_SURFACE ( )  B_SPLINE_SURFACE ( 3, 2, ( 
 ( #48744, #153035, #34359 ),
 ( #51290, #232558, #53894 ),
 ( #250800, #113865, #193422 ),
 ( #30497, #173890, #210417 ) ),
 .UNSPECIFIED., .F., .F., .F. ) 
 B_SPLINE_SURFACE_WITH_KNOTS ( ( 4, 4 ),
 ( 3, 3 ),
 ( -5.827586677109586333E-19, 0.0003124336117481331431 ),
 ( 0.000000000000000000, 1.000000000000000000 ),
 .UNSPECIFIED. ) 
 GEOMETRIC_REPRESENTATION_ITEM ( )  RATIONAL_B_SPLINE_SURFACE ( (
 ( 1.000000000000000000, 0.7040654476015839602, 1.000000000000000000),
 ( 1.000000000000000000, 0.7039193538781748360, 1.000000000000000000),
 ( 1.000000000000000000, 0.7089171279145581872, 1.000000000000000000),
 ( 1.000000000000000000, 0.7071067811865509034, 1.000000000000000000) ) ) 
 REPRESENTATION_ITEM ( '' )  SURFACE ( )  );
#39591=EDGE_CURVE ( 'NONE', #12734, #44233, #240440, .T. ) ;
#39605=VECTOR ( 'NONE', #218248, 1000.000000000000000 ) ;
#39623=ORIENTED_EDGE ( 'NONE', *, *, #94311, .F. ) ;
#39639=CARTESIAN_POINT ( 'NONE',  ( 23.14999999999999503, 64.35000000001146248, -43.03791325517834565 ) ) ;
#39646=AXIS2_PLACEMENT_3D ( 'NONE', #103737, #201579, #141609 ) ;
#39664=CARTESIAN_POINT ( 'NONE',  ( 21.70464131381650219, 68.90464198104380955, -69.52310748452435973 ) ) ;
#39694=ADVANCED_FACE ( 'NONE', ( #229309 ), #151056, .T. ) ;
#39703=DIRECTION ( 'NONE',  ( -0.000000000000000000, 6.982962677686266711E-15, -1.000000000000000000 ) ) ;
#39722=ORIENTED_EDGE ( 'NONE', *, *, #64176, .F. ) ;
#39728=ORIENTED_EDGE ( 'NONE', *, *, #208662, .F. ) ;
#39743=EDGE_CURVE ( 'NONE', #114996, #124577, #140469, .T. ) ;
#39781=CIRCLE ( 'NONE', #168975, 0.1000000000000028644 ) ;
#39798=CARTESIAN_POINT ( 'NONE',  ( -21.05000000000000071, 77.83534155023599510, -57.96795619196132776 ) ) ;
#39804=LINE ( 'NONE', #124457, #145728 ) ;
#39813=DIRECTION ( 'NONE',  ( 0.000000000000000000, 7.026728003956683390E-15, -1.000000000000000000 ) ) ;
#39816=EDGE_LOOP ( 'NONE', ( #58151, #186485, #167571, #77373 ) ) ;
#39835=CYLINDRICAL_SURFACE ( 'NONE', #246050, 0.09999999999999520384 ) ;
#39848=DIRECTION ( 'NONE',  ( -1.000000000000000000, 0.000000000000000000, -0.000000000000000000 ) ) ;
#39894=EDGE_CURVE ( 'NONE', #119497, #147150, #169058, .T. ) ;
#39899=DIRECTION ( 'NONE',  ( 0.000000000000000000, -0.6728971962616412394, -0.7397360091703134577 ) ) ;
#39909=AXIS2_PLACEMENT_3D ( 'NONE', #38148, #21167, #100633 ) ;
#39917=FACE_BOUND ( 'NONE', #249044, .T. ) ;
#39962=EDGE_LOOP ( 'NONE', ( #14636, #226550, #17108, #149156 ) ) ;
#40004=DIRECTION ( 'NONE',  ( 1.000000000000000000, 0.000000000000000000, 0.000000000000000000 ) ) ;
#40008=EDGE_CURVE ( 'NONE', #58504, #211306, #46167, .T. ) ;
#40058=AXIS2_PLACEMENT_3D ( 'NONE', #218838, #255356, #19378 ) ;
#40064=EDGE_LOOP ( 'NONE', ( #194397, #61448, #238085, #153307 ) ) ;
#40072=CARTESIAN_POINT ( 'NONE',  ( 20.04142135623730070, 64.35000000001150511, -48.17310748452440095 ) ) ;
#40080=ORIENTED_EDGE ( 'NONE', *, *, #18115, .T. ) ;
#40098=AXIS2_PLACEMENT_3D ( 'NONE', #202980, #66038, #225091 ) ;
#40102=DIRECTION ( 'NONE',  ( 3.265361837132813093E-16, 1.000000000000000000, 6.982962677686266711E-15 ) ) ;
#40138=VERTEX_POINT ( 'NONE', #64158 ) ;
#40186=EDGE_CURVE ( 'NONE', #205489, #241008, #136554, .T. ) ;
#40190=FACE_OUTER_BOUND ( 'NONE', #88620, .T. ) ;
#40193=AXIS2_PLACEMENT_3D ( 'NONE', #171057, #225811, #32822 ) ;
#40209=DIRECTION ( 'NONE',  ( 0.000000000000000000, 1.000000000000000000, 6.938893903907222067E-15 ) ) ;
#40244=EDGE_CURVE ( 'NONE', #46294, #159190, #19908, .T. ) ;
#40246=CARTESIAN_POINT ( 'NONE',  ( -20.93302460841142931, 65.68434038414308418, -30.48668807260656521 ) ) ;
#40252=DIRECTION ( 'NONE',  ( -1.000000000000000000, 0.000000000000000000, -0.000000000000000000 ) ) ;
#40259=AXIS2_PLACEMENT_3D ( 'NONE', #184283, #206422, #87739 ) ;
#40275=ORIENTED_EDGE ( 'NONE', *, *, #241334, .F. ) ;
#40283=EDGE_CURVE ( 'NONE', #166990, #159227, #225771, .T. ) ;
#40297=VERTEX_POINT ( 'NONE', #125421 ) ;
#40308=CARTESIAN_POINT ( 'NONE',  ( -20.00857864376270001, 66.75000000001151079, -48.37310748452438247 ) ) ;
#40317=FACE_OUTER_BOUND ( 'NONE', #199020, .T. ) ;
#40321=EDGE_CURVE ( 'NONE', #176232, #49225, #28468, .T. ) ;
#40336=DIRECTION ( 'NONE',  ( 0.000000000000000000, 0.000000000000000000, 1.000000000000000000 ) ) ;
#40344=DIRECTION ( 'NONE',  ( 1.000000000000000000, 0.000000000000000000, 0.000000000000000000 ) ) ;
#40353=AXIS2_PLACEMENT_3D ( 'NONE', #87186, #209731, #34981 ) ;
#40360=CIRCLE ( 'NONE', #119431, 0.09999999999999939493 ) ;
#40371=CARTESIAN_POINT ( 'NONE',  ( -20.54999999999999716, 74.00000000001156764, -56.29848556176223440 ) ) ;
#40414=ORIENTED_EDGE ( 'NONE', *, *, #111879, .T. ) ;
#40456=ORIENTED_EDGE ( 'NONE', *, *, #25258, .T. ) ;
#40463=CARTESIAN_POINT ( 'NONE',  ( -21.07016717456947319, 69.67905916191141102, -69.52310748452435973 ) ) ;
#40518=CARTESIAN_POINT ( 'NONE',  ( -18.45068461519106506, 85.48650652910070846, -62.45433031561956483 ) ) ;
#40565=DIRECTION ( 'NONE',  ( 0.000000000000000000, 0.000000000000000000, 1.000000000000000000 ) ) ;
#40569=TOROIDAL_SURFACE ( 'NONE', #190398, 11.70000000000000639, 0.1000000000000000056 ) ;
#40611=DIRECTION ( 'NONE',  ( 1.000000000000000000, -0.000000000000000000, 0.000000000000000000 ) ) ;
#40625=VERTEX_POINT ( 'NONE', #217758 ) ;
#40659=FACE_OUTER_BOUND ( 'NONE', #45671, .T. ) ;
#40694=CARTESIAN_POINT ( 'NONE',  ( -18.59117750673696889, 65.66751761918619934, -30.42826094061123854 ) ) ;
#40697=DIRECTION ( 'NONE',  ( 0.000000000000000000, -6.982962677686266711E-15, 1.000000000000000000 ) ) ;
#40721=DIRECTION ( 'NONE',  ( 0.000000000000000000, -7.429790795770647916E-15, 1.000000000000000000 ) ) ;
#40742=DIRECTION ( 'NONE',  ( -0.000000000000000000, 0.8660254037844377084, 0.5000000000000016653 ) ) ;
#40784=ORIENTED_EDGE ( 'NONE', *, *, #125244, .F. ) ;
#40799=ORIENTED_EDGE ( 'NONE', *, *, #12293, .F. ) ;
#40805=DIRECTION ( 'NONE',  ( 0.000000000000000000, -7.086529944415894657E-15, 1.000000000000000000 ) ) ;
#40822=CARTESIAN_POINT ( 'NONE',  ( -20.93284271247462058, 64.25000000001148237, -43.03791325517833855 ) ) ;
#40858=AXIS2_PLACEMENT_3D ( 'NONE', #239692, #216257, #218821 ) ;
#40882=CIRCLE ( 'NONE', #119993, 0.1999999999999987899 ) ;
#40916=CARTESIAN_POINT ( 'NONE',  ( 18.59999999999999787, 77.85102823015243700, -57.86919421510181394 ) ) ;
#40939=EDGE_CURVE ( 'NONE', #729, #202471, #175801, .T. ) ;
#40968=VECTOR ( 'NONE', #138859, 1000.000000000000000 ) ;
#40982=ORIENTED_EDGE ( 'NONE', *, *, #63294, .T. ) ;
#40997=CARTESIAN_POINT ( 'NONE',  ( -21.07928932188134041, 75.90110485435729970, -75.85162414091762173 ) ) ;
#41008=CARTESIAN_POINT ( 'NONE',  ( 22.48660254037843842, 64.25000000001163869, -69.57310748452439952 ) ) ;
#41010=AXIS2_PLACEMENT_3D ( 'NONE', #96472, #59911, #157802 ) ;
#41044=FACE_OUTER_BOUND ( 'NONE', #191359, .T. ) ;
#41054=DIRECTION ( 'NONE',  ( 1.000000000000000000, -0.000000000000000000, 0.000000000000000000 ) ) ;
#41059=ADVANCED_FACE ( 'NONE', ( #145622 ), #82917, .F. ) ;
#41079=ORIENTED_EDGE ( 'NONE', *, *, #91786, .F. ) ;
#41080=ADVANCED_FACE ( 'NONE', ( #49093 ), #253805, .T. ) ;
#41111=VERTEX_POINT ( 'NONE', #105177 ) ;
#41162=CARTESIAN_POINT ( 'NONE',  ( -18.50000000000000000, 64.25000000001158185, -57.37310748452440379 ) ) ;
#41166=LINE ( 'NONE', #179385, #164640 ) ;
#41183=EDGE_LOOP ( 'NONE', ( #40799, #140376, #47841, #62121 ) ) ;
#41198=AXIS2_PLACEMENT_3D ( 'NONE', #144558, #229258, #127579 ) ;
#41199=EDGE_CURVE ( 'NONE', #82836, #209151, #44066, .T. ) ;
#41207=AXIS2_PLACEMENT_3D ( 'NONE', #79502, #253015, #76946 ) ;
#41208=ORIENTED_EDGE ( 'NONE', *, *, #43336, .T. ) ;
#41212=CIRCLE ( 'NONE', #174526, 0.09999999999999939493 ) ;
#41216=EDGE_CURVE ( 'NONE', #117567, #14406, #41467, .T. ) ;
#41256=EDGE_CURVE ( 'NONE', #111234, #175346, #81470, .T. ) ;
#41266=DIRECTION ( 'NONE',  ( 0.000000000000000000, -1.000000000000000000, -6.982962677686266711E-15 ) ) ;
#41286=ORIENTED_EDGE ( 'NONE', *, *, #69667, .T. ) ;
#41288=CARTESIAN_POINT ( 'NONE',  ( -20.85000000000000142, 77.36242903720467723, -28.13422623660311217 ) ) ;
#41312=VERTEX_POINT ( 'NONE', #76351 ) ;
#41349=ORIENTED_EDGE ( 'NONE', *, *, #76768, .F. ) ;
#41354=CARTESIAN_POINT ( 'NONE',  ( 20.53930447208010790, 67.02285131248657990, -61.08060034294610574 ) ) ;
#41355=AXIS2_PLACEMENT_3D ( 'NONE', #96092, #37441, #116961 ) ;
#41360=DIRECTION ( 'NONE',  ( 6.938893903907270030E-14, 0.000000000000000000, -1.000000000000000000 ) ) ;
#41395=DIRECTION ( 'NONE',  ( 0.000000000000000000, -6.982962677686266711E-15, 1.000000000000000000 ) ) ;
#41404=ORIENTED_EDGE ( 'NONE', *, *, #237772, .F. ) ;
#41467=CIRCLE ( 'NONE', #212142, 11.80000000000000426 ) ;
#41498=DIRECTION ( 'NONE',  ( 1.000000000000000000, 0.000000000000000000, 0.000000000000000000 ) ) ;
#41506=EDGE_LOOP ( 'NONE', ( #26591, #100726, #113671, #10822, #121953 ) ) ;
#41507=CARTESIAN_POINT ( 'NONE',  ( 21.05000000000000426, 69.74118280533018321, -69.55674021985801403 ) ) ;
#41523=ORIENTED_EDGE ( 'NONE', *, *, #92262, .F. ) ;
#41549=EDGE_CURVE ( 'NONE', #161837, #214123, #58162, .T. ) ;
#41598=ORIENTED_EDGE ( 'NONE', *, *, #42292, .T. ) ;
#41615=DIRECTION ( 'NONE',  ( -1.000000000000000000, 1.836970198721029934E-16, 1.282749433769087582E-30 ) ) ;
#41630=CARTESIAN_POINT ( 'NONE',  ( 23.24999999999999645, 76.00000000001165290, -69.52310748452431710 ) ) ;
#41637=AXIS2_PLACEMENT_3D ( 'NONE', #197252, #77295, #58995 ) ;
#41646=ADVANCED_FACE ( 'NONE', ( #174905 ), #216410, .T. ) ;
#41665=DIRECTION ( 'NONE',  ( -1.000000000000000000, 0.000000000000000000, -0.000000000000000000 ) ) ;
#41683=CARTESIAN_POINT ( 'NONE',  ( 21.05000000000000071, 87.65000000001144542, -39.12310748452424747 ) ) ;
#41690=LINE ( 'NONE', #181203, #222957 ) ;
#41756=EDGE_CURVE ( 'NONE', #142525, #12040, #112377, .T. ) ;
#41777=ADVANCED_FACE ( 'NONE', ( #88562 ), #186419, .T. ) ;
#41781=EDGE_LOOP ( 'NONE', ( #93904, #64874, #178006, #257211 ) ) ;
#41790=ORIENTED_EDGE ( 'NONE', *, *, #48770, .T. ) ;
#41808=VERTEX_POINT ( 'NONE', #50709 ) ;
#41818=EDGE_CURVE ( 'NONE', #237026, #58504, #162271, .T. ) ;
#41831=CARTESIAN_POINT ( 'NONE',  ( 20.95512820512820440, 65.37615131629968346, -57.37310748452439668 ) ) ;
#41844=EDGE_CURVE ( 'NONE', #218009, #20467, #53313, .T. ) ;
#41891=CARTESIAN_POINT ( 'NONE',  ( 23.14999999999999147, 71.85000000001166143, -69.52310748452434552 ) ) ;
#41900=CARTESIAN_POINT ( 'NONE',  ( -18.59999999999999787, 66.85000000001150511, -48.37310748452438247 ) ) ;
#41977=CIRCLE ( 'NONE', #50306, 0.1000000000000028644 ) ;
#41978=ORIENTED_EDGE ( 'NONE', *, *, #184171, .F. ) ;
#42019=ORIENTED_EDGE ( 'NONE', *, *, #31208, .T. ) ;
#42077=AXIS2_PLACEMENT_3D ( 'NONE', #144312, #85613, #69966 ) ;
#42091=EDGE_LOOP ( 'NONE', ( #241259, #9184, #164050, #82562 ) ) ;
#42115=CARTESIAN_POINT ( 'NONE',  ( -18.59999996769639097, 85.36327376984198168, -62.34161356905849516 ) ) ;
#42118=CARTESIAN_POINT ( 'NONE',  ( -21.05000000000000071, 74.73821383144657204, -61.43660852097884373 ) ) ;
#42205=DIRECTION ( 'NONE',  ( 2.915501640297156255E-16, 1.000000000000000000, 6.997203936713175802E-15 ) ) ;
#42236=ORIENTED_EDGE ( 'NONE', *, *, #22240, .T. ) ;
#42248=AXIS2_PLACEMENT_3D ( 'NONE', #211106, #32510, #191569 ) ;
#42260=CARTESIAN_POINT ( 'NONE',  ( 20.95203847575071521, 65.49893946073758855, -61.95603613590083825 ) ) ;
#42285=FACE_OUTER_BOUND ( 'NONE', #65027, .T. ) ;
#42291=VERTEX_POINT ( 'NONE', #50196 ) ;
#42292=EDGE_CURVE ( 'NONE', #85480, #52627, #95408, .T. ) ;
#42293=DIRECTION ( 'NONE',  ( 0.000000000000000000, 0.000000000000000000, 1.000000000000000000 ) ) ;
#42301=ORIENTED_EDGE ( 'NONE', *, *, #34109, .F. ) ;
#42368=CIRCLE ( 'NONE', #158923, 12.97499999999999964 ) ;
#42378=DIRECTION ( 'NONE',  ( -0.000000000000000000, 6.982962677686266711E-15, -1.000000000000000000 ) ) ;
#42392=CARTESIAN_POINT ( 'NONE',  ( -21.14999999999999858, 87.75000000001165290, -69.52310748452424605 ) ) ;
#42405=VERTEX_POINT ( 'NONE', #80995 ) ;
#42410=CIRCLE ( 'NONE', #129709, 0.5000000000000004441 ) ;
#42411=ORIENTED_EDGE ( 'NONE', *, *, #76353, .T. ) ;
#42442=CARTESIAN_POINT ( 'NONE',  ( 20.94999999999999574, 74.16465844978715438, -57.86795619196134766 ) ) ;
#42448=DIRECTION ( 'NONE',  ( 1.000000000000000000, 0.000000000000000000, 0.000000000000000000 ) ) ;
#42455=CARTESIAN_POINT ( 'NONE',  ( 20.04142135623731136, 64.25000000001148237, -44.75595019699901655 ) ) ;
#42463=DIRECTION ( 'NONE',  ( 0.000000000000000000, -1.000000000000000000, -6.982962677686266711E-15 ) ) ;
#42466=CARTESIAN_POINT ( 'NONE',  ( -22.50000000000000000, 75.90736249940226799, -81.17280469156507650 ) ) ;
#42488=EDGE_LOOP ( 'NONE', ( #57621, #148224, #70057, #99708 ) ) ;
#42506=DIRECTION ( 'NONE',  ( 0.000000000000000000, 0.000000000000000000, 1.000000000000000000 ) ) ;
#42508=AXIS2_PLACEMENT_3D ( 'NONE', #121319, #83399, #26040 ) ;
#42525=CYLINDRICAL_SURFACE ( 'NONE', #205973, 0.1000000000000052097 ) ;
#42526=ORIENTED_EDGE ( 'NONE', *, *, #224276, .T. ) ;
#42543=CARTESIAN_POINT ( 'NONE',  ( -21.05000000000000071, 70.15000000001163016, -59.39061026024639744 ) ) ;
#42557=CARTESIAN_POINT ( 'NONE',  ( -21.08479644141222664, 69.65496134227977620, -69.58166192708848996 ) ) ;
#42570=EDGE_CURVE ( 'NONE', #198094, #90093, #168307, .T. ) ;
#42574=DIRECTION ( 'NONE',  ( 0.000000000000000000, -1.387778780781454006E-13, -1.000000000000000000 ) ) ;
#42578=ORIENTED_EDGE ( 'NONE', *, *, #106856, .T. ) ;
#42587=DIRECTION ( 'NONE',  ( 0.000000000000000000, -1.000000000000000000, -6.982962677686266711E-15 ) ) ;
#42597=EDGE_CURVE ( 'NONE', #38899, #94760, #58148, .T. ) ;
#42613=ORIENTED_EDGE ( 'NONE', *, *, #240506, .T. ) ;
#42635=CARTESIAN_POINT ( 'NONE',  ( 23.24999999999999289, 69.35000000001156195, -57.37310748452436826 ) ) ;
#42641=ADVANCED_FACE ( 'NONE', ( #11783 ), #92558, .T. ) ;
#42677=DIRECTION ( 'NONE',  ( 0.000000000000000000, 0.000000000000000000, -1.000000000000000000 ) ) ;
#42785=CARTESIAN_POINT ( 'NONE',  ( -20.94983749550516450, 65.70233904876961617, -30.54874109119683823 ) ) ;
#42799=ADVANCED_FACE ( 'NONE', ( #121160 ), #45705, .T. ) ;
#42804=ORIENTED_EDGE ( 'NONE', *, *, #184521, .T. ) ;
#42826=FACE_OUTER_BOUND ( 'NONE', #220946, .T. ) ;
#42829=DIRECTION ( 'NONE',  ( 0.000000000000000000, 1.000000000000000000, 6.608470384673536824E-15 ) ) ;
#42864=CARTESIAN_POINT ( 'NONE',  ( -21.05000000000000071, 87.65000000001144542, -38.92310748452424463 ) ) ;
#42894=CARTESIAN_POINT ( 'NONE',  ( -20.94999999999999929, 74.16465844978715438, -57.96795619196134908 ) ) ;
#42913=EDGE_CURVE ( 'NONE', #201784, #187652, #191676, .T. ) ;
#42946=DIRECTION ( 'NONE',  ( 1.000000000000000000, 0.000000000000000000, 0.000000000000000000 ) ) ;
#42964=DIRECTION ( 'NONE',  ( 0.000000000000000000, -1.000000000000000000, -6.982962677686266711E-15 ) ) ;
#42966=ORIENTED_EDGE ( 'NONE', *, *, #129954, .F. ) ;
#42978=DIRECTION ( 'NONE',  ( 1.000000000000000000, 0.000000000000000000, 0.000000000000000000 ) ) ;
#42992=CARTESIAN_POINT ( 'NONE',  ( 20.94999999999999929, 74.16465844978715438, -57.96795619196134908 ) ) ;
#43037=CARTESIAN_POINT ( 'NONE',  ( -20.54999999999999716, 71.65000000001151648, -48.37310748452434694 ) ) ;
#43059=ORIENTED_EDGE ( 'NONE', *, *, #11665, .T. ) ;
#43074=EDGE_LOOP ( 'NONE', ( #102996, #195395, #157314, #30128 ) ) ;
#43098=VERTEX_POINT ( 'NONE', #196488 ) ;
#43107=ORIENTED_EDGE ( 'NONE', *, *, #194158, .F. ) ;
#43109=EDGE_CURVE ( 'NONE', #186334, #180734, #153575, .T. ) ;
#43150=ORIENTED_EDGE ( 'NONE', *, *, #178085, .T. ) ;
#43164=CARTESIAN_POINT ( 'NONE',  ( -20.54999999999999716, 68.75000000001158185, -57.27310748452437394 ) ) ;
#43165=FACE_BOUND ( 'NONE', #60408, .T. ) ;
#43181=ADVANCED_FACE ( 'NONE', ( #99936 ), #104136, .F. ) ;
#43190=DIRECTION ( 'NONE',  ( 1.000000000000000000, 0.000000000000000000, 0.000000000000000000 ) ) ;
#43195=CARTESIAN_POINT ( 'NONE',  ( -23.15000000000000213, 64.25000000001173817, -81.27310748452440237 ) ) ;
#43196=AXIS2_PLACEMENT_3D ( 'NONE', #150142, #88837, #229662 ) ;
#43208=CARTESIAN_POINT ( 'NONE',  ( -20.94999999999999929, 87.48912529308749697, -39.12310748452424747 ) ) ;
#43224=CARTESIAN_POINT ( 'NONE',  ( -18.53317502108577486, 65.67736539654895012, -30.46251168765719797 ) ) ;
#43230=CARTESIAN_POINT ( 'NONE',  ( 20.95512820512820440, 65.37615131629968346, -57.37310748452439668 ) ) ;
#43280=EDGE_LOOP ( 'NONE', ( #5261, #162991, #164040, #222219 ) ) ;
#43293=DIRECTION ( 'NONE',  ( 0.000000000000000000, 6.982962677686267499E-15, -1.000000000000000000 ) ) ;
#43336=EDGE_CURVE ( 'NONE', #177661, #105159, #116620, .T. ) ;
#43344=ORIENTED_EDGE ( 'NONE', *, *, #186719, .F. ) ;
#43355=CIRCLE ( 'NONE', #189101, 2.000000000000001776 ) ;
#43406=VECTOR ( 'NONE', #4727, 1000.000000000000114 ) ;
#43433=ORIENTED_EDGE ( 'NONE', *, *, #130619, .T. ) ;
#43471=VECTOR ( 'NONE', #119524, 1000.000000000000000 ) ;
#43499=CARTESIAN_POINT ( 'NONE',  ( -18.59999999999999787, 64.35000000001174669, -81.27310748452440237 ) ) ;
#43546=ORIENTED_EDGE ( 'NONE', *, *, #97325, .F. ) ;
#43549=EDGE_CURVE ( 'NONE', #81112, #39027, #71038, .T. ) ;
#43567=DIRECTION ( 'NONE',  ( 0.000000000000000000, 0.000000000000000000, 1.000000000000000000 ) ) ;
#43571=VECTOR ( 'NONE', #236082, 1000.000000000000000 ) ;
#43589=CARTESIAN_POINT ( 'NONE',  ( -18.50000000000000000, 64.35000000001157616, -57.37310748452440379 ) ) ;
#43591=AXIS2_PLACEMENT_3D ( 'NONE', #2604, #242507, #125146 ) ;
#43608=DIRECTION ( 'NONE',  ( 0.000000000000000000, -7.487053152578127080E-15, 1.000000000000000000 ) ) ;
#43616=CARTESIAN_POINT ( 'NONE',  ( 18.49999999999999289, 69.15387683765879956, -32.28538121767450519 ) ) ;
#43626=DIRECTION ( 'NONE',  ( 1.000000000000000000, 0.000000000000000000, 0.000000000000000000 ) ) ;
#43630=EDGE_CURVE ( 'NONE', #146658, #16741, #179363, .T. ) ;
#43631=ORIENTED_EDGE ( 'NONE', *, *, #119104, .T. ) ;
#43636=EDGE_CURVE ( 'NONE', #91949, #6351, #98721, .T. ) ;
#43637=SPHERICAL_SURFACE ( 'NONE', #147932, 0.1000000000000000056 ) ;
#43651=ADVANCED_FACE ( 'NONE', ( #125639 ), #91859, .F. ) ;
#43658=DIRECTION ( 'NONE',  ( 0.000000000000000000, 0.1298341882519953583, 0.9915357197604862671 ) ) ;
#43683=VERTEX_POINT ( 'NONE', #210328 ) ;
#43748=VECTOR ( 'NONE', #79240, 1000.000000000000000 ) ;
#43767=VECTOR ( 'NONE', #106554, 1000.000000000000000 ) ;
#43790=AXIS2_PLACEMENT_3D ( 'NONE', #62977, #81233, #1706 ) ;
#43818=VERTEX_POINT ( 'NONE', #91653 ) ;
#43819=ORIENTED_EDGE ( 'NONE', *, *, #193202, .T. ) ;
#43822=ORIENTED_EDGE ( 'NONE', *, *, #205097, .T. ) ;
#43827=CARTESIAN_POINT ( 'NONE',  ( -23.25000000000000000, 87.65000000001174385, -81.27310748452423184 ) ) ;
#43839=CARTESIAN_POINT ( 'NONE',  ( -23.15000000000000213, 76.00000000001165290, -69.52310748452431710 ) ) ;
#43858=CARTESIAN_POINT ( 'NONE',  ( 19.87657994472038325, 64.25000000001148237, -44.75731935989819021 ) ) ;
#43862=CARTESIAN_POINT ( 'NONE',  ( -20.94999999999999929, 74.75000000001159606, -61.52310748452433131 ) ) ;
#43876=DIRECTION ( 'NONE',  ( 1.000000000000000000, 0.000000000000000000, 0.000000000000000000 ) ) ;
#43903=CARTESIAN_POINT ( 'NONE',  ( 20.94999999999999929, 87.65000000001144542, -39.02310748452423894 ) ) ;
#43930=CARTESIAN_POINT ( 'NONE',  ( -21.05000000000000071, 69.72991413632250612, -69.55797548753746185 ) ) ;
#43956=CARTESIAN_POINT ( 'NONE',  ( -20.95000000000000284, 64.35000000001147669, -43.03791325517834565 ) ) ;
#43988=VERTEX_POINT ( 'NONE', #23703 ) ;
#43992=ADVANCED_FACE ( 'NONE', ( #103184 ), #240158, .F. ) ;
#43996=EDGE_LOOP ( 'NONE', ( #62289, #151888, #103339, #3681, #199751 ) ) ;
#44011=ORIENTED_EDGE ( 'NONE', *, *, #110132, .F. ) ;
#44016=ORIENTED_EDGE ( 'NONE', *, *, #179289, .T. ) ;
#44017=AXIS2_PLACEMENT_3D ( 'NONE', #10385, #229426, #248998 ) ;
#44047=DIRECTION ( 'NONE',  ( -2.342056488767301376E-15, 0.1350103645451974088, -0.9908441862701587999 ) ) ;
#44057=AXIS2_PLACEMENT_3D ( 'NONE', #183947, #5277, #165696 ) ;
#44066=B_SPLINE_CURVE_WITH_KNOTS ( 'NONE', 3,
 ( #9979, #149514, #192470, #93358, #54227, #89498, #210746 ),
 .UNSPECIFIED., .F., .F.,
 ( 4, 3, 4 ),
 ( 0.000000000000000000, 0.0009834301579440022593, 0.001767853679402679300 ),
 .UNSPECIFIED. ) ;
#44069=EDGE_LOOP ( 'NONE', ( #195983, #206047, #54950 ) ) ;
#44071=CARTESIAN_POINT ( 'NONE',  ( 23.14999999999999858, 71.00000000001151079, -48.42837350343745584 ) ) ;
#44095=AXIS2_PLACEMENT_3D ( 'NONE', #181676, #206371, #107256 ) ;
#44159=CARTESIAN_POINT ( 'NONE',  ( -18.59999999999999787, 74.14897176987071248, -57.86919421510183525 ) ) ;
#44165=ORIENTED_EDGE ( 'NONE', *, *, #131190, .F. ) ;
#44203=EDGE_CURVE ( 'NONE', #172081, #223901, #233877, .T. ) ;
#44217=DIRECTION ( 'NONE',  ( 0.000000000000000000, -0.9998779222360097974, 0.01562500000000363945 ) ) ;
#44233=VERTEX_POINT ( 'NONE', #77857 ) ;
#44291=CARTESIAN_POINT ( 'NONE',  ( 18.59999999999999076, 64.25000000001161027, -61.42310748452440095 ) ) ;
#44302=CARTESIAN_POINT ( 'NONE',  ( 18.60000000000000142, 85.32100840337290037, -62.28716923544637041 ) ) ;
#44321=VERTEX_POINT ( 'NONE', #184667 ) ;
#44339=SURFACE_SIDE_STYLE ('',( #26061 ) ) ;
#44347=VERTEX_POINT ( 'NONE', #239524 ) ;
#44365=DIRECTION ( 'NONE',  ( -0.000000000000000000, -0.8660254037844468122, -0.4999999999999860112 ) ) ;
#44379=EDGE_LOOP ( 'NONE', ( #89694, #160178, #165545, #11415 ) ) ;
#44390=ORIENTED_EDGE ( 'NONE', *, *, #68038, .T. ) ;
#44439=AXIS2_PLACEMENT_3D ( 'NONE', #220870, #100885, #4388 ) ;
#44479=CARTESIAN_POINT ( 'NONE',  ( -20.85000000000000142, 77.25000000001136868, -28.22262673010922995 ) ) ;
#44485=DIRECTION ( 'NONE',  ( 0.000000000000000000, 2.362176648138630895E-15, 1.000000000000000000 ) ) ;
#44490=LINE ( 'NONE', #165731, #186221 ) ;
#44501=LINE ( 'NONE', #64049, #58087 ) ;
#44516=ORIENTED_EDGE ( 'NONE', *, *, #129794, .T. ) ;
#44536=DIRECTION ( 'NONE',  ( 0.000000000000000000, -0.4999999999999689138, -0.8660254037844565822 ) ) ;
#44555=DIRECTION ( 'NONE',  ( 1.000000000000000000, -0.000000000000000000, 0.000000000000000000 ) ) ;
#44578=ORIENTED_EDGE ( 'NONE', *, *, #200265, .T. ) ;
#44594=DIRECTION ( 'NONE',  ( 1.000000000000000000, 0.000000000000000000, 0.000000000000000000 ) ) ;
#44606=ADVANCED_FACE ( 'NONE', ( #119277 ), #791, .F. ) ;
#44646=CARTESIAN_POINT ( 'NONE',  ( 21.05000000000000071, 67.22371711014383777, -57.34689234345615461 ) ) ;
#44661=VERTEX_POINT ( 'NONE', #142655 ) ;
#44663=DIRECTION ( 'NONE',  ( -0.000000000000000000, 7.272083257015735086E-15, -1.000000000000000000 ) ) ;
#44681=ORIENTED_EDGE ( 'NONE', *, *, #113245, .T. ) ;
#44704=ORIENTED_EDGE ( 'NONE', *, *, #235285, .F. ) ;
#44724=ORIENTED_EDGE ( 'NONE', *, *, #223017, .T. ) ;
#44740=ADVANCED_FACE ( 'NONE', ( #61864 ), #181806, .T. ) ;
#44742=ADVANCED_FACE ( 'NONE', ( #220910 ), #100928, .F. ) ;
#44769=ADVANCED_FACE ( 'NONE', ( #47413 ), #168717, .F. ) ;
#44794=AXIS2_PLACEMENT_3D ( 'NONE', #199450, #177334, #239849 ) ;
#44799=DIRECTION ( 'NONE',  ( 1.000000000000000000, 0.000000000000000000, 0.000000000000000000 ) ) ;
#44804=ORIENTED_EDGE ( 'NONE', *, *, #213651, .T. ) ;
#44821=CARTESIAN_POINT ( 'NONE',  ( 20.95568717954149562, 65.39800594611979534, -61.92059911625574387 ) ) ;
#44843=AXIS2_PLACEMENT_3D ( 'NONE', #206231, #87545, #167138 ) ;
#44881=ORIENTED_EDGE ( 'NONE', *, *, #163943, .F. ) ;
#44891=FACE_OUTER_BOUND ( 'NONE', #218297, .T. ) ;
#44938=EDGE_CURVE ( 'NONE', #160483, #156337, #188445, .T. ) ;
#44946=DIRECTION ( 'NONE',  ( 0.000000000000000000, 0.9876197685951241256, 0.1568667991644932258 ) ) ;
#44959=TOROIDAL_SURFACE ( 'NONE', #190733, 0.4000000000000009104, 0.1000000000000000056 ) ;
#45032=VECTOR ( 'NONE', #193458, 999.9999999999998863 ) ;
#45041=CARTESIAN_POINT ( 'NONE',  ( -22.49072729836729678, 75.94351806727812004, -81.17311573367925348 ) ) ;
#45051=EDGE_LOOP ( 'NONE', ( #2496, #73122, #224673 ) ) ;
#45082=AXIS2_PLACEMENT_3D ( 'NONE', #86789, #166385, #187217 ) ;
#45111=AXIS2_PLACEMENT_3D ( 'NONE', #84066, #119404, #198926 ) ;
#45117=DIRECTION ( 'NONE',  ( 0.000000000000000000, -1.000000000000000000, -6.982962677686266711E-15 ) ) ;
#45121=FACE_OUTER_BOUND ( 'NONE', #187791, .T. ) ;
#45134=CARTESIAN_POINT ( 'NONE',  ( 19.80993210785466374, 64.25000000001149658, -44.75598973563685234 ) ) ;
#45158=ORIENTED_EDGE ( 'NONE', *, *, #40283, .T. ) ;
#45159=DIRECTION ( 'NONE',  ( -1.000000000000000000, 7.304098846218134667E-16, 5.100424963727255829E-30 ) ) ;
#45162=PLANE ( 'NONE',  #237867 ) ;
#45191=ORIENTED_EDGE ( 'NONE', *, *, #24321, .T. ) ;
#45196=CARTESIAN_POINT ( 'NONE',  ( -21.05000000000000071, 76.10000000001171827, -76.06376443622556849 ) ) ;
#45202=DIRECTION ( 'NONE',  ( 0.000000000000000000, -7.304098846218112382E-15, 1.000000000000000000 ) ) ;
#45256=VERTEX_POINT ( 'NONE', #254153 ) ;
#45308=DIRECTION ( 'NONE',  ( 0.000000000000000000, 0.000000000000000000, -1.000000000000000000 ) ) ;
#45311=EDGE_CURVE ( 'NONE', #179727, #248043, #155358, .T. ) ;
#45332=CIRCLE ( 'NONE', #178647, 0.1000000000000028644 ) ;
#45349=DIRECTION ( 'NONE',  ( 1.000000000000000000, -2.952720810173289112E-16, -2.061873921506763405E-30 ) ) ;
#45369=ORIENTED_EDGE ( 'NONE', *, *, #137522, .F. ) ;
#45385=DIRECTION ( 'NONE',  ( 0.000000000000000000, -7.056502275159890832E-15, 1.000000000000000000 ) ) ;
#45408=EDGE_LOOP ( 'NONE', ( #41079, #52868, #161667, #51830 ) ) ;
#45424=VECTOR ( 'NONE', #99047, 1000.000000000000000 ) ;
#45434=CARTESIAN_POINT ( 'NONE',  ( 21.07928932188134397, 69.67148334361836248, -69.62200263017875557 ) ) ;
#45437=ORIENTED_EDGE ( 'NONE', *, *, #165402, .F. ) ;
#45443=CARTESIAN_POINT ( 'NONE',  ( -18.59999999999999787, 64.35000000001157616, -57.37310748452440379 ) ) ;
#45549=AXIS2_PLACEMENT_3D ( 'NONE', #186871, #231140, #245551 ) ;
#45586=ORIENTED_EDGE ( 'NONE', *, *, #85648, .F. ) ;
#45592=ORIENTED_EDGE ( 'NONE', *, *, #189092, .F. ) ;
#45610=ADVANCED_FACE ( 'NONE', ( #231517 ), #122192, .F. ) ;
#45621=VECTOR ( 'NONE', #11226, 1000.000000000000000 ) ;
#45671=EDGE_LOOP ( 'NONE', ( #239280, #240975, #246468, #62200, #15139 ) ) ;
#45679=ORIENTED_EDGE ( 'NONE', *, *, #193195, .F. ) ;
#45696=CARTESIAN_POINT ( 'NONE',  ( 23.14999999999999503, 69.35000000001151932, -48.17310748452437252 ) ) ;
#45697=VERTEX_POINT ( 'NONE', #211957 ) ;
#45705=TOROIDAL_SURFACE ( 'NONE', #66565, 11.90000000000000391, 0.1000000000000000056 ) ;
#45707=CIRCLE ( 'NONE', #8119, 2.000000000000001776 ) ;
#45730=ORIENTED_EDGE ( 'NONE', *, *, #43630, .T. ) ;
#45772=EDGE_LOOP ( 'NONE', ( #237236, #53437, #105927, #53514 ) ) ;
#45805=FACE_OUTER_BOUND ( 'NONE', #151199, .T. ) ;
#45808=DIRECTION ( 'NONE',  ( 4.336808689942128965E-15, -0.8660254037844367092, 0.5000000000000037748 ) ) ;
#45830=AXIS2_PLACEMENT_3D ( 'NONE', #5327, #203562, #226977 ) ;
#45845=ORIENTED_EDGE ( 'NONE', *, *, #97186, .T. ) ;
#45854=ORIENTED_EDGE ( 'NONE', *, *, #85600, .F. ) ;
#45877=DIRECTION ( 'NONE',  ( 0.000000000000000000, 0.000000000000000000, 1.000000000000000000 ) ) ;
#45924=CARTESIAN_POINT ( 'NONE',  ( 20.85000000000000142, 87.75000000001142553, -39.02310748452423894 ) ) ;
#45968=CIRCLE ( 'NONE', #237522, 0.2000000000000057288 ) ;
#45987=ORIENTED_EDGE ( 'NONE', *, *, #37411, .T. ) ;
#46022=TOROIDAL_SURFACE ( 'NONE', #183412, 11.90000000000000213, 0.1000000000000000056 ) ;
#46033=ADVANCED_FACE ( 'NONE', ( #151701 ), #227341, .F. ) ;
#46037=DIRECTION ( 'NONE',  ( 0.000000000000000000, -7.124650136758292359E-15, 1.000000000000000000 ) ) ;
#46068=CARTESIAN_POINT ( 'NONE',  ( -21.05000000000000071, 77.25000000001159606, -61.52310748452431710 ) ) ;
#46070=EDGE_LOOP ( 'NONE', ( #164667, #186472, #12732, #103200 ) ) ;
#46088=DIRECTION ( 'NONE',  ( 0.000000000000000000, -7.056502275159894776E-15, 1.000000000000000000 ) ) ;
#46100=CIRCLE ( 'NONE', #21203, 7.900000000000003908 ) ;
#46102=CARTESIAN_POINT ( 'NONE',  ( 21.93340585898594597, 76.00000000001170974, -76.84725450665315805 ) ) ;
#46107=EDGE_CURVE ( 'NONE', #216920, #150942, #199473, .T. ) ;
#46108=ORIENTED_EDGE ( 'NONE', *, *, #166112, .F. ) ;
#46125=DIRECTION ( 'NONE',  ( 1.000000000000000000, 0.000000000000000000, 0.000000000000000000 ) ) ;
#46132=CARTESIAN_POINT ( 'NONE',  ( -21.09813707148783379, 75.96864850048226003, -75.90816959026101074 ) ) ;
#46163=DIRECTION ( 'NONE',  ( 0.000000000000000000, -7.116814260417668513E-15, 1.000000000000000000 ) ) ;
#46167=LINE ( 'NONE', #65738, #15801 ) ;
#46175=DIRECTION ( 'NONE',  ( 0.000000000000000000, 6.982962677686267499E-15, -1.000000000000000000 ) ) ;
#46209=DIRECTION ( 'NONE',  ( 0.000000000000000000, 0.9893560106964510714, -0.1455152366551481502 ) ) ;
#46211=CARTESIAN_POINT ( 'NONE',  ( -22.59999999999999787, 64.35042919246686210, -69.62310748452439668 ) ) ;
#46216=CYLINDRICAL_SURFACE ( 'NONE', #100462, 0.5000000000000004441 ) ;
#46272=FACE_OUTER_BOUND ( 'NONE', #216034, .T. ) ;
#46291=CARTESIAN_POINT ( 'NONE',  ( 23.14999999999999858, 78.00000000001142553, -36.02310748452431000 ) ) ;
#46294=VERTEX_POINT ( 'NONE', #247562 ) ;
#46316=CARTESIAN_POINT ( 'NONE',  ( -23.15000000000000213, 76.00000000001139711, -32.02310748452432421 ) ) ;
#46389=DIRECTION ( 'NONE',  ( 1.000000000000000000, -0.000000000000000000, 0.000000000000000000 ) ) ;
#46395=DIRECTION ( 'NONE',  ( 0.000000000000000000, -0.4999999999999689138, 0.8660254037844565822 ) ) ;
#46405=FACE_OUTER_BOUND ( 'NONE', #110173, .T. ) ;
#46408=EDGE_CURVE ( 'NONE', #120086, #47209, #122570, .T. ) ;
#46434=CARTESIAN_POINT ( 'NONE',  ( 23.24999999999999289, 64.35000000001156195, -57.37310748452439668 ) ) ;
#46447=DIRECTION ( 'NONE',  ( 0.000000000000000000, 0.000000000000000000, 1.000000000000000000 ) ) ;
#46459=VECTOR ( 'NONE', #32721, 1000.000000000000000 ) ;
#46476=CARTESIAN_POINT ( 'NONE',  ( 21.05000000000000071, 69.35000000001159037, -59.50608031408435039 ) ) ;
#46478=AXIS2_PLACEMENT_3D ( 'NONE', #63857, #222916, #108120 ) ;
#46497=AXIS2_PLACEMENT_3D ( 'NONE', #42992, #226742, #48107 ) ;
#46512=DIRECTION ( 'NONE',  ( -1.000000000000000000, 0.000000000000000000, -0.000000000000000000 ) ) ;
#46516=ADVANCED_FACE ( 'NONE', ( #135299 ), #230718, .T. ) ;
#46534=ORIENTED_EDGE ( 'NONE', *, *, #42597, .F. ) ;
#46580=DIRECTION ( 'NONE',  ( 0.000000000000000000, -1.411300455031978166E-14, 1.000000000000000000 ) ) ;
#46587=CARTESIAN_POINT ( 'NONE',  ( -18.59999999999999787, 74.36282728704118483, -57.94095411905231430 ) ) ;
#46629=CARTESIAN_POINT ( 'NONE',  ( 20.84999999999998721, 64.25000000001142553, -36.02310748452440237 ) ) ;
#46634=CIRCLE ( 'NONE', #117397, 11.70000000000000284 ) ;
#46659=CIRCLE ( 'NONE', #50747, 0.1000000000000026007 ) ;
#46671=ORIENTED_EDGE ( 'NONE', *, *, #32016, .F. ) ;
#46692=ORIENTED_EDGE ( 'NONE', *, *, #120097, .F. ) ;
#46708=EDGE_CURVE ( 'NONE', #50336, #110098, #163678, .T. ) ;
#46741=VERTEX_POINT ( 'NONE', #189847 ) ;
#46796=CARTESIAN_POINT ( 'NONE',  ( 18.50000000000000000, 85.40000000001160174, -62.22584772486096227 ) ) ;
#46802=ORIENTED_EDGE ( 'NONE', *, *, #196288, .T. ) ;
#46844=EDGE_CURVE ( 'NONE', #169064, #250549, #97120, .T. ) ;
#46870=CARTESIAN_POINT ( 'NONE',  ( 23.14999999999999503, 64.35000000001146248, -43.03791325517834565 ) ) ;
#46883=ORIENTED_EDGE ( 'NONE', *, *, #12205, .F. ) ;
#46887=CARTESIAN_POINT ( 'NONE',  ( 18.59999999999999432, 74.27191306321728348, -82.63867247935655769 ) ) ;
#46897=CARTESIAN_POINT ( 'NONE',  ( 23.15000000000000213, 87.75000000001156764, -57.37310748452424036 ) ) ;
#46909=VERTEX_POINT ( 'NONE', #240535 ) ;
#46919=EDGE_CURVE ( 'NONE', #160725, #196143, #172669, .T. ) ;
#46971=ORIENTED_EDGE ( 'NONE', *, *, #102616, .F. ) ;
#46985=DIRECTION ( 'NONE',  ( 0.000000000000000000, 6.982962677686266711E-15, -1.000000000000000000 ) ) ;
#47002=VERTEX_POINT ( 'NONE', #3183 ) ;
#47004=EDGE_CURVE ( 'NONE', #218009, #97734, #126256, .T. ) ;
#47127=FACE_OUTER_BOUND ( 'NONE', #10642, .T. ) ;
#47197=ORIENTED_EDGE ( 'NONE', *, *, #164266, .T. ) ;
#47199=ORIENTED_EDGE ( 'NONE', *, *, #142546, .F. ) ;
#47209=VERTEX_POINT ( 'NONE', #253370 ) ;
#47214=EDGE_CURVE ( 'NONE', #111790, #162078, #18619, .T. ) ;
#47256=VECTOR ( 'NONE', #91440, 1000.000000000000114 ) ;
#47260=CARTESIAN_POINT ( 'NONE',  ( -20.00857864376270001, 66.65000000001150227, -48.37310748452438958 ) ) ;
#47278=DIRECTION ( 'NONE',  ( 0.000000000000000000, 0.000000000000000000, 1.000000000000000000 ) ) ;
#47288=CARTESIAN_POINT ( 'NONE',  ( -21.59142135623730852, 68.15000000001150227, -48.27310748452437394 ) ) ;
#47289=AXIS2_PLACEMENT_3D ( 'NONE', #154873, #234367, #111881 ) ;
#47305=CARTESIAN_POINT ( 'NONE',  ( 21.08489247129321242, 67.12232480914150301, -57.17310748452439384 ) ) ;
#47313=CARTESIAN_POINT ( 'NONE',  ( 21.05000000000000071, 65.51540711881749246, -62.06639391394066507 ) ) ;
#47362=VECTOR ( 'NONE', #76831, 1000.000000000000000 ) ;
#47366=DIRECTION ( 'NONE',  ( -1.000000000000000000, 0.000000000000000000, 0.000000000000000000 ) ) ;
#47369=EDGE_CURVE ( 'NONE', #167778, #53080, #134793, .T. ) ;
#47378=CARTESIAN_POINT ( 'NONE',  ( 21.07094088545369104, 75.90110629745947790, -75.84327470644146274 ) ) ;
#47401=SPHERICAL_SURFACE ( 'NONE', #191013, 0.1000000000000000056 ) ;
#47413=FACE_OUTER_BOUND ( 'NONE', #44069, .T. ) ;
#47449=VERTEX_POINT ( 'NONE', #249227 ) ;
#47466=CARTESIAN_POINT ( 'NONE',  ( -21.14999999999999858, 76.10000000001174669, -81.17267829206912211 ) ) ;
#47474=ADVANCED_FACE ( 'NONE', ( #210108 ), #159977, .F. ) ;
#47482=EDGE_CURVE ( 'NONE', #67782, #214123, #30791, .T. ) ;
#47484=CARTESIAN_POINT ( 'NONE',  ( -23.25000000000000000, 77.25000000001136868, -28.22262673010923351 ) ) ;
#47485=ORIENTED_EDGE ( 'NONE', *, *, #204221, .F. ) ;
#47522=CYLINDRICAL_SURFACE ( 'NONE', #67320, 0.09999999999999939493 ) ;
#47525=CIRCLE ( 'NONE', #122588, 0.1000000000000028644 ) ;
#47544=FACE_OUTER_BOUND ( 'NONE', #104449, .T. ) ;
#47582=EDGE_CURVE ( 'NONE', #17664, #230778, #172297, .T. ) ;
#47640=VERTEX_POINT ( 'NONE', #3879 ) ;
#47658=ORIENTED_EDGE ( 'NONE', *, *, #108341, .T. ) ;
#47687=VECTOR ( 'NONE', #52331, 1000.000000000000114 ) ;
#47700=EDGE_LOOP ( 'NONE', ( #41286, #65419, #30341, #155565 ) ) ;
#47704=CARTESIAN_POINT ( 'NONE',  ( 23.14999999999999858, 76.00000000001142553, -36.02310748452432421 ) ) ;
#47713=CARTESIAN_POINT ( 'NONE',  ( 20.94999999999999929, 71.14953271029189352, -48.05737489352603120 ) ) ;
#47730=CIRCLE ( 'NONE', #201867, 0.1000000000000028644 ) ;
#47773=CARTESIAN_POINT ( 'NONE',  ( 20.96428641294107820, 64.25000000001146816, -42.84821430658371355 ) ) ;
#47775=VERTEX_POINT ( 'NONE', #2580 ) ;
#47800=ORIENTED_EDGE ( 'NONE', *, *, #205583, .T. ) ;
#47808=CARTESIAN_POINT ( 'NONE',  ( 21.05000000000000071, 61.95000000001146390, -41.53680255528533394 ) ) ;
#47813=ORIENTED_EDGE ( 'NONE', *, *, #1896, .F. ) ;
#47825=CARTESIAN_POINT ( 'NONE',  ( 18.49999999999987566, 65.62657994473185852, -44.75731935989774257 ) ) ;
#47831=DIRECTION ( 'NONE',  ( -1.000000000000000000, 1.875376730785737719E-16, 1.309568571767809260E-30 ) ) ;
#47841=ORIENTED_EDGE ( 'NONE', *, *, #188386, .T. ) ;
#47844=DIRECTION ( 'NONE',  ( 0.000000000000000000, 8.770518838402102073E-15, -1.000000000000000000 ) ) ;
#47848=CARTESIAN_POINT ( 'NONE',  ( -21.44999999999999929, 68.85000000001156195, -57.27310748452436684 ) ) ;
#47850=CARTESIAN_POINT ( 'NONE',  ( 23.14999999999999147, 80.15000000001165859, -69.52310748452430289 ) ) ;
#47889=ADVANCED_FACE ( 'NONE', ( #136296 ), #80168, .T. ) ;
#47911=CARTESIAN_POINT ( 'NONE',  ( -21.29999999999995808, 76.00000000001168132, -73.57310748452432847 ) ) ;
#47927=DIRECTION ( 'NONE',  ( 1.000000000000000000, 0.000000000000000000, 0.000000000000000000 ) ) ;
#47933=VERTEX_POINT ( 'NONE', #98435 ) ;
#47935=DIRECTION ( 'NONE',  ( 0.000000000000000000, 0.000000000000000000, 1.000000000000000000 ) ) ;
#47970=CARTESIAN_POINT ( 'NONE',  ( -20.94999999999999929, 74.73821383144657204, -61.43660852097884373 ) ) ;
#47971=VERTEX_POINT ( 'NONE', #95902 ) ;
#47978=VECTOR ( 'NONE', #90608, 1000.000000000000000 ) ;
#48014=CARTESIAN_POINT ( 'NONE',  ( -22.39999999999999858, 64.35000000001166143, -69.62310748452439668 ) ) ;
#48035=ADVANCED_FACE ( 'NONE', ( #164888 ), #104863, .T. ) ;
#48044=DIRECTION ( 'NONE',  ( 0.000000000000000000, -1.000000000000000000, -6.982962677686265922E-15 ) ) ;
#48057=CARTESIAN_POINT ( 'NONE',  ( 18.49999999999998934, 65.75000000001149658, -44.77310748452439526 ) ) ;
#48088=EDGE_LOOP ( 'NONE', ( #66403, #228808, #211333, #53364 ) ) ;
#48096=EDGE_CURVE ( 'NONE', #207310, #119594, #114334, .T. ) ;
#48107=DIRECTION ( 'NONE',  ( 1.000000000000000000, 0.000000000000000000, 0.000000000000000000 ) ) ;
#48117=DIRECTION ( 'NONE',  ( 0.000000000000000000, 0.000000000000000000, 1.000000000000000000 ) ) ;
#48161=CARTESIAN_POINT ( 'NONE',  ( 18.49351773456752213, 85.44302569515704704, -62.33778195849721016 ) ) ;
#48166=CARTESIAN_POINT ( 'NONE',  ( -23.25000000000000000, 64.25000000001142553, -36.02310748452440237 ) ) ;
#48170=ORIENTED_EDGE ( 'NONE', *, *, #154682, .F. ) ;
#48177=ORIENTED_EDGE ( 'NONE', *, *, #130897, .F. ) ;
#48181=ADVANCED_FACE ( 'NONE', ( #149197 ), #10099, .F. ) ;
#48199=EDGE_CURVE ( 'NONE', #178423, #38202, #60347, .T. ) ;
#48201=DIRECTION ( 'NONE',  ( 0.000000000000000000, -0.9908441862701605762, 0.1350103645451835310 ) ) ;
#48204=DIRECTION ( 'NONE',  ( -1.000000000000000000, -0.000000000000000000, -0.000000000000000000 ) ) ;
#48221=ORIENTED_EDGE ( 'NONE', *, *, #146241, .T. ) ;
#48247=ORIENTED_EDGE ( 'NONE', *, *, #181449, .T. ) ;
#48254=DIRECTION ( 'NONE',  ( 0.000000000000000000, 6.982962677686266711E-15, -1.000000000000000000 ) ) ;
#48300=ADVANCED_BREP_SHAPE_REPRESENTATION ( '', ( #24390, #2425 ), #106268 ) ;
#48302=ORIENTED_EDGE ( 'NONE', *, *, #47482, .T. ) ;
#48312=DIRECTION ( 'NONE',  ( 1.734723475976823250E-13, 0.7899159663865635839, 0.6132151058540398214 ) ) ;
#48316=EDGE_CURVE ( 'NONE', #156105, #201868, #96862, .T. ) ;
#48347=ADVANCED_FACE ( 'NONE', ( #117746 ), #78610, .F. ) ;
#48356=DIRECTION ( 'NONE',  ( 0.000000000000000000, 0.000000000000000000, 1.000000000000000000 ) ) ;
#48360=DIRECTION ( 'NONE',  ( 0.000000000000000000, 0.000000000000000000, -1.000000000000000000 ) ) ;
#48365=ORIENTED_EDGE ( 'NONE', *, *, #93162, .T. ) ;
#48405=VERTEX_POINT ( 'NONE', #160763 ) ;
#48421=CARTESIAN_POINT ( 'NONE',  ( -20.64999999999999858, 74.00000000001156764, -56.29848556176223440 ) ) ;
#48441=DIRECTION ( 'NONE',  ( 0.000000000000000000, 0.000000000000000000, 1.000000000000000000 ) ) ;
#48445=ADVANCED_FACE ( 'NONE', ( #165889 ), #6790, .F. ) ;
#48462=CARTESIAN_POINT ( 'NONE',  ( 21.05000000000000782, 75.96513199699860763, -75.79319334821346388 ) ) ;
#48495=DIRECTION ( 'NONE',  ( 0.000000000000000000, -6.608470384673547079E-15, 1.000000000000000000 ) ) ;
#48503=CARTESIAN_POINT ( 'NONE',  ( -18.49513951962167368, 85.43772502668907975, -29.24503490949512141 ) ) ;
#48539=ORIENTED_EDGE ( 'NONE', *, *, #47214, .F. ) ;
#48581=FACE_OUTER_BOUND ( 'NONE', #75793, .T. ) ;
#48582=CYLINDRICAL_SURFACE ( 'NONE', #57783, 0.1000000000000028644 ) ;
#48596=ORIENTED_EDGE ( 'NONE', *, *, #101465, .T. ) ;
#48600=( BOUNDED_SURFACE ( )  B_SPLINE_SURFACE ( 3, 2, ( 
 ( #85191, #162228, #163488 ),
 ( #6972, #26560, #86483 ),
 ( #246860, #126931, #25277 ),
 ( #241736, #185619, #5663 ) ),
 .UNSPECIFIED., .F., .F., .F. ) 
 B_SPLINE_SURFACE_WITH_KNOTS ( ( 4, 4 ),
 ( 3, 3 ),
 ( 0.000000000000000000, 0.001979672783031562362 ),
 ( 0.000000000000000000, 1.000000000000000000 ),
 .UNSPECIFIED. ) 
 GEOMETRIC_REPRESENTATION_ITEM ( )  RATIONAL_B_SPLINE_SURFACE ( (
 ( 1.000000000000000000, 0.7103081912008383236, 1.000000000000000000),
 ( 1.000000000000000000, 0.7104998333558377732, 1.000000000000000000),
 ( 1.000000000000000000, 0.7107238315755368685, 1.000000000000000000),
 ( 1.000000000000000000, 0.7110073749539289611, 1.000000000000000000) ) ) 
 REPRESENTATION_ITEM ( '' )  SURFACE ( )  );
#48613=AXIS2_PLACEMENT_3D ( 'NONE', #112493, #52485, #92900 ) ;
#48629=ADVANCED_FACE ( 'NONE', ( #228427 ), #77734, .F. ) ;
#48643=AXIS2_PLACEMENT_3D ( 'NONE', #19015, #178118, #39899 ) ;
#48665=AXIS2_PLACEMENT_3D ( 'NONE', #63047, #215692, #116613 ) ;
#48744=CARTESIAN_POINT ( 'NONE',  ( -22.39999999999999858, 76.00000000001173817, -81.17267829206912211 ) ) ;
#48747=EDGE_CURVE ( 'NONE', #37986, #56908, #57459, .T. ) ;
#48748=DIRECTION ( 'NONE',  ( 7.304098846218134667E-16, 1.000000000000000000, 6.982962677686267499E-15 ) ) ;
#48755=ORIENTED_EDGE ( 'NONE', *, *, #25961, .T. ) ;
#48767=ORIENTED_EDGE ( 'NONE', *, *, #208335, .T. ) ;
#48770=EDGE_CURVE ( 'NONE', #138858, #130839, #37937, .T. ) ;
#48781=CIRCLE ( 'NONE', #82076, 0.09999999999999939493 ) ;
#48782=DIRECTION ( 'NONE',  ( -0.000000000000000000, -1.000000000000000000, -8.609265936414532828E-15 ) ) ;
#48789=FACE_OUTER_BOUND ( 'NONE', #235280, .T. ) ;
#48829=VECTOR ( 'NONE', #251318, 1000.000000000000000 ) ;
#48846=CARTESIAN_POINT ( 'NONE',  ( 21.05000000000000071, 65.27628288308652316, -57.34686788338628105 ) ) ;
#48864=ORIENTED_EDGE ( 'NONE', *, *, #50047, .F. ) ;
#48874=CARTESIAN_POINT ( 'NONE',  ( 23.14999999999999858, 76.00000000001142553, -36.02310748452432421 ) ) ;
#48899=ORIENTED_EDGE ( 'NONE', *, *, #99699, .F. ) ;
#49016=ORIENTED_EDGE ( 'NONE', *, *, #79236, .F. ) ;
#49020=AXIS2_PLACEMENT_3D ( 'NONE', #205805, #246226, #90991 ) ;
#49028=EDGE_LOOP ( 'NONE', ( #169057, #223948, #67492, #23262 ) ) ;
#49031=LINE ( 'NONE', #191141, #34999 ) ;
#49087=DIRECTION ( 'NONE',  ( -0.000000000000000000, 1.000000000000000000, 6.982962677686267499E-15 ) ) ;
#49093=FACE_OUTER_BOUND ( 'NONE', #253752, .T. ) ;
#49100=LINE ( 'NONE', #656, #172514 ) ;
#49112=ORIENTED_EDGE ( 'NONE', *, *, #46708, .T. ) ;
#49132=CARTESIAN_POINT ( 'NONE',  ( 18.50000000000000000, 85.50000000001136868, -29.42291809330221142 ) ) ;
#49149=AXIS2_PLACEMENT_3D ( 'NONE', #51345, #130922, #53947 ) ;
#49167=TOROIDAL_SURFACE ( 'NONE', #3350, 12.97499999999999609, 0.1000000000000000056 ) ;
#49174=DIRECTION ( 'NONE',  ( 0.000000000000000000, 6.982962677686266711E-15, -1.000000000000000000 ) ) ;
#49201=CARTESIAN_POINT ( 'NONE',  ( 20.94999999999999574, 87.48912529308769592, -66.52310748452423184 ) ) ;
#49225=VERTEX_POINT ( 'NONE', #228641 ) ;
#49235=VERTEX_POINT ( 'NONE', #189500 ) ;
#49243=ORIENTED_EDGE ( 'NONE', *, *, #58339, .T. ) ;
#49267=( NAMED_UNIT ( * ) PLANE_ANGLE_UNIT ( ) SI_UNIT ( $, .RADIAN. ) );
#49299=FACE_OUTER_BOUND ( 'NONE', #71276, .T. ) ;
#49304=LINE ( 'NONE', #114419, #207122 ) ;
#49329=FACE_OUTER_BOUND ( 'NONE', #243486, .T. ) ;
#49332=DIRECTION ( 'NONE',  ( -1.000000000000000000, 1.387778780781454006E-13, 0.000000000000000000 ) ) ;
#49338=ORIENTED_EDGE ( 'NONE', *, *, #174541, .T. ) ;
#49364=ORIENTED_EDGE ( 'NONE', *, *, #250849, .F. ) ;
#49372=AXIS2_PLACEMENT_3D ( 'NONE', #179213, #76216, #239161 ) ;
#49383=DIRECTION ( 'NONE',  ( -3.265361837132813093E-16, -1.000000000000000000, -6.982962677686266711E-15 ) ) ;
#49404=ORIENTED_EDGE ( 'NONE', *, *, #131432, .T. ) ;
#49417=ORIENTED_EDGE ( 'NONE', *, *, #154083, .T. ) ;
#49420=ORIENTED_EDGE ( 'NONE', *, *, #114088, .T. ) ;
#49458=CARTESIAN_POINT ( 'NONE',  ( -18.50000000000000000, 77.16270174994961906, -61.42310748452431568 ) ) ;
#49467=DIRECTION ( 'NONE',  ( 0.000000000000000000, -0.1575844902526579161, -0.9875055080513779338 ) ) ;
#49480=AXIS2_PLACEMENT_3D ( 'NONE', #208069, #225019, #106355 ) ;
#49558=ORIENTED_EDGE ( 'NONE', *, *, #26483, .T. ) ;
#49562=CIRCLE ( 'NONE', #195332, 4.049999999999998046 ) ;
#49593=CARTESIAN_POINT ( 'NONE',  ( -21.05000000000000071, 76.00000000001149658, -47.82310748452432847 ) ) ;
#49597=DIRECTION ( 'NONE',  ( -0.000000000000000000, 6.982962677686266711E-15, -1.000000000000000000 ) ) ;
#49614=CARTESIAN_POINT ( 'NONE',  ( -18.59999999999999787, 77.73625713160897988, -57.95445515550681392 ) ) ;
#49657=CARTESIAN_POINT ( 'NONE',  ( 22.50000000000000000, 64.35042919246686210, -69.62310748452439668 ) ) ;
#49666=DIRECTION ( 'NONE',  ( 1.000000000000000000, 0.000000000000000000, 0.000000000000000000 ) ) ;
#49686=CIRCLE ( 'NONE', #195456, 12.87499999999999822 ) ;
#49710=AXIS2_PLACEMENT_3D ( 'NONE', #118542, #134212, #213769 ) ;
#49720=CYLINDRICAL_SURFACE ( 'NONE', #44843, 0.1000000000000028644 ) ;
#49725=ORIENTED_EDGE ( 'NONE', *, *, #257404, .T. ) ;
#49728=EDGE_LOOP ( 'NONE', ( #212446, #219053, #32588, #60217 ) ) ;
#49734=DIRECTION ( 'NONE',  ( 0.000000000000000000, 7.056502275159894776E-15, -1.000000000000000000 ) ) ;
#49748=ORIENTED_EDGE ( 'NONE', *, *, #190658, .F. ) ;
#49758=DIRECTION ( 'NONE',  ( 0.000000000000000000, -6.982962677686266711E-15, 1.000000000000000000 ) ) ;
#49777=DIRECTION ( 'NONE',  ( 1.000000000000000000, -0.000000000000000000, 0.000000000000000000 ) ) ;
#49807=DIRECTION ( 'NONE',  ( -1.000000000000000000, 1.836970198721029934E-16, 1.282749433769087757E-30 ) ) ;
#49812=CARTESIAN_POINT ( 'NONE',  ( 18.59999999999999076, 74.16465844978715438, -57.96795619196135618 ) ) ;
#49945=ORIENTED_EDGE ( 'NONE', *, *, #211029, .T. ) ;
#49946=CARTESIAN_POINT ( 'NONE',  ( 20.95556889135987788, 65.37805641227650710, -61.88071326266687322 ) ) ;
#49963=SPHERICAL_SURFACE ( 'NONE', #32865, 0.1000000000000000056 ) ;
#49965=CARTESIAN_POINT ( 'NONE',  ( 22.59999999999999432, 64.25012875563515991, -69.58853707553808476 ) ) ;
#49999=CARTESIAN_POINT ( 'NONE',  ( -22.39999999999999858, 68.20922040163824818, -69.62310748452438247 ) ) ;
#50011=ORIENTED_EDGE ( 'NONE', *, *, #61961, .F. ) ;
#50017=ORIENTED_EDGE ( 'NONE', *, *, #233545, .F. ) ;
#50047=EDGE_CURVE ( 'NONE', #53080, #7765, #191480, .T. ) ;
#50054=DIRECTION ( 'NONE',  ( 0.000000000000000000, -0.5000000000000209832, 0.8660254037844264952 ) ) ;
#50074=CARTESIAN_POINT ( 'NONE',  ( 21.05193202509564543, 65.27606398031439028, -57.35057288119863728 ) ) ;
#50082=ORIENTED_EDGE ( 'NONE', *, *, #47369, .T. ) ;
#50094=ORIENTED_EDGE ( 'NONE', *, *, #40939, .T. ) ;
#50104=EDGE_CURVE ( 'NONE', #59781, #65824, #116350, .T. ) ;
#50156=CARTESIAN_POINT ( 'NONE',  ( -23.25000000000000000, 64.35000000001146248, -43.03791325517835276 ) ) ;
#50160=EDGE_LOOP ( 'NONE', ( #34725, #121665, #193949, #64705 ) ) ;
#50183=AXIS2_PLACEMENT_3D ( 'NONE', #46211, #183180, #200165 ) ;
#50187=CYLINDRICAL_SURFACE ( 'NONE', #13276, 0.1000000000000055705 ) ;
#50196=CARTESIAN_POINT ( 'NONE',  ( 21.05000000000000071, 77.16270174994961906, -61.62310748452431142 ) ) ;
#50211=CIRCLE ( 'NONE', #112602, 0.1000000000000028644 ) ;
#50215=VERTEX_POINT ( 'NONE', #2210 ) ;
#50254=LINE ( 'NONE', #153262, #142552 ) ;
#50260=CARTESIAN_POINT ( 'NONE',  ( -21.05000000000000071, 77.85102823015243700, -57.86919421510181394 ) ) ;
#50263=ORIENTED_EDGE ( 'NONE', *, *, #204497, .F. ) ;
#50278=DIRECTION ( 'NONE',  ( 0.000000000000000000, 6.982962677686266711E-15, -1.000000000000000000 ) ) ;
#50280=LINE ( 'NONE', #128558, #54525 ) ;
#50302=DIRECTION ( 'NONE',  ( 0.000000000000000000, 1.000000000000000000, 0.000000000000000000 ) ) ;
#50306=AXIS2_PLACEMENT_3D ( 'NONE', #180972, #203086, #121024 ) ;
#50317=CARTESIAN_POINT ( 'NONE',  ( 21.14999999999999858, 64.35000000001156195, -57.37310748452439668 ) ) ;
#50329=CARTESIAN_POINT ( 'NONE',  ( -23.25000000000000000, 85.00000000001149658, -45.91707660717669626 ) ) ;
#50335=CARTESIAN_POINT ( 'NONE',  ( -23.25000000000000000, 76.10085836911045476, -81.27267460801371612 ) ) ;
#50336=VERTEX_POINT ( 'NONE', #208152 ) ;
#50337=CARTESIAN_POINT ( 'NONE',  ( 20.94560253601876809, 64.25000000001146816, -43.01302397200912964 ) ) ;
#50341=CARTESIAN_POINT ( 'NONE',  ( 23.14999999999998437, 80.05000000001165006, -69.52310748452430289 ) ) ;
#50364=EDGE_LOOP ( 'NONE', ( #38056, #202097, #109521, #34394 ) ) ;
#50375=FACE_OUTER_BOUND ( 'NONE', #236672, .T. ) ;
#50385=CIRCLE ( 'NONE', #104373, 0.1000000000000028644 ) ;
#50393=CIRCLE ( 'NONE', #83703, 0.1000000000000028644 ) ;
#50394=ORIENTED_EDGE ( 'NONE', *, *, #50584, .T. ) ;
#50399=LINE ( 'NONE', #109103, #169320 ) ;
#50400=ADVANCED_FACE ( 'NONE', ( #51587 ), #231556, .F. ) ;
#50435=CIRCLE ( 'NONE', #62938, 0.09999999999999971412 ) ;
#50440=CARTESIAN_POINT ( 'NONE',  ( -2.995603634470891112E-16, 87.75000000001156764, -57.27310748452423894 ) ) ;
#50479=DIRECTION ( 'NONE',  ( 0.000000000000000000, 0.000000000000000000, -1.000000000000000000 ) ) ;
#50559=DIRECTION ( 'NONE',  ( -1.000000000000000000, 0.000000000000000000, 0.000000000000000000 ) ) ;
#50562=DIRECTION ( 'NONE',  ( 0.000000000000000000, -1.000000000000000000, 0.000000000000000000 ) ) ;
#50584=EDGE_CURVE ( 'NONE', #191153, #147896, #199919, .T. ) ;
#50614=EDGE_CURVE ( 'NONE', #142859, #25020, #145712, .T. ) ;
#50618=ORIENTED_EDGE ( 'NONE', *, *, #164980, .F. ) ;
#50620=ORIENTED_EDGE ( 'NONE', *, *, #69375, .T. ) ;
#50640=ORIENTED_EDGE ( 'NONE', *, *, #41756, .T. ) ;
#50684=VECTOR ( 'NONE', #216822, 999.9999999999998863 ) ;
#50692=DIRECTION ( 'NONE',  ( 0.000000000000000000, -7.116814260417668513E-15, 1.000000000000000000 ) ) ;
#50701=AXIS2_PLACEMENT_3D ( 'NONE', #154594, #234086, #55424 ) ;
#50709=CARTESIAN_POINT ( 'NONE',  ( 21.05000000000000071, 71.18691588786198565, -47.96462524104817504 ) ) ;
#50747=AXIS2_PLACEMENT_3D ( 'NONE', #115360, #52811, #132361 ) ;
#50759=ORIENTED_EDGE ( 'NONE', *, *, #174852, .F. ) ;
#50765=ORIENTED_EDGE ( 'NONE', *, *, #123107, .F. ) ;
#50775=CIRCLE ( 'NONE', #38346, 0.1000000000000028644 ) ;
#50789=EDGE_CURVE ( 'NONE', #86432, #44321, #87460, .T. ) ;
#50812=DIRECTION ( 'NONE',  ( -1.000000000000000000, 3.265361837132813093E-16, 2.280189983783949500E-30 ) ) ;
#50887=EDGE_CURVE ( 'NONE', #10713, #228818, #21050, .T. ) ;
#50888=FACE_OUTER_BOUND ( 'NONE', #165974, .T. ) ;
#50922=ORIENTED_EDGE ( 'NONE', *, *, #5191, .F. ) ;
#50931=DIRECTION ( 'NONE',  ( -1.000000000000000000, 0.000000000000000000, 0.000000000000000000 ) ) ;
#50941=ORIENTED_EDGE ( 'NONE', *, *, #68505, .T. ) ;
#51027=LINE ( 'NONE', #10664, #69750 ) ;
#51109=AXIS2_PLACEMENT_3D ( 'NONE', #216420, #237282, #37818 ) ;
#51118=AXIS2_PLACEMENT_3D ( 'NONE', #238721, #79623, #163060 ) ;
#51138=AXIS2_PLACEMENT_3D ( 'NONE', #160086, #62247, #201748 ) ;
#51183=VERTEX_POINT ( 'NONE', #194075 ) ;
#51192=CARTESIAN_POINT ( 'NONE',  ( 20.94999999999999929, 76.00000000001145395, -38.92310748452432279 ) ) ;
#51211=DIRECTION ( 'NONE',  ( 1.000000000000000000, -2.952720810173289112E-16, -2.061873921506763405E-30 ) ) ;
#51219=ADVANCED_FACE ( 'NONE', ( #161358 ), #38842, .T. ) ;
#51226=EDGE_CURVE ( 'NONE', #106961, #159851, #200473, .T. ) ;
#51241=EDGE_LOOP ( 'NONE', ( #70715, #80161, #74035, #92426 ) ) ;
#51276=CIRCLE ( 'NONE', #205227, 0.2000000000000057288 ) ;
#51290=CARTESIAN_POINT ( 'NONE',  ( -22.45437739390953169, 76.00000000001173817, -81.17267829612076468 ) ) ;
#51299=EDGE_LOOP ( 'NONE', ( #197517, #191951, #221711, #205131 ) ) ;
#51320=ORIENTED_EDGE ( 'NONE', *, *, #169672, .T. ) ;
#51345=CARTESIAN_POINT ( 'NONE',  ( -20.64999999999999858, 85.00000000001149658, -45.91707660717669626 ) ) ;
#51350=AXIS2_PLACEMENT_3D ( 'NONE', #165826, #43293, #245347 ) ;
#51383=CARTESIAN_POINT ( 'NONE',  ( 20.97468175916167610, 65.37473483564055243, -57.26834604911160653 ) ) ;
#51399=EDGE_CURVE ( 'NONE', #138152, #90553, #196010, .T. ) ;
#51413=AXIS2_PLACEMENT_3D ( 'NONE', #52550, #205197, #86519 ) ;
#51419=DIRECTION ( 'NONE',  ( -0.000000000000000000, 0.9908441862701591329, 0.1350103645451946055 ) ) ;
#51453=TOROIDAL_SURFACE ( 'NONE', #234662, 0.2000000000000000111, 0.1000000000000000056 ) ;
#51458=VECTOR ( 'NONE', #35711, 1000.000000000000000 ) ;
#51474=CARTESIAN_POINT ( 'NONE',  ( 18.59999999999999787, 77.73670573947892137, -24.50568489690058627 ) ) ;
#51480=DIRECTION ( 'NONE',  ( 0.000000000000000000, 0.000000000000000000, 1.000000000000000000 ) ) ;
#51493=CARTESIAN_POINT ( 'NONE',  ( -18.50000000000000000, 65.70729864260955821, -30.56574559737245167 ) ) ;
#51541=ORIENTED_EDGE ( 'NONE', *, *, #48747, .F. ) ;
#51545=DIRECTION ( 'NONE',  ( 0.000000000000000000, 0.000000000000000000, 1.000000000000000000 ) ) ;
#51559=CARTESIAN_POINT ( 'NONE',  ( 20.95512820512820440, 65.37615131629972609, -61.85819391543678591 ) ) ;
#51586=CARTESIAN_POINT ( 'NONE',  ( -21.05000000000000071, 76.00000000001165290, -69.52310748452431710 ) ) ;
#51587=FACE_OUTER_BOUND ( 'NONE', #699, .T. ) ;
#51591=AXIS2_PLACEMENT_3D ( 'NONE', #97439, #177039, #196565 ) ;
#51613=VERTEX_POINT ( 'NONE', #159759 ) ;
#51622=( BOUNDED_SURFACE ( )  B_SPLINE_SURFACE ( 3, 2, ( 
 ( #980, #23177, #102656 ),
 ( #182237, #3576, #83080 ),
 ( #162671, #242189, #143080 ),
 ( #150800, #47825, #247323 ),
 ( #191242, #30890, #189931 ),
 ( #246058, #12600, #29602 ) ),
 .UNSPECIFIED., .F., .F., .F. ) 
 B_SPLINE_SURFACE_WITH_KNOTS ( ( 4, 2, 4 ),
 ( 3, 3 ),
 ( 3.141592653589783346, 3.926990816987233845, 4.712388980384684345 ),
 ( 0.000000000000000000, 1.000000000000000000 ),
 .UNSPECIFIED. ) 
 GEOMETRIC_REPRESENTATION_ITEM ( )  RATIONAL_B_SPLINE_SURFACE ( (
 ( 1.000000000000000000, 0.9238795325112774126, 1.000000000000000000),
 ( 1.000000000000000000, 0.9240297172242109003, 1.000000000000000000),
 ( 1.000000000000000000, 0.9038128468041503050, 1.000000000000000000),
 ( 1.000000000000000000, 0.8282379607647244457, 1.000000000000000000),
 ( 1.000000000000000000, 0.7727932973492797064, 1.000000000000000000),
 ( 1.000000000000000000, 0.7071067811865843211, 1.000000000000000000) ) ) 
 REPRESENTATION_ITEM ( '' )  SURFACE ( )  );
#51623=ORIENTED_EDGE ( 'NONE', *, *, #169377, .F. ) ;
#51630=DIRECTION ( 'NONE',  ( 0.000000000000000000, 0.000000000000000000, 1.000000000000000000 ) ) ;
#51634=DIRECTION ( 'NONE',  ( 0.000000000000000000, -0.2605042016806740079, 0.9654727137038698892 ) ) ;
#51648=( BOUNDED_SURFACE ( )  B_SPLINE_SURFACE ( 3, 2, ( 
 ( #205413, #86743, #106304 ),
 ( #166341, #245844, #240285 ),
 ( #83723, #119049, #59025 ),
 ( #64206, #103308, #5482 ),
 ( #180301, #182889, #44646 ),
 ( #39539, #163313, #201141 ) ),
 .UNSPECIFIED., .F., .F., .F. ) 
 B_SPLINE_SURFACE_WITH_KNOTS ( ( 4, 2, 4 ),
 ( 3, 3 ),
 ( 0.0001381104793128073169, 0.0002947094729387728746, 0.0004513084665647384324 ),
 ( 0.000000000000000000, 1.000000000000000000 ),
 .UNSPECIFIED. ) 
 GEOMETRIC_REPRESENTATION_ITEM ( )  RATIONAL_B_SPLINE_SURFACE ( (
 ( 1.000000000000000000, 0.7071067811865229258, 1.000000000000000000),
 ( 1.000000000000000000, 0.6919563088098916737, 1.000000000000000000),
 ( 1.000000000000000000, 0.6959445945717528392, 1.000000000000000000),
 ( 1.000000000000000000, 0.7137882985313381834, 1.000000000000000000),
 ( 1.000000000000000000, 0.7257496306096212768, 1.000000000000000000),
 ( 1.000000000000000000, 0.7250110520819876836, 1.000000000000000000) ) ) 
 REPRESENTATION_ITEM ( '' )  SURFACE ( )  );
#51649=DIRECTION ( 'NONE',  ( 1.000000000000000000, 0.000000000000000000, 0.000000000000000000 ) ) ;
#51653=ADVANCED_FACE ( 'NONE', ( #119350 ), #167174, .T. ) ;
#51669=CIRCLE ( 'NONE', #93203, 0.1000000000000028644 ) ;
#51696=EDGE_CURVE ( 'NONE', #42405, #95482, #233068, .T. ) ;
#51698=ORIENTED_EDGE ( 'NONE', *, *, #178132, .F. ) ;
#51713=SPHERICAL_SURFACE ( 'NONE', #90275, 0.1000000000000000056 ) ;
#51733=EDGE_CURVE ( 'NONE', #1074, #177806, #50393, .T. ) ;
#51738=DIRECTION ( 'NONE',  ( 1.000000000000000000, 7.304098846218135653E-16, 5.100424963727256530E-30 ) ) ;
#51739=ADVANCED_FACE ( 'NONE', ( #188300 ), #46216, .F. ) ;
#51763=B_SPLINE_CURVE_WITH_KNOTS ( 'NONE', 3,
 ( #38933, #118474, #98853, #119762, #41507, #199287 ),
 .UNSPECIFIED., .F., .F.,
 ( 4, 2, 4 ),
 ( 0.000000000000000000, 0.0001895189928937356105, 0.0003790379857874712211 ),
 .UNSPECIFIED. ) ;
#51773=ORIENTED_EDGE ( 'NONE', *, *, #140895, .F. ) ;
#51774=ORIENTED_EDGE ( 'NONE', *, *, #110074, .T. ) ;
#51779=CARTESIAN_POINT ( 'NONE',  ( -18.59999999999999787, 64.25000000001158185, -57.37310748452440379 ) ) ;
#51784=ORIENTED_EDGE ( 'NONE', *, *, #234632, .F. ) ;
#51830=ORIENTED_EDGE ( 'NONE', *, *, #15029, .F. ) ;
#51844=FACE_OUTER_BOUND ( 'NONE', #35646, .T. ) ;
#51855=CARTESIAN_POINT ( 'NONE',  ( 22.57856590037849287, 76.00412833007608526, -81.27316594719980003 ) ) ;
#51898=CIRCLE ( 'NONE', #1832, 0.1999999999999987899 ) ;
#51921=AXIS2_PLACEMENT_3D ( 'NONE', #158697, #176976, #2140 ) ;
#51923=AXIS2_PLACEMENT_3D ( 'NONE', #50329, #114176, #32099 ) ;
#51941=DIRECTION ( 'NONE',  ( -1.000000000000000000, 2.952720810173289112E-16, 2.061873921506763405E-30 ) ) ;
#51942=EDGE_CURVE ( 'NONE', #136430, #68363, #108859, .T. ) ;
#51968=EDGE_CURVE ( 'NONE', #68040, #196986, #215567, .T. ) ;
#51971=CARTESIAN_POINT ( 'NONE',  ( 22.46250603428203618, 75.97885582387293368, -81.17297058186441916 ) ) ;
#51973=CARTESIAN_POINT ( 'NONE',  ( -18.59999999999999787, 77.13501884592155022, -28.30613060109199353 ) ) ;
#51985=CARTESIAN_POINT ( 'NONE',  ( 20.94999999999999929, 76.00000000001142553, -36.02310748452432421 ) ) ;
#52011=DIRECTION ( 'NONE',  ( 0.000000000000000000, 0.000000000000000000, -1.000000000000000000 ) ) ;
#52032=EDGE_CURVE ( 'NONE', #215740, #126512, #222288, .T. ) ;
#52089=DIRECTION ( 'NONE',  ( 0.000000000000000000, 6.608470384673547079E-15, -1.000000000000000000 ) ) ;
#52102=B_SPLINE_CURVE_WITH_KNOTS ( 'NONE', 3,
 ( #90370, #68257, #49965, #169967 ),
 .UNSPECIFIED., .F., .F.,
 ( 4, 4 ),
 ( 3.469446951953614189E-18, 0.0001058379652594568606 ),
 .UNSPECIFIED. ) ;
#52113=CARTESIAN_POINT ( 'NONE',  ( 20.94999999999999929, 77.83534155023599510, -57.96795619196132776 ) ) ;
#52116=VERTEX_POINT ( 'NONE', #246683 ) ;
#52121=ORIENTED_EDGE ( 'NONE', *, *, #15182, .T. ) ;
#52125=LINE ( 'NONE', #35190, #183086 ) ;
#52148=CARTESIAN_POINT ( 'NONE',  ( 21.07094088545303734, 69.67983277809517517, -69.62200118707659158 ) ) ;
#52153=FACE_OUTER_BOUND ( 'NONE', #73551, .T. ) ;
#52171=EDGE_LOOP ( 'NONE', ( #40414, #139676, #217580, #12955 ) ) ;
#52203=EDGE_CURVE ( 'NONE', #87393, #211799, #105871, .T. ) ;
#52212=EDGE_CURVE ( 'NONE', #36755, #77589, #87598, .T. ) ;
#52217=CARTESIAN_POINT ( 'NONE',  ( -23.15000000000000213, 85.00000000001149658, -45.91707660717669626 ) ) ;
#52237=CARTESIAN_POINT ( 'NONE',  ( -20.64999999999999858, 68.75000000001151079, -48.37310748452436826 ) ) ;
#52238=EDGE_CURVE ( 'NONE', #47971, #182741, #113149, .T. ) ;
#52239=ORIENTED_EDGE ( 'NONE', *, *, #63762, .F. ) ;
#52251=CARTESIAN_POINT ( 'NONE',  ( -20.94999999999999929, 77.16412189325258453, -28.10825939895270764 ) ) ;
#52263=CARTESIAN_POINT ( 'NONE',  ( -20.94999999999999929, 68.87972903831379767, -32.36354444268504693 ) ) ;
#52324=DIRECTION ( 'NONE',  ( 1.000000000000000000, 0.000000000000000000, 0.000000000000000000 ) ) ;
#52331=DIRECTION ( 'NONE',  ( -0.7071067811865474617, 0.7071067811865474617, 4.937700262164531476E-15 ) ) ;
#52345=EDGE_CURVE ( 'NONE', #162036, #32328, #120827, .T. ) ;
#52348=EDGE_CURVE ( 'NONE', #30729, #85564, #42410, .T. ) ;
#52356=VERTEX_POINT ( 'NONE', #182242 ) ;
#52370=EDGE_LOOP ( 'NONE', ( #135710, #51698, #48899, #126215 ) ) ;
#52375=ORIENTED_EDGE ( 'NONE', *, *, #123107, .T. ) ;
#52385=CARTESIAN_POINT ( 'NONE',  ( 21.05000000000000071, 76.00000000001165290, -69.52310748452431710 ) ) ;
#52402=AXIS2_PLACEMENT_3D ( 'NONE', #248690, #247388, #128750 ) ;
#52426=CYLINDRICAL_SURFACE ( 'NONE', #7944, 0.09999999999999939493 ) ;
#52438=ORIENTED_EDGE ( 'NONE', *, *, #243724, .F. ) ;
#52451=EDGE_LOOP ( 'NONE', ( #18392, #30817, #209918, #161057 ) ) ;
#52465=DIRECTION ( 'NONE',  ( 0.000000000000000000, 0.000000000000000000, -1.000000000000000000 ) ) ;
#52478=ORIENTED_EDGE ( 'NONE', *, *, #79236, .T. ) ;
#52485=DIRECTION ( 'NONE',  ( -1.000000000000000000, -0.000000000000000000, -0.000000000000000000 ) ) ;
#52527=DIRECTION ( 'NONE',  ( 0.7071067811865474617, -0.7071067811865474617, -4.937700262164531476E-15 ) ) ;
#52529=AXIS2_PLACEMENT_3D ( 'NONE', #141545, #42448, #22918 ) ;
#52550=CARTESIAN_POINT ( 'NONE',  ( 20.94999999999999929, 85.00000000001149658, -45.91707660717670336 ) ) ;
#52584=DIRECTION ( 'NONE',  ( -1.000000000000000000, 0.000000000000000000, -0.000000000000000000 ) ) ;
#52585=ADVANCED_FACE ( 'NONE', ( #68708 ), #204903, .F. ) ;
#52612=AXIS2_PLACEMENT_3D ( 'NONE', #41288, #3389, #82910 ) ;
#52620=DIRECTION ( 'NONE',  ( 0.000000000000000000, 0.000000000000000000, -1.000000000000000000 ) ) ;
#52622=DIRECTION ( 'NONE',  ( 1.000000000000000000, 0.000000000000000000, 0.000000000000000000 ) ) ;
#52627=VERTEX_POINT ( 'NONE', #99651 ) ;
#52642=CARTESIAN_POINT ( 'NONE',  ( -20.94999999999999929, 68.97833521811131163, -32.18954208262707795 ) ) ;
#52659=CARTESIAN_POINT ( 'NONE',  ( 18.59999999999997655, 76.00000000001142553, -36.02310748452432421 ) ) ;
#52664=DIRECTION ( 'NONE',  ( 0.000000000000000000, -1.000000000000000000, -6.938893903907030216E-14 ) ) ;
#52682=EDGE_CURVE ( 'NONE', #79119, #253401, #221644, .T. ) ;
#52706=AXIS2_PLACEMENT_3D ( 'NONE', #63065, #22696, #240434 ) ;
#52707=VECTOR ( 'NONE', #181842, 1000.000000000000000 ) ;
#52737=CARTESIAN_POINT ( 'NONE',  ( 21.13435531349811569, 76.00000000001169553, -76.01682854811622292 ) ) ;
#52800=ORIENTED_EDGE ( 'NONE', *, *, #173531, .F. ) ;
#52811=DIRECTION ( 'NONE',  ( -0.7071067811865475727, 0.7071067811865475727, 4.937700262164531476E-15 ) ) ;
#52868=ORIENTED_EDGE ( 'NONE', *, *, #230674, .T. ) ;
#52888=EDGE_CURVE ( 'NONE', #204082, #33572, #205069, .T. ) ;
#52896=CYLINDRICAL_SURFACE ( 'NONE', #132697, 0.09999999999999939493 ) ;
#52967=AXIS2_PLACEMENT_3D ( 'NONE', #113911, #134737, #19966 ) ;
#52969=CARTESIAN_POINT ( 'NONE',  ( 18.50000000000000000, 85.40000000001160174, -62.52382180668540457 ) ) ;
#52990=CARTESIAN_POINT ( 'NONE',  ( 18.49999999999999289, 65.67426406872341715, -44.67310748452440095 ) ) ;
#53002=VERTEX_POINT ( 'NONE', #208016 ) ;
#53004=PLANE ( 'NONE',  #191027 ) ;
#53080=VERTEX_POINT ( 'NONE', #133588 ) ;
#53111=CARTESIAN_POINT ( 'NONE',  ( 21.05000000000000071, 85.00000000001149658, -45.91707660717670336 ) ) ;
#53139=ORIENTED_EDGE ( 'NONE', *, *, #150428, .F. ) ;
#53162=LINE ( 'NONE', #550, #91570 ) ;
#53197=( BOUNDED_CURVE ( )  B_SPLINE_CURVE ( 3, ( #60185, #122762, #84853, #223111 ),
 .UNSPECIFIED., .F., .F. ) 
 B_SPLINE_CURVE_WITH_KNOTS ( ( 4, 4 ),
 ( 0.06456096931748350753, 3.077031684272309775 ),
 .UNSPECIFIED. ) 
 CURVE ( )  GEOMETRIC_REPRESENTATION_ITEM ( )  RATIONAL_B_SPLINE_CURVE ( ( 1.000000000000000000, 0.3763440860215095940, 0.3763440860215095940, 1.000000000000000000 ) ) 
 REPRESENTATION_ITEM ( '' )  );
#53230=CIRCLE ( 'NONE', #140712, 0.1000000000000028644 ) ;
#53258=EDGE_CURVE ( 'NONE', #114996, #189246, #14575, .T. ) ;
#53286=DIRECTION ( 'NONE',  ( 1.000000000000000000, -0.000000000000000000, 0.000000000000000000 ) ) ;
#53313=LINE ( 'NONE', #94997, #129123 ) ;
#53317=CARTESIAN_POINT ( 'NONE',  ( 20.85000000000000142, 87.65000000001144542, -38.92310748452424463 ) ) ;
#53364=ORIENTED_EDGE ( 'NONE', *, *, #93326, .F. ) ;
#53424=LINE ( 'NONE', #91278, #168998 ) ;
#53437=ORIENTED_EDGE ( 'NONE', *, *, #200586, .T. ) ;
#53444=DIRECTION ( 'NONE',  ( 0.000000000000000000, -0.8700118002898357128, 0.4930308989875170633 ) ) ;
#53451=ORIENTED_EDGE ( 'NONE', *, *, #96735, .F. ) ;
#53470=CARTESIAN_POINT ( 'NONE',  ( 18.59999999999999787, 77.25000000001136868, -28.22262673010923706 ) ) ;
#53472=DIRECTION ( 'NONE',  ( 0.7071359030027419834, 0.000000000000000000, -0.7070776581709371511 ) ) ;
#53484=ORIENTED_EDGE ( 'NONE', *, *, #97584, .T. ) ;
#53512=CARTESIAN_POINT ( 'NONE',  ( -23.25000000000000000, 77.73670573947892137, -24.50568489690058627 ) ) ;
#53514=ORIENTED_EDGE ( 'NONE', *, *, #64214, .F. ) ;
#53525=DIRECTION ( 'NONE',  ( 1.000000000000000000, -1.875376730785737719E-16, -1.309568571767809260E-30 ) ) ;
#53531=DIRECTION ( 'NONE',  ( 0.000000000000000000, 7.147358527629762208E-15, -1.000000000000000000 ) ) ;
#53555=CIRCLE ( 'NONE', #7769, 0.1000000000000043771 ) ;
#53556=CARTESIAN_POINT ( 'NONE',  ( 21.07928932188134397, 69.67148334361836248, -69.62200263017875557 ) ) ;
#53597=CARTESIAN_POINT ( 'NONE',  ( -23.25000000000000000, 76.00000000001156764, -56.74810748452433273 ) ) ;
#53668=CARTESIAN_POINT ( 'NONE',  ( -18.59999999999999787, 74.25000000001156764, -57.85359592662268824 ) ) ;
#53674=CIRCLE ( 'NONE', #182877, 0.09999999999999939493 ) ;
#53781=VECTOR ( 'NONE', #104821, 999.9999999999998863 ) ;
#53825=ADVANCED_FACE ( 'NONE', ( #248776 ), #208377, .F. ) ;
#53844=DIRECTION ( 'NONE',  ( 1.000000000000000000, 0.000000000000000000, 0.000000000000000000 ) ) ;
#53850=ADVANCED_FACE ( 'NONE', ( #191392 ), #92243, .T. ) ;
#53855=DIRECTION ( 'NONE',  ( -1.000000000000000000, 2.952720810173289112E-16, 2.061873921506763405E-30 ) ) ;
#53888=ORIENTED_EDGE ( 'NONE', *, *, #242921, .F. ) ;
#53894=CARTESIAN_POINT ( 'NONE',  ( -22.50875500270927532, 76.10085791378634212, -81.27267461192221276 ) ) ;
#53931=CARTESIAN_POINT ( 'NONE',  ( 21.10642757222115407, 65.27684371085297244, -57.28240996073919433 ) ) ;
#53947=DIRECTION ( 'NONE',  ( 0.000000000000000000, 0.000000000000000000, 1.000000000000000000 ) ) ;
#53955=AXIS2_PLACEMENT_3D ( 'NONE', #198754, #197468, #114078 ) ;
#53959=ORIENTED_EDGE ( 'NONE', *, *, #223491, .F. ) ;
#53980=ORIENTED_EDGE ( 'NONE', *, *, #70326, .F. ) ;
#54019=EDGE_CURVE ( 'NONE', #153767, #118994, #88338, .T. ) ;
#54035=CIRCLE ( 'NONE', #116419, 11.74999999999999645 ) ;
#54048=ADVANCED_FACE ( 'NONE', ( #24294 ), #166386, .F. ) ;
#54075=CARTESIAN_POINT ( 'NONE',  ( -18.59999999999999787, 85.50000000001161027, -61.42310748452425884 ) ) ;
#54088=AXIS2_PLACEMENT_3D ( 'NONE', #46870, #87280, #248956 ) ;
#54099=CARTESIAN_POINT ( 'NONE',  ( 20.94999999999999929, 76.00000000001142553, -36.02310748452432421 ) ) ;
#54105=CARTESIAN_POINT ( 'NONE',  ( -20.54999999999999716, 87.75000000001153921, -52.77310748452423894 ) ) ;
#54113=DIRECTION ( 'NONE',  ( 0.000000000000000000, 0.000000000000000000, -1.000000000000000000 ) ) ;
#54139=CARTESIAN_POINT ( 'NONE',  ( -21.05000000000000071, 74.83729825007360148, -61.42310748452432989 ) ) ;
#54153=EDGE_CURVE ( 'NONE', #124577, #177733, #124664, .T. ) ;
#54173=ORIENTED_EDGE ( 'NONE', *, *, #81753, .T. ) ;
#54184=AXIS2_PLACEMENT_3D ( 'NONE', #167210, #246702, #28994 ) ;
#54223=DIRECTION ( 'NONE',  ( 7.589415207398576792E-15, 1.000000000000000000, 6.982962677686266711E-15 ) ) ;
#54227=CARTESIAN_POINT ( 'NONE',  ( -21.51976009735018991, 69.08954155835245103, -69.52310748452435973 ) ) ;
#54244=EDGE_CURVE ( 'NONE', #88538, #121084, #146794, .T. ) ;
#54245=CARTESIAN_POINT ( 'NONE',  ( -18.59999999999999787, 64.35000000001150511, -48.17310748452440095 ) ) ;
#54281=DIRECTION ( 'NONE',  ( 1.000000000000000000, 0.000000000000000000, 0.000000000000000000 ) ) ;
#54284=DIRECTION ( 'NONE',  ( 0.000000000000000000, -6.352154140967427193E-15, 1.000000000000000000 ) ) ;
#54302=ORIENTED_EDGE ( 'NONE', *, *, #190407, .T. ) ;
#54336=CARTESIAN_POINT ( 'NONE',  ( -21.05000000000000071, 76.10000000001174669, -81.17267829206912211 ) ) ;
#54346=CIRCLE ( 'NONE', #108529, 0.1000000000000028644 ) ;
#54369=ORIENTED_EDGE ( 'NONE', *, *, #235817, .T. ) ;
#54378=ORIENTED_EDGE ( 'NONE', *, *, #230674, .F. ) ;
#54391=AXIS2_PLACEMENT_3D ( 'NONE', #42864, #143231, #222764 ) ;
#54399=ORIENTED_EDGE ( 'NONE', *, *, #132931, .F. ) ;
#54438=ORIENTED_EDGE ( 'NONE', *, *, #64106, .T. ) ;
#54452=ORIENTED_EDGE ( 'NONE', *, *, #46919, .F. ) ;
#54482=CARTESIAN_POINT ( 'NONE',  ( 23.14999999999999858, 70.10000000001149090, -46.24220724918073699 ) ) ;
#54514=DIRECTION ( 'NONE',  ( -0.000000000000000000, 1.000000000000000000, 6.982962677686266711E-15 ) ) ;
#54525=VECTOR ( 'NONE', #191123, 1000.000000000000000 ) ;
#54558=AXIS2_PLACEMENT_3D ( 'NONE', #152159, #49174, #208268 ) ;
#54585=CARTESIAN_POINT ( 'NONE',  ( -18.44232395689941129, 85.55228255706126106, -29.18085549971751291 ) ) ;
#54591=DIRECTION ( 'NONE',  ( 1.224646799147353207E-16, -1.000000000000000000, -6.982962677686266711E-15 ) ) ;
#54593=CARTESIAN_POINT ( 'NONE',  ( -22.49533356619859603, 64.34999999370755575, -69.58823006484709595 ) ) ;
#54614=LINE ( 'NONE', #230709, #117112 ) ;
#54619=EDGE_LOOP ( 'NONE', ( #143222, #53959, #187745, #63399 ) ) ;
#54670=DIRECTION ( 'NONE',  ( 1.000000000000000000, 0.000000000000000000, 0.000000000000000000 ) ) ;
#54686=CYLINDRICAL_SURFACE ( 'NONE', #49710, 0.1000000000000028644 ) ;
#54730=ORIENTED_EDGE ( 'NONE', *, *, #72374, .T. ) ;
#54743=DIRECTION ( 'NONE',  ( 0.000000000000000000, 6.982962677686266711E-15, -1.000000000000000000 ) ) ;
#54749=CARTESIAN_POINT ( 'NONE',  ( -23.25000000000000000, 76.00000000001165290, -69.52310748452431710 ) ) ;
#54770=CYLINDRICAL_SURFACE ( 'NONE', #211024, 0.1000000000000028644 ) ;
#54794=AXIS2_PLACEMENT_3D ( 'NONE', #201119, #137284, #79860 ) ;
#54808=LINE ( 'NONE', #195644, #142260 ) ;
#54835=DIRECTION ( 'NONE',  ( 1.000000000000000000, 0.000000000000000000, 0.000000000000000000 ) ) ;
#54837=CARTESIAN_POINT ( 'NONE',  ( -20.85000000000000142, 64.25000000001148237, -42.80697314750250371 ) ) ;
#54849=CIRCLE ( 'NONE', #200610, 0.09999999999999939493 ) ;
#54857=AXIS2_PLACEMENT_3D ( 'NONE', #62260, #230309, #188616 ) ;
#54916=DIRECTION ( 'NONE',  ( 0.000000000000000000, -6.982962677686267499E-15, 1.000000000000000000 ) ) ;
#54923=CARTESIAN_POINT ( 'NONE',  ( -23.25000000000000000, 85.00000000001149658, -45.31707660717669484 ) ) ;
#54930=ORIENTED_EDGE ( 'NONE', *, *, #157543, .F. ) ;
#54940=ORIENTED_EDGE ( 'NONE', *, *, #15429, .F. ) ;
#54947=FACE_OUTER_BOUND ( 'NONE', #190374, .T. ) ;
#54950=ORIENTED_EDGE ( 'NONE', *, *, #118830, .F. ) ;
#54963=DIRECTION ( 'NONE',  ( 1.000000000000000000, 0.000000000000000000, 0.000000000000000000 ) ) ;
#54982=CARTESIAN_POINT ( 'NONE',  ( 18.59999999999999432, 74.83729825007360148, -61.42310748452432989 ) ) ;
#54993=FACE_OUTER_BOUND ( 'NONE', #46070, .T. ) ;
#55036=FACE_OUTER_BOUND ( 'NONE', #182535, .T. ) ;
#55049=EDGE_CURVE ( 'NONE', #192458, #170828, #193176, .T. ) ;
#55149=CIRCLE ( 'NONE', #234225, 0.1000000000000028644 ) ;
#55166=CARTESIAN_POINT ( 'NONE',  ( 20.94999999999999574, 76.00000000001165290, -69.52310748452431710 ) ) ;
#55183=DIRECTION ( 'NONE',  ( 0.000000000000000000, 0.1455152366551500653, 0.9893560106964507384 ) ) ;
#55193=DIRECTION ( 'NONE',  ( -1.000000000000000000, 0.000000000000000000, -0.000000000000000000 ) ) ;
#55208=DIRECTION ( 'NONE',  ( 0.000000000000000000, -6.982962677686266711E-15, 1.000000000000000000 ) ) ;
#55244=CARTESIAN_POINT ( 'NONE',  ( 21.14999999999999858, 76.10000000001174669, -81.17267829206912211 ) ) ;
#55266=EDGE_CURVE ( 'NONE', #245547, #95482, #234860, .T. ) ;
#55282=CIRCLE ( 'NONE', #201072, 0.1000000000000028644 ) ;
#55365=CARTESIAN_POINT ( 'NONE',  ( -20.64999999999999858, 71.65000000001151648, -48.37310748452434694 ) ) ;
#55366=DIRECTION ( 'NONE',  ( 0.000000000000000000, 0.000000000000000000, 1.000000000000000000 ) ) ;
#55406=CARTESIAN_POINT ( 'NONE',  ( 18.59999999999999432, 74.83729825007360148, -61.52310748452433131 ) ) ;
#55421=DIRECTION ( 'NONE',  ( -1.000000000000000000, 0.000000000000000000, -0.000000000000000000 ) ) ;
#55424=DIRECTION ( 'NONE',  ( 0.000000000000000000, 0.8700118002898356018, -0.4930308989875170078 ) ) ;
#55446=DIRECTION ( 'NONE',  ( 1.000000000000000000, 0.000000000000000000, 0.000000000000000000 ) ) ;
#55448=VECTOR ( 'NONE', #8025, 1000.000000000000000 ) ;
#55457=VERTEX_POINT ( 'NONE', #57974 ) ;
#55458=CARTESIAN_POINT ( 'NONE',  ( -20.94999999999999929, 77.13501884592155022, -28.30613060109199353 ) ) ;
#55521=ORIENTED_EDGE ( 'NONE', *, *, #123060, .T. ) ;
#55525=CARTESIAN_POINT ( 'NONE',  ( -21.05315837417582614, 64.25000000264169842, -42.86475148229496313 ) ) ;
#55533=CARTESIAN_POINT ( 'NONE',  ( 21.14999999999999858, 69.45934304831041572, -69.52310748452435973 ) ) ;
#55540=LINE ( 'NONE', #140228, #198503 ) ;
#55543=CARTESIAN_POINT ( 'NONE',  ( 23.15000000000000213, 85.00000000001149658, -45.91707660717670336 ) ) ;
#55596=VERTEX_POINT ( 'NONE', #65697 ) ;
#55610=AXIS2_PLACEMENT_3D ( 'NONE', #8055, #228385, #10619 ) ;
#55619=EDGE_LOOP ( 'NONE', ( #64279, #72221, #183296, #64535 ) ) ;
#55644=DIRECTION ( 'NONE',  ( 0.000000000000000000, 0.000000000000000000, 1.000000000000000000 ) ) ;
#55663=EDGE_LOOP ( 'NONE', ( #167233, #113966, #137149, #66744 ) ) ;
#55676=AXIS2_PLACEMENT_3D ( 'NONE', #157931, #140893, #237422 ) ;
#55716=CARTESIAN_POINT ( 'NONE',  ( 21.14999999999999503, 64.35000000001164722, -69.42310748452440805 ) ) ;
#55753=CARTESIAN_POINT ( 'NONE',  ( 21.05000000000000071, 85.50000000001149658, -45.91707660717669626 ) ) ;
#55812=ORIENTED_EDGE ( 'NONE', *, *, #142407, .T. ) ;
#55825=DIRECTION ( 'NONE',  ( 0.000000000000000000, 6.982962677686266711E-15, -1.000000000000000000 ) ) ;
#55834=CARTESIAN_POINT ( 'NONE',  ( -18.59999999999999787, 85.52395432076417592, -29.14109042769694469 ) ) ;
#55857=ORIENTED_EDGE ( 'NONE', *, *, #76512, .F. ) ;
#55893=EDGE_CURVE ( 'NONE', #22349, #23444, #251786, .T. ) ;
#55898=AXIS2_PLACEMENT_3D ( 'NONE', #71916, #174913, #254364 ) ;
#55941=EDGE_CURVE ( 'NONE', #174912, #68363, #35349, .T. ) ;
#55950=CARTESIAN_POINT ( 'NONE',  ( -20.64999999999999858, 71.65000000001155911, -57.17310748452435121 ) ) ;
#55952=ORIENTED_EDGE ( 'NONE', *, *, #192029, .T. ) ;
#55987=ORIENTED_EDGE ( 'NONE', *, *, #193493, .F. ) ;
#55991=CARTESIAN_POINT ( 'NONE',  ( -21.04999999999999716, 69.65527659592140708, -69.53782534104793456 ) ) ;
#56025=CIRCLE ( 'NONE', #214281, 0.1999999999999987899 ) ;
#56034=DIRECTION ( 'NONE',  ( 0.000000000000000000, -1.000000000000000000, 0.000000000000000000 ) ) ;
#56035=CIRCLE ( 'NONE', #185246, 4.000000000000003553 ) ;
#56039=CARTESIAN_POINT ( 'NONE',  ( -18.59999999999999787, 66.85000000001173248, -81.27310748452438816 ) ) ;
#56052=AXIS2_PLACEMENT_3D ( 'NONE', #21532, #118046, #215841 ) ;
#56059=DIRECTION ( 'NONE',  ( 1.000000000000000000, 0.000000000000000000, 0.000000000000000000 ) ) ;
#56083=CARTESIAN_POINT ( 'NONE',  ( -23.25000000000000000, 77.83585931145498193, -24.51866831572578675 ) ) ;
#56216=EDGE_LOOP ( 'NONE', ( #209271, #248660, #239222, #206755 ) ) ;
#56228=EDGE_LOOP ( 'NONE', ( #238879, #66438, #154902, #53484, #108836, #151509, #77766, #154542, #2515, #129532, #170216, #99964, #173056, #90914, #107770, #134899, #96280, #73255, #217305, #90995, #24914, #123941, #73302 ) ) ;
#56244=AXIS2_PLACEMENT_3D ( 'NONE', #152140, #89557, #112992 ) ;
#56250=CIRCLE ( 'NONE', #231081, 4.299999999999956302 ) ;
#56257=LINE ( 'NONE', #217891, #173334 ) ;
#56261=VERTEX_POINT ( 'NONE', #149641 ) ;
#56285=CIRCLE ( 'NONE', #214683, 0.5000000000000004441 ) ;
#56355=DIRECTION ( 'NONE',  ( 0.000000000000000000, -6.352154140967427193E-15, 1.000000000000000000 ) ) ;
#56390=AXIS2_PLACEMENT_3D ( 'NONE', #24851, #185175, #106910 ) ;
#56414=LINE ( 'NONE', #173870, #26785 ) ;
#56417=ADVANCED_FACE ( 'NONE', ( #14888 ), #189654, .F. ) ;
#56440=CYLINDRICAL_SURFACE ( 'NONE', #184128, 0.1000000000000038219 ) ;
#56451=ORIENTED_EDGE ( 'NONE', *, *, #163634, .T. ) ;
#56457=DIRECTION ( 'NONE',  ( 0.000000000000000000, 0.000000000000000000, 1.000000000000000000 ) ) ;
#56462=AXIS2_PLACEMENT_3D ( 'NONE', #32810, #133158, #13221 ) ;
#56478=AXIS2_PLACEMENT_3D ( 'NONE', #164397, #142251, #182687 ) ;
#56494=CARTESIAN_POINT ( 'NONE',  ( 20.94999999999999929, 76.00000000001142553, -36.02310748452432421 ) ) ;
#56495=CARTESIAN_POINT ( 'NONE',  ( -18.49999999999997158, 85.32100840337291459, -62.28716923544639172 ) ) ;
#56563=CARTESIAN_POINT ( 'NONE',  ( 21.07954640115298162, 75.93399229287204832, -75.85239518054815733 ) ) ;
#56627=VERTEX_POINT ( 'NONE', #24848 ) ;
#56651=CARTESIAN_POINT ( 'NONE',  ( 22.49999999999999645, 64.35012909624747124, -69.60562737539740397 ) ) ;
#56653=EDGE_LOOP ( 'NONE', ( #81500, #142920, #22603, #158494 ) ) ;
#56667=CIRCLE ( 'NONE', #19106, 7.900000000000003908 ) ;
#56669=AXIS2_PLACEMENT_3D ( 'NONE', #93837, #95127, #212531 ) ;
#56709=EDGE_LOOP ( 'NONE', ( #78093, #254427, #242639, #93009 ) ) ;
#56728=CARTESIAN_POINT ( 'NONE',  ( -22.39999999999999858, 75.90000000001170122, -77.31388708289772183 ) ) ;
#56737=DIRECTION ( 'NONE',  ( 0.000000000000000000, -7.086529944415894657E-15, 1.000000000000000000 ) ) ;
#56751=CIRCLE ( 'NONE', #152511, 0.09999999999999799327 ) ;
#56758=FACE_OUTER_BOUND ( 'NONE', #13116, .T. ) ;
#56760=DIRECTION ( 'NONE',  ( 2.952720810173289112E-16, 1.000000000000000000, 9.912705577010238578E-15 ) ) ;
#56779=CIRCLE ( 'NONE', #40098, 0.1999999999999987899 ) ;
#56805=AXIS2_PLACEMENT_3D ( 'NONE', #164207, #106773, #24715 ) ;
#56808=TOROIDAL_SURFACE ( 'NONE', #227528, 12.97499999999999787, 0.1000000000000000056 ) ;
#56821=CARTESIAN_POINT ( 'NONE',  ( 21.05000000000000071, 69.45934304831041572, -69.42310748452436542 ) ) ;
#56837=DIRECTION ( 'NONE',  ( 0.7071067811865475727, -0.7071067811865475727, -4.937700262164531476E-15 ) ) ;
#56887=ORIENTED_EDGE ( 'NONE', *, *, #81238, .F. ) ;
#56904=ORIENTED_EDGE ( 'NONE', *, *, #108069, .F. ) ;
#56908=VERTEX_POINT ( 'NONE', #59749 ) ;
#56950=DIRECTION ( 'NONE',  ( 1.000000000000000000, 0.000000000000000000, 0.000000000000000000 ) ) ;
#56959=EDGE_LOOP ( 'NONE', ( #42411, #63999, #122757, #43107 ) ) ;
#56960=ORIENTED_EDGE ( 'NONE', *, *, #213269, .T. ) ;
#56972=VERTEX_POINT ( 'NONE', #182312 ) ;
#56990=EDGE_CURVE ( 'NONE', #182741, #12734, #242256, .T. ) ;
#56996=VECTOR ( 'NONE', #3269, 1000.000000000000000 ) ;
#57007=CARTESIAN_POINT ( 'NONE',  ( 20.30531438145591139, 65.90309893892023752, -61.72708967725128559 ) ) ;
#57016=CIRCLE ( 'NONE', #202783, 0.1000000000000014488 ) ;
#57052=EDGE_CURVE ( 'NONE', #137039, #65850, #6626, .T. ) ;
#57063=FACE_OUTER_BOUND ( 'NONE', #75084, .T. ) ;
#57070=AXIS2_PLACEMENT_3D ( 'NONE', #17660, #51634, #131197 ) ;
#57091=EDGE_LOOP ( 'NONE', ( #215270, #136259, #102258, #166209 ) ) ;
#57133=FACE_OUTER_BOUND ( 'NONE', #185787, .T. ) ;
#57139=EDGE_LOOP ( 'NONE', ( #101826, #119471, #215333, #247889 ) ) ;
#57141=AXIS2_PLACEMENT_3D ( 'NONE', #26360, #245409, #109722 ) ;
#57153=ORIENTED_EDGE ( 'NONE', *, *, #216228, .F. ) ;
#57162=DIRECTION ( 'NONE',  ( 0.000000000000000000, 0.000000000000000000, 1.000000000000000000 ) ) ;
#57176=EDGE_CURVE ( 'NONE', #108484, #52356, #219002, .T. ) ;
#57178=EDGE_CURVE ( 'NONE', #106961, #161837, #252312, .T. ) ;
#57185=CARTESIAN_POINT ( 'NONE',  ( -20.94999999999999929, 65.70729864260954400, -30.56574559737245877 ) ) ;
#57220=CARTESIAN_POINT ( 'NONE',  ( 18.50000000000000000, 85.50000000001173817, -81.27310748452426026 ) ) ;
#57223=DIRECTION ( 'NONE',  ( 1.000000000000000000, 0.000000000000000000, 0.000000000000000000 ) ) ;
#57225=CARTESIAN_POINT ( 'NONE',  ( -21.44999999999999929, 68.75000000001158185, -57.17310748452437252 ) ) ;
#57231=EDGE_CURVE ( 'NONE', #100350, #94397, #98342, .T. ) ;
#57249=ORIENTED_EDGE ( 'NONE', *, *, #161959, .T. ) ;
#57277=CARTESIAN_POINT ( 'NONE',  ( -21.05000000000000071, 69.74218538953013535, -69.62089777583359762 ) ) ;
#57285=EDGE_CURVE ( 'NONE', #64016, #201514, #73489, .T. ) ;
#57334=AXIS2_PLACEMENT_3D ( 'NONE', #209508, #225202, #8752 ) ;
#57370=CARTESIAN_POINT ( 'NONE',  ( 21.08035267497491105, 69.66829316022864305, -69.60579610930049910 ) ) ;
#57390=CARTESIAN_POINT ( 'NONE',  ( 18.39999999999999858, 85.68240343348776378, -29.36626410711146207 ) ) ;
#57397=CIRCLE ( 'NONE', #178053, 0.3999999999999975797 ) ;
#57437=LINE ( 'NONE', #134399, #123091 ) ;
#57459=LINE ( 'NONE', #138274, #211046 ) ;
#57464=CARTESIAN_POINT ( 'NONE',  ( -21.05000000000000071, 77.16270174994961906, -61.42310748452431568 ) ) ;
#57503=ORIENTED_EDGE ( 'NONE', *, *, #37358, .T. ) ;
#57519=EDGE_LOOP ( 'NONE', ( #55812, #239740, #196543, #31020, #90900 ) ) ;
#57530=CLOSED_SHELL ( 'NONE', ( #29935, #33391, #105727, #99563, #235712, #248815, #175774, #48181, #17199, #68512, #52585, #188533, #45610, #120662, #73512, #60017, #18704, #232403, #108749, #150100, #67771, #27669, #130238, #159018, #234690, #227478, #253767, #192839, #88051, #208931, #252134, #222385, #135111, #89385, #136859, #113049, #125881, #218149, #41777, #197119, #127993, #33017, #69073, #240685, #8982, #122495, #248275, #146505, #47889, #248332, #183656, #48347, #221663, #471, #61495, #39424, #105591, #105135, #252456, #61095, #182136, #148828, #166582, #215958, #200470, #74081, #186372, #183342, #257066, #61161, #222687, #116860, #173382, #201884, #177015, #133339, #145999, #248142, #83216, #168104, #105597, #159208, #250722, #39203, #122258, #237983, #97967, #112604, #9528, #120051, #200121, #116865, #224528, #48445, #185079, #226709, #72700, #53825, #183633, #231391, #253287, #218334, #172727, #202737, #20991, #244700, #24687, #1154, #237938, #191266, #199510, #189687, #119095, #103886, #46033, #205112, #98, #117117, #201089, #158576, #51739, #107164, #240267, #177101, #241924, #8755, #228628, #131853, #4868, #203436, #26368, #234011, #110641, #199343, #177695, #242982, #9962, #190281, #143567, #54048, #220893, #196858, #171351, #109506, #44742, #81979, #58349, #58236, #245344, #187134, #24722, #32096, #158492, #41646, #35307, #243081, #231317, #174291, #22583, #68094, #197756, #218532, #230331, #132517, #213015, #31204, #128301, #56417, #65552, #57743, #88459, #124364, #71566, #161568, #154996, #240469, #153320, #202892, #208835, #208424, #227392, #233849, #70278, #100137, #79206, #25609, #65023, #65997, #76221, #250571, #58848, #239777, #82083, #230481, #86522, #8751, #155257, #236136, #225124, #75228, #158286, #71959, #149543, #160842, #191948, #146817, #79656, #248986, #192996, #206910, #119155, #122586, #42641, #181520, #255945, #249587, #5155, #7952, #17792, #81071, #51219, #253983, #7870, #139983, #243326, #39694, #147806, #53850, #34118, #6580, #208112, #78287, #99969, #149045, #122978, #172792, #180211, #249209, #20110, #190962, #30542, #202294, #176324, #35673, #209371, #89478, #87708, #151149, #208569, #221932, #164633, #80455, #226593, #79921, #151688, #201252, #170194, #207980, #41080, #191041, #175021, #72608, #138518, #230962, #11172, #211224, #227840, #189801, #38697, #104774, #70232, #95254, #130988, #7293, #86908, #86152, #63581, #140974, #26602, #236854, #180519, #205095, #6923, #192396, #65080, #37974, #176560, #199650, #106420, #83013, #144077, #29057, #143565, #117939, #125567, #12785, #23562, #150063, #191627, #78092, #189317, #20667, #60611, #92761, #120452, #130279, #116724, #98776, #170842, #106578, #222607, #171548, #33902, #126228, #257389, #19003, #254723, #74629, #121517, #189592, #127650, #126476, #117121, #235372, #156597, #244900, #42799, #73236, #186588, #128057, #15262, #182823, #211250, #235078, #43992, #234044, #167553, #96813, #73157, #12645, #7976, #194656, #161668, #30773, #75701, #20550, #234553, #187485, #1172, #188546, #62667, #76050, #161621, #97775, #77014, #61148, #44740, #1372, #192210, #99693, #127823, #148747, #189477, #167644, #30069, #119228, #62943, #167253, #79752, #253346, #158248, #43651, #131578, #242553, #185895, #192222, #107724, #86153, #98531, #219517, #167687, #189805, #115581, #168762, #110299, #175718, #131657, #170717, #135808, #147755, #244542, #179390, #200416, #28498, #245063, #99839, #74405, #48629, #109674, #252711, #82230, #19097, #162122, #44606, #47474, #240970, #248658, #105722, #99170, #92605, #174418, #4084, #228391, #185913, #108008, #104708, #190323, #20786, #230426, #202780, #93648, #109940, #163129, #21786, #224271, #31122, #231315, #51653, #136380, #246598, #78813, #118286, #186564, #157429, #119242, #122033, #240106, #44769, #41059, #200790, #132037, #214601, #1732, #176994, #87821, #39014, #43181, #128852, #27652, #177908, #46516, #15177, #21448, #141579, #82306, #7353, #84256, #228581, #191534, #231408, #188588, #14275, #27499, #156003, #50400, #37546, #159258, #28809, #247523, #156651, #164921, #79279, #168897, #62950, #117375, #101333, #48035, #121899 ) ) ;
#57604=ORIENTED_EDGE ( 'NONE', *, *, #204221, .T. ) ;
#57609=CARTESIAN_POINT ( 'NONE',  ( 23.14999999999999503, 69.35000000001156195, -57.27310748452436684 ) ) ;
#57621=ORIENTED_EDGE ( 'NONE', *, *, #18151, .F. ) ;
#57637=CARTESIAN_POINT ( 'NONE',  ( -20.54999999999999716, 76.00000000001149658, -48.89810748452431710 ) ) ;
#57641=CARTESIAN_POINT ( 'NONE',  ( 19.97071067811864609, 64.27928932189283273, -44.87310748452440379 ) ) ;
#57661=EDGE_CURVE ( 'NONE', #106961, #45697, #39781, .T. ) ;
#57725=CARTESIAN_POINT ( 'NONE',  ( -18.39999999999999858, 85.51932773110404185, -62.55013110796492271 ) ) ;
#57727=CARTESIAN_POINT ( 'NONE',  ( -21.05000000000000071, 69.60000000001157616, -59.59268285446279378 ) ) ;
#57728=ORIENTED_EDGE ( 'NONE', *, *, #170804, .T. ) ;
#57743=ADVANCED_FACE ( 'NONE', ( #116576 ), #158305, .F. ) ;
#57758=DIRECTION ( 'NONE',  ( 0.000000000000000000, 6.982962677686267499E-15, -1.000000000000000000 ) ) ;
#57759=ORIENTED_EDGE ( 'NONE', *, *, #222976, .F. ) ;
#57762=EDGE_CURVE ( 'NONE', #60411, #41111, #40360, .T. ) ;
#57765=LINE ( 'NONE', #38232, #149474 ) ;
#57769=CARTESIAN_POINT ( 'NONE',  ( -21.05000000000000071, 64.25000000001146816, -43.03791325517834565 ) ) ;
#57783=AXIS2_PLACEMENT_3D ( 'NONE', #128137, #29068, #108567 ) ;
#57854=CARTESIAN_POINT ( 'NONE',  ( -20.94999999999999929, 77.16270174994961906, -61.42310748452431568 ) ) ;
#57882=CARTESIAN_POINT ( 'NONE',  ( 22.60000000000000142, 76.00000000001165290, -69.52310748452431710 ) ) ;
#57884=CIRCLE ( 'NONE', #166279, 0.9750000000000036415 ) ;
#57909=CARTESIAN_POINT ( 'NONE',  ( 18.59999999999999076, 69.35000000001151932, -48.27310748452436684 ) ) ;
#57945=VERTEX_POINT ( 'NONE', #130689 ) ;
#57954=ORIENTED_EDGE ( 'NONE', *, *, #133036, .T. ) ;
#57974=CARTESIAN_POINT ( 'NONE',  ( -20.94999999999999929, 87.29603075034673054, -39.07100664418810965 ) ) ;
#57981=CARTESIAN_POINT ( 'NONE',  ( -20.64999999999999858, 85.00000000001149658, -45.91707660717669626 ) ) ;
#57993=CARTESIAN_POINT ( 'NONE',  ( -18.50000000000000000, 66.65000000001157332, -57.17310748452438673 ) ) ;
#58007=CARTESIAN_POINT ( 'NONE',  ( -20.85000000000000142, 65.66751761918619934, -30.42826094061123854 ) ) ;
#58061=CARTESIAN_POINT ( 'NONE',  ( 18.59999999999999076, 69.45000000001149942, -48.27310748452436684 ) ) ;
#58087=VECTOR ( 'NONE', #164448, 1000.000000000000000 ) ;
#58114=CARTESIAN_POINT ( 'NONE',  ( 21.05000000000000071, 69.45934304831041572, -69.52310748452437394 ) ) ;
#58148=CIRCLE ( 'NONE', #12409, 0.09999999999999976963 ) ;
#58151=ORIENTED_EDGE ( 'NONE', *, *, #22070, .F. ) ;
#58162=CIRCLE ( 'NONE', #4029, 0.5000000000000004441 ) ;
#58168=DIRECTION ( 'NONE',  ( -0.000000000000000000, -6.982962677686266711E-15, 1.000000000000000000 ) ) ;
#58175=EDGE_LOOP ( 'NONE', ( #109414, #75260 ) ) ;
#58191=FACE_OUTER_BOUND ( 'NONE', #153195, .T. ) ;
#58205=EDGE_LOOP ( 'NONE', ( #210021, #12744, #134562, #9658 ) ) ;
#58215=CARTESIAN_POINT ( 'NONE',  ( 23.24999999999999645, 70.40000000001157332, -57.11784146561127073 ) ) ;
#58218=EDGE_CURVE ( 'NONE', #234494, #105159, #27510, .T. ) ;
#58236=ADVANCED_FACE ( 'NONE', ( #64004 ), #123992, .T. ) ;
#58240=CIRCLE ( 'NONE', #203997, 0.1000000000000028644 ) ;
#58300=CARTESIAN_POINT ( 'NONE',  ( 20.58091095332318332, 66.98152984665915710, -61.10445730236583017 ) ) ;
#58339=EDGE_CURVE ( 'NONE', #128522, #65850, #6607, .T. ) ;
#58344=DIRECTION ( 'NONE',  ( 0.000000000000000000, -7.026728003956686545E-15, 1.000000000000000000 ) ) ;
#58349=ADVANCED_FACE ( 'NONE', ( #43165, #86099 ), #4024, .T. ) ;
#58397=EDGE_LOOP ( 'NONE', ( #44165, #145829, #208081, #205535 ) ) ;
#58436=CARTESIAN_POINT ( 'NONE',  ( 21.05000000000000071, 76.00000000001165290, -69.52310748452431710 ) ) ;
#58444=ORIENTED_EDGE ( 'NONE', *, *, #166199, .T. ) ;
#58501=VERTEX_POINT ( 'NONE', #122062 ) ;
#58504=VERTEX_POINT ( 'NONE', #176926 ) ;
#58518=DIRECTION ( 'NONE',  ( -2.812466655313719426E-14, -0.1350103645451835865, -0.9908441862701605762 ) ) ;
#58537=EDGE_LOOP ( 'NONE', ( #80991, #253234, #86993, #94416 ) ) ;
#58547=EDGE_CURVE ( 'NONE', #73365, #124582, #94274, .T. ) ;
#58566=CARTESIAN_POINT ( 'NONE',  ( -21.05000000000000426, 69.50298221357934381, -69.50856179395341883 ) ) ;
#58571=CARTESIAN_POINT ( 'NONE',  ( -23.25000000000000000, 76.00000000001142553, -36.02310748452432421 ) ) ;
#58595=CIRCLE ( 'NONE', #154342, 0.4000000000000045186 ) ;
#58631=CARTESIAN_POINT ( 'NONE',  ( -18.50000000000000000, 64.25000000001152500, -48.17310748452440805 ) ) ;
#58633=EDGE_LOOP ( 'NONE', ( #161866, #103797, #139598, #213744 ) ) ;
#58646=AXIS2_PLACEMENT_3D ( 'NONE', #142123, #84679, #245079 ) ;
#58649=CARTESIAN_POINT ( 'NONE',  ( 21.08884785362045378, 69.64280663258641368, -69.57289057959120271 ) ) ;
#58651=AXIS2_PLACEMENT_3D ( 'NONE', #200344, #120836, #219901 ) ;
#58705=ORIENTED_EDGE ( 'NONE', *, *, #32828, .T. ) ;
#58725=ORIENTED_EDGE ( 'NONE', *, *, #210895, .F. ) ;
#58789=DIRECTION ( 'NONE',  ( -1.000000000000000000, 2.952720810173289112E-16, 2.061873921506763405E-30 ) ) ;
#58811=FACE_OUTER_BOUND ( 'NONE', #152812, .T. ) ;
#58812=CARTESIAN_POINT ( 'NONE',  ( 21.56666275994539461, 76.00000000001169553, -76.48047589141765457 ) ) ;
#58829=ORIENTED_EDGE ( 'NONE', *, *, #150042, .T. ) ;
#58830=CARTESIAN_POINT ( 'NONE',  ( -18.59999999999999787, 77.83585931145498193, -24.51866831572578675 ) ) ;
#58840=FACE_OUTER_BOUND ( 'NONE', #152852, .T. ) ;
#58842=DIRECTION ( 'NONE',  ( 0.000000000000000000, -6.982962677686266711E-15, 1.000000000000000000 ) ) ;
#58848=ADVANCED_FACE ( 'NONE', ( #197424 ), #216978, .T. ) ;
#58851=ORIENTED_EDGE ( 'NONE', *, *, #12293, .T. ) ;
#58881=DIRECTION ( 'NONE',  ( 0.000000000000000000, 0.000000000000000000, -1.000000000000000000 ) ) ;
#58888=EDGE_CURVE ( 'NONE', #174034, #33900, #231857, .T. ) ;
#58905=ORIENTED_EDGE ( 'NONE', *, *, #200030, .F. ) ;
#58909=CARTESIAN_POINT ( 'NONE',  ( 19.97071067811865319, 64.27928932189281852, -44.81452884076170307 ) ) ;
#58914=CIRCLE ( 'NONE', #225515, 0.1000000000000052097 ) ;
#58950=ORIENTED_EDGE ( 'NONE', *, *, #177076, .T. ) ;
#58995=DIRECTION ( 'NONE',  ( 0.000000000000000000, 0.9908441862701697911, -0.1350103645451153911 ) ) ;
#59017=CARTESIAN_POINT ( 'NONE',  ( 21.05000000000000071, 67.12338541492448485, -61.13802700567971016 ) ) ;
#59022=CARTESIAN_POINT ( 'NONE',  ( -23.25000000000000000, 87.75000000001143974, -39.12310748452424747 ) ) ;
#59025=CARTESIAN_POINT ( 'NONE',  ( 21.09787244211745971, 67.22462929267425125, -57.28385410020680268 ) ) ;
#59042=ORIENTED_EDGE ( 'NONE', *, *, #193195, .T. ) ;
#59051=CARTESIAN_POINT ( 'NONE',  ( -18.49346865148326202, 85.44307379853647433, -62.33791122920943906 ) ) ;
#59052=AXIS2_PLACEMENT_3D ( 'NONE', #3145, #125679, #21469 ) ;
#59065=EDGE_CURVE ( 'NONE', #246301, #158894, #57016, .T. ) ;
#59068=DIRECTION ( 'NONE',  ( 1.000000000000000000, -3.469446951953718318E-14, 2.003086131649645455E-14 ) ) ;
#59082=FACE_OUTER_BOUND ( 'NONE', #201557, .T. ) ;
#59099=AXIS2_PLACEMENT_3D ( 'NONE', #258074, #41665, #196850 ) ;
#59113=EDGE_CURVE ( 'NONE', #203476, #32613, #236115, .T. ) ;
#59127=CARTESIAN_POINT ( 'NONE',  ( -21.05000000000000071, 64.35000000001166143, -69.42310748452440805 ) ) ;
#59143=CARTESIAN_POINT ( 'NONE',  ( -20.15000000000000568, 66.70857864377420299, -48.27310748452438816 ) ) ;
#59148=DIRECTION ( 'NONE',  ( 0.000000000000000000, 6.769652589177784668E-15, -1.000000000000000000 ) ) ;
#59169=DIRECTION ( 'NONE',  ( -1.000000000000000000, -0.000000000000000000, -0.000000000000000000 ) ) ;
#59173=DIRECTION ( 'NONE',  ( -0.000000000000000000, -1.000000000000000000, -6.982962677686266711E-15 ) ) ;
#59196=( BOUNDED_CURVE ( )  B_SPLINE_CURVE ( 3, ( #235667, #194007, #93604, #94877 ),
 .UNSPECIFIED., .F., .F. ) 
 B_SPLINE_CURVE_WITH_KNOTS ( ( 4, 4 ),
 ( 1.570796326794895448, 3.141592653589791784 ),
 .UNSPECIFIED. ) 
 CURVE ( )  GEOMETRIC_REPRESENTATION_ITEM ( )  RATIONAL_B_SPLINE_CURVE ( ( 1.000000000000000000, 0.8047378541243650485, 0.8047378541243650485, 1.000000000000000000 ) ) 
 REPRESENTATION_ITEM ( '' )  );
#59225=CARTESIAN_POINT ( 'NONE',  ( 20.94999999999999574, 70.10000000001163301, -59.30400771986794695 ) ) ;
#59236=CARTESIAN_POINT ( 'NONE',  ( 21.13920837816993270, 67.21675294989165650, -57.27310748452438105 ) ) ;
#59246=EDGE_CURVE ( 'NONE', #42405, #130839, #208306, .T. ) ;
#59275=VERTEX_POINT ( 'NONE', #198418 ) ;
#59287=AXIS2_PLACEMENT_3D ( 'NONE', #66652, #245291, #225680 ) ;
#59294=CIRCLE ( 'NONE', #167509, 0.1000000000000028644 ) ;
#59313=AXIS2_PLACEMENT_3D ( 'NONE', #203356, #105496, #257177 ) ;
#59318=ORIENTED_EDGE ( 'NONE', *, *, #40186, .F. ) ;
#59334=ORIENTED_EDGE ( 'NONE', *, *, #23010, .T. ) ;
#59535=ORIENTED_EDGE ( 'NONE', *, *, #23788, .F. ) ;
#59567=CARTESIAN_POINT ( 'NONE',  ( 20.19326291201647194, 65.84393901210765421, -61.76124567692164646 ) ) ;
#59569=EDGE_LOOP ( 'NONE', ( #133535, #90247, #60040, #247375 ) ) ;
#59570=FACE_OUTER_BOUND ( 'NONE', #99062, .T. ) ;
#59576=EDGE_CURVE ( 'NONE', #42291, #66731, #250174, .T. ) ;
#59577=ORIENTED_EDGE ( 'NONE', *, *, #33971, .T. ) ;
#59614=ORIENTED_EDGE ( 'NONE', *, *, #109317, .F. ) ;
#59624=DIRECTION ( 'NONE',  ( 0.000000000000000000, -6.530723674265620862E-15, 1.000000000000000000 ) ) ;
#59626=AXIS2_PLACEMENT_3D ( 'NONE', #128167, #9488, #168628 ) ;
#59712=CARTESIAN_POINT ( 'NONE',  ( 20.94999999999999929, 76.00000000001139711, -32.02310748452432421 ) ) ;
#59715=CYLINDRICAL_SURFACE ( 'NONE', #35288, 0.1000000000000028644 ) ;
#59738=ORIENTED_EDGE ( 'NONE', *, *, #200247, .T. ) ;
#59749=CARTESIAN_POINT ( 'NONE',  ( 21.14999999999999503, 87.75000000001162448, -66.62310748452424036 ) ) ;
#59768=ORIENTED_EDGE ( 'NONE', *, *, #243897, .F. ) ;
#59781=VERTEX_POINT ( 'NONE', #121185 ) ;
#59855=FACE_OUTER_BOUND ( 'NONE', #255300, .T. ) ;
#59899=DIRECTION ( 'NONE',  ( 0.000000000000000000, 0.1350103645451945777, -0.9908441862701589109 ) ) ;
#59900=ORIENTED_EDGE ( 'NONE', *, *, #51968, .F. ) ;
#59911=DIRECTION ( 'NONE',  ( -1.000000000000000000, -9.012599976027990443E-15, -6.882867235861669241E-14 ) ) ;
#59926=CARTESIAN_POINT ( 'NONE',  ( 18.58222699835054570, 65.66799936921481162, -30.42993998886010232 ) ) ;
#59927=AXIS2_PLACEMENT_3D ( 'NONE', #250553, #92759, #190608 ) ;
#59928=CARTESIAN_POINT ( 'NONE',  ( -23.25000000000000000, 76.00000000001165290, -69.52310748452431710 ) ) ;
#59934=CARTESIAN_POINT ( 'NONE',  ( 21.13498764882293557, 69.50438185653779044, -69.52476387925570123 ) ) ;
#59965=DIRECTION ( 'NONE',  ( 1.000000000000000000, 0.000000000000000000, 0.000000000000000000 ) ) ;
#59996=B_SPLINE_CURVE_WITH_KNOTS ( 'NONE', 3,
 ( #135389, #97526, #237078, #255297, #233254, #174596 ),
 .UNSPECIFIED., .F., .F.,
 ( 4, 2, 4 ),
 ( 0.000000000000000000, 0.0001891491689349579291, 0.0003782983378699158582 ),
 .UNSPECIFIED. ) ;
#60000=ORIENTED_EDGE ( 'NONE', *, *, #118488, .F. ) ;
#60017=ADVANCED_FACE ( 'NONE', ( #183235 ), #200464, .F. ) ;
#60019=FACE_OUTER_BOUND ( 'NONE', #130857, .T. ) ;
#60040=ORIENTED_EDGE ( 'NONE', *, *, #255069, .F. ) ;
#60046=AXIS2_PLACEMENT_3D ( 'NONE', #150838, #73905, #90858 ) ;
#60075=CARTESIAN_POINT ( 'NONE',  ( -20.94999999999999929, 74.83729825007360148, -61.42310748452432989 ) ) ;
#60076=ORIENTED_EDGE ( 'NONE', *, *, #227461, .F. ) ;
#60078=ORIENTED_EDGE ( 'NONE', *, *, #143009, .F. ) ;
#60088=PLANE ( 'NONE',  #163193 ) ;
#60104=ORIENTED_EDGE ( 'NONE', *, *, #5748, .T. ) ;
#60129=ORIENTED_EDGE ( 'NONE', *, *, #70209, .T. ) ;
#60148=EDGE_LOOP ( 'NONE', ( #208226, #80676, #68858, #74259 ) ) ;
#60168=DIRECTION ( 'NONE',  ( -0.000000000000000000, 6.982962677686266711E-15, -1.000000000000000000 ) ) ;
#60169=TOROIDAL_SURFACE ( 'NONE', #205925, 0.2000000000000000111, 0.1000000000000000056 ) ;
#60173=DIRECTION ( 'NONE',  ( 0.000000000000000000, 0.000000000000000000, 1.000000000000000000 ) ) ;
#60177=CARTESIAN_POINT ( 'NONE',  ( -20.94999999999999929, 76.00000000001165290, -69.52310748452431710 ) ) ;
#60185=CARTESIAN_POINT ( 'NONE',  ( 20.94999999999999574, 65.52661458509869874, -61.94445302027585143 ) ) ;
#60217=ORIENTED_EDGE ( 'NONE', *, *, #144720, .F. ) ;
#60232=CARTESIAN_POINT ( 'NONE',  ( -20.64999999999999858, 76.00000000001165290, -69.52310748452431710 ) ) ;
#60289=DIRECTION ( 'NONE',  ( 0.000000000000000000, -7.109473446599835262E-15, 1.000000000000000000 ) ) ;
#60292=ORIENTED_EDGE ( 'NONE', *, *, #215887, .F. ) ;
#60299=EDGE_LOOP ( 'NONE', ( #130861, #189906, #224239, #77770 ) ) ;
#60309=AXIS2_PLACEMENT_3D ( 'NONE', #156001, #56837, #154722 ) ;
#60347=CIRCLE ( 'NONE', #81184, 0.1000000000000028644 ) ;
#60362=DIRECTION ( 'NONE',  ( 1.000000000000000000, 0.000000000000000000, 0.000000000000000000 ) ) ;
#60389=AXIS2_PLACEMENT_3D ( 'NONE', #25123, #147613, #5512 ) ;
#60391=VERTEX_POINT ( 'NONE', #123467 ) ;
#60398=CYLINDRICAL_SURFACE ( 'NONE', #207685, 0.09999999999999939493 ) ;
#60408=EDGE_LOOP ( 'NONE', ( #158610, #239021 ) ) ;
#60411=VERTEX_POINT ( 'NONE', #161325 ) ;
#60425=VERTEX_POINT ( 'NONE', #80445 ) ;
#60427=AXIS2_PLACEMENT_3D ( 'NONE', #56728, #234112, #55446 ) ;
#60429=DIRECTION ( 'NONE',  ( 0.000000000000000000, 1.000000000000000000, 6.982962677686266711E-15 ) ) ;
#60437=CARTESIAN_POINT ( 'NONE',  ( 20.94999999999999929, 76.00000000001142553, -36.02310748452432421 ) ) ;
#60439=DIRECTION ( 'NONE',  ( -0.000000000000000000, -0.8700118002898356018, 0.4930308989875170078 ) ) ;
#60462=CARTESIAN_POINT ( 'NONE',  ( 21.51976009735019346, 69.08954155835245103, -69.52310748452435973 ) ) ;
#60465=CARTESIAN_POINT ( 'NONE',  ( 22.50000000000000000, 76.00000000001165290, -69.52310748452431710 ) ) ;
#60477=DIRECTION ( 'NONE',  ( -0.000000000000000000, -0.8660254037844420383, 0.4999999999999943379 ) ) ;
#60526=CARTESIAN_POINT ( 'NONE',  ( 22.59999985501178799, 64.25013020700868083, -69.58870615432387297 ) ) ;
#60542=DIRECTION ( 'NONE',  ( -3.469446951953433697E-14, 0.9908441862701605762, 0.1350103645451835310 ) ) ;
#60546=DIRECTION ( 'NONE',  ( 0.000000000000000000, -1.000000000000000000, -6.982962677686265922E-15 ) ) ;
#60556=CARTESIAN_POINT ( 'NONE',  ( 21.07199075132371746, 67.22505500089548036, -57.30957532291152745 ) ) ;
#60573=DIRECTION ( 'NONE',  ( 1.000000000000000000, 0.000000000000000000, 0.000000000000000000 ) ) ;
#60575=CARTESIAN_POINT ( 'NONE',  ( -21.05000000000000071, 76.00000000001142553, -36.02310748452432421 ) ) ;
#60611=ADVANCED_FACE ( 'NONE', ( #214547 ), #231560, .T. ) ;
#60619=AXIS2_PLACEMENT_3D ( 'NONE', #166036, #63041, #21387 ) ;
#60639=EDGE_LOOP ( 'NONE', ( #57604, #184513, #234256, #140953 ) ) ;
#60658=ORIENTED_EDGE ( 'NONE', *, *, #162057, .F. ) ;
#60701=CARTESIAN_POINT ( 'NONE',  ( -20.54999999999999716, 74.00000000001156764, -56.29848556176223440 ) ) ;
#60707=ORIENTED_EDGE ( 'NONE', *, *, #4202, .T. ) ;
#60736=CYLINDRICAL_SURFACE ( 'NONE', #152670, 0.1000000000000028644 ) ;
#60763=ORIENTED_EDGE ( 'NONE', *, *, #39591, .T. ) ;
#60788=DIRECTION ( 'NONE',  ( -1.000000000000000000, 0.000000000000000000, 0.000000000000000000 ) ) ;
#60806=CIRCLE ( 'NONE', #127655, 0.1000000000000028644 ) ;
#60810=EDGE_CURVE ( 'NONE', #165845, #84743, #99714, .T. ) ;
#60817=DIRECTION ( 'NONE',  ( 0.000000000000000000, 0.000000000000000000, -1.000000000000000000 ) ) ;
#60878=CARTESIAN_POINT ( 'NONE',  ( 20.22483756094572271, 66.49809532113982868, -61.38356835580996318 ) ) ;
#60901=CARTESIAN_POINT ( 'NONE',  ( -21.04999999999999716, 75.90156250001170690, -75.82233839461120795 ) ) ;
#60904=AXIS2_PLACEMENT_3D ( 'NONE', #183255, #224925, #207972 ) ;
#60906=DIRECTION ( 'NONE',  ( -1.000000000000000000, -0.000000000000000000, -0.000000000000000000 ) ) ;
#60918=ORIENTED_EDGE ( 'NONE', *, *, #28805, .F. ) ;
#60992=DIRECTION ( 'NONE',  ( 0.000000000000000000, -6.938893903907222067E-15, 1.000000000000000000 ) ) ;
#61018=CARTESIAN_POINT ( 'NONE',  ( -20.85000000000000142, 77.16412189325258453, -28.20825939895270551 ) ) ;
#61022=EDGE_LOOP ( 'NONE', ( #255349, #170517, #30678, #69424, #146403 ) ) ;
#61057=CIRCLE ( 'NONE', #15300, 2.100000000000004530 ) ;
#61089=TOROIDAL_SURFACE ( 'NONE', #236067, 12.97499999999999609, 0.1000000000000000056 ) ;
#61095=ADVANCED_FACE ( 'NONE', ( #177732 ), #79851, .T. ) ;
#61100=CARTESIAN_POINT ( 'NONE',  ( 23.24999999999999645, 76.00000000001142553, -36.02310748452432421 ) ) ;
#61106=AXIS2_PLACEMENT_3D ( 'NONE', #90895, #212146, #109161 ) ;
#61125=AXIS2_PLACEMENT_3D ( 'NONE', #141526, #240634, #62012 ) ;
#61135=ORIENTED_EDGE ( 'NONE', *, *, #205024, .F. ) ;
#61148=ADVANCED_FACE ( 'NONE', ( #26008 ), #78586, .T. ) ;
#61161=ADVANCED_FACE ( 'NONE', ( #164240 ), #27326, .F. ) ;
#61226=CARTESIAN_POINT ( 'NONE',  ( -18.39999999999999858, 85.60000000001137721, -29.32291809330221355 ) ) ;
#61235=DIRECTION ( 'NONE',  ( 0.000000000000000000, -1.000000000000000000, -6.982962677686266711E-15 ) ) ;
#61236=CARTESIAN_POINT ( 'NONE',  ( 18.51697539158856642, 65.68434038414308418, -30.48668807260655456 ) ) ;
#61247=AXIS2_PLACEMENT_3D ( 'NONE', #104352, #183918, #84779 ) ;
#61266=ORIENTED_EDGE ( 'NONE', *, *, #23509, .T. ) ;
#61292=CARTESIAN_POINT ( 'NONE',  ( 21.05000000000000071, 74.83729825007360148, -61.42310748452432989 ) ) ;
#61300=ORIENTED_EDGE ( 'NONE', *, *, #165048, .F. ) ;
#61328=AXIS2_PLACEMENT_3D ( 'NONE', #244846, #6232, #204433 ) ;
#61338=PLANE ( 'NONE',  #171772 ) ;
#61365=VERTEX_POINT ( 'NONE', #147224 ) ;
#61385=CARTESIAN_POINT ( 'NONE',  ( -21.05000000000000071, 87.41227409416133298, -66.52310748452423184 ) ) ;
#61422=DIRECTION ( 'NONE',  ( 0.000000000000000000, -6.608470384673536824E-15, 1.000000000000000000 ) ) ;
#61443=PLANE ( 'NONE',  #114215 ) ;
#61448=ORIENTED_EDGE ( 'NONE', *, *, #157310, .F. ) ;
#61450=AXIS2_PLACEMENT_3D ( 'NONE', #82806, #2006, #99807 ) ;
#61469=CARTESIAN_POINT ( 'NONE',  ( -20.94999999999999929, 64.40000000001161595, -62.59490425424885274 ) ) ;
#61495=ADVANCED_FACE ( 'NONE', ( #220036 ), #182202, .F. ) ;
#61547=AXIS2_PLACEMENT_3D ( 'NONE', #79125, #42587, #140389 ) ;
#61565=EDGE_LOOP ( 'NONE', ( #36160, #4962, #141567, #218922 ) ) ;
#61606=AXIS2_PLACEMENT_3D ( 'NONE', #158514, #21557, #18964 ) ;
#61615=FACE_OUTER_BOUND ( 'NONE', #246592, .T. ) ;
#61657=CARTESIAN_POINT ( 'NONE',  ( -18.43473496883427032, 85.49495241101085696, -62.47723591229602391 ) ) ;
#61662=CYLINDRICAL_SURFACE ( 'NONE', #5676, 0.09999999999999939493 ) ;
#61713=ORIENTED_EDGE ( 'NONE', *, *, #97325, .T. ) ;
#61716=ORIENTED_EDGE ( 'NONE', *, *, #169887, .F. ) ;
#61727=ORIENTED_EDGE ( 'NONE', *, *, #62043, .T. ) ;
#61731=CARTESIAN_POINT ( 'NONE',  ( 21.05000000000000071, 76.00000000001142553, -36.02310748452432421 ) ) ;
#61745=ORIENTED_EDGE ( 'NONE', *, *, #4567, .F. ) ;
#61760=TOROIDAL_SURFACE ( 'NONE', #203235, 11.70000000000000639, 0.1000000000000000056 ) ;
#61771=CARTESIAN_POINT ( 'NONE',  ( -20.94999999999999929, 77.16270174994961906, -61.42310748452431568 ) ) ;
#61807=VERTEX_POINT ( 'NONE', #118054 ) ;
#61820=CARTESIAN_POINT ( 'NONE',  ( -21.53551880898957904, 75.90103026544004194, -76.30790524594065971 ) ) ;
#61823=CARTESIAN_POINT ( 'NONE',  ( 18.52351027002948669, 85.64216290470656645, -29.30806053401447286 ) ) ;
#61826=EDGE_CURVE ( 'NONE', #98003, #60425, #154650, .T. ) ;
#61855=ORIENTED_EDGE ( 'NONE', *, *, #232868, .F. ) ;
#61861=CARTESIAN_POINT ( 'NONE',  ( -18.59999999999999787, 77.85161776048025217, -24.41991776492064758 ) ) ;
#61864=FACE_OUTER_BOUND ( 'NONE', #3300, .T. ) ;
#61876=AXIS2_PLACEMENT_3D ( 'NONE', #251238, #11367, #90894 ) ;
#61893=LINE ( 'NONE', #99698, #52707 ) ;
#61894=EDGE_LOOP ( 'NONE', ( #224425, #151281, #14659, #141332 ) ) ;
#61912=CIRCLE ( 'NONE', #107689, 0.09999999999999520384 ) ;
#61961=EDGE_CURVE ( 'NONE', #180734, #149751, #140169, .T. ) ;
#62012=DIRECTION ( 'NONE',  ( 1.000000000000000000, 0.000000000000000000, 0.000000000000000000 ) ) ;
#62019=ORIENTED_EDGE ( 'NONE', *, *, #189806, .F. ) ;
#62030=PLANE ( 'NONE',  #52529 ) ;
#62040=VERTEX_POINT ( 'NONE', #240578 ) ;
#62043=EDGE_CURVE ( 'NONE', #44661, #126512, #1944, .T. ) ;
#62050=AXIS2_PLACEMENT_3D ( 'NONE', #22100, #2499, #204564 ) ;
#62081=CARTESIAN_POINT ( 'NONE',  ( 20.85000000000000142, 76.00000000001142553, -36.02310748452432421 ) ) ;
#62088=ORIENTED_EDGE ( 'NONE', *, *, #63465, .T. ) ;
#62089=CIRCLE ( 'NONE', #103744, 0.09999999999999939493 ) ;
#62107=LINE ( 'NONE', #223722, #251759 ) ;
#62121=ORIENTED_EDGE ( 'NONE', *, *, #232868, .T. ) ;
#62137=CARTESIAN_POINT ( 'NONE',  ( -21.10257677756356642, 69.60161825747893261, -69.54805823409236609 ) ) ;
#62182=CARTESIAN_POINT ( 'NONE',  ( 20.84451136049642272, 65.37985808520329556, -62.02918292499334285 ) ) ;
#62187=DIRECTION ( 'NONE',  ( 0.000000000000000000, 6.982962677686266711E-15, -1.000000000000000000 ) ) ;
#62190=DIRECTION ( 'NONE',  ( -1.000000000000000000, 1.836970198721029934E-16, 1.282749433769087582E-30 ) ) ;
#62200=ORIENTED_EDGE ( 'NONE', *, *, #23443, .T. ) ;
#62221=EDGE_LOOP ( 'NONE', ( #24769, #80841, #95971, #181342, #66476 ) ) ;
#62246=DIRECTION ( 'NONE',  ( 1.000000000000000000, 0.000000000000000000, 0.000000000000000000 ) ) ;
#62247=DIRECTION ( 'NONE',  ( 1.000000000000000000, 0.000000000000000000, 0.000000000000000000 ) ) ;
#62260=CARTESIAN_POINT ( 'NONE',  ( -23.15000000000000213, 71.85000000001151932, -48.37310748452435405 ) ) ;
#62262=CARTESIAN_POINT ( 'NONE',  ( 20.94999999999999929, 76.00000000001142553, -36.02310748452432421 ) ) ;
#62284=VECTOR ( 'NONE', #174450, 1000.000000000000000 ) ;
#62289=ORIENTED_EDGE ( 'NONE', *, *, #52345, .T. ) ;
#62307=EDGE_CURVE ( 'NONE', #62686, #17722, #159884, .T. ) ;
#62337=ORIENTED_EDGE ( 'NONE', *, *, #220248, .F. ) ;
#62355=CARTESIAN_POINT ( 'NONE',  ( -20.85000000000000142, 65.66751761918619934, -30.42826094061123854 ) ) ;
#62406=CARTESIAN_POINT ( 'NONE',  ( 23.14999999999999858, 70.40000000001157332, -57.11784146561127073 ) ) ;
#62428=EDGE_CURVE ( 'NONE', #183793, #182847, #176457, .T. ) ;
#62431=ORIENTED_EDGE ( 'NONE', *, *, #64214, .T. ) ;
#62432=EDGE_CURVE ( 'NONE', #198388, #201923, #64211, .T. ) ;
#62452=AXIS2_PLACEMENT_3D ( 'NONE', #251130, #72534, #152077 ) ;
#62461=CARTESIAN_POINT ( 'NONE',  ( -21.05000000000000071, 70.10000000001163301, -59.30400771986794695 ) ) ;
#62516=FACE_OUTER_BOUND ( 'NONE', #39962, .T. ) ;
#62528=ORIENTED_EDGE ( 'NONE', *, *, #203986, .T. ) ;
#62545=DIRECTION ( 'NONE',  ( 0.000000000000000000, -7.189901751995755791E-15, 1.000000000000000000 ) ) ;
#62587=CIRCLE ( 'NONE', #75258, 0.1000000000000052097 ) ;
#62593=EDGE_LOOP ( 'NONE', ( #209428, #235897, #842, #117613, #159003, #6275, #27041, #101623 ) ) ;
#62612=DIRECTION ( 'NONE',  ( -0.000000000000000000, 1.000000000000000000, 6.982962677686266711E-15 ) ) ;
#62614=CARTESIAN_POINT ( 'NONE',  ( -20.94999999999999929, 76.00000000001142553, -36.02310748452432421 ) ) ;
#62628=DIRECTION ( 'NONE',  ( 0.000000000000000000, -1.000000000000000000, -6.982962677686265922E-15 ) ) ;
#62667=ADVANCED_FACE ( 'NONE', ( #74527 ), #34110, .T. ) ;
#62679=ORIENTED_EDGE ( 'NONE', *, *, #209811, .F. ) ;
#62686=VERTEX_POINT ( 'NONE', #253100 ) ;
#62736=CIRCLE ( 'NONE', #154356, 0.1000000000000028644 ) ;
#62753=CARTESIAN_POINT ( 'NONE',  ( -21.05000000000000071, 64.37928932189296916, -62.65469083218336266 ) ) ;
#62767=FACE_OUTER_BOUND ( 'NONE', #238155, .T. ) ;
#62774=CIRCLE ( 'NONE', #58646, 0.09999999999999939493 ) ;
#62812=CARTESIAN_POINT ( 'NONE',  ( 22.50000000000000000, 75.95437663941535789, -81.17361182307570289 ) ) ;
#62817=AXIS2_PLACEMENT_3D ( 'NONE', #215109, #73075, #53472 ) ;
#62823=CARTESIAN_POINT ( 'NONE',  ( -22.50000000000000000, 64.35000000001167564, -69.52310748452438816 ) ) ;
#62836=CARTESIAN_POINT ( 'NONE',  ( -18.50000000000000000, 85.40000000001160174, -62.22584772486096938 ) ) ;
#62886=AXIS2_PLACEMENT_3D ( 'NONE', #155903, #37229, #178026 ) ;
#62893=CARTESIAN_POINT ( 'NONE',  ( -18.59999999999999787, 76.00000000001142553, -36.02310748452432421 ) ) ;
#62899=DIRECTION ( 'NONE',  ( -3.265361837132813093E-16, -1.000000000000000000, 7.445645354460596589E-46 ) ) ;
#62938=AXIS2_PLACEMENT_3D ( 'NONE', #257901, #79297, #158883 ) ;
#62943=ADVANCED_FACE ( 'NONE', ( #5179 ), #123887, .T. ) ;
#62950=ADVANCED_FACE ( 'NONE', ( #205979 ), #176258, .T. ) ;
#62954=EDGE_LOOP ( 'NONE', ( #179418, #124777, #133492, #233026 ) ) ;
#62973=CARTESIAN_POINT ( 'NONE',  ( -18.59999999999999787, 69.06610602788505560, -32.23746165015079868 ) ) ;
#62977=CARTESIAN_POINT ( 'NONE',  ( -20.64999999999999858, 71.65000000001155911, -57.17310748452435121 ) ) ;
#62989=CARTESIAN_POINT ( 'NONE',  ( -21.55000000000000071, 68.65000000001150227, -48.37310748452437537 ) ) ;
#63000=EDGE_CURVE ( 'NONE', #9118, #207310, #38880, .T. ) ;
#63020=ORIENTED_EDGE ( 'NONE', *, *, #249922, .T. ) ;
#63030=CYLINDRICAL_SURFACE ( 'NONE', #24936, 0.1000000000000028644 ) ;
#63039=ORIENTED_EDGE ( 'NONE', *, *, #82390, .F. ) ;
#63041=DIRECTION ( 'NONE',  ( -1.000000000000000000, 3.265361837132813093E-16, 2.280189983783949500E-30 ) ) ;
#63042=ORIENTED_EDGE ( 'NONE', *, *, #211467, .T. ) ;
#63047=CARTESIAN_POINT ( 'NONE',  ( -20.85000000000000142, 68.97833521811131163, -32.18954208262707795 ) ) ;
#63048=LINE ( 'NONE', #100853, #182430 ) ;
#63051=LINE ( 'NONE', #86444, #170048 ) ;
#63065=CARTESIAN_POINT ( 'NONE',  ( -21.14999999999999858, 87.65000000001165859, -69.52310748452424605 ) ) ;
#63078=CARTESIAN_POINT ( 'NONE',  ( 23.14999999999999503, 69.55000000001150795, -48.37310748452436826 ) ) ;
#63092=ORIENTED_EDGE ( 'NONE', *, *, #57231, .F. ) ;
#63093=CARTESIAN_POINT ( 'NONE',  ( 20.94999999999999929, 67.12338541492449906, -61.13802700567970305 ) ) ;
#63118=CARTESIAN_POINT ( 'NONE',  ( -21.14250536705909411, 76.00000000001169553, -76.04127966140507056 ) ) ;
#63121=CARTESIAN_POINT ( 'NONE',  ( 21.11747605621531321, 67.22129199451867976, -57.27854431473461005 ) ) ;
#63231=B_SPLINE_CURVE_WITH_KNOTS ( 'NONE', 3,
 ( #221098, #42466, #85410, #122013, #5895, #45041, #146680, #241952, #124591, #185832, #201539, #22939, #24215, #107573, #82842, #145415 ),
 .UNSPECIFIED., .F., .F.,
 ( 4, 3, 3, 3, 3, 4 ),
 ( 0.000000000000000000, 2.209075297431620268E-05, 5.594258369009780208E-05, 8.979524372341998934E-05, 0.0001236472815274569225, 0.0001574990747609545522 ),
 .UNSPECIFIED. ) ;
#63232=ORIENTED_EDGE ( 'NONE', *, *, #207451, .F. ) ;
#63289=LINE ( 'NONE', #124569, #254635 ) ;
#63294=EDGE_CURVE ( 'NONE', #6026, #74560, #88910, .T. ) ;
#63342=CARTESIAN_POINT ( 'NONE',  ( 18.60000000000000142, 85.40000000001154490, -62.22584772486096227 ) ) ;
#63346=VECTOR ( 'NONE', #205944, 1000.000000000000114 ) ;
#63363=CYLINDRICAL_SURFACE ( 'NONE', #1756, 0.1000000000000028644 ) ;
#63399=ORIENTED_EDGE ( 'NONE', *, *, #78594, .F. ) ;
#63400=AXIS2_PLACEMENT_3D ( 'NONE', #245109, #62628, #221670 ) ;
#63404=CARTESIAN_POINT ( 'NONE',  ( -21.05000000000000071, 76.00000000001165290, -69.52310748452431710 ) ) ;
#63423=CARTESIAN_POINT ( 'NONE',  ( 21.05000000000000071, 76.00000000001142553, -36.02310748452432421 ) ) ;
#63426=VECTOR ( 'NONE', #228948, 1000.000000000000000 ) ;
#63449=ORIENTED_EDGE ( 'NONE', *, *, #213971, .F. ) ;
#63450=CYLINDRICAL_SURFACE ( 'NONE', #29367, 0.09999999999999939493 ) ;
#63465=EDGE_CURVE ( 'NONE', #89290, #41111, #68275, .T. ) ;
#63468=DIRECTION ( 'NONE',  ( 0.000000000000000000, 0.000000000000000000, -1.000000000000000000 ) ) ;
#63480=DIRECTION ( 'NONE',  ( -0.000000000000000000, -6.982962677686266711E-15, 1.000000000000000000 ) ) ;
#63575=CIRCLE ( 'NONE', #138562, 0.1000000000000028644 ) ;
#63581=ADVANCED_FACE ( 'NONE', ( #104615 ), #5528, .T. ) ;
#63585=AXIS2_PLACEMENT_3D ( 'NONE', #148661, #10429, #245186 ) ;
#63591=CARTESIAN_POINT ( 'NONE',  ( -18.59999999999999787, 66.75000000001158185, -57.27310748452438816 ) ) ;
#63627=CARTESIAN_POINT ( 'NONE',  ( 18.59999999999999076, 74.75000000001158185, -61.52310748452433131 ) ) ;
#63640=ORIENTED_EDGE ( 'NONE', *, *, #50789, .T. ) ;
#63659=DIRECTION ( 'NONE',  ( 1.000000000000000000, 0.000000000000000000, 0.000000000000000000 ) ) ;
#63681=ORIENTED_EDGE ( 'NONE', *, *, #246397, .T. ) ;
#63720=EDGE_CURVE ( 'NONE', #142525, #201784, #105844, .T. ) ;
#63730=DIRECTION ( 'NONE',  ( 0.000000000000000000, -6.982962677686266711E-15, 1.000000000000000000 ) ) ;
#63732=CARTESIAN_POINT ( 'NONE',  ( -23.15000000000000213, 87.65000000001144542, -39.12310748452424747 ) ) ;
#63739=AXIS2_PLACEMENT_3D ( 'NONE', #247591, #89787, #66393 ) ;
#63751=DIRECTION ( 'NONE',  ( 0.000000000000000000, -1.000000000000000000, -8.717686153663073805E-15 ) ) ;
#63753=EDGE_LOOP ( 'NONE', ( #210058, #245614, #43344, #192509, #40982 ) ) ;
#63762=EDGE_CURVE ( 'NONE', #20329, #73365, #5886, .T. ) ;
#63766=DIRECTION ( 'NONE',  ( 1.000000000000000000, 0.000000000000000000, 0.000000000000000000 ) ) ;
#63822=CYLINDRICAL_SURFACE ( 'NONE', #258104, 0.1000000000000028644 ) ;
#63834=CARTESIAN_POINT ( 'NONE',  ( 18.47135592147649774, 85.47108861327711793, -29.33951254468060554 ) ) ;
#63857=CARTESIAN_POINT ( 'NONE',  ( 20.85000000000000142, 69.15387683765879956, -32.28538121767450519 ) ) ;
#63860=DIRECTION ( 'NONE',  ( 0.000000000000000000, 1.000000000000000000, 0.000000000000000000 ) ) ;
#63866=EDGE_CURVE ( 'NONE', #68194, #56261, #96611, .T. ) ;
#63884=CARTESIAN_POINT ( 'NONE',  ( 18.49713797159854778, 85.44648232759047346, -62.45164936291396884 ) ) ;
#63904=SPHERICAL_SURFACE ( 'NONE', #63400, 0.1000000000000000056 ) ;
#63928=VECTOR ( 'NONE', #37837, 1000.000000000000000 ) ;
#63938=ORIENTED_EDGE ( 'NONE', *, *, #154801, .F. ) ;
#63966=EDGE_LOOP ( 'NONE', ( #8696, #71935, #52375, #16477 ) ) ;
#63999=ORIENTED_EDGE ( 'NONE', *, *, #63866, .F. ) ;
#64004=FACE_OUTER_BOUND ( 'NONE', #143171, .T. ) ;
#64008=CARTESIAN_POINT ( 'NONE',  ( 21.14999999999999858, 69.35000000001156195, -57.37310748452436826 ) ) ;
#64012=AXIS2_PLACEMENT_3D ( 'NONE', #242840, #159463, #100723 ) ;
#64016=VERTEX_POINT ( 'NONE', #114636 ) ;
#64039=DIRECTION ( 'NONE',  ( 1.000000000000000000, 0.000000000000000000, 0.000000000000000000 ) ) ;
#64049=CARTESIAN_POINT ( 'NONE',  ( -21.05000000000000071, 77.83534155023598089, -57.86795619196132634 ) ) ;
#64061=CARTESIAN_POINT ( 'NONE',  ( -18.54148534481894472, 65.67467670974366456, -30.45317318268843110 ) ) ;
#64076=FACE_OUTER_BOUND ( 'NONE', #67548, .T. ) ;
#64093=EDGE_CURVE ( 'NONE', #88576, #134285, #145738, .T. ) ;
#64106=EDGE_CURVE ( 'NONE', #172217, #97864, #25804, .T. ) ;
#64114=DIRECTION ( 'NONE',  ( 0.000000000000000000, -7.086529944415894657E-15, 1.000000000000000000 ) ) ;
#64158=CARTESIAN_POINT ( 'NONE',  ( 18.50000000000000000, 85.40000000001137437, -29.14106563635157698 ) ) ;
#64159=DIRECTION ( 'NONE',  ( -0.7071067811865474617, 0.7071067811865474617, 4.937700262164531476E-15 ) ) ;
#64176=EDGE_CURVE ( 'NONE', #80057, #49235, #222549, .T. ) ;
#64179=EDGE_CURVE ( 'NONE', #53002, #729, #1973, .T. ) ;
#64192=CYLINDRICAL_SURFACE ( 'NONE', #136856, 0.09999999999999867328 ) ;
#64205=EDGE_LOOP ( 'NONE', ( #218593, #89313, #17021, #251589 ) ) ;
#64206=CARTESIAN_POINT ( 'NONE',  ( 20.97462148592276776, 67.12526242356098294, -57.26846315279335897 ) ) ;
#64211=LINE ( 'NONE', #223267, #209760 ) ;
#64214=EDGE_CURVE ( 'NONE', #31422, #31772, #90906, .T. ) ;
#64225=DIRECTION ( 'NONE',  ( -1.000000000000000000, 0.000000000000000000, -0.000000000000000000 ) ) ;
#64253=ORIENTED_EDGE ( 'NONE', *, *, #256570, .T. ) ;
#64277=CIRCLE ( 'NONE', #222467, 4.000000000000003553 ) ;
#64279=ORIENTED_EDGE ( 'NONE', *, *, #19117, .T. ) ;
#64321=FACE_OUTER_BOUND ( 'NONE', #80357, .T. ) ;
#64334=ORIENTED_EDGE ( 'NONE', *, *, #81753, .F. ) ;
#64363=VECTOR ( 'NONE', #6226, 1000.000000000000000 ) ;
#64373=EDGE_CURVE ( 'NONE', #4242, #34877, #10211, .T. ) ;
#64383=EDGE_CURVE ( 'NONE', #228818, #97848, #75229, .T. ) ;
#64389=CARTESIAN_POINT ( 'NONE',  ( 20.95545211741311320, 65.41358668846766022, -61.93696062493610555 ) ) ;
#64399=DIRECTION ( 'NONE',  ( 1.000000000000000000, 0.000000000000000000, 0.000000000000000000 ) ) ;
#64413=DIRECTION ( 'NONE',  ( 5.421010862427554711E-16, 1.000000000000000000, 1.023556919514279895E-14 ) ) ;
#64426=CARTESIAN_POINT ( 'NONE',  ( -21.13498764882296044, 75.99834360528038246, -76.01872562799826483 ) ) ;
#64449=CARTESIAN_POINT ( 'NONE',  ( -20.64999999999999858, 68.85000000001151932, -48.37310748452436826 ) ) ;
#64462=AXIS2_PLACEMENT_3D ( 'NONE', #250547, #249285, #48495 ) ;
#64473=DIRECTION ( 'NONE',  ( 0.000000000000000000, 0.000000000000000000, 1.000000000000000000 ) ) ;
#64493=CARTESIAN_POINT ( 'NONE',  ( -23.15000000000000213, 71.65000000001151648, -48.37310748452435405 ) ) ;
#64500=CIRCLE ( 'NONE', #210260, 7.900000000000003908 ) ;
#64529=DIRECTION ( 'NONE',  ( 0.000000000000000000, -1.000000000000000000, 0.000000000000000000 ) ) ;
#64535=ORIENTED_EDGE ( 'NONE', *, *, #110074, .F. ) ;
#64551=CARTESIAN_POINT ( 'NONE',  ( -23.25000000000000000, 74.08971962617972906, -48.65447533972326966 ) ) ;
#64573=ORIENTED_EDGE ( 'NONE', *, *, #28805, .T. ) ;
#64614=CIRCLE ( 'NONE', #10478, 0.09999999999999939493 ) ;
#64617=CIRCLE ( 'NONE', #256679, 0.1000000000000028644 ) ;
#64621=PLANE ( 'NONE',  #67312 ) ;
#64683=VERTEX_POINT ( 'NONE', #101808 ) ;
#64684=DIRECTION ( 'NONE',  ( -1.000000000000000000, -0.000000000000000000, -0.000000000000000000 ) ) ;
#64705=ORIENTED_EDGE ( 'NONE', *, *, #192497, .F. ) ;
#64736=CARTESIAN_POINT ( 'NONE',  ( 18.59999999999999076, 65.50857864377418593, -44.67310748452439384 ) ) ;
#64738=ORIENTED_EDGE ( 'NONE', *, *, #137773, .F. ) ;
#64752=AXIS2_PLACEMENT_3D ( 'NONE', #82003, #3793, #142006 ) ;
#64757=CARTESIAN_POINT ( 'NONE',  ( -21.05000000000000071, 76.08579911628613957, -75.93708636601274975 ) ) ;
#64789=CIRCLE ( 'NONE', #139804, 0.1000000000000028644 ) ;
#64792=VERTEX_POINT ( 'NONE', #123988 ) ;
#64813=ORIENTED_EDGE ( 'NONE', *, *, #220569, .F. ) ;
#64855=EDGE_CURVE ( 'NONE', #13565, #232528, #23236, .T. ) ;
#64874=ORIENTED_EDGE ( 'NONE', *, *, #126659, .F. ) ;
#64886=CARTESIAN_POINT ( 'NONE',  ( -23.15000000000000213, 73.40000000001157332, -56.29848556176223440 ) ) ;
#64894=EDGE_CURVE ( 'NONE', #215740, #44321, #53424, .T. ) ;
#64921=VERTEX_POINT ( 'NONE', #208669 ) ;
#64945=VERTEX_POINT ( 'NONE', #233376 ) ;
#64952=CARTESIAN_POINT ( 'NONE',  ( 23.14999999999998437, 76.00000000001165290, -69.52310748452431710 ) ) ;
#64991=ORIENTED_EDGE ( 'NONE', *, *, #41216, .F. ) ;
#65009=EDGE_CURVE ( 'NONE', #99760, #39027, #178536, .T. ) ;
#65023=ADVANCED_FACE ( 'NONE', ( #40317 ), #196771, .F. ) ;
#65027=EDGE_LOOP ( 'NONE', ( #187442, #234807, #101400, #123163 ) ) ;
#65035=VECTOR ( 'NONE', #86958, 1000.000000000000000 ) ;
#65080=ADVANCED_FACE ( 'NONE', ( #234628 ), #195532, .F. ) ;
#65088=EDGE_LOOP ( 'NONE', ( #154515, #48221, #82483, #217906 ) ) ;
#65112=CARTESIAN_POINT ( 'NONE',  ( -22.00356870143097154, 68.74575763753914259, -69.52310748452435973 ) ) ;
#65119=LINE ( 'NONE', #123826, #152633 ) ;
#65120=VERTEX_POINT ( 'NONE', #47970 ) ;
#65145=CARTESIAN_POINT ( 'NONE',  ( 21.14999999999999858, 69.35000000001156195, -57.27310748452436684 ) ) ;
#65158=CARTESIAN_POINT ( 'NONE',  ( -23.15000000000000213, 64.35000000001156195, -57.37310748452439668 ) ) ;
#65161=ORIENTED_EDGE ( 'NONE', *, *, #131737, .F. ) ;
#65162=DIRECTION ( 'NONE',  ( 0.000000000000000000, 0.000000000000000000, -1.000000000000000000 ) ) ;
#65173=EDGE_CURVE ( 'NONE', #36355, #196464, #248255, .T. ) ;
#65190=CARTESIAN_POINT ( 'NONE',  ( -21.14999999999999858, 76.10000000001174669, -81.17267829206912211 ) ) ;
#65217=AXIS2_PLACEMENT_3D ( 'NONE', #22034, #256724, #200660 ) ;
#65271=DIRECTION ( 'NONE',  ( 0.000000000000000000, -6.982962677686266711E-15, 1.000000000000000000 ) ) ;
#65291=AXIS2_PLACEMENT_3D ( 'NONE', #178581, #63730, #81978 ) ;
#65317=CARTESIAN_POINT ( 'NONE',  ( 20.95483826173900255, 67.12383379524162308, -60.97683193162487925 ) ) ;
#65339=EDGE_CURVE ( 'NONE', #108629, #92943, #230474, .T. ) ;
#65345=EDGE_CURVE ( 'NONE', #48405, #47449, #56667, .T. ) ;
#65413=FACE_OUTER_BOUND ( 'NONE', #75835, .T. ) ;
#65418=CARTESIAN_POINT ( 'NONE',  ( -23.15000000000000213, 71.75000000001151079, -48.37310748452435405 ) ) ;
#65419=ORIENTED_EDGE ( 'NONE', *, *, #23237, .F. ) ;
#65448=CIRCLE ( 'NONE', #44794, 0.1000000000000028644 ) ;
#65452=CIRCLE ( 'NONE', #69567, 0.1000000000000017680 ) ;
#65510=CIRCLE ( 'NONE', #211281, 0.09999999999999520384 ) ;
#65516=DIRECTION ( 'NONE',  ( -3.265361837132813093E-16, -1.000000000000000000, -6.982962677686266711E-15 ) ) ;
#65529=AXIS2_PLACEMENT_3D ( 'NONE', #62614, #182574, #80863 ) ;
#65533=EDGE_LOOP ( 'NONE', ( #40456, #222465, #40784 ) ) ;
#65551=EDGE_CURVE ( 'NONE', #225338, #56627, #252507, .T. ) ;
#65552=ADVANCED_FACE ( 'NONE', ( #224995 ), #162505, .F. ) ;
#65587=CARTESIAN_POINT ( 'NONE',  ( -20.94999999999999929, 77.83534155023599510, -57.96795619196132776 ) ) ;
#65634=PLANE ( 'NONE',  #205729 ) ;
#65636=ORIENTED_EDGE ( 'NONE', *, *, #188301, .F. ) ;
#65667=FACE_OUTER_BOUND ( 'NONE', #185529, .T. ) ;
#65678=ORIENTED_EDGE ( 'NONE', *, *, #177768, .T. ) ;
#65697=CARTESIAN_POINT ( 'NONE',  ( 21.13461538461538325, 65.38541703798603066, -57.17310748452439384 ) ) ;
#65700=CARTESIAN_POINT ( 'NONE',  ( -21.14999999999999858, 87.75000000001163869, -66.62310748452424036 ) ) ;
#65728=EDGE_CURVE ( 'NONE', #60411, #111234, #194304, .T. ) ;
#65733=DIRECTION ( 'NONE',  ( -1.000000000000000000, 0.000000000000000000, -0.000000000000000000 ) ) ;
#65738=CARTESIAN_POINT ( 'NONE',  ( -23.15000000000000213, 64.25000000001173817, -81.27310748452440237 ) ) ;
#65820=DIRECTION ( 'NONE',  ( -0.000000000000000000, -1.000000000000000000, -6.982962677686266711E-15 ) ) ;
#65824=VERTEX_POINT ( 'NONE', #253558 ) ;
#65830=ORIENTED_EDGE ( 'NONE', *, *, #185252, .T. ) ;
#65850=VERTEX_POINT ( 'NONE', #174084 ) ;
#65883=DIRECTION ( 'NONE',  ( -1.000000000000000000, -0.000000000000000000, -0.000000000000000000 ) ) ;
#65947=ORIENTED_EDGE ( 'NONE', *, *, #118488, .T. ) ;
#65954=LINE ( 'NONE', #43827, #239994 ) ;
#65959=EDGE_CURVE ( 'NONE', #118151, #36208, #69564, .T. ) ;
#65997=ADVANCED_FACE ( 'NONE', ( #244264 ), #179203, .T. ) ;
#66019=CIRCLE ( 'NONE', #203573, 0.09999999999999939493 ) ;
#66029=EDGE_CURVE ( 'NONE', #100678, #149751, #231890, .T. ) ;
#66031=CARTESIAN_POINT ( 'NONE',  ( -20.85000000000000142, 87.75000000001142553, -36.02310748452423894 ) ) ;
#66038=DIRECTION ( 'NONE',  ( 1.000000000000000000, -0.000000000000000000, 0.000000000000000000 ) ) ;
#66063=EDGE_LOOP ( 'NONE', ( #104711, #207296, #202304, #31699 ) ) ;
#66079=CARTESIAN_POINT ( 'NONE',  ( 21.05000000000000071, 76.00000000001143974, -38.02310748452432421 ) ) ;
#66141=CARTESIAN_POINT ( 'NONE',  ( -18.50000000000000000, 64.35000000001157616, -57.27310748452440237 ) ) ;
#66165=CARTESIAN_POINT ( 'NONE',  ( -18.59999999999999787, 64.35000000001157616, -57.37310748452440379 ) ) ;
#66169=EDGE_CURVE ( 'NONE', #172794, #79018, #115329, .T. ) ;
#66243=VERTEX_POINT ( 'NONE', #192039 ) ;
#66250=ORIENTED_EDGE ( 'NONE', *, *, #151798, .F. ) ;
#66305=CYLINDRICAL_SURFACE ( 'NONE', #169878, 0.09999999999999939493 ) ;
#66346=CARTESIAN_POINT ( 'NONE',  ( 23.14999999999999503, 64.35000000001156195, -57.37310748452439668 ) ) ;
#66350=EDGE_CURVE ( 'NONE', #28556, #85045, #136329, .T. ) ;
#66393=DIRECTION ( 'NONE',  ( 0.000000000000000000, 0.000000000000000000, 1.000000000000000000 ) ) ;
#66398=TOROIDAL_SURFACE ( 'NONE', #24734, 12.77499999999999858, 0.1000000000000000056 ) ;
#66403=ORIENTED_EDGE ( 'NONE', *, *, #177076, .F. ) ;
#66438=ORIENTED_EDGE ( 'NONE', *, *, #194445, .T. ) ;
#66449=AXIS2_PLACEMENT_3D ( 'NONE', #214856, #192744, #14116 ) ;
#66451=CARTESIAN_POINT ( 'NONE',  ( 18.48536876927968109, 85.46352724987909255, -62.47448921944115341 ) ) ;
#66452=CARTESIAN_POINT ( 'NONE',  ( -21.14999999999999858, 76.00000000001173817, -81.17267829206912211 ) ) ;
#66475=EDGE_CURVE ( 'NONE', #119497, #218147, #149720, .T. ) ;
#66476=ORIENTED_EDGE ( 'NONE', *, *, #90529, .T. ) ;
#66483=DIRECTION ( 'NONE',  ( -1.000000000000000000, 0.000000000000000000, 0.000000000000000000 ) ) ;
#66492=AXIS2_PLACEMENT_3D ( 'NONE', #158840, #16757, #238344 ) ;
#66504=EDGE_CURVE ( 'NONE', #79556, #134587, #49304, .T. ) ;
#66530=CARTESIAN_POINT ( 'NONE',  ( -20.54999999999999716, 76.00000000001141132, -34.12310748452431852 ) ) ;
#66558=ORIENTED_EDGE ( 'NONE', *, *, #185727, .F. ) ;
#66564=VECTOR ( 'NONE', #171313, 1000.000000000000000 ) ;
#66565=AXIS2_PLACEMENT_3D ( 'NONE', #165392, #243634, #220240 ) ;
#66568=CARTESIAN_POINT ( 'NONE',  ( -23.25000000000000000, 76.00000000001142553, -36.02310748452432421 ) ) ;
#66583=DIRECTION ( 'NONE',  ( 0.000000000000000000, 6.982962677686266711E-15, -1.000000000000000000 ) ) ;
#66602=DIRECTION ( 'NONE',  ( 1.000000000000000000, 0.000000000000000000, 0.000000000000000000 ) ) ;
#66614=FACE_OUTER_BOUND ( 'NONE', #205830, .T. ) ;
#66615=CARTESIAN_POINT ( 'NONE',  ( 20.95289811251229750, 67.10683199555300860, -61.02129799060586635 ) ) ;
#66652=CARTESIAN_POINT ( 'NONE',  ( -20.54999999999999716, 76.00000000001165290, -69.52310748452431710 ) ) ;
#66654=DIRECTION ( 'NONE',  ( 0.000000000000000000, -7.086529944415894657E-15, 1.000000000000000000 ) ) ;
#66658=ORIENTED_EDGE ( 'NONE', *, *, #138933, .T. ) ;
#66731=VERTEX_POINT ( 'NONE', #24322 ) ;
#66744=ORIENTED_EDGE ( 'NONE', *, *, #96704, .F. ) ;
#66782=EDGE_CURVE ( 'NONE', #162036, #239074, #32538, .T. ) ;
#66828=ORIENTED_EDGE ( 'NONE', *, *, #7308, .F. ) ;
#66843=EDGE_CURVE ( 'NONE', #79119, #160483, #150668, .T. ) ;
#66899=CARTESIAN_POINT ( 'NONE',  ( 20.95595012432475457, 65.39582078693585743, -61.92733815430646871 ) ) ;
#66910=CARTESIAN_POINT ( 'NONE',  ( -23.25000000000000000, 71.85000000001157616, -57.17310748452435121 ) ) ;
#66920=CARTESIAN_POINT ( 'NONE',  ( 20.84999999999998721, 87.75000000001142553, -36.02310748452423894 ) ) ;
#67018=DIRECTION ( 'NONE',  ( 1.000000000000000000, 0.000000000000000000, 0.000000000000000000 ) ) ;
#67048=FACE_OUTER_BOUND ( 'NONE', #115121, .T. ) ;
#67086=CIRCLE ( 'NONE', #204618, 6.329289321881370611 ) ;
#67093=FACE_OUTER_BOUND ( 'NONE', #223992, .T. ) ;
#67094=AXIS2_PLACEMENT_3D ( 'NONE', #75105, #111631, #71241 ) ;
#67098=DIRECTION ( 'NONE',  ( -1.000000000000000000, 0.000000000000000000, 0.000000000000000000 ) ) ;
#67135=EDGE_CURVE ( 'NONE', #47002, #248655, #52102, .T. ) ;
#67154=VERTEX_POINT ( 'NONE', #70851 ) ;
#67161=CARTESIAN_POINT ( 'NONE',  ( 18.59999999999999076, 69.55000000001159322, -59.50608031408435039 ) ) ;
#67197=ORIENTED_EDGE ( 'NONE', *, *, #22329, .T. ) ;
#67243=DIRECTION ( 'NONE',  ( -1.000000000000000000, 2.952720810173289112E-16, 2.061873921506763405E-30 ) ) ;
#67245=CARTESIAN_POINT ( 'NONE',  ( 21.05000000000000071, 76.00000000001165290, -69.42310748452432279 ) ) ;
#67249=EDGE_CURVE ( 'NONE', #215584, #17744, #227742, .T. ) ;
#67277=EDGE_LOOP ( 'NONE', ( #167742, #114457, #107914, #109669 ) ) ;
#67285=CARTESIAN_POINT ( 'NONE',  ( -23.25000000000000000, 71.85000000001151932, -48.27310748452434552 ) ) ;
#67312=AXIS2_PLACEMENT_3D ( 'NONE', #224963, #148024, #163739 ) ;
#67320=AXIS2_PLACEMENT_3D ( 'NONE', #146621, #127083, #25428 ) ;
#67355=VECTOR ( 'NONE', #255295, 1000.000000000000000 ) ;
#67381=DIRECTION ( 'NONE',  ( 0.000000000000000000, 0.000000000000000000, 1.000000000000000000 ) ) ;
#67418=LINE ( 'NONE', #86955, #24155 ) ;
#67420=CIRCLE ( 'NONE', #146519, 0.09999999999999958922 ) ;
#67435=CIRCLE ( 'NONE', #246511, 0.09999999999999939493 ) ;
#67452=AXIS2_PLACEMENT_3D ( 'NONE', #196949, #174888, #159148 ) ;
#67465=CARTESIAN_POINT ( 'NONE',  ( -20.15000000000000568, 66.70857864377425983, -57.27310748452438816 ) ) ;
#67474=DIRECTION ( 'NONE',  ( -1.000000000000000000, 0.000000000000000000, -0.000000000000000000 ) ) ;
#67492=ORIENTED_EDGE ( 'NONE', *, *, #150270, .T. ) ;
#67529=FACE_OUTER_BOUND ( 'NONE', #174362, .T. ) ;
#67542=ORIENTED_EDGE ( 'NONE', *, *, #188144, .F. ) ;
#67548=EDGE_LOOP ( 'NONE', ( #217358, #75193, #230978, #78663 ) ) ;
#67556=DIRECTION ( 'NONE',  ( -1.000000000000000000, 1.836970198721029934E-16, 1.282749433769087582E-30 ) ) ;
#67638=ORIENTED_EDGE ( 'NONE', *, *, #150069, .F. ) ;
#67656=DIRECTION ( 'NONE',  ( -0.000000000000000000, -0.1350103645451807555, -0.9908441862701610203 ) ) ;
#67674=DIRECTION ( 'NONE',  ( -1.000000000000000000, -0.000000000000000000, -0.000000000000000000 ) ) ;
#67701=DIRECTION ( 'NONE',  ( 0.000000000000000000, 0.000000000000000000, 1.000000000000000000 ) ) ;
#67708=AXIS2_PLACEMENT_3D ( 'NONE', #68540, #227598, #148076 ) ;
#67709=DIRECTION ( 'NONE',  ( 1.000000000000000000, 0.000000000000000000, 0.000000000000000000 ) ) ;
#67771=ADVANCED_FACE ( 'NONE', ( #203963 ), #127989, .T. ) ;
#67779=LINE ( 'NONE', #84735, #83206 ) ;
#67780=ORIENTED_EDGE ( 'NONE', *, *, #254255, .F. ) ;
#67782=VERTEX_POINT ( 'NONE', #192138 ) ;
#67812=LINE ( 'NONE', #144760, #127781 ) ;
#67828=ORIENTED_EDGE ( 'NONE', *, *, #241356, .F. ) ;
#67861=CIRCLE ( 'NONE', #60046, 0.1000000000000060146 ) ;
#67923=FACE_OUTER_BOUND ( 'NONE', #61565, .T. ) ;
#67946=ORIENTED_EDGE ( 'NONE', *, *, #207560, .T. ) ;
#68008=DIRECTION ( 'NONE',  ( 1.000000000000000000, 0.000000000000000000, 0.000000000000000000 ) ) ;
#68033=CARTESIAN_POINT ( 'NONE',  ( 21.05000000000000071, 76.10000000001170406, -76.06376443622556849 ) ) ;
#68035=AXIS2_PLACEMENT_3D ( 'NONE', #195864, #70786, #229827 ) ;
#68038=EDGE_CURVE ( 'NONE', #69280, #50336, #186439, .T. ) ;
#68040=VERTEX_POINT ( 'NONE', #207537 ) ;
#68070=ORIENTED_EDGE ( 'NONE', *, *, #196040, .T. ) ;
#68084=ORIENTED_EDGE ( 'NONE', *, *, #216869, .T. ) ;
#68094=ADVANCED_FACE ( 'NONE', ( #25061 ), #187966, .F. ) ;
#68132=ORIENTED_EDGE ( 'NONE', *, *, #87850, .T. ) ;
#68142=AXIS2_PLACEMENT_3D ( 'NONE', #247001, #179672, #140513 ) ;
#68153=DIRECTION ( 'NONE',  ( 1.000000000000000000, -2.952720810173289112E-16, -2.061873921506763405E-30 ) ) ;
#68169=DIRECTION ( 'NONE',  ( 1.000000000000000000, 0.000000000000000000, 0.000000000000000000 ) ) ;
#68194=VERTEX_POINT ( 'NONE', #194402 ) ;
#68198=CARTESIAN_POINT ( 'NONE',  ( -18.59999999999999787, 76.00000000001142553, -36.02310748452432421 ) ) ;
#68215=DIRECTION ( 'NONE',  ( -1.000000000000000000, 0.000000000000000000, 0.000000000000000000 ) ) ;
#68234=CARTESIAN_POINT ( 'NONE',  ( 23.24999999999999289, 64.35000000001173248, -81.27310748452440237 ) ) ;
#68248=DIRECTION ( 'NONE',  ( -1.000000000000000000, 0.000000000000000000, -0.000000000000000000 ) ) ;
#68251=EDGE_CURVE ( 'NONE', #136580, #51183, #161494, .T. ) ;
#68257=CARTESIAN_POINT ( 'NONE',  ( 22.59080734064467677, 64.25000000001165290, -69.55385719262146438 ) ) ;
#68275=CIRCLE ( 'NONE', #9818, 0.1000000000000028644 ) ;
#68318=DIRECTION ( 'NONE',  ( 0.000000000000000000, 0.000000000000000000, -1.000000000000000000 ) ) ;
#68323=ORIENTED_EDGE ( 'NONE', *, *, #97341, .T. ) ;
#68357=CARTESIAN_POINT ( 'NONE',  ( 23.25000000000000000, 87.75000000001173817, -81.27310748452423184 ) ) ;
#68359=AXIS2_PLACEMENT_3D ( 'NONE', #56083, #211340, #71847 ) ;
#68363=VERTEX_POINT ( 'NONE', #238640 ) ;
#68399=CARTESIAN_POINT ( 'NONE',  ( 21.14999999999999858, 69.45000000001157048, -57.37310748452436115 ) ) ;
#68416=DIRECTION ( 'NONE',  ( 0.000000000000000000, -6.853228547068871147E-15, 1.000000000000000000 ) ) ;
#68418=DIRECTION ( 'NONE',  ( -1.000000000000000000, 0.000000000000000000, 0.000000000000000000 ) ) ;
#68426=DIRECTION ( 'NONE',  ( 0.000000000000000000, 0.000000000000000000, -1.000000000000000000 ) ) ;
#68451=EDGE_CURVE ( 'NONE', #61365, #121084, #39189, .T. ) ;
#68485=ORIENTED_EDGE ( 'NONE', *, *, #115307, .T. ) ;
#68499=EDGE_LOOP ( 'NONE', ( #219786, #146212, #4461, #179965 ) ) ;
#68505=EDGE_CURVE ( 'NONE', #199664, #19568, #124081, .T. ) ;
#68512=ADVANCED_FACE ( 'NONE', ( #104238 ), #44959, .F. ) ;
#68517=CARTESIAN_POINT ( 'NONE',  ( -20.94999999999999929, 76.25610579210386675, -69.55800392619661920 ) ) ;
#68540=CARTESIAN_POINT ( 'NONE',  ( 18.39999999999999858, 85.60000000001160458, -62.49103808782458458 ) ) ;
#68574=DIRECTION ( 'NONE',  ( 0.000000000000000000, 0.000000000000000000, -1.000000000000000000 ) ) ;
#68578=DIRECTION ( 'NONE',  ( 1.000000000000000000, -2.952720810173289112E-16, -2.061873921506763405E-30 ) ) ;
#68610=DIRECTION ( 'NONE',  ( -0.000000000000000000, 0.8660254037844377084, 0.5000000000000016653 ) ) ;
#68654=CARTESIAN_POINT ( 'NONE',  ( 20.94999999999999929, 64.35000000001146248, -42.80697314750249660 ) ) ;
#68666=UNCERTAINTY_MEASURE_WITH_UNIT (LENGTH_MEASURE( 1.000000000000000082E-05 ), #32308, 'distance_accuracy_value', 'NONE');
#68677=CARTESIAN_POINT ( 'NONE',  ( -20.94999999999999929, 77.73625713160897988, -57.95445515550681392 ) ) ;
#68701=CARTESIAN_POINT ( 'NONE',  ( -21.98333005346336932, 76.00000000001170974, -76.89718281358099716 ) ) ;
#68708=FACE_OUTER_BOUND ( 'NONE', #39816, .T. ) ;
#68717=ORIENTED_EDGE ( 'NONE', *, *, #43549, .T. ) ;
#68719=AXIS2_PLACEMENT_3D ( 'NONE', #18368, #178768, #222975 ) ;
#68745=CARTESIAN_POINT ( 'NONE',  ( 21.05000000000000071, 76.10000000001174669, -81.17267829206912211 ) ) ;
#68750=CIRCLE ( 'NONE', #135366, 0.1000000000000017680 ) ;
#68786=CARTESIAN_POINT ( 'NONE',  ( -23.25000000000000000, 71.65000000001151648, -48.17310748452435831 ) ) ;
#68826=DIRECTION ( 'NONE',  ( 1.000000000000000000, -0.000000000000000000, 0.000000000000000000 ) ) ;
#68839=ORIENTED_EDGE ( 'NONE', *, *, #52888, .T. ) ;
#68857=ORIENTED_EDGE ( 'NONE', *, *, #64093, .F. ) ;
#68858=ORIENTED_EDGE ( 'NONE', *, *, #198394, .F. ) ;
#68933=DIRECTION ( 'NONE',  ( 0.000000000000000000, -0.1350103645451945777, 0.9908441862701590219 ) ) ;
#69015=DIRECTION ( 'NONE',  ( 1.000000000000000000, 0.000000000000000000, 0.000000000000000000 ) ) ;
#69016=DIRECTION ( 'NONE',  ( 1.000000000000000000, -3.469446951953718318E-14, 2.003086131649645455E-14 ) ) ;
#69027=DIRECTION ( 'NONE',  ( 0.000000000000000000, 0.000000000000000000, 1.000000000000000000 ) ) ;
#69070=EDGE_CURVE ( 'NONE', #201868, #182718, #49100, .T. ) ;
#69073=ADVANCED_FACE ( 'NONE', ( #256221 ), #219726, .T. ) ;
#69074=EDGE_LOOP ( 'NONE', ( #50394, #78869, #237601, #145599 ) ) ;
#69088=ORIENTED_EDGE ( 'NONE', *, *, #32016, .T. ) ;
#69095=CARTESIAN_POINT ( 'NONE',  ( -21.55000000000000426, 68.29142135624881860, -48.27310748452437394 ) ) ;
#69104=CARTESIAN_POINT ( 'NONE',  ( -23.15000000000000213, 74.00000000001151079, -48.74772940728643533 ) ) ;
#69125=CARTESIAN_POINT ( 'NONE',  ( -21.52071067811865746, 68.22071067813014622, -48.27310748452437394 ) ) ;
#69128=VECTOR ( 'NONE', #82355, 1000.000000000000000 ) ;
#69151=ORIENTED_EDGE ( 'NONE', *, *, #111961, .F. ) ;
#69172=CARTESIAN_POINT ( 'NONE',  ( 23.25000000000000000, 69.45000000001157048, -57.17310748452436542 ) ) ;
#69207=DIRECTION ( 'NONE',  ( 1.000000000000000000, 0.000000000000000000, 0.000000000000000000 ) ) ;
#69234=ORIENTED_EDGE ( 'NONE', *, *, #236942, .T. ) ;
#69278=DIRECTION ( 'NONE',  ( 0.000000000000000000, 0.000000000000000000, 1.000000000000000000 ) ) ;
#69280=VERTEX_POINT ( 'NONE', #145323 ) ;
#69281=ORIENTED_EDGE ( 'NONE', *, *, #153128, .T. ) ;
#69332=CARTESIAN_POINT ( 'NONE',  ( 21.05000000000000071, 76.08561306081568887, -75.93686721833462627 ) ) ;
#69374=CARTESIAN_POINT ( 'NONE',  ( -18.46907102845854709, 85.47372736477545629, -29.34707274578775582 ) ) ;
#69375=EDGE_CURVE ( 'NONE', #110098, #119594, #35384, .T. ) ;
#69378=VERTEX_POINT ( 'NONE', #151458 ) ;
#69410=EDGE_LOOP ( 'NONE', ( #244030, #60707, #186180, #69281 ) ) ;
#69424=ORIENTED_EDGE ( 'NONE', *, *, #141188, .T. ) ;
#69433=EDGE_CURVE ( 'NONE', #218543, #249063, #226799, .T. ) ;
#69524=VERTEX_POINT ( 'NONE', #120048 ) ;
#69545=CARTESIAN_POINT ( 'NONE',  ( -20.64999999999999858, 71.75000000001156764, -57.17310748452435121 ) ) ;
#69564=CIRCLE ( 'NONE', #19499, 2.100000000000004530 ) ;
#69567=AXIS2_PLACEMENT_3D ( 'NONE', #215571, #197294, #55183 ) ;
#69594=ORIENTED_EDGE ( 'NONE', *, *, #219815, .F. ) ;
#69611=DIRECTION ( 'NONE',  ( 1.000000000000000000, 0.000000000000000000, 0.000000000000000000 ) ) ;
#69619=ORIENTED_EDGE ( 'NONE', *, *, #148272, .F. ) ;
#69620=DIRECTION ( 'NONE',  ( 0.000000000000000000, 0.000000000000000000, 1.000000000000000000 ) ) ;
#69632=AXIS2_PLACEMENT_3D ( 'NONE', #60437, #20057, #237809 ) ;
#69667=EDGE_CURVE ( 'NONE', #38617, #45256, #81034, .T. ) ;
#69680=EDGE_CURVE ( 'NONE', #28771, #152443, #139291, .T. ) ;
#69682=EDGE_CURVE ( 'NONE', #14406, #155813, #72713, .T. ) ;
#69684=CARTESIAN_POINT ( 'NONE',  ( -22.59999999999999787, 64.25012875563515991, -69.58853707553808476 ) ) ;
#69750=VECTOR ( 'NONE', #49777, 1000.000000000000000 ) ;
#69752=VERTEX_POINT ( 'NONE', #72914 ) ;
#69761=DIRECTION ( 'NONE',  ( -1.000000000000000000, 2.952720810173289112E-16, 2.061873921506763405E-30 ) ) ;
#69770=CARTESIAN_POINT ( 'NONE',  ( -20.64999999999999858, 85.00000000001159606, -60.12913836187181715 ) ) ;
#69772=EDGE_CURVE ( 'NONE', #146292, #83438, #201855, .T. ) ;
#69812=AXIS2_PLACEMENT_3D ( 'NONE', #64952, #201909, #246174 ) ;
#69816=ORIENTED_EDGE ( 'NONE', *, *, #255381, .F. ) ;
#69851=FACE_OUTER_BOUND ( 'NONE', #27065, .T. ) ;
#69887=FACE_OUTER_BOUND ( 'NONE', #127431, .T. ) ;
#69942=CARTESIAN_POINT ( 'NONE',  ( -20.64999999999999858, 68.85000000001151932, -48.37310748452436826 ) ) ;
#69950=CARTESIAN_POINT ( 'NONE',  ( 20.96077737575330247, 64.37609936600661342, -42.88231552741775943 ) ) ;
#69964=DIRECTION ( 'NONE',  ( -1.000000000000000000, 0.000000000000000000, -0.000000000000000000 ) ) ;
#69966=DIRECTION ( 'NONE',  ( 0.000000000000000000, 0.9654727137038715545, -0.2605042016806676242 ) ) ;
#69968=CARTESIAN_POINT ( 'NONE',  ( -21.05000000000000426, 64.40000000001161595, -62.59490425424885274 ) ) ;
#69987=DIRECTION ( 'NONE',  ( -1.000000000000000000, 0.000000000000000000, -0.000000000000000000 ) ) ;
#70057=ORIENTED_EDGE ( 'NONE', *, *, #106856, .F. ) ;
#70058=FACE_OUTER_BOUND ( 'NONE', #118252, .T. ) ;
#70064=VERTEX_POINT ( 'NONE', #246079 ) ;
#70085=AXIS2_PLACEMENT_3D ( 'NONE', #169509, #166933, #89911 ) ;
#70172=DIRECTION ( 'NONE',  ( -0.000000000000000000, 6.982962677686266711E-15, -1.000000000000000000 ) ) ;
#70173=CIRCLE ( 'NONE', #178496, 0.09999999999999939493 ) ;
#70183=ORIENTED_EDGE ( 'NONE', *, *, #208089, .F. ) ;
#70209=EDGE_CURVE ( 'NONE', #238726, #206520, #217729, .T. ) ;
#70212=DIRECTION ( 'NONE',  ( -3.265361837132813093E-16, -1.000000000000000000, 7.445645354460596589E-46 ) ) ;
#70220=ORIENTED_EDGE ( 'NONE', *, *, #211029, .F. ) ;
#70225=DIRECTION ( 'NONE',  ( 0.7071067811865475727, 0.7071067811865475727, 4.937700262164531476E-15 ) ) ;
#70232=ADVANCED_FACE ( 'NONE', ( #234186 ), #231289, .T. ) ;
#70234=ORIENTED_EDGE ( 'NONE', *, *, #118793, .T. ) ;
#70278=ADVANCED_FACE ( 'NONE', ( #174282 ), #84412, .T. ) ;
#70298=FACE_OUTER_BOUND ( 'NONE', #181741, .T. ) ;
#70304=EDGE_CURVE ( 'NONE', #13565, #16741, #41166, .T. ) ;
#70326=EDGE_CURVE ( 'NONE', #208846, #41312, #56285, .T. ) ;
#70330=CARTESIAN_POINT ( 'NONE',  ( -20.85000000000000142, 77.83585931145498193, -24.41866831572578533 ) ) ;
#70345=DIRECTION ( 'NONE',  ( -1.000000000000000000, 0.000000000000000000, -0.000000000000000000 ) ) ;
#70394=EDGE_LOOP ( 'NONE', ( #169325, #4050, #221303, #236829, #246086 ) ) ;
#70400=DIRECTION ( 'NONE',  ( 0.000000000000000000, -6.467318590049456648E-15, 1.000000000000000000 ) ) ;
#70433=DIRECTION ( 'NONE',  ( 0.000000000000000000, 0.9908441862701605762, 0.1350103645451835310 ) ) ;
#70436=DIRECTION ( 'NONE',  ( 0.000000000000000000, 1.000000000000000000, 6.938893903907222067E-15 ) ) ;
#70459=PLANE ( 'NONE',  #80470 ) ;
#70483=FACE_OUTER_BOUND ( 'NONE', #240295, .T. ) ;
#70492=DIRECTION ( 'NONE',  ( 0.000000000000000000, 6.982962677686266711E-15, -1.000000000000000000 ) ) ;
#70499=CARTESIAN_POINT ( 'NONE',  ( 20.95392731769792150, 67.11693852082284195, -61.00087950495308320 ) ) ;
#70555=CARTESIAN_POINT ( 'NONE',  ( -23.15000000000000213, 87.41227409416113403, -39.02310748452423894 ) ) ;
#70564=CIRCLE ( 'NONE', #174636, 0.1000000000000028644 ) ;
#70646=AXIS2_PLACEMENT_3D ( 'NONE', #198698, #154475, #59148 ) ;
#70665=VERTEX_POINT ( 'NONE', #197324 ) ;
#70715=ORIENTED_EDGE ( 'NONE', *, *, #125252, .T. ) ;
#70716=CARTESIAN_POINT ( 'NONE',  ( 18.47654891039379166, 85.46527494839392602, -62.39713157932961707 ) ) ;
#70741=CIRCLE ( 'NONE', #208104, 0.09999999999999939493 ) ;
#70749=EDGE_CURVE ( 'NONE', #60391, #117855, #94066, .T. ) ;
#70786=DIRECTION ( 'NONE',  ( -1.000000000000000000, -0.000000000000000000, -0.000000000000000000 ) ) ;
#70803=CARTESIAN_POINT ( 'NONE',  ( -21.37071067811865532, 67.92928932189292368, -57.27310748452438105 ) ) ;
#70804=DIRECTION ( 'NONE',  ( 0.000000000000000000, -7.304098846218112382E-15, 1.000000000000000000 ) ) ;
#70833=CARTESIAN_POINT ( 'NONE',  ( 20.95576188350343116, 65.39101945504820890, -61.91187376177009583 ) ) ;
#70845=AXIS2_PLACEMENT_3D ( 'NONE', #95911, #223248, #240274 ) ;
#70851=CARTESIAN_POINT ( 'NONE',  ( 18.49999999999999645, 77.16270174994961906, -61.42310748452431568 ) ) ;
#70865=CARTESIAN_POINT ( 'NONE',  ( 23.24999999999999289, 69.35000000001151932, -48.37310748452436826 ) ) ;
#70868=CARTESIAN_POINT ( 'NONE',  ( 20.85000000000000142, 68.92903212821255465, -32.27654326265606954 ) ) ;
#70881=DIRECTION ( 'NONE',  ( 0.000000000000000000, -1.000000000000000000, -6.982962677686265922E-15 ) ) ;
#70903=LINE ( 'NONE', #74767, #66564 ) ;
#70922=ORIENTED_EDGE ( 'NONE', *, *, #174852, .T. ) ;
#70931=AXIS2_PLACEMENT_3D ( 'NONE', #10275, #169379, #128935 ) ;
#70948=EDGE_CURVE ( 'NONE', #131663, #253340, #225426, .T. ) ;
#70963=CARTESIAN_POINT ( 'NONE',  ( -21.05000000000000071, 85.51932773110404185, -62.55013110796492271 ) ) ;
#70971=DIRECTION ( 'NONE',  ( -3.265361837132813093E-16, -1.000000000000000000, 7.445645354460596589E-46 ) ) ;
#70996=TOROIDAL_SURFACE ( 'NONE', #216712, 0.2000000000000000111, 0.1000000000000000056 ) ;
#71017=DIRECTION ( 'NONE',  ( -1.000000000000000000, -0.000000000000000000, -0.000000000000000000 ) ) ;
#71037=EDGE_CURVE ( 'NONE', #198432, #88303, #23571, .T. ) ;
#71038=CIRCLE ( 'NONE', #116801, 0.09999999999999939493 ) ;
#71068=DIRECTION ( 'NONE',  ( -1.000000000000000000, 2.952720810173289112E-16, 2.061873921506763405E-30 ) ) ;
#71074=DIRECTION ( 'NONE',  ( 0.000000000000000000, 0.1298341882519953583, 0.9915357197604861561 ) ) ;
#71143=CARTESIAN_POINT ( 'NONE',  ( 20.94999999999999574, 87.48912529308769592, -66.42310748452423752 ) ) ;
#71234=ORIENTED_EDGE ( 'NONE', *, *, #8409, .T. ) ;
#71241=DIRECTION ( 'NONE',  ( 0.000000000000000000, 0.000000000000000000, 1.000000000000000000 ) ) ;
#71268=DIRECTION ( 'NONE',  ( 1.000000000000000000, 0.000000000000000000, 0.000000000000000000 ) ) ;
#71271=EDGE_CURVE ( 'NONE', #4242, #212844, #89976, .T. ) ;
#71276=EDGE_LOOP ( 'NONE', ( #167438, #247113, #182920, #68857 ) ) ;
#71277=ORIENTED_EDGE ( 'NONE', *, *, #137245, .T. ) ;
#71302=ORIENTED_EDGE ( 'NONE', *, *, #182170, .F. ) ;
#71311=ORIENTED_EDGE ( 'NONE', *, *, #152456, .F. ) ;
#71319=DIRECTION ( 'NONE',  ( -1.000000000000000000, 0.000000000000000000, 0.000000000000000000 ) ) ;
#71331=DIRECTION ( 'NONE',  ( 0.000000000000000000, 0.000000000000000000, 1.000000000000000000 ) ) ;
#71368=EDGE_CURVE ( 'NONE', #37986, #201109, #55540, .T. ) ;
#71376=EDGE_CURVE ( 'NONE', #215584, #208846, #86030, .T. ) ;
#71427=ORIENTED_EDGE ( 'NONE', *, *, #237285, .F. ) ;
#71428=ORIENTED_EDGE ( 'NONE', *, *, #228046, .F. ) ;
#71444=ORIENTED_EDGE ( 'NONE', *, *, #18581, .F. ) ;
#71455=ORIENTED_EDGE ( 'NONE', *, *, #75336, .F. ) ;
#71478=DIRECTION ( 'NONE',  ( 0.000000000000000000, -7.109473446599835262E-15, 1.000000000000000000 ) ) ;
#71566=ADVANCED_FACE ( 'NONE', ( #46272 ), #81526, .T. ) ;
#71567=DIRECTION ( 'NONE',  ( -0.000000000000000000, -6.982962677686266711E-15, 1.000000000000000000 ) ) ;
#71573=ORIENTED_EDGE ( 'NONE', *, *, #199354, .F. ) ;
#71580=CARTESIAN_POINT ( 'NONE',  ( 22.44352723754029810, 75.99072290496846449, -81.17282882987304049 ) ) ;
#71583=EDGE_CURVE ( 'NONE', #221113, #205489, #206869, .T. ) ;
#71620=AXIS2_PLACEMENT_3D ( 'NONE', #236169, #21006, #22277 ) ;
#71640=CARTESIAN_POINT ( 'NONE',  ( -18.59999999999999787, 64.35000000001150511, -48.27310748452440237 ) ) ;
#71690=AXIS2_PLACEMENT_3D ( 'NONE', #39041, #182398, #41615 ) ;
#71747=CARTESIAN_POINT ( 'NONE',  ( 22.00411653962175862, 68.74655713164172255, -69.62214559032500460 ) ) ;
#71810=CARTESIAN_POINT ( 'NONE',  ( -21.05000000000000071, 87.65000000001163016, -66.52310748452423184 ) ) ;
#71815=CIRCLE ( 'NONE', #134134, 0.1000000000000028644 ) ;
#71833=AXIS2_PLACEMENT_3D ( 'NONE', #118593, #64684, #177296 ) ;
#71835=VERTEX_POINT ( 'NONE', #180371 ) ;
#71846=ORIENTED_EDGE ( 'NONE', *, *, #236942, .F. ) ;
#71847=DIRECTION ( 'NONE',  ( 0.000000000000000000, 0.000000000000000000, 1.000000000000000000 ) ) ;
#71877=ORIENTED_EDGE ( 'NONE', *, *, #219815, .T. ) ;
#71885=B_SPLINE_CURVE_WITH_KNOTS ( 'NONE', 3,
 ( #167252, #206357, #208910, #70716, #111095, #171120, #245486, #195794, #34165, #15879 ),
 .UNSPECIFIED., .F., .F.,
 ( 4, 2, 2, 2, 4 ),
 ( 0.000000000000000000, 0.0001584437871624896237, 0.0002376656807437438411, 0.0002772766275343796776, 0.0003168875743250154598 ),
 .UNSPECIFIED. ) ;
#71888=VERTEX_POINT ( 'NONE', #184200 ) ;
#71889=EDGE_CURVE ( 'NONE', #82836, #91161, #194618, .T. ) ;
#71908=DIRECTION ( 'NONE',  ( -1.000000000000000000, 0.000000000000000000, 0.000000000000000000 ) ) ;
#71916=CARTESIAN_POINT ( 'NONE',  ( -20.94999999999999929, 76.00000000001142553, -36.02310748452432421 ) ) ;
#71928=TOROIDAL_SURFACE ( 'NONE', #101066, 11.65000000000000036, 0.1000000000000000056 ) ;
#71931=CARTESIAN_POINT ( 'NONE',  ( 21.05000000000000071, 71.00000000001151079, -47.92837350343745584 ) ) ;
#71935=ORIENTED_EDGE ( 'NONE', *, *, #33729, .T. ) ;
#71955=ORIENTED_EDGE ( 'NONE', *, *, #135745, .F. ) ;
#71956=ORIENTED_EDGE ( 'NONE', *, *, #145568, .T. ) ;
#71958=DIRECTION ( 'NONE',  ( 0.000000000000000000, -1.000000000000000000, 0.000000000000000000 ) ) ;
#71959=ADVANCED_FACE ( 'NONE', ( #231069 ), #107099, .T. ) ;
#71960=ORIENTED_EDGE ( 'NONE', *, *, #169563, .F. ) ;
#71961=CARTESIAN_POINT ( 'NONE',  ( 20.94999999999999929, 87.48912529308749697, -39.12310748452424747 ) ) ;
#71964=CIRCLE ( 'NONE', #92787, 11.74999999999999645 ) ;
#71981=CARTESIAN_POINT ( 'NONE',  ( 20.46382478191414833, 67.09862044130898084, -60.97737938964129967 ) ) ;
#72030=ORIENTED_EDGE ( 'NONE', *, *, #206876, .F. ) ;
#72034=EDGE_LOOP ( 'NONE', ( #49404, #62528, #168167, #112933 ) ) ;
#72049=ORIENTED_EDGE ( 'NONE', *, *, #93162, .F. ) ;
#72054=EDGE_CURVE ( 'NONE', #206496, #88538, #71885, .T. ) ;
#72061=CARTESIAN_POINT ( 'NONE',  ( -18.50000000000000000, 66.75000000001151079, -48.27310748452438816 ) ) ;
#72062=DIRECTION ( 'NONE',  ( 1.000000000000000000, 0.000000000000000000, -0.000000000000000000 ) ) ;
#72070=DIRECTION ( 'NONE',  ( 0.000000000000000000, -7.026728003956686545E-15, 1.000000000000000000 ) ) ;
#72080=ORIENTED_EDGE ( 'NONE', *, *, #168381, .T. ) ;
#72093=CIRCLE ( 'NONE', #251113, 0.5000000000000004441 ) ;
#72096=DIRECTION ( 'NONE',  ( -1.000000000000000000, 2.952720810173289112E-16, 2.061873921506763405E-30 ) ) ;
#72108=CARTESIAN_POINT ( 'NONE',  ( 23.24999999999999289, 69.35000000001156195, -57.17310748452436542 ) ) ;
#72127=LINE ( 'NONE', #169973, #198437 ) ;
#72137=DIRECTION ( 'NONE',  ( 0.000000000000000000, -1.000000000000000000, -6.982962677686265922E-15 ) ) ;
#72174=CARTESIAN_POINT ( 'NONE',  ( 18.49999999999999289, 69.35000000001151932, -48.17310748452437252 ) ) ;
#72194=VERTEX_POINT ( 'NONE', #39289 ) ;
#72221=ORIENTED_EDGE ( 'NONE', *, *, #23448, .F. ) ;
#72230=DIRECTION ( 'NONE',  ( 0.000000000000000000, -6.982962677686266711E-15, 1.000000000000000000 ) ) ;
#72237=CARTESIAN_POINT ( 'NONE',  ( -22.50000000000000000, 76.00000000001169553, -75.77310748452431710 ) ) ;
#72241=DIRECTION ( 'NONE',  ( -1.000000000000000000, 0.000000000000000000, -0.000000000000000000 ) ) ;
#72287=TOROIDAL_SURFACE ( 'NONE', #76344, 0.2000000000000000111, 0.1000000000000000056 ) ;
#72294=FACE_OUTER_BOUND ( 'NONE', #241548, .T. ) ;
#72330=B_SPLINE_CURVE_WITH_KNOTS ( 'NONE', 3,
 ( #20132, #200047, #18827, #218290, #82621, #81339, #201319, #61820, #141348, #40997 ),
 .UNSPECIFIED., .F., .F.,
 ( 4, 3, 3, 4 ),
 ( 1.551583845779545699E-17, 0.0002000000000002884074, 0.001000000000045107602, 0.001967863649472132576 ),
 .UNSPECIFIED. ) ;
#72374=EDGE_CURVE ( 'NONE', #70665, #88995, #115093, .T. ) ;
#72375=CARTESIAN_POINT ( 'NONE',  ( 21.05000000000000071, 84.73084112150679914, -45.62118220350859588 ) ) ;
#72397=AXIS2_PLACEMENT_3D ( 'NONE', #88919, #228466, #49807 ) ;
#72450=DIRECTION ( 'NONE',  ( 0.000000000000000000, -0.9915357197604892647, 0.1298341882519715440 ) ) ;
#72486=FACE_OUTER_BOUND ( 'NONE', #17127, .T. ) ;
#72534=DIRECTION ( 'NONE',  ( 0.000000000000000000, 0.9999176327611370985, -0.01283462868041289687 ) ) ;
#72542=CYLINDRICAL_SURFACE ( 'NONE', #105856, 0.1000000000000028644 ) ;
#72559=LINE ( 'NONE', #131225, #230137 ) ;
#72587=ORIENTED_EDGE ( 'NONE', *, *, #184829, .T. ) ;
#72591=EDGE_LOOP ( 'NONE', ( #103716, #43059, #104997, #94919 ) ) ;
#72608=ADVANCED_FACE ( 'NONE', ( #180718 ), #2049, .T. ) ;
#72637=CARTESIAN_POINT ( 'NONE',  ( -22.39999999999999858, 64.35000000001166143, -69.62310748452439668 ) ) ;
#72657=CARTESIAN_POINT ( 'NONE',  ( -20.54999999999999716, 76.00000000001143974, -38.02310748452432421 ) ) ;
#72671=VERTEX_POINT ( 'NONE', #46316 ) ;
#72693=CARTESIAN_POINT ( 'NONE',  ( -18.50000000000000000, 74.16465844978715438, -57.96795619196135618 ) ) ;
#72700=ADVANCED_FACE ( 'NONE', ( #184544 ), #206694, .F. ) ;
#72707=ORIENTED_EDGE ( 'NONE', *, *, #130000, .F. ) ;
#72709=DIRECTION ( 'NONE',  ( 1.000000000000000000, 0.000000000000000000, 0.000000000000000000 ) ) ;
#72713=CIRCLE ( 'NONE', #201676, 0.09999999999999938105 ) ;
#72727=DIRECTION ( 'NONE',  ( 0.000000000000000000, -0.5000000000000016653, 0.8660254037844377084 ) ) ;
#72780=LINE ( 'NONE', #170618, #143794 ) ;
#72794=AXIS2_PLACEMENT_3D ( 'NONE', #194357, #191791, #253009 ) ;
#72840=CARTESIAN_POINT ( 'NONE',  ( 21.05000000000000071, 70.60000000001149090, -45.91707660717680284 ) ) ;
#72849=ORIENTED_EDGE ( 'NONE', *, *, #248251, .F. ) ;
#72888=EDGE_LOOP ( 'NONE', ( #214491, #254100, #183515 ) ) ;
#72914=CARTESIAN_POINT ( 'NONE',  ( -20.54999999999999716, 85.00000000001149658, -45.51707660717670478 ) ) ;
#72952=ORIENTED_EDGE ( 'NONE', *, *, #103292, .F. ) ;
#72971=ORIENTED_EDGE ( 'NONE', *, *, #61826, .T. ) ;
#73046=CARTESIAN_POINT ( 'NONE',  ( -18.59999999999999787, 68.97833521811131163, -32.28954208262708647 ) ) ;
#73059=CARTESIAN_POINT ( 'NONE',  ( -21.04999999999999716, 69.45934304831042994, -69.52310748452438816 ) ) ;
#73064=LINE ( 'NONE', #112172, #251080 ) ;
#73075=DIRECTION ( 'NONE',  ( -0.7070776581709311559, 4.937903618720164857E-15, -0.7071359030027479786 ) ) ;
#73114=CARTESIAN_POINT ( 'NONE',  ( 22.49231231312462853, 64.35001509633437422, -69.58416037212577976 ) ) ;
#73122=ORIENTED_EDGE ( 'NONE', *, *, #242921, .T. ) ;
#73140=LINE ( 'NONE', #127948, #201036 ) ;
#73141=DIRECTION ( 'NONE',  ( 0.000000000000000000, 0.000000000000000000, -1.000000000000000000 ) ) ;
#73149=ORIENTED_EDGE ( 'NONE', *, *, #42570, .F. ) ;
#73157=ADVANCED_FACE ( 'NONE', ( #15925 ), #95429, .T. ) ;
#73181=EDGE_CURVE ( 'NONE', #93396, #230638, #217567, .T. ) ;
#73191=DIRECTION ( 'NONE',  ( -0.000000000000000000, 6.982962677686266711E-15, -1.000000000000000000 ) ) ;
#73236=ADVANCED_FACE ( 'NONE', ( #58840 ), #215415, .F. ) ;
#73241=VECTOR ( 'NONE', #67474, 1000.000000000000000 ) ;
#73251=VERTEX_POINT ( 'NONE', #24907 ) ;
#73255=ORIENTED_EDGE ( 'NONE', *, *, #224874, .T. ) ;
#73302=ORIENTED_EDGE ( 'NONE', *, *, #70209, .F. ) ;
#73347=ORIENTED_EDGE ( 'NONE', *, *, #121852, .F. ) ;
#73351=EDGE_CURVE ( 'NONE', #224073, #235880, #28193, .T. ) ;
#73365=VERTEX_POINT ( 'NONE', #143534 ) ;
#73377=CIRCLE ( 'NONE', #85202, 0.5000000000000004441 ) ;
#73386=ORIENTED_EDGE ( 'NONE', *, *, #252822, .T. ) ;
#73419=AXIS2_PLACEMENT_3D ( 'NONE', #74092, #17920, #97437 ) ;
#73424=DIRECTION ( 'NONE',  ( 0.000000000000000000, -0.9998779222360104635, -0.01562499999996343723 ) ) ;
#73446=ORIENTED_EDGE ( 'NONE', *, *, #34626, .T. ) ;
#73460=DIRECTION ( 'NONE',  ( 0.000000000000000000, 0.000000000000000000, 1.000000000000000000 ) ) ;
#73467=CARTESIAN_POINT ( 'NONE',  ( -20.94999999999999929, 74.83729825007360148, -61.62310748452433273 ) ) ;
#73489=CIRCLE ( 'NONE', #248412, 7.720710678118663850 ) ;
#73495=ORIENTED_EDGE ( 'NONE', *, *, #256880, .T. ) ;
#73512=ADVANCED_FACE ( 'NONE', ( #247777 ), #90498, .T. ) ;
#73514=AXIS2_PLACEMENT_3D ( 'NONE', #41630, #201971, #22059 ) ;
#73517=DIRECTION ( 'NONE',  ( 1.000000000000000000, 0.000000000000000000, 0.000000000000000000 ) ) ;
#73544=AXIS2_PLACEMENT_3D ( 'NONE', #140044, #176650, #155809 ) ;
#73551=EDGE_LOOP ( 'NONE', ( #167939, #71444, #231036, #162083 ) ) ;
#73575=AXIS2_PLACEMENT_3D ( 'NONE', #149097, #10860, #73424 ) ;
#73581=CARTESIAN_POINT ( 'NONE',  ( 21.12642695952774119, 75.90109671682233738, -75.89876740655950016 ) ) ;
#73584=AXIS2_PLACEMENT_3D ( 'NONE', #114223, #193764, #75128 ) ;
#73586=CIRCLE ( 'NONE', #215207, 0.09999999999999939493 ) ;
#73587=CARTESIAN_POINT ( 'NONE',  ( 21.11344571971309136, 65.38212097649309840, -57.27708659212506603 ) ) ;
#73609=CARTESIAN_POINT ( 'NONE',  ( -18.59999999999999787, 77.83534155023598089, -57.86795619196132634 ) ) ;
#73616=PLANE ( 'NONE',  #35176 ) ;
#73652=FACE_OUTER_BOUND ( 'NONE', #112474, .T. ) ;
#73674=AXIS2_PLACEMENT_3D ( 'NONE', #120513, #202587, #103463 ) ;
#73714=TOROIDAL_SURFACE ( 'NONE', #219414, 0.6000000000000004219, 0.1000000000000000056 ) ;
#73722=ORIENTED_EDGE ( 'NONE', *, *, #234061, .T. ) ;
#73767=CIRCLE ( 'NONE', #231983, 0.5000000000000004441 ) ;
#73768=VECTOR ( 'NONE', #133289, 1000.000000000000000 ) ;
#73778=EDGE_CURVE ( 'NONE', #175343, #90665, #209361, .T. ) ;
#73791=DIRECTION ( 'NONE',  ( 0.000000000000000000, 0.000000000000000000, 1.000000000000000000 ) ) ;
#73794=FACE_OUTER_BOUND ( 'NONE', #159355, .T. ) ;
#73813=ORIENTED_EDGE ( 'NONE', *, *, #177621, .T. ) ;
#73826=EDGE_CURVE ( 'NONE', #126775, #209328, #232373, .T. ) ;
#73878=EDGE_CURVE ( 'NONE', #236713, #199664, #161642, .T. ) ;
#73884=CARTESIAN_POINT ( 'NONE',  ( 18.49999999999999289, 65.50857864377418593, -44.67310748452439384 ) ) ;
#73891=CARTESIAN_POINT ( 'NONE',  ( 21.04999999999999716, 69.70076908992476206, -69.62154498452436258 ) ) ;
#73905=DIRECTION ( 'NONE',  ( -0.000000000000000000, 0.1298341882520009927, 0.9915357197604854900 ) ) ;
#73951=DIRECTION ( 'NONE',  ( 1.000000000000000000, 0.000000000000000000, 0.000000000000000000 ) ) ;
#73969=CARTESIAN_POINT ( 'NONE',  ( -20.07928932188135107, 66.77928932189291800, -57.17310748452438673 ) ) ;
#73978=ORIENTED_EDGE ( 'NONE', *, *, #57231, .T. ) ;
#73979=VECTOR ( 'NONE', #67556, 1000.000000000000000 ) ;
#73988=CARTESIAN_POINT ( 'NONE',  ( 21.05000000000000071, 77.16270174994961906, -61.42310748452431568 ) ) ;
#74035=ORIENTED_EDGE ( 'NONE', *, *, #222822, .F. ) ;
#74069=EDGE_CURVE ( 'NONE', #89706, #206520, #63051, .T. ) ;
#74081=ADVANCED_FACE ( 'NONE', ( #186887 ), #184288, .F. ) ;
#74092=CARTESIAN_POINT ( 'NONE',  ( 23.14999999999998792, 64.35000000001166143, -69.52310748452440237 ) ) ;
#74103=DIRECTION ( 'NONE',  ( 0.000000000000000000, 6.982962677686266711E-15, -1.000000000000000000 ) ) ;
#74105=CYLINDRICAL_SURFACE ( 'NONE', #141264, 0.1000000000000028644 ) ;
#74122=ORIENTED_EDGE ( 'NONE', *, *, #82305, .F. ) ;
#74129=TOROIDAL_SURFACE ( 'NONE', #190643, 11.70000000000000107, 0.1000000000000000056 ) ;
#74136=DIRECTION ( 'NONE',  ( 0.000000000000000000, 0.000000000000000000, 1.000000000000000000 ) ) ;
#74202=DIRECTION ( 'NONE',  ( -1.000000000000000000, -0.000000000000000000, -0.000000000000000000 ) ) ;
#74210=DIRECTION ( 'NONE',  ( 0.000000000000000000, -0.8660254037844377084, -0.5000000000000016653 ) ) ;
#74217=FACE_OUTER_BOUND ( 'NONE', #97765, .T. ) ;
#74219=DIRECTION ( 'NONE',  ( 0.000000000000000000, -6.982962677686266711E-15, 1.000000000000000000 ) ) ;
#74259=ORIENTED_EDGE ( 'NONE', *, *, #180062, .F. ) ;
#74263=DIRECTION ( 'NONE',  ( 1.000000000000000000, 0.000000000000000000, 0.000000000000000000 ) ) ;
#74265=ORIENTED_EDGE ( 'NONE', *, *, #81700, .F. ) ;
#74280=ORIENTED_EDGE ( 'NONE', *, *, #196165, .T. ) ;
#74297=VECTOR ( 'NONE', #244417, 1000.000000000000000 ) ;
#74320=VECTOR ( 'NONE', #48254, 1000.000000000000000 ) ;
#74337=CARTESIAN_POINT ( 'NONE',  ( 21.93340585971891343, 68.67585297715665149, -69.52310748452435973 ) ) ;
#74351=FACE_OUTER_BOUND ( 'NONE', #3267, .T. ) ;
#74368=ORIENTED_EDGE ( 'NONE', *, *, #111090, .T. ) ;
#74405=ADVANCED_FACE ( 'NONE', ( #74217 ), #103330, .F. ) ;
#74406=LINE ( 'NONE', #58631, #191028 ) ;
#74411=CARTESIAN_POINT ( 'NONE',  ( -23.25000000000000000, 65.66751761918619934, -30.42826094061123854 ) ) ;
#74416=DIRECTION ( 'NONE',  ( -6.938893903907222067E-15, -1.000000000000000000, -7.272083257015735086E-15 ) ) ;
#74419=DIRECTION ( 'NONE',  ( 0.000000000000000000, -0.4999999999999689138, 0.8660254037844565822 ) ) ;
#74457=DIRECTION ( 'NONE',  ( 0.000000000000000000, -1.000000000000000000, -8.609265936414504429E-15 ) ) ;
#74478=EDGE_LOOP ( 'NONE', ( #108828, #80563, #217309, #148134 ) ) ;
#74502=CIRCLE ( 'NONE', #86898, 0.09999999999999939493 ) ;
#74522=EDGE_LOOP ( 'NONE', ( #131029, #6578, #174984, #158939 ) ) ;
#74527=FACE_OUTER_BOUND ( 'NONE', #4428, .T. ) ;
#74528=DIRECTION ( 'NONE',  ( -0.000000000000000000, -1.000000000000000000, -7.272083257015735086E-15 ) ) ;
#74534=CIRCLE ( 'NONE', #161996, 0.09999999999999939493 ) ;
#74548=VECTOR ( 'NONE', #133148, 1000.000000000000000 ) ;
#74560=VERTEX_POINT ( 'NONE', #184121 ) ;
#74586=ORIENTED_EDGE ( 'NONE', *, *, #199354, .T. ) ;
#74589=CARTESIAN_POINT ( 'NONE',  ( 21.05000000000000071, 65.27628289530409234, -61.85819391543678591 ) ) ;
#74629=ADVANCED_FACE ( 'NONE', ( #204958 ), #64192, .T. ) ;
#74647=DIRECTION ( 'NONE',  ( 0.000000000000000000, 0.9908441862701605762, -0.1350103645451835310 ) ) ;
#74662=EDGE_LOOP ( 'NONE', ( #78626, #243738, #149735, #62019 ) ) ;
#74693=TOROIDAL_SURFACE ( 'NONE', #116359, 0.2000000000000000111, 0.1000000000000000056 ) ;
#74709=EDGE_CURVE ( 'NONE', #26749, #19568, #173610, .T. ) ;
#74740=EDGE_CURVE ( 'NONE', #52116, #68194, #37104, .T. ) ;
#74749=ORIENTED_EDGE ( 'NONE', *, *, #124949, .T. ) ;
#74754=DIRECTION ( 'NONE',  ( -1.000000000000000000, -0.000000000000000000, -0.000000000000000000 ) ) ;
#74767=CARTESIAN_POINT ( 'NONE',  ( 23.14999999999999503, 64.25000000001172396, -81.27310748452440237 ) ) ;
#74805=DIRECTION ( 'NONE',  ( -0.000000000000000000, -1.000000000000000000, -6.982962677686266711E-15 ) ) ;
#74815=DIRECTION ( 'NONE',  ( 1.000000000000000000, 0.000000000000000000, 0.000000000000000000 ) ) ;
#74849=CARTESIAN_POINT ( 'NONE',  ( 18.52928932188133970, 65.72071067813013201, -44.77310748452439526 ) ) ;
#74855=CARTESIAN_POINT ( 'NONE',  ( 23.14999999999999858, 64.35000000001146248, -43.03791325517834565 ) ) ;
#74896=TOROIDAL_SURFACE ( 'NONE', #66492, 0.2000000000000000111, 0.1000000000000000056 ) ;
#74912=CARTESIAN_POINT ( 'NONE',  ( 21.07928932188134397, 75.90110485435707233, -75.85162414092303607 ) ) ;
#74928=ORIENTED_EDGE ( 'NONE', *, *, #94074, .T. ) ;
#74944=ORIENTED_EDGE ( 'NONE', *, *, #81872, .F. ) ;
#74952=AXIS2_PLACEMENT_3D ( 'NONE', #220837, #81299, #21390 ) ;
#75061=CARTESIAN_POINT ( 'NONE',  ( -18.59999999999999787, 68.97833521811131163, -32.18954208262707795 ) ) ;
#75068=CARTESIAN_POINT ( 'NONE',  ( 20.94999999999999929, 76.00000000001142553, -36.02310748452432421 ) ) ;
#75081=SPHERICAL_SURFACE ( 'NONE', #60427, 0.1000000000000000056 ) ;
#75084=EDGE_LOOP ( 'NONE', ( #90513, #133973, #205267, #136001 ) ) ;
#75085=FACE_OUTER_BOUND ( 'NONE', #248741, .T. ) ;
#75105=CARTESIAN_POINT ( 'NONE',  ( -23.25000000000000000, 68.97833521811131163, -32.18954208262707795 ) ) ;
#75128=DIRECTION ( 'NONE',  ( 0.000000000000000000, 0.000000000000000000, -1.000000000000000000 ) ) ;
#75162=CARTESIAN_POINT ( 'NONE',  ( -20.94560253601877164, 64.25000000001148237, -43.01302397200913674 ) ) ;
#75164=ORIENTED_EDGE ( 'NONE', *, *, #159776, .F. ) ;
#75166=ORIENTED_EDGE ( 'NONE', *, *, #165020, .F. ) ;
#75176=ORIENTED_EDGE ( 'NONE', *, *, #26412, .T. ) ;
#75193=ORIENTED_EDGE ( 'NONE', *, *, #232606, .F. ) ;
#75225=CARTESIAN_POINT ( 'NONE',  ( -18.50000000000000000, 76.00000000001165290, -69.52310748452431710 ) ) ;
#75226=ORIENTED_EDGE ( 'NONE', *, *, #135548, .F. ) ;
#75228=ADVANCED_FACE ( 'NONE', ( #98802 ), #74896, .T. ) ;
#75229=LINE ( 'NONE', #36087, #155960 ) ;
#75237=ORIENTED_EDGE ( 'NONE', *, *, #239772, .F. ) ;
#75258=AXIS2_PLACEMENT_3D ( 'NONE', #179731, #38938, #21939 ) ;
#75260=ORIENTED_EDGE ( 'NONE', *, *, #150428, .T. ) ;
#75282=AXIS2_PLACEMENT_3D ( 'NONE', #122741, #81001, #26198 ) ;
#75294=( BOUNDED_SURFACE ( )  B_SPLINE_SURFACE ( 3, 2, ( 
 ( #215747, #77507, #239180 ),
 ( #60526, #38414, #56651 ),
 ( #140056, #159652, #157094 ),
 ( #155816, #41008, #120543 ) ),
 .UNSPECIFIED., .F., .F., .F. ) 
 B_SPLINE_SURFACE_WITH_KNOTS ( ( 4, 4 ),
 ( 3, 3 ),
 ( 0.0006461284895273917582, 0.0007503702773985875939 ),
 ( 0.000000000000000000, 1.000000000000000000 ),
 .UNSPECIFIED. ) 
 GEOMETRIC_REPRESENTATION_ITEM ( )  RATIONAL_B_SPLINE_SURFACE ( (
 ( 1.000000000000000000, 0.7071067811865475727, 1.000000000000000000),
 ( 1.000000000000000000, 0.7076476444648721609, 1.000000000000000000),
 ( 1.000000000000000000, 0.7075727925191875878, 1.000000000000000000),
 ( 1.000000000000000000, 0.7071067811865475727, 1.000000000000000000) ) ) 
 REPRESENTATION_ITEM ( '' )  SURFACE ( )  );
#75311=CARTESIAN_POINT ( 'NONE',  ( 21.14999999999999503, 76.10000000001174669, -81.17267829206912211 ) ) ;
#75322=CARTESIAN_POINT ( 'NONE',  ( -22.49806830649814060, 64.35011034517256689, -69.60057180084992012 ) ) ;
#75324=ORIENTED_EDGE ( 'NONE', *, *, #50887, .T. ) ;
#75336=EDGE_CURVE ( 'NONE', #115457, #89961, #141488, .T. ) ;
#75361=ORIENTED_EDGE ( 'NONE', *, *, #146778, .F. ) ;
#75380=CARTESIAN_POINT ( 'NONE',  ( 23.14999999999999503, 64.35000000001146248, -42.93791325517834423 ) ) ;
#75385=DIRECTION ( 'NONE',  ( -1.836970198721029934E-16, -1.000000000000000000, -6.982962677686266711E-15 ) ) ;
#75407=DIRECTION ( 'NONE',  ( 0.000000000000000000, 6.982962677686266711E-15, -1.000000000000000000 ) ) ;
#75414=CARTESIAN_POINT ( 'NONE',  ( 18.59999999999997655, 77.16412189325258453, -28.10825939895270764 ) ) ;
#75436=DIRECTION ( 'NONE',  ( 1.000000000000000000, 0.000000000000000000, 0.000000000000000000 ) ) ;
#75439=DIRECTION ( 'NONE',  ( 0.000000000000000000, 0.9893560106964510714, -0.1455152366551481502 ) ) ;
#75471=CARTESIAN_POINT ( 'NONE',  ( -18.41817142474035762, 85.49870306661347286, -29.41914199688725162 ) ) ;
#75472=VERTEX_POINT ( 'NONE', #38247 ) ;
#75477=AXIS2_PLACEMENT_3D ( 'NONE', #228077, #246351, #67709 ) ;
#75483=FACE_OUTER_BOUND ( 'NONE', #7191, .T. ) ;
#75509=CARTESIAN_POINT ( 'NONE',  ( -18.39999999999999858, 85.40000000001174385, -81.27310748452426026 ) ) ;
#75548=ORIENTED_EDGE ( 'NONE', *, *, #180110, .T. ) ;
#75571=ORIENTED_EDGE ( 'NONE', *, *, #138421, .F. ) ;
#75583=ORIENTED_EDGE ( 'NONE', *, *, #184521, .F. ) ;
#75594=AXIS2_PLACEMENT_3D ( 'NONE', #155897, #133726, #73791 ) ;
#75609=ORIENTED_EDGE ( 'NONE', *, *, #28797, .F. ) ;
#75622=PLANE ( 'NONE',  #173060 ) ;
#75625=DIRECTION ( 'NONE',  ( 0.000000000000000000, 6.982962677686266711E-15, -1.000000000000000000 ) ) ;
#75653=CARTESIAN_POINT ( 'NONE',  ( -23.25000000000000000, 64.25000000001142553, -36.02310748452440237 ) ) ;
#75682=CARTESIAN_POINT ( 'NONE',  ( 20.91682497891422798, 65.67736539654895012, -30.46251168765720152 ) ) ;
#75699=DIRECTION ( 'NONE',  ( 0.000000000000000000, 1.000000000000000000, 6.938893903907222067E-15 ) ) ;
#75701=ADVANCED_FACE ( 'NONE', ( #207605 ), #148911, .T. ) ;
#75710=DIRECTION ( 'NONE',  ( 0.000000000000000000, -6.938893903907222067E-15, 1.000000000000000000 ) ) ;
#75714=DIRECTION ( 'NONE',  ( -1.000000000000000000, 0.000000000000000000, -0.000000000000000000 ) ) ;
#75747=EDGE_CURVE ( 'NONE', #38899, #2960, #83742, .T. ) ;
#75793=EDGE_LOOP ( 'NONE', ( #34426, #205792, #47485, #217182, #256544, #59535 ) ) ;
#75835=EDGE_LOOP ( 'NONE', ( #138773, #240008, #9273 ) ) ;
#75843=AXIS2_PLACEMENT_3D ( 'NONE', #57993, #78840, #134951 ) ;
#75860=AXIS2_PLACEMENT_3D ( 'NONE', #83959, #207848, #43608 ) ;
#75861=DIRECTION ( 'NONE',  ( 1.000000000000000000, 0.000000000000000000, 0.000000000000000000 ) ) ;
#75888=CIRCLE ( 'NONE', #221605, 0.1000000000000028644 ) ;
#75906=CARTESIAN_POINT ( 'NONE',  ( -23.25000000000000000, 85.60000000001150511, -45.91707660717669626 ) ) ;
#75925=ORIENTED_EDGE ( 'NONE', *, *, #125809, .F. ) ;
#75939=EDGE_CURVE ( 'NONE', #151382, #221285, #256932, .T. ) ;
#75998=CARTESIAN_POINT ( 'NONE',  ( 23.14999999999999858, 74.00000000001141132, -36.02310748452433842 ) ) ;
#76008=AXIS2_PLACEMENT_3D ( 'NONE', #223671, #205387, #244525 ) ;
#76019=FACE_OUTER_BOUND ( 'NONE', #254956, .T. ) ;
#76050=ADVANCED_FACE ( 'NONE', ( #226841 ), #185152, .T. ) ;
#76076=AXIS2_PLACEMENT_3D ( 'NONE', #56039, #16960, #135587 ) ;
#76078=CARTESIAN_POINT ( 'NONE',  ( -18.39999999999999858, 85.50000000001161027, -62.49103808782459168 ) ) ;
#76092=ORIENTED_EDGE ( 'NONE', *, *, #159776, .T. ) ;
#76110=CARTESIAN_POINT ( 'NONE',  ( 22.47071067811865319, 75.90090754530910999, -77.24318222902238062 ) ) ;
#76114=DIRECTION ( 'NONE',  ( 1.000000000000000000, 0.000000000000000000, 0.000000000000000000 ) ) ;
#76134=FACE_OUTER_BOUND ( 'NONE', #154106, .T. ) ;
#76135=EDGE_LOOP ( 'NONE', ( #107296, #253708, #80384, #96120 ) ) ;
#76138=CYLINDRICAL_SURFACE ( 'NONE', #185753, 0.09999999999999939493 ) ;
#76151=CARTESIAN_POINT ( 'NONE',  ( 21.05000000000000071, 76.09999993531877749, -76.00118570561897968 ) ) ;
#76155=EDGE_CURVE ( 'NONE', #191840, #255281, #54614, .T. ) ;
#76216=DIRECTION ( 'NONE',  ( -1.000000000000000000, 3.265361837132813093E-16, 2.280189983783949500E-30 ) ) ;
#76220=CIRCLE ( 'NONE', #80886, 0.09999999999999939493 ) ;
#76221=ADVANCED_FACE ( 'NONE', ( #37649 ), #80571, .F. ) ;
#76260=AXIS2_PLACEMENT_3D ( 'NONE', #197627, #190285, #11651 ) ;
#76279=CARTESIAN_POINT ( 'NONE',  ( -18.59999999999999787, 77.16412189325258453, -28.10825939895270764 ) ) ;
#76295=ORIENTED_EDGE ( 'NONE', *, *, #33638, .F. ) ;
#76310=EDGE_CURVE ( 'NONE', #122621, #55457, #50435, .T. ) ;
#76317=ORIENTED_EDGE ( 'NONE', *, *, #16502, .T. ) ;
#76344=AXIS2_PLACEMENT_3D ( 'NONE', #107541, #87958, #245784 ) ;
#76351=CARTESIAN_POINT ( 'NONE',  ( 23.15000000000000213, 85.50000000001159606, -59.62913836187181715 ) ) ;
#76353=EDGE_CURVE ( 'NONE', #198469, #56261, #187868, .T. ) ;
#76361=CIRCLE ( 'NONE', #222089, 11.90000000000000746 ) ;
#76363=LINE ( 'NONE', #214598, #130435 ) ;
#76370=ORIENTED_EDGE ( 'NONE', *, *, #24683, .T. ) ;
#76381=ORIENTED_EDGE ( 'NONE', *, *, #112441, .T. ) ;
#76403=CARTESIAN_POINT ( 'NONE',  ( 21.05000000000000071, 69.58602111852277972, -69.43730836824991570 ) ) ;
#76430=VERTEX_POINT ( 'NONE', #81844 ) ;
#76448=CARTESIAN_POINT ( 'NONE',  ( 21.30000000000002558, 76.00000000001168132, -73.57310748452432847 ) ) ;
#76449=EDGE_CURVE ( 'NONE', #233233, #101698, #233643, .T. ) ;
#76451=DIRECTION ( 'NONE',  ( -0.000000000000000000, 0.8660254037844377084, 0.5000000000000016653 ) ) ;
#76471=DIRECTION ( 'NONE',  ( -0.000000000000000000, -6.982962677686266711E-15, 1.000000000000000000 ) ) ;
#76494=FACE_OUTER_BOUND ( 'NONE', #31165, .T. ) ;
#76512=EDGE_CURVE ( 'NONE', #169064, #146292, #167035, .T. ) ;
#76522=AXIS2_PLACEMENT_3D ( 'NONE', #64493, #223540, #184428 ) ;
#76550=CYLINDRICAL_SURFACE ( 'NONE', #129362, 0.09999999999999939493 ) ;
#76582=EDGE_CURVE ( 'NONE', #234345, #729, #217216, .T. ) ;
#76613=CIRCLE ( 'NONE', #164124, 0.1999999999999987899 ) ;
#76646=EDGE_CURVE ( 'NONE', #83134, #99760, #25707, .T. ) ;
#76647=CARTESIAN_POINT ( 'NONE',  ( -23.25000000000000000, 76.00000000001142553, -36.02310748452432421 ) ) ;
#76670=CARTESIAN_POINT ( 'NONE',  ( -21.00448002041608575, 64.25000000001159606, -62.67476662221319117 ) ) ;
#76695=CARTESIAN_POINT ( 'NONE',  ( 21.05000000000000071, 69.55000000001159322, -59.50608031408435039 ) ) ;
#76696=CARTESIAN_POINT ( 'NONE',  ( 23.14999999999999503, 69.45000000001149942, -48.27310748452436684 ) ) ;
#76712=ORIENTED_EDGE ( 'NONE', *, *, #113718, .T. ) ;
#76748=LINE ( 'NONE', #250259, #217983 ) ;
#76768=EDGE_CURVE ( 'NONE', #196290, #136430, #63289, .T. ) ;
#76778=ORIENTED_EDGE ( 'NONE', *, *, #118481, .F. ) ;
#76818=EDGE_LOOP ( 'NONE', ( #244797, #185271, #134796, #81605 ) ) ;
#76831=DIRECTION ( 'NONE',  ( 0.000000000000000000, 6.982962677686266711E-15, -1.000000000000000000 ) ) ;
#76853=CARTESIAN_POINT ( 'NONE',  ( 22.39999999999999147, 68.20922040163827660, -69.52310748452435973 ) ) ;
#76856=DIRECTION ( 'NONE',  ( 1.000000000000000000, -3.265361837132813093E-16, -2.280189983783949500E-30 ) ) ;
#76898=AXIS2_PLACEMENT_3D ( 'NONE', #181077, #58518, #81914 ) ;
#76902=CIRCLE ( 'NONE', #255918, 0.09999999999999799327 ) ;
#76944=ORIENTED_EDGE ( 'NONE', *, *, #123322, .F. ) ;
#76946=DIRECTION ( 'NONE',  ( 0.000000000000000000, 0.3738317757009942399, -0.9274965247785252886 ) ) ;
#76963=CARTESIAN_POINT ( 'NONE',  ( 18.41815437325351823, 85.49870985315280336, -29.41916164572225156 ) ) ;
#76990=CARTESIAN_POINT ( 'NONE',  ( 21.05000000000000071, 70.60000000001157616, -57.11784146561126363 ) ) ;
#77014=ADVANCED_FACE ( 'NONE', ( #76134 ), #253480, .F. ) ;
#77092=CYLINDRICAL_SURFACE ( 'NONE', #71620, 12.87499999999999822 ) ;
#77107=CIRCLE ( 'NONE', #247978, 0.1000000000000021427 ) ;
#77134=DIRECTION ( 'NONE',  ( 0.000000000000000000, 0.1350103645451974088, -0.9908441862701587999 ) ) ;
#77146=EDGE_CURVE ( 'NONE', #106243, #231649, #54346, .T. ) ;
#77180=CARTESIAN_POINT ( 'NONE',  ( 21.14999999999999858, 76.10000000001170406, -76.06376443622556849 ) ) ;
#77220=ORIENTED_EDGE ( 'NONE', *, *, #39146, .F. ) ;
#77267=ORIENTED_EDGE ( 'NONE', *, *, #205563, .F. ) ;
#77295=DIRECTION ( 'NONE',  ( 0.000000000000000000, -0.1350103645451557199, -0.9908441862701644620 ) ) ;
#77306=LINE ( 'NONE', #155610, #152421 ) ;
#77311=CARTESIAN_POINT ( 'NONE',  ( 20.94999999999999574, 74.83729825007360148, -61.62310748452433273 ) ) ;
#77328=DIRECTION ( 'NONE',  ( -1.000000000000000000, -0.000000000000000000, -0.000000000000000000 ) ) ;
#77347=ORIENTED_EDGE ( 'NONE', *, *, #149901, .T. ) ;
#77350=ORIENTED_EDGE ( 'NONE', *, *, #238339, .T. ) ;
#77373=ORIENTED_EDGE ( 'NONE', *, *, #142407, .F. ) ;
#77386=CARTESIAN_POINT ( 'NONE',  ( -22.39999999999999858, 64.25000000001165290, -69.62310748452439668 ) ) ;
#77422=CARTESIAN_POINT ( 'NONE',  ( 21.05000000000000071, 75.90156250001138005, -75.82233839461660807 ) ) ;
#77432=CARTESIAN_POINT ( 'NONE',  ( -21.05000000000000071, 76.00000000001165290, -69.52310748452431710 ) ) ;
#77453=CARTESIAN_POINT ( 'NONE',  ( -18.59999999999999787, 76.00000000001142553, -36.02310748452432421 ) ) ;
#77499=CARTESIAN_POINT ( 'NONE',  ( 20.94999999999999929, 70.50000000001158185, -57.11784146561126363 ) ) ;
#77507=CARTESIAN_POINT ( 'NONE',  ( 22.49999999999999645, 64.25043287652226809, -69.62396585362311896 ) ) ;
#77521=AXIS2_PLACEMENT_3D ( 'NONE', #33300, #256089, #213171 ) ;
#77522=VECTOR ( 'NONE', #72709, 1000.000000000000000 ) ;
#77555=CYLINDRICAL_SURFACE ( 'NONE', #158144, 4.049999999999998046 ) ;
#77566=VECTOR ( 'NONE', #9441, 1000.000000000000000 ) ;
#77579=CARTESIAN_POINT ( 'NONE',  ( -18.59999999999999787, 66.75000000001158185, -57.17310748452438673 ) ) ;
#77589=VERTEX_POINT ( 'NONE', #46629 ) ;
#77592=DIRECTION ( 'NONE',  ( 1.000000000000000000, -0.000000000000000000, 0.000000000000000000 ) ) ;
#77597=EDGE_CURVE ( 'NONE', #12394, #201923, #83730, .T. ) ;
#77623=CYLINDRICAL_SURFACE ( 'NONE', #186074, 0.09999999999999939493 ) ;
#77657=ORIENTED_EDGE ( 'NONE', *, *, #184256, .F. ) ;
#77673=DIRECTION ( 'NONE',  ( 0.000000000000000000, 1.000000000000000000, 1.387778780781444413E-14 ) ) ;
#77683=CARTESIAN_POINT ( 'NONE',  ( -20.94999999999999929, 65.70729864260954400, -30.56574559737245877 ) ) ;
#77726=DIRECTION ( 'NONE',  ( 0.000000000000000000, 1.000000000000000000, 6.982962677686266711E-15 ) ) ;
#77734=TOROIDAL_SURFACE ( 'NONE', #40193, 0.9750000000000019762, 0.1000000000000000056 ) ;
#77766=ORIENTED_EDGE ( 'NONE', *, *, #63000, .F. ) ;
#77770=ORIENTED_EDGE ( 'NONE', *, *, #184829, .F. ) ;
#77778=DIRECTION ( 'NONE',  ( 1.000000000000000000, -3.265361837132813093E-16, -2.280189983783949500E-30 ) ) ;
#77792=LINE ( 'NONE', #116940, #43471 ) ;
#77804=ORIENTED_EDGE ( 'NONE', *, *, #254807, .F. ) ;
#77854=LINE ( 'NONE', #81678, #4405 ) ;
#77855=ORIENTED_EDGE ( 'NONE', *, *, #234159, .T. ) ;
#77856=DIRECTION ( 'NONE',  ( 1.000000000000000000, 0.000000000000000000, 0.000000000000000000 ) ) ;
#77857=CARTESIAN_POINT ( 'NONE',  ( 18.59999999999999432, 77.26178616857662007, -61.43660852097883662 ) ) ;
#77871=AXIS2_PLACEMENT_3D ( 'NONE', #121097, #215024, #80626 ) ;
#77897=CARTESIAN_POINT ( 'NONE',  ( -21.07928932188134397, 75.90110485435729970, -75.85162414091763594 ) ) ;
#77916=EDGE_CURVE ( 'NONE', #186334, #151382, #225853, .T. ) ;
#77925=CARTESIAN_POINT ( 'NONE',  ( -18.59999999999999787, 68.75000000001151079, -48.17310748452437252 ) ) ;
#77929=LINE ( 'NONE', #135331, #118407 ) ;
#77939=DIRECTION ( 'NONE',  ( 1.000000000000000000, 0.000000000000000000, 0.000000000000000000 ) ) ;
#77941=EDGE_CURVE ( 'NONE', #96681, #37986, #71964, .T. ) ;
#77960=DIRECTION ( 'NONE',  ( -0.000000000000000000, 1.000000000000000000, 6.982962677686266711E-15 ) ) ;
#77964=EDGE_LOOP ( 'NONE', ( #233215, #198143, #43546, #133794 ) ) ;
#77985=CARTESIAN_POINT ( 'NONE',  ( -18.52328366898032996, 85.64232108905262919, -29.30828814695420803 ) ) ;
#77990=CARTESIAN_POINT ( 'NONE',  ( -18.40904629823849348, 85.50000000001138289, -29.42291792204254364 ) ) ;
#78049=CIRCLE ( 'NONE', #211350, 0.09999999999999939493 ) ;
#78073=AXIS2_PLACEMENT_3D ( 'NONE', #30189, #126702, #9317 ) ;
#78092=ADVANCED_FACE ( 'NONE', ( #241538 ), #38829, .T. ) ;
#78093=ORIENTED_EDGE ( 'NONE', *, *, #130000, .T. ) ;
#78099=DIRECTION ( 'NONE',  ( 0.000000000000000000, -0.1568667991644355497, -0.9876197685951332295 ) ) ;
#78125=DIRECTION ( 'NONE',  ( 0.000000000000000000, -0.008583690987162452199, -0.9999631594459053030 ) ) ;
#78147=DIRECTION ( 'NONE',  ( 0.000000000000000000, 0.000000000000000000, -1.000000000000000000 ) ) ;
#78180=AXIS2_PLACEMENT_3D ( 'NONE', #101458, #244861, #63659 ) ;
#78193=EDGE_LOOP ( 'NONE', ( #116902, #202116, #25312, #114722 ) ) ;
#78252=DIRECTION ( 'NONE',  ( 0.000000000000000000, 0.000000000000000000, -1.000000000000000000 ) ) ;
#78287=ADVANCED_FACE ( 'NONE', ( #86429 ), #251223, .F. ) ;
#78296=DIRECTION ( 'NONE',  ( 0.000000000000000000, 7.162729191130023213E-15, -1.000000000000000000 ) ) ;
#78306=EDGE_CURVE ( 'NONE', #165183, #177806, #251171, .T. ) ;
#78319=ORIENTED_EDGE ( 'NONE', *, *, #21735, .T. ) ;
#78335=CARTESIAN_POINT ( 'NONE',  ( -1.739115166359751801E-14, 64.35000000001157616, -57.27310748452440237 ) ) ;
#78345=AXIS2_PLACEMENT_3D ( 'NONE', #109637, #190500, #50931 ) ;
#78366=AXIS2_PLACEMENT_3D ( 'NONE', #89859, #183835, #65162 ) ;
#78457=CARTESIAN_POINT ( 'NONE',  ( -21.05000000000000071, 76.00000000001139711, -31.92310748452432279 ) ) ;
#78470=EDGE_LOOP ( 'NONE', ( #189407, #198023, #227564, #213622 ) ) ;
#78483=EDGE_CURVE ( 'NONE', #69752, #32613, #238923, .T. ) ;
#78570=DIRECTION ( 'NONE',  ( -1.000000000000000000, 0.000000000000000000, 0.000000000000000000 ) ) ;
#78586=CYLINDRICAL_SURFACE ( 'NONE', #163422, 0.09999999999999939493 ) ;
#78590=EDGE_CURVE ( 'NONE', #203482, #152525, #101168, .T. ) ;
#78594=EDGE_CURVE ( 'NONE', #44321, #121991, #161875, .T. ) ;
#78596=LINE ( 'NONE', #81154, #50684 ) ;
#78608=CARTESIAN_POINT ( 'NONE',  ( -21.45000000000000284, 68.29142135624881860, -48.37310748452437537 ) ) ;
#78610=CYLINDRICAL_SURFACE ( 'NONE', #143559, 0.5000000000000004441 ) ;
#78626=ORIENTED_EDGE ( 'NONE', *, *, #110116, .F. ) ;
#78636=AXIS2_PLACEMENT_3D ( 'NONE', #202629, #64413, #86503 ) ;
#78658=LINE ( 'NONE', #215606, #248555 ) ;
#78663=ORIENTED_EDGE ( 'NONE', *, *, #133033, .F. ) ;
#78665=EDGE_CURVE ( 'NONE', #77589, #102370, #34740, .T. ) ;
#78673=ORIENTED_EDGE ( 'NONE', *, *, #181449, .F. ) ;
#78690=CARTESIAN_POINT ( 'NONE',  ( 21.05000000000000071, 64.35000000001146248, -43.03791325517834565 ) ) ;
#78718=AXIS2_PLACEMENT_3D ( 'NONE', #12751, #113109, #251320 ) ;
#78726=DIRECTION ( 'NONE',  ( -3.265361837132813093E-16, -1.000000000000000000, -1.156482317317891801E-14 ) ) ;
#78731=DIRECTION ( 'NONE',  ( 0.000000000000000000, -7.086529944415894657E-15, 1.000000000000000000 ) ) ;
#78743=EDGE_LOOP ( 'NONE', ( #12453, #212063, #14666, #69619 ) ) ;
#78787=LINE ( 'NONE', #20137, #244185 ) ;
#78790=DIRECTION ( 'NONE',  ( 0.000000000000000000, 0.000000000000000000, 1.000000000000000000 ) ) ;
#78813=ADVANCED_FACE ( 'NONE', ( #109563 ), #249111, .T. ) ;
#78837=LINE ( 'NONE', #179272, #250119 ) ;
#78840=DIRECTION ( 'NONE',  ( 1.000000000000000000, 0.000000000000000000, 0.000000000000000000 ) ) ;
#78844=ORIENTED_EDGE ( 'NONE', *, *, #202030, .T. ) ;
#78854=DIRECTION ( 'NONE',  ( 0.000000000000000000, 0.000000000000000000, 1.000000000000000000 ) ) ;
#78869=ORIENTED_EDGE ( 'NONE', *, *, #222209, .F. ) ;
#78907=CARTESIAN_POINT ( 'NONE',  ( 21.14999999999999858, 76.10000000001166143, -69.52310748452431710 ) ) ;
#78944=VERTEX_POINT ( 'NONE', #81640 ) ;
#79008=CARTESIAN_POINT ( 'NONE',  ( 18.45139536634708577, 85.48608172029256025, -29.38259586671361134 ) ) ;
#79012=CARTESIAN_POINT ( 'NONE',  ( 23.25000000000000000, 84.59626168225457832, -60.07297996737398194 ) ) ;
#79018=VERTEX_POINT ( 'NONE', #42543 ) ;
#79037=DIRECTION ( 'NONE',  ( 1.000000000000000000, 0.000000000000000000, 0.000000000000000000 ) ) ;
#79087=DIRECTION ( 'NONE',  ( 0.000000000000000000, 0.000000000000000000, 1.000000000000000000 ) ) ;
#79119=VERTEX_POINT ( 'NONE', #9842 ) ;
#79125=CARTESIAN_POINT ( 'NONE',  ( -20.64999999999999858, 68.75000000001151079, -48.37310748452436826 ) ) ;
#79150=CARTESIAN_POINT ( 'NONE',  ( 20.97438252431638972, 67.07457649393559507, -61.05073679551357202 ) ) ;
#79181=DIRECTION ( 'NONE',  ( -1.000000000000000000, 0.000000000000000000, -0.000000000000000000 ) ) ;
#79199=DIRECTION ( 'NONE',  ( 1.000000000000000000, -0.000000000000000000, 0.000000000000000000 ) ) ;
#79206=ADVANCED_FACE ( 'NONE', ( #35845 ), #16290, .T. ) ;
#79208=ORIENTED_EDGE ( 'NONE', *, *, #245089, .T. ) ;
#79210=ORIENTED_EDGE ( 'NONE', *, *, #212137, .F. ) ;
#79212=CYLINDRICAL_SURFACE ( 'NONE', #241074, 0.1000000000000028644 ) ;
#79223=CARTESIAN_POINT ( 'NONE',  ( -20.54999999999999716, 74.07476635515169505, -48.75335101765046630 ) ) ;
#79236=EDGE_CURVE ( 'NONE', #232528, #87393, #123529, .T. ) ;
#79237=CARTESIAN_POINT ( 'NONE',  ( 20.94999999999999929, 64.35000000001146248, -42.86470817442145886 ) ) ;
#79240=DIRECTION ( 'NONE',  ( -0.000000000000000000, 7.172728831056617961E-15, -1.000000000000000000 ) ) ;
#79262=CARTESIAN_POINT ( 'NONE',  ( -18.36527282682062534, 85.50000060000994040, -29.10095852002216077 ) ) ;
#79272=TOROIDAL_SURFACE ( 'NONE', #220761, 0.2000000000000000111, 0.1000000000000000056 ) ;
#79274=CARTESIAN_POINT ( 'NONE',  ( -22.49544290803788371, 64.25012976215435856, -69.58841944378173139 ) ) ;
#79279=ADVANCED_FACE ( 'NONE', ( #3095 ), #240064, .T. ) ;
#79297=DIRECTION ( 'NONE',  ( 4.377807931758639578E-15, -0.2605042016806606298, -0.9654727137038736640 ) ) ;
#79303=ORIENTED_EDGE ( 'NONE', *, *, #76512, .T. ) ;
#79359=ORIENTED_EDGE ( 'NONE', *, *, #48316, .T. ) ;
#79371=TOROIDAL_SURFACE ( 'NONE', #266, 6.258578643762712446, 0.1000000000000000056 ) ;
#79376=AXIS2_PLACEMENT_3D ( 'NONE', #169007, #151996, #29491 ) ;
#79400=FACE_OUTER_BOUND ( 'NONE', #142094, .T. ) ;
#79456=AXIS2_PLACEMENT_3D ( 'NONE', #137827, #256438, #77856 ) ;
#79472=ORIENTED_EDGE ( 'NONE', *, *, #10415, .T. ) ;
#79481=CARTESIAN_POINT ( 'NONE',  ( 21.00000000000000000, 66.25000000001158185, -57.27310748452438816 ) ) ;
#79489=DIRECTION ( 'NONE',  ( -1.000000000000000000, -0.000000000000000000, 0.000000000000000000 ) ) ;
#79493=DIRECTION ( 'NONE',  ( 1.000000000000000000, 0.000000000000000000, 0.000000000000000000 ) ) ;
#79502=CARTESIAN_POINT ( 'NONE',  ( 23.14999999999999858, 71.22429906543214884, -57.67433938047838637 ) ) ;
#79503=CARTESIAN_POINT ( 'NONE',  ( 21.11101077988997332, 69.57631526528561494, -69.53839275343867143 ) ) ;
#79517=CARTESIAN_POINT ( 'NONE',  ( 18.40000000000000568, 85.50000000001136868, -29.10095763519384704 ) ) ;
#79519=ORIENTED_EDGE ( 'NONE', *, *, #183603, .F. ) ;
#79556=VERTEX_POINT ( 'NONE', #175084 ) ;
#79567=EDGE_CURVE ( 'NONE', #189058, #153937, #154236, .T. ) ;
#79623=DIRECTION ( 'NONE',  ( -1.000000000000000000, -0.000000000000000000, 0.000000000000000000 ) ) ;
#79656=ADVANCED_FACE ( 'NONE', ( #255804 ), #236140, .T. ) ;
#79660=EDGE_LOOP ( 'NONE', ( #181628, #50011, #74265, #170520 ) ) ;
#79662=ORIENTED_EDGE ( 'NONE', *, *, #158622, .T. ) ;
#79675=CARTESIAN_POINT ( 'NONE',  ( 18.49999999999999289, 64.35000000001141984, -36.02310748452440237 ) ) ;
#79691=DIRECTION ( 'NONE',  ( 1.000000000000000000, -0.000000000000000000, 0.000000000000000000 ) ) ;
#79719=CARTESIAN_POINT ( 'NONE',  ( -21.05000000000000071, 87.48912529308769592, -66.42310748452423752 ) ) ;
#79748=FACE_OUTER_BOUND ( 'NONE', #104354, .T. ) ;
#79752=ADVANCED_FACE ( 'NONE', ( #67923 ), #28852, .F. ) ;
#79803=VECTOR ( 'NONE', #215780, 1000.000000000000000 ) ;
#79832=DIRECTION ( 'NONE',  ( 1.000000000000000000, -2.952720810173289112E-16, -2.061873921506763405E-30 ) ) ;
#79837=CARTESIAN_POINT ( 'NONE',  ( -18.59999999999999787, 69.01799029515495931, -32.32695536626808774 ) ) ;
#79851=PLANE ( 'NONE',  #59313 ) ;
#79860=DIRECTION ( 'NONE',  ( 0.7071359030027593029, -0.7070776581709197206, 0.000000000000000000 ) ) ;
#79864=CARTESIAN_POINT ( 'NONE',  ( -23.25000000000000000, 84.59626168225457832, -60.07297996737398194 ) ) ;
#79883=CARTESIAN_POINT ( 'NONE',  ( -21.05000000000000071, 77.16270174994961906, -61.52310748452431710 ) ) ;
#79903=CARTESIAN_POINT ( 'NONE',  ( -21.05000000000000071, 64.35000000001166143, -69.42310748452440805 ) ) ;
#79921=ADVANCED_FACE ( 'NONE', ( #195601 ), #54770, .T. ) ;
#79940=CARTESIAN_POINT ( 'NONE',  ( -21.14999999999999858, 76.10000000001174669, -81.17267829206912211 ) ) ;
#79942=EDGE_CURVE ( 'NONE', #147896, #77589, #210016, .T. ) ;
#80013=FACE_OUTER_BOUND ( 'NONE', #37430, .T. ) ;
#80024=EDGE_CURVE ( 'NONE', #108484, #238989, #65448, .T. ) ;
#80027=CARTESIAN_POINT ( 'NONE',  ( 18.49999999999999645, 76.00000000001165290, -69.52310748452431710 ) ) ;
#80057=VERTEX_POINT ( 'NONE', #121212 ) ;
#80060=AXIS2_PLACEMENT_3D ( 'NONE', #19342, #160163, #218807 ) ;
#80071=CARTESIAN_POINT ( 'NONE',  ( -20.85000000000000142, 77.14957036958705316, -28.20719500002235236 ) ) ;
#80072=AXIS2_PLACEMENT_3D ( 'NONE', #51985, #208533, #50692 ) ;
#80077=LINE ( 'NONE', #194955, #20226 ) ;
#80078=CARTESIAN_POINT ( 'NONE',  ( -18.59999999999999787, 77.83534155023598089, -57.96795619196132776 ) ) ;
#80115=VECTOR ( 'NONE', #196668, 1000.000000000000000 ) ;
#80116=DIRECTION ( 'NONE',  ( 1.000000000000000000, 0.000000000000000000, 0.000000000000000000 ) ) ;
#80122=ORIENTED_EDGE ( 'NONE', *, *, #18151, .T. ) ;
#80153=ORIENTED_EDGE ( 'NONE', *, *, #256880, .F. ) ;
#80161=ORIENTED_EDGE ( 'NONE', *, *, #94963, .F. ) ;
#80168=CYLINDRICAL_SURFACE ( 'NONE', #56052, 12.87499999999999822 ) ;
#80189=CARTESIAN_POINT ( 'NONE',  ( 20.94999999999999929, 76.00000000001142553, -36.02310748452432421 ) ) ;
#80223=VECTOR ( 'NONE', #169415, 999.9999999999998863 ) ;
#80250=TOROIDAL_SURFACE ( 'NONE', #9368, 0.6000000000000009770, 0.1000000000000000056 ) ;
#80252=CARTESIAN_POINT ( 'NONE',  ( 18.39999999999999858, 85.50000000001136868, -29.42291809330221497 ) ) ;
#80298=CIRCLE ( 'NONE', #1213, 0.1000000000000026007 ) ;
#80300=CIRCLE ( 'NONE', #151288, 0.1000000000000028644 ) ;
#80310=DIRECTION ( 'NONE',  ( 0.000000000000000000, 0.000000000000000000, 1.000000000000000000 ) ) ;
#80356=VECTOR ( 'NONE', #228155, 1000.000000000000000 ) ;
#80357=EDGE_LOOP ( 'NONE', ( #22355, #251021, #257630, #205769 ) ) ;
#80375=DIRECTION ( 'NONE',  ( -1.000000000000000000, 3.265361837132813093E-16, 2.280189983783949500E-30 ) ) ;
#80381=CARTESIAN_POINT ( 'NONE',  ( -23.15000000000000213, 64.35000000001150511, -48.17310748452440095 ) ) ;
#80384=ORIENTED_EDGE ( 'NONE', *, *, #210416, .F. ) ;
#80445=CARTESIAN_POINT ( 'NONE',  ( 18.59999999999999076, 69.45000000001158469, -59.50608031408435039 ) ) ;
#80448=CARTESIAN_POINT ( 'NONE',  ( -21.05000000000000426, 69.66772772607600928, -69.48557142123871699 ) ) ;
#80455=ADVANCED_FACE ( 'NONE', ( #199118 ), #242864, .T. ) ;
#80468=AXIS2_PLACEMENT_3D ( 'NONE', #239067, #96942, #216915 ) ;
#80470=AXIS2_PLACEMENT_3D ( 'NONE', #212518, #233374, #191689 ) ;
#80473=EDGE_CURVE ( 'NONE', #180491, #238726, #19861, .T. ) ;
#80488=ORIENTED_EDGE ( 'NONE', *, *, #16126, .F. ) ;
#80489=ORIENTED_EDGE ( 'NONE', *, *, #212807, .T. ) ;
#80519=CIRCLE ( 'NONE', #238782, 0.09999999999999913125 ) ;
#80524=DIRECTION ( 'NONE',  ( 0.000000000000000000, -6.938893903907233900E-15, 1.000000000000000000 ) ) ;
#80539=DIRECTION ( 'NONE',  ( 0.000000000000000000, 6.853228547068871147E-15, -1.000000000000000000 ) ) ;
#80563=ORIENTED_EDGE ( 'NONE', *, *, #46107, .F. ) ;
#80571=CYLINDRICAL_SURFACE ( 'NONE', #162919, 0.1000000000000028644 ) ;
#80575=ORIENTED_EDGE ( 'NONE', *, *, #48747, .T. ) ;
#80576=DIRECTION ( 'NONE',  ( 0.000000000000000000, 6.982962677686266711E-15, -1.000000000000000000 ) ) ;
#80622=AXIS2_PLACEMENT_3D ( 'NONE', #91542, #147663, #227190 ) ;
#80626=DIRECTION ( 'NONE',  ( 0.000000000000000000, 0.000000000000000000, 1.000000000000000000 ) ) ;
#80662=DIRECTION ( 'NONE',  ( 0.000000000000000000, 1.000000000000000000, 6.982962677686266711E-15 ) ) ;
#80664=CARTESIAN_POINT ( 'NONE',  ( -20.54999999999999716, 68.85000000001154774, -52.77310748452437394 ) ) ;
#80676=ORIENTED_EDGE ( 'NONE', *, *, #118512, .F. ) ;
#80702=CIRCLE ( 'NONE', #101114, 0.1000000000000060146 ) ;
#80727=ORIENTED_EDGE ( 'NONE', *, *, #15541, .F. ) ;
#80772=CYLINDRICAL_SURFACE ( 'NONE', #127096, 3.999999999999996447 ) ;
#80836=CARTESIAN_POINT ( 'NONE',  ( 23.14999999999999858, 76.00000000001142553, -36.02310748452432421 ) ) ;
#80839=ORIENTED_EDGE ( 'NONE', *, *, #104986, .T. ) ;
#80841=ORIENTED_EDGE ( 'NONE', *, *, #107191, .T. ) ;
#80848=EDGE_CURVE ( 'NONE', #203482, #172794, #237629, .T. ) ;
#80863=DIRECTION ( 'NONE',  ( 0.000000000000000000, 7.056502275159894776E-15, -1.000000000000000000 ) ) ;
#80886=AXIS2_PLACEMENT_3D ( 'NONE', #196376, #221068, #178128 ) ;
#80908=EDGE_LOOP ( 'NONE', ( #140581, #144692, #93511, #194742, #245584, #5917 ) ) ;
#80918=CARTESIAN_POINT ( 'NONE',  ( -18.59999999999999787, 64.35000000001150511, -48.17310748452440095 ) ) ;
#80925=EDGE_CURVE ( 'NONE', #200, #236713, #178456, .T. ) ;
#80947=ORIENTED_EDGE ( 'NONE', *, *, #232504, .T. ) ;
#80965=DIRECTION ( 'NONE',  ( 1.000000000000000000, 0.000000000000000000, 0.000000000000000000 ) ) ;
#80966=ORIENTED_EDGE ( 'NONE', *, *, #20549, .F. ) ;
#80991=ORIENTED_EDGE ( 'NONE', *, *, #239245, .F. ) ;
#80995=CARTESIAN_POINT ( 'NONE',  ( 21.14999999999999858, 76.00000000001169553, -76.06376443622556849 ) ) ;
#81001=DIRECTION ( 'NONE',  ( 1.000000000000000000, 0.000000000000000000, 0.000000000000000000 ) ) ;
#81005=VERTEX_POINT ( 'NONE', #31449 ) ;
#81009=DIRECTION ( 'NONE',  ( 0.000000000000000000, 0.9908441862701605762, -0.1350103645451835310 ) ) ;
#81034=CIRCLE ( 'NONE', #205955, 0.1000000000000028644 ) ;
#81037=CARTESIAN_POINT ( 'NONE',  ( -21.44999999999999929, 68.85000000001151932, -48.27310748452437394 ) ) ;
#81046=CARTESIAN_POINT ( 'NONE',  ( -20.94999999999999929, 68.92903212821255465, -32.27654326265606954 ) ) ;
#81071=ADVANCED_FACE ( 'NONE', ( #194367 ), #199280, .F. ) ;
#81091=AXIS2_PLACEMENT_3D ( 'NONE', #210704, #8655, #28252 ) ;
#81112=VERTEX_POINT ( 'NONE', #52237 ) ;
#81115=CIRCLE ( 'NONE', #72794, 0.1000000000000026007 ) ;
#81154=CARTESIAN_POINT ( 'NONE',  ( -20.94999999999999929, 77.84915357198738661, -24.41714086472725853 ) ) ;
#81184=AXIS2_PLACEMENT_3D ( 'NONE', #12255, #48782, #111338 ) ;
#81216=ORIENTED_EDGE ( 'NONE', *, *, #154756, .T. ) ;
#81230=DIRECTION ( 'NONE',  ( 1.000000000000000000, 0.000000000000000000, 0.000000000000000000 ) ) ;
#81233=DIRECTION ( 'NONE',  ( 1.000000000000000000, -0.000000000000000000, 0.000000000000000000 ) ) ;
#81238=EDGE_CURVE ( 'NONE', #110098, #146658, #191108, .T. ) ;
#81266=DIRECTION ( 'NONE',  ( 0.000000000000000000, -1.000000000000000000, -6.352154140967427193E-15 ) ) ;
#81272=CARTESIAN_POINT ( 'NONE',  ( -21.07928932188134041, 75.90110485435729970, -75.85162414091762173 ) ) ;
#81293=DIRECTION ( 'NONE',  ( 0.000000000000000000, -6.982962677686266711E-15, 1.000000000000000000 ) ) ;
#81299=DIRECTION ( 'NONE',  ( 0.000000000000000000, -1.000000000000000000, -6.982962677686266711E-15 ) ) ;
#81308=CARTESIAN_POINT ( 'NONE',  ( 20.94999999999999929, 87.29603075034691528, -66.47520832486038955 ) ) ;
#81326=CIRCLE ( 'NONE', #227103, 11.74999999999999645 ) ;
#81329=CARTESIAN_POINT ( 'NONE',  ( -23.15000000000000213, 76.00000000001142553, -36.02310748452432421 ) ) ;
#81339=CARTESIAN_POINT ( 'NONE',  ( -21.95218792049438861, 75.90097156021178648, -76.72461504577100300 ) ) ;
#81342=DIRECTION ( 'NONE',  ( 0.000000000000000000, 0.9915357197604849349, -0.1298341882520056834 ) ) ;
#81351=CARTESIAN_POINT ( 'NONE',  ( 22.50000000000000000, 64.35042919246686210, -69.62310748452439668 ) ) ;
#81352=CARTESIAN_POINT ( 'NONE',  ( 22.00411653889212715, 75.90096189422493467, -76.77655035216474744 ) ) ;
#81450=EDGE_CURVE ( 'NONE', #214123, #3677, #92351, .T. ) ;
#81470=LINE ( 'NONE', #178060, #174599 ) ;
#81486=CIRCLE ( 'NONE', #227268, 0.1000000000000028783 ) ;
#81500=ORIENTED_EDGE ( 'NONE', *, *, #181033, .T. ) ;
#81526=SPHERICAL_SURFACE ( 'NONE', #61125, 0.1000000000000000056 ) ;
#81562=PLANE ( 'NONE',  #90117 ) ;
#81602=ORIENTED_EDGE ( 'NONE', *, *, #112441, .F. ) ;
#81605=ORIENTED_EDGE ( 'NONE', *, *, #37411, .F. ) ;
#81640=CARTESIAN_POINT ( 'NONE',  ( -20.00857864376270001, 66.65000000001157332, -57.27310748452438816 ) ) ;
#81647=ORIENTED_EDGE ( 'NONE', *, *, #29131, .T. ) ;
#81653=CARTESIAN_POINT ( 'NONE',  ( -21.14999999999999858, 69.45934304831041572, -69.52310748452435973 ) ) ;
#81654=CARTESIAN_POINT ( 'NONE',  ( 19.90621891164687440, 64.25000000001148237, -44.69466220664675404 ) ) ;
#81658=VERTEX_POINT ( 'NONE', #6075 ) ;
#81659=ORIENTED_EDGE ( 'NONE', *, *, #124436, .F. ) ;
#81671=EDGE_CURVE ( 'NONE', #191947, #11272, #26968, .T. ) ;
#81678=CARTESIAN_POINT ( 'NONE',  ( 18.59999999999999076, 69.45000000001149942, -48.27310748452436684 ) ) ;
#81693=CARTESIAN_POINT ( 'NONE',  ( 20.44999100639871514, 65.56028929679979456, -61.76403175855386962 ) ) ;
#81700=EDGE_CURVE ( 'NONE', #115794, #180734, #62089, .T. ) ;
#81721=CARTESIAN_POINT ( 'NONE',  ( 23.14999999999999503, 69.35000000001151932, -48.27310748452436684 ) ) ;
#81730=EDGE_CURVE ( 'NONE', #178236, #216194, #99649, .T. ) ;
#81737=CARTESIAN_POINT ( 'NONE',  ( -21.05000000000000071, 69.74218538953553548, -69.62089777583315708 ) ) ;
#81753=EDGE_CURVE ( 'NONE', #214318, #227579, #158186, .T. ) ;
#81769=LINE ( 'NONE', #124793, #95999 ) ;
#81795=EDGE_LOOP ( 'NONE', ( #176421, #94266, #215421, #191904 ) ) ;
#81805=ORIENTED_EDGE ( 'NONE', *, *, #99994, .T. ) ;
#81844=CARTESIAN_POINT ( 'NONE',  ( -20.64999999999999858, 71.65000000001151648, -48.27310748452435263 ) ) ;
#81850=TOROIDAL_SURFACE ( 'NONE', #131960, 0.2000000000000000111, 0.1000000000000000056 ) ;
#81872=EDGE_CURVE ( 'NONE', #69378, #96547, #183084, .T. ) ;
#81879=DIRECTION ( 'NONE',  ( 0.000000000000000000, 0.1568667991644355497, -0.9876197685951332295 ) ) ;
#81881=ORIENTED_EDGE ( 'NONE', *, *, #167829, .F. ) ;
#81914=DIRECTION ( 'NONE',  ( 0.000000000000000000, 0.9908441862701605762, -0.1350103645451835310 ) ) ;
#81948=CARTESIAN_POINT ( 'NONE',  ( -22.45305610364635385, 76.10085836911046897, -81.27267460801373034 ) ) ;
#81963=CARTESIAN_POINT ( 'NONE',  ( 20.94999999999999929, 64.35000000001146248, -42.80697314750249660 ) ) ;
#81977=CARTESIAN_POINT ( 'NONE',  ( -21.14999999999999858, 64.25000000001165290, -69.42310748452440805 ) ) ;
#81978=DIRECTION ( 'NONE',  ( -1.000000000000000000, 0.000000000000000000, 0.000000000000000000 ) ) ;
#81979=ADVANCED_FACE ( 'NONE', ( #217090 ), #20212, .F. ) ;
#82003=CARTESIAN_POINT ( 'NONE',  ( 22.59999999999999787, 64.35042919246686210, -69.62310748452439668 ) ) ;
#82047=VERTEX_POINT ( 'NONE', #39798 ) ;
#82067=DIRECTION ( 'NONE',  ( 1.000000000000000000, 0.000000000000000000, 0.000000000000000000 ) ) ;
#82076=AXIS2_PLACEMENT_3D ( 'NONE', #78608, #57758, #35676 ) ;
#82082=AXIS2_PLACEMENT_3D ( 'NONE', #235246, #197399, #78726 ) ;
#82083=ADVANCED_FACE ( 'NONE', ( #104832 ), #202685, .F. ) ;
#82090=DIRECTION ( 'NONE',  ( 1.000000000000000000, 0.000000000000000000, 0.000000000000000000 ) ) ;
#82098=VECTOR ( 'NONE', #183949, 1000.000000000000114 ) ;
#82109=CARTESIAN_POINT ( 'NONE',  ( -22.39999999999999858, 64.35000000001166143, -69.52310748452438816 ) ) ;
#82123=FACE_OUTER_BOUND ( 'NONE', #148437, .T. ) ;
#82135=DIRECTION ( 'NONE',  ( -1.000000000000000000, 0.000000000000000000, 0.000000000000000000 ) ) ;
#82149=FACE_OUTER_BOUND ( 'NONE', #176973, .T. ) ;
#82155=ORIENTED_EDGE ( 'NONE', *, *, #23851, .T. ) ;
#82176=ORIENTED_EDGE ( 'NONE', *, *, #19281, .T. ) ;
#82179=ORIENTED_EDGE ( 'NONE', *, *, #2040, .T. ) ;
#82194=CARTESIAN_POINT ( 'NONE',  ( -23.25000000000000000, 76.00000000001162448, -65.47310748452431994 ) ) ;
#82229=AXIS2_PLACEMENT_3D ( 'NONE', #121123, #221443, #24578 ) ;
#82230=ADVANCED_FACE ( 'NONE', ( #14798 ), #241523, .F. ) ;
#82234=ORIENTED_EDGE ( 'NONE', *, *, #59113, .F. ) ;
#82242=CARTESIAN_POINT ( 'NONE',  ( -18.59999999999999787, 77.83534155023598089, -57.96795619196132776 ) ) ;
#82300=DIRECTION ( 'NONE',  ( 1.000000000000000000, 0.000000000000000000, 0.000000000000000000 ) ) ;
#82301=LINE ( 'NONE', #214440, #219384 ) ;
#82303=VECTOR ( 'NONE', #189697, 1000.000000000000000 ) ;
#82305=EDGE_CURVE ( 'NONE', #211121, #37986, #104132, .T. ) ;
#82306=ADVANCED_FACE ( 'NONE', ( #229959 ), #39568, .T. ) ;
#82311=CARTESIAN_POINT ( 'NONE',  ( -18.59999999999999787, 65.66751761918619934, -30.42826094061123854 ) ) ;
#82355=DIRECTION ( 'NONE',  ( -1.000000000000000000, -0.000000000000000000, -0.000000000000000000 ) ) ;
#82379=EDGE_CURVE ( 'NONE', #147021, #134468, #212499, .T. ) ;
#82387=EDGE_CURVE ( 'NONE', #116521, #95061, #179016, .T. ) ;
#82389=DIRECTION ( 'NONE',  ( -1.000000000000000000, 0.000000000000000000, 0.000000000000000000 ) ) ;
#82390=EDGE_CURVE ( 'NONE', #92040, #243492, #158345, .T. ) ;
#82397=ORIENTED_EDGE ( 'NONE', *, *, #254255, .T. ) ;
#82399=LINE ( 'NONE', #5433, #203334 ) ;
#82436=CARTESIAN_POINT ( 'NONE',  ( -18.50000000000000000, 66.65000000001157332, -57.37310748452438247 ) ) ;
#82440=AXIS2_PLACEMENT_3D ( 'NONE', #248728, #132633, #207034 ) ;
#82460=ORIENTED_EDGE ( 'NONE', *, *, #146241, .F. ) ;
#82471=ORIENTED_EDGE ( 'NONE', *, *, #96920, .F. ) ;
#82478=ORIENTED_EDGE ( 'NONE', *, *, #137773, .T. ) ;
#82483=ORIENTED_EDGE ( 'NONE', *, *, #258100, .F. ) ;
#82496=DIRECTION ( 'NONE',  ( -1.000000000000000000, 0.000000000000000000, -0.000000000000000000 ) ) ;
#82522=CARTESIAN_POINT ( 'NONE',  ( -21.05000000000000071, 76.00000000001142553, -36.02310748452432421 ) ) ;
#82562=ORIENTED_EDGE ( 'NONE', *, *, #72054, .T. ) ;
#82576=ORIENTED_EDGE ( 'NONE', *, *, #69667, .F. ) ;
#82578=DIRECTION ( 'NONE',  ( 0.000000000000000000, -6.982962677686266711E-15, 1.000000000000000000 ) ) ;
#82587=LINE ( 'NONE', #17507, #107816 ) ;
#82600=LINE ( 'NONE', #164752, #19408 ) ;
#82609=DIRECTION ( 'NONE',  ( -0.000000000000000000, -1.000000000000000000, -6.982962677686266711E-15 ) ) ;
#82621=CARTESIAN_POINT ( 'NONE',  ( -22.14074124539699895, 75.90094710416764201, -76.91318533556810166 ) ) ;
#82623=CARTESIAN_POINT ( 'NONE',  ( 20.95496329884391784, 65.43256679391856778, -61.94879755223957574 ) ) ;
#82624=CARTESIAN_POINT ( 'NONE',  ( 18.59999999999999432, 85.48068669529034480, -29.08199231576640287 ) ) ;
#82703=CARTESIAN_POINT ( 'NONE',  ( -21.45000000000000284, 68.29142135624881860, -48.27310748452437394 ) ) ;
#82723=DIRECTION ( 'NONE',  ( 1.000000000000000000, 0.000000000000000000, 0.000000000000000000 ) ) ;
#82739=ORIENTED_EDGE ( 'NONE', *, *, #154409, .F. ) ;
#82806=CARTESIAN_POINT ( 'NONE',  ( -20.94999999999999929, 87.65000000001163016, -66.62310748452424036 ) ) ;
#82817=CARTESIAN_POINT ( 'NONE',  ( -20.85000000000000142, 77.83585931145498193, -24.51866831572578320 ) ) ;
#82834=CARTESIAN_POINT ( 'NONE',  ( 19.75857864376268935, 64.25000000001148237, -44.67310748452440095 ) ) ;
#82836=VERTEX_POINT ( 'NONE', #225134 ) ;
#82842=CARTESIAN_POINT ( 'NONE',  ( -22.41119224318417125, 76.00000000001173817, -81.17267829206912211 ) ) ;
#82883=CARTESIAN_POINT ( 'NONE',  ( -23.25000000000000000, 77.16412189325258453, -28.10825939895270764 ) ) ;
#82890=VECTOR ( 'NONE', #63480, 1000.000000000000000 ) ;
#82907=ORIENTED_EDGE ( 'NONE', *, *, #205583, .F. ) ;
#82908=FACE_OUTER_BOUND ( 'NONE', #145057, .T. ) ;
#82910=DIRECTION ( 'NONE',  ( 0.000000000000000000, 0.9915357197604849349, -0.1298341882520056834 ) ) ;
#82917=TOROIDAL_SURFACE ( 'NONE', #28846, 7.791421356237335338, 0.1000000000000000056 ) ;
#82937=ORIENTED_EDGE ( 'NONE', *, *, #200976, .F. ) ;
#82938=CARTESIAN_POINT ( 'NONE',  ( 18.49999999999999645, 74.16465844978715438, -57.96795619196135618 ) ) ;
#82939=CARTESIAN_POINT ( 'NONE',  ( 19.75857864376269291, 64.25000000001148237, -44.67310748452440095 ) ) ;
#82946=DIRECTION ( 'NONE',  ( 1.000000000000000000, 0.000000000000000000, 6.938893903907270030E-14 ) ) ;
#82989=LINE ( 'NONE', #43903, #159870 ) ;
#83012=DIRECTION ( 'NONE',  ( -0.7071067811865475727, 0.7071067811865475727, 4.937700262164531476E-15 ) ) ;
#83013=ADVANCED_FACE ( 'NONE', ( #191199 ), #110341, .F. ) ;
#83047=CARTESIAN_POINT ( 'NONE',  ( 20.94999999999999929, 71.00000000001151079, -48.42837350343745584 ) ) ;
#83080=CARTESIAN_POINT ( 'NONE',  ( 18.49999999999999289, 65.79142135392832813, -44.82060061889436753 ) ) ;
#83134=VERTEX_POINT ( 'NONE', #119343 ) ;
#83163=CIRCLE ( 'NONE', #20686, 0.1000000000000028644 ) ;
#83192=FACE_OUTER_BOUND ( 'NONE', #50364, .T. ) ;
#83196=FACE_OUTER_BOUND ( 'NONE', #121715, .T. ) ;
#83206=VECTOR ( 'NONE', #125198, 1000.000000000000000 ) ;
#83216=ADVANCED_FACE ( 'NONE', ( #29276 ), #185738, .F. ) ;
#83344=DIRECTION ( 'NONE',  ( 0.000000000000000000, 0.000000000000000000, 1.000000000000000000 ) ) ;
#83354=ORIENTED_EDGE ( 'NONE', *, *, #181033, .F. ) ;
#83394=ORIENTED_EDGE ( 'NONE', *, *, #223654, .F. ) ;
#83399=DIRECTION ( 'NONE',  ( -1.000000000000000000, 2.952720810173289112E-16, 2.061873921506763405E-30 ) ) ;
#83402=DIRECTION ( 'NONE',  ( -0.000000000000000000, 6.982962677686266711E-15, -1.000000000000000000 ) ) ;
#83438=VERTEX_POINT ( 'NONE', #120360 ) ;
#83449=DIRECTION ( 'NONE',  ( -0.000000000000000000, 1.000000000000000000, 6.982962677686266711E-15 ) ) ;
#83493=EDGE_CURVE ( 'NONE', #15384, #177806, #38229, .T. ) ;
#83532=CARTESIAN_POINT ( 'NONE',  ( 21.00000000000000000, 66.25000000001151079, -48.27310748452438816 ) ) ;
#83537=FACE_OUTER_BOUND ( 'NONE', #219162, .T. ) ;
#83545=EDGE_LOOP ( 'NONE', ( #19291, #184296, #100513, #224708 ) ) ;
#83549=DIRECTION ( 'NONE',  ( 0.000000000000000000, 6.982962677686266711E-15, -1.000000000000000000 ) ) ;
#83587=CARTESIAN_POINT ( 'NONE',  ( -18.55121869061588669, 65.67252876774480796, -30.44570419949945617 ) ) ;
#83594=CARTESIAN_POINT ( 'NONE',  ( 21.13461538461538325, 65.38541703798603066, -57.17310748452439384 ) ) ;
#83630=DIRECTION ( 'NONE',  ( -1.000000000000000000, 7.304098846218135653E-16, 4.639676173203994055E-30 ) ) ;
#83647=DIRECTION ( 'NONE',  ( -1.000000000000000000, -0.000000000000000000, -0.000000000000000000 ) ) ;
#83664=CARTESIAN_POINT ( 'NONE',  ( -23.15000000000000213, 76.00000000001165290, -69.52310748452431710 ) ) ;
#83672=DIRECTION ( 'NONE',  ( -0.000000000000000000, 0.8700118002898356018, -0.4930308989875170078 ) ) ;
#83703=AXIS2_PLACEMENT_3D ( 'NONE', #145312, #4517, #187051 ) ;
#83723=CARTESIAN_POINT ( 'NONE',  ( 21.04105312098505109, 67.12466737696794894, -57.19460073731235639 ) ) ;
#83725=CARTESIAN_POINT ( 'NONE',  ( -21.05000000000000071, 70.10000000001163301, -59.30400771986794695 ) ) ;
#83730=CIRCLE ( 'NONE', #116898, 0.5000000000000004441 ) ;
#83742=LINE ( 'NONE', #191909, #116733 ) ;
#83790=EDGE_CURVE ( 'NONE', #147579, #53002, #253096, .T. ) ;
#83842=DIRECTION ( 'NONE',  ( 0.000000000000000000, 0.000000000000000000, -1.000000000000000000 ) ) ;
#83850=PLANE ( 'NONE',  #220155 ) ;
#83853=DIRECTION ( 'NONE',  ( -0.000000000000000000, 0.2605042016806385363, 0.9654727137038795481 ) ) ;
#83863=DIRECTION ( 'NONE',  ( 1.000000000000000000, 0.000000000000000000, 0.000000000000000000 ) ) ;
#83897=EDGE_LOOP ( 'NONE', ( #136444, #6756, #230539, #255293 ) ) ;
#83898=CARTESIAN_POINT ( 'NONE',  ( 20.95462737510932882, 65.44321804836786782, -61.95315742796210401 ) ) ;
#83899=DIRECTION ( 'NONE',  ( 1.000000000000000000, 0.000000000000000000, 0.000000000000000000 ) ) ;
#83905=CARTESIAN_POINT ( 'NONE',  ( -23.15000000000000213, 64.25000000001151079, -48.17310748452440805 ) ) ;
#83907=FACE_OUTER_BOUND ( 'NONE', #77964, .T. ) ;
#83959=CARTESIAN_POINT ( 'NONE',  ( -20.54999999999999716, 76.00000000001165290, -69.52310748452431710 ) ) ;
#83965=ORIENTED_EDGE ( 'NONE', *, *, #146273, .F. ) ;
#84013=FACE_OUTER_BOUND ( 'NONE', #18646, .T. ) ;
#84066=CARTESIAN_POINT ( 'NONE',  ( 18.59999999999999076, 70.05000000001165006, -59.21740517948951066 ) ) ;
#84086=DIRECTION ( 'NONE',  ( 0.000000000000000000, -2.771150684185008344E-14, -1.000000000000000000 ) ) ;
#84102=DIRECTION ( 'NONE',  ( 1.000000000000000000, 0.000000000000000000, 0.000000000000000000 ) ) ;
#84148=DIRECTION ( 'NONE',  ( 0.000000000000000000, 6.982962677686266711E-15, -1.000000000000000000 ) ) ;
#84177=FACE_OUTER_BOUND ( 'NONE', #185652, .T. ) ;
#84184=DIRECTION ( 'NONE',  ( -0.000000000000000000, 7.109473446599835262E-15, -1.000000000000000000 ) ) ;
#84187=DIRECTION ( 'NONE',  ( 0.000000000000000000, 0.000000000000000000, 1.000000000000000000 ) ) ;
#84251=DIRECTION ( 'NONE',  ( 0.000000000000000000, 7.109473446599835262E-15, -1.000000000000000000 ) ) ;
#84256=ADVANCED_FACE ( 'NONE', ( #217501 ), #176618, .T. ) ;
#84286=CARTESIAN_POINT ( 'NONE',  ( -18.50000000000000000, 77.16412189325258453, -28.10825939895270764 ) ) ;
#84320=DIRECTION ( 'NONE',  ( -1.836970198721029934E-16, -1.000000000000000000, -6.982962677686266711E-15 ) ) ;
#84323=EDGE_LOOP ( 'NONE', ( #225872, #17958, #30009 ) ) ;
#84324=EDGE_CURVE ( 'NONE', #31772, #118151, #41977, .T. ) ;
#84372=AXIS2_PLACEMENT_3D ( 'NONE', #86702, #65883, #247072 ) ;
#84390=DIRECTION ( 'NONE',  ( 0.000000000000000000, 7.086529944415894657E-15, -1.000000000000000000 ) ) ;
#84391=AXIS2_PLACEMENT_3D ( 'NONE', #135381, #36317, #92410 ) ;
#84412=( BOUNDED_SURFACE ( )  B_SPLINE_SURFACE ( 3, 2, ( 
 ( #231655, #34748, #109108 ),
 ( #132541, #193799, #114257 ),
 ( #154697, #33481, #252466 ),
 ( #192514, #253751, #75162 ),
 ( #169136, #55525, #1992 ),
 ( #97210, #37307, #116827 ) ),
 .UNSPECIFIED., .F., .F., .F. ) 
 B_SPLINE_SURFACE_WITH_KNOTS ( ( 4, 2, 4 ),
 ( 3, 3 ),
 ( 1.570796326794897668, 2.356194490192346169, 3.141592653589794448 ),
 ( 0.000000000000000000, 1.000000000000000000 ),
 .UNSPECIFIED. ) 
 GEOMETRIC_REPRESENTATION_ITEM ( )  RATIONAL_B_SPLINE_SURFACE ( (
 ( 1.000000000000000000, 0.7071067811865597852, 1.000000000000000000),
 ( 1.000000000000000000, 0.6611148371776831567, 1.000000000000000000),
 ( 1.000000000000000000, 0.6092287576699134677, 1.000000000000000000),
 ( 1.000000000000000000, 0.5278258667055114595, 1.000000000000000000),
 ( 1.000000000000000000, 0.4993418825336375932, 1.000000000000000000),
 ( 1.000000000000000000, 0.4999999999999704681, 1.000000000000000000) ) ) 
 REPRESENTATION_ITEM ( '' )  SURFACE ( )  );
#84424=DIRECTION ( 'NONE',  ( 2.827886303505249259E-16, 0.8660254037844377084, 0.5000000000000016653 ) ) ;
#84425=DIRECTION ( 'NONE',  ( 1.000000000000000000, 0.000000000000000000, 0.000000000000000000 ) ) ;
#84463=LINE ( 'NONE', #222726, #149251 ) ;
#84507=CARTESIAN_POINT ( 'NONE',  ( 21.53551880898956838, 69.21520223859533871, -69.62207721909604174 ) ) ;
#84524=ORIENTED_EDGE ( 'NONE', *, *, #52032, .F. ) ;
#84525=ORIENTED_EDGE ( 'NONE', *, *, #41844, .F. ) ;
#84543=CARTESIAN_POINT ( 'NONE',  ( -20.85000000000000142, 77.85161776048025217, -24.41991776492064758 ) ) ;
#84568=EDGE_CURVE ( 'NONE', #250305, #95482, #67086, .T. ) ;
#84579=CARTESIAN_POINT ( 'NONE',  ( 20.85000000000000142, 87.65000000001141700, -36.02310748452423894 ) ) ;
#84589=CARTESIAN_POINT ( 'NONE',  ( 20.94999999999999574, 76.00000000001165290, -69.52310748452431710 ) ) ;
#84600=LINE ( 'NONE', #160368, #239540 ) ;
#84621=CARTESIAN_POINT ( 'NONE',  ( -20.64999999999999858, 76.00000000001155342, -56.64810748452432421 ) ) ;
#84641=DIRECTION ( 'NONE',  ( -3.265361837132813093E-16, -1.000000000000000000, -6.982962677686266711E-15 ) ) ;
#84679=DIRECTION ( 'NONE',  ( -0.000000000000000000, -6.982962677686266711E-15, 1.000000000000000000 ) ) ;
#84697=CARTESIAN_POINT ( 'NONE',  ( 18.59999999999999076, 77.83585931145498193, -24.51866831572578675 ) ) ;
#84722=CARTESIAN_POINT ( 'NONE',  ( -21.64999999999999858, 68.65000000001150227, -48.37310748452437537 ) ) ;
#84735=CARTESIAN_POINT ( 'NONE',  ( -18.50000000000000000, 66.75000000001151079, -48.17310748452438673 ) ) ;
#84736=ORIENTED_EDGE ( 'NONE', *, *, #133036, .F. ) ;
#84743=VERTEX_POINT ( 'NONE', #105901 ) ;
#84779=DIRECTION ( 'NONE',  ( 1.000000000000000000, 0.000000000000000000, 0.000000000000000000 ) ) ;
#84837=VERTEX_POINT ( 'NONE', #152799 ) ;
#84839=AXIS2_PLACEMENT_3D ( 'NONE', #61292, #183803, #26025 ) ;
#84841=VERTEX_POINT ( 'NONE', #168522 ) ;
#84851=DIRECTION ( 'NONE',  ( 0.000000000000000000, -0.9908441862701605762, 0.1350103645451835310 ) ) ;
#84853=CARTESIAN_POINT ( 'NONE',  ( 19.58285714285715073, 66.98499851036301322, -61.10245466844266815 ) ) ;
#84854=CARTESIAN_POINT ( 'NONE',  ( 20.85000000000000142, 64.25000000001146816, -42.80697314750249660 ) ) ;
#84863=CIRCLE ( 'NONE', #209807, 0.6000000000000033085 ) ;
#84869=CARTESIAN_POINT ( 'NONE',  ( -18.58222699835055280, 65.66799936921481162, -30.42993998886009521 ) ) ;
#84893=AXIS2_PLACEMENT_3D ( 'NONE', #76990, #35345, #255580 ) ;
#84898=DIRECTION ( 'NONE',  ( -0.8660254037843878594, 0.000000000000000000, 0.5000000000000880407 ) ) ;
#84907=CARTESIAN_POINT ( 'NONE',  ( 22.40000000000010516, 76.00000000001269029, -81.27354037698326295 ) ) ;
#84953=DIRECTION ( 'NONE',  ( 0.000000000000000000, -6.982962677686266711E-15, 1.000000000000000000 ) ) ;
#85006=AXIS2_PLACEMENT_3D ( 'NONE', #54982, #77134, #96664 ) ;
#85029=VERTEX_POINT ( 'NONE', #147175 ) ;
#85040=CIRCLE ( 'NONE', #155832, 0.09999999999999938105 ) ;
#85045=VERTEX_POINT ( 'NONE', #224138 ) ;
#85079=ORIENTED_EDGE ( 'NONE', *, *, #52682, .F. ) ;
#85157=LINE ( 'NONE', #227273, #26883 ) ;
#85164=ORIENTED_EDGE ( 'NONE', *, *, #143649, .F. ) ;
#85176=CIRCLE ( 'NONE', #185364, 0.09999999999999907574 ) ;
#85191=CARTESIAN_POINT ( 'NONE',  ( -22.47071067811865319, 75.90090754530910999, -77.24318222902239484 ) ) ;
#85202=AXIS2_PLACEMENT_3D ( 'NONE', #128362, #207915, #25420 ) ;
#85274=DIRECTION ( 'NONE',  ( 1.000000000000000000, 0.000000000000000000, 0.000000000000000000 ) ) ;
#85310=CARTESIAN_POINT ( 'NONE',  ( -20.94999999999999929, 76.00000000001142553, -36.02310748452432421 ) ) ;
#85341=CARTESIAN_POINT ( 'NONE',  ( -22.59080734064477625, 64.25000000001165290, -69.55385719262143596 ) ) ;
#85351=ORIENTED_EDGE ( 'NONE', *, *, #94074, .F. ) ;
#85386=ORIENTED_EDGE ( 'NONE', *, *, #2790, .F. ) ;
#85410=CARTESIAN_POINT ( 'NONE',  ( -22.49917693094574389, 75.91477003579007032, -81.17290326905498432 ) ) ;
#85473=EDGE_CURVE ( 'NONE', #119594, #168638, #25950, .T. ) ;
#85480=VERTEX_POINT ( 'NONE', #47911 ) ;
#85497=AXIS2_PLACEMENT_3D ( 'NONE', #17468, #38333, #197382 ) ;
#85502=CARTESIAN_POINT ( 'NONE',  ( 19.75857864376269291, 64.35000000001147669, -44.77310748452440947 ) ) ;
#85546=DIRECTION ( 'NONE',  ( 0.000000000000000000, 1.000000000000000000, 6.982962677686266711E-15 ) ) ;
#85564=VERTEX_POINT ( 'NONE', #94745 ) ;
#85600=EDGE_CURVE ( 'NONE', #46741, #16741, #946, .T. ) ;
#85613=DIRECTION ( 'NONE',  ( 0.000000000000000000, -0.2605042016806647931, -0.9654727137038724427 ) ) ;
#85629=TOROIDAL_SURFACE ( 'NONE', #231427, 0.4000000000000005773, 0.1000000000000000056 ) ;
#85645=DIRECTION ( 'NONE',  ( 0.000000000000000000, 0.000000000000000000, 1.000000000000000000 ) ) ;
#85648=EDGE_CURVE ( 'NONE', #87492, #239369, #67435, .T. ) ;
#85659=AXIS2_PLACEMENT_3D ( 'NONE', #223905, #201786, #60992 ) ;
#85689=DIRECTION ( 'NONE',  ( 0.000000000000000000, 0.9915357197604849349, -0.1298341882520056834 ) ) ;
#85726=DIRECTION ( 'NONE',  ( 1.000000000000000000, -3.265361837132813093E-16, -2.280189983783949500E-30 ) ) ;
#85735=ORIENTED_EDGE ( 'NONE', *, *, #238737, .T. ) ;
#85755=DIRECTION ( 'NONE',  ( 1.000000000000000000, -2.952720810173289112E-16, -2.061873921506763405E-30 ) ) ;
#85775=ORIENTED_EDGE ( 'NONE', *, *, #70948, .F. ) ;
#85791=EDGE_CURVE ( 'NONE', #218866, #101771, #230115, .T. ) ;
#85812=ORIENTED_EDGE ( 'NONE', *, *, #229620, .T. ) ;
#85866=ORIENTED_EDGE ( 'NONE', *, *, #142470, .F. ) ;
#85880=VECTOR ( 'NONE', #114784, 1000.000000000000000 ) ;
#85882=DIRECTION ( 'NONE',  ( 1.000000000000000000, 0.000000000000000000, 0.000000000000000000 ) ) ;
#85964=VERTEX_POINT ( 'NONE', #69770 ) ;
#85967=DIRECTION ( 'NONE',  ( -0.000000000000000000, -6.982962677686266711E-15, 1.000000000000000000 ) ) ;
#85985=CARTESIAN_POINT ( 'NONE',  ( -20.94999999999999929, 76.00000000001142553, -36.02310748452432421 ) ) ;
#85986=PRESENTATION_STYLE_ASSIGNMENT (( #120044 ) ) ;
#86008=CYLINDRICAL_SURFACE ( 'NONE', #89545, 0.09999999999999939493 ) ;
#86014=ORIENTED_EDGE ( 'NONE', *, *, #228046, .T. ) ;
#86030=CIRCLE ( 'NONE', #48643, 0.09999999999999739653 ) ;
#86099=FACE_OUTER_BOUND ( 'NONE', #148590, .T. ) ;
#86114=DIRECTION ( 'NONE',  ( -1.000000000000000000, 0.000000000000000000, 0.000000000000000000 ) ) ;
#86137=CARTESIAN_POINT ( 'NONE',  ( 20.95443524775735256, 67.12144573613879572, -60.98938520892424009 ) ) ;
#86151=FACE_OUTER_BOUND ( 'NONE', #108397, .T. ) ;
#86152=ADVANCED_FACE ( 'NONE', ( #5591 ), #71928, .T. ) ;
#86153=ADVANCED_FACE ( 'NONE', ( #105979 ), #230790, .F. ) ;
#86175=DIRECTION ( 'NONE',  ( 1.000000000000000000, 0.000000000000000000, 0.000000000000000000 ) ) ;
#86176=FACE_OUTER_BOUND ( 'NONE', #122969, .T. ) ;
#86178=CARTESIAN_POINT ( 'NONE',  ( -20.64999999999999858, 71.65000000001155911, -57.17310748452435121 ) ) ;
#86191=CARTESIAN_POINT ( 'NONE',  ( -20.94999999999999929, 77.16270174994961906, -61.52310748452431710 ) ) ;
#86225=CARTESIAN_POINT ( 'NONE',  ( -23.15000000000000213, 76.00000000001142553, -36.02310748452432421 ) ) ;
#86228=AXIS2_PLACEMENT_3D ( 'NONE', #236460, #237747, #14873 ) ;
#86229=ORIENTED_EDGE ( 'NONE', *, *, #23788, .T. ) ;
#86237=AXIS2_PLACEMENT_3D ( 'NONE', #7859, #125229, #166957 ) ;
#86246=CARTESIAN_POINT ( 'NONE',  ( -20.85000000000000142, 64.35000000001141984, -36.02310748452440237 ) ) ;
#86257=ORIENTED_EDGE ( 'NONE', *, *, #222976, .T. ) ;
#86261=ORIENTED_EDGE ( 'NONE', *, *, #99185, .T. ) ;
#86283=CARTESIAN_POINT ( 'NONE',  ( -23.25000000000000000, 71.85000000001151932, -48.37310748452435405 ) ) ;
#86304=DIRECTION ( 'NONE',  ( 1.000000000000000000, 0.000000000000000000, 0.000000000000000000 ) ) ;
#86324=CYLINDRICAL_SURFACE ( 'NONE', #60389, 0.1000000000000028644 ) ;
#86326=ORIENTED_EDGE ( 'NONE', *, *, #202030, .F. ) ;
#86341=EDGE_CURVE ( 'NONE', #88995, #70665, #242769, .T. ) ;
#86353=CARTESIAN_POINT ( 'NONE',  ( -18.59999999999999787, 64.25000000001161027, -62.50830171387040934 ) ) ;
#86357=ORIENTED_EDGE ( 'NONE', *, *, #123735, .T. ) ;
#86366=EDGE_LOOP ( 'NONE', ( #175514, #205724, #169865, #253237 ) ) ;
#86429=FACE_OUTER_BOUND ( 'NONE', #147043, .T. ) ;
#86430=DIRECTION ( 'NONE',  ( 0.000000000000000000, -6.467318590049456648E-15, 1.000000000000000000 ) ) ;
#86432=VERTEX_POINT ( 'NONE', #24581 ) ;
#86439=DIRECTION ( 'NONE',  ( 0.000000000000000000, 0.5000000000000209832, 0.8660254037844264952 ) ) ;
#86444=CARTESIAN_POINT ( 'NONE',  ( 18.49999999999999289, 65.79142135624904597, -81.27310748452438816 ) ) ;
#86447=AXIS2_PLACEMENT_3D ( 'NONE', #64736, #85546, #46447 ) ;
#86481=CARTESIAN_POINT ( 'NONE',  ( 20.95539060131842746, 65.37613784235595915, -61.86937367086819961 ) ) ;
#86483=CARTESIAN_POINT ( 'NONE',  ( -21.93340585899449380, 76.00000000001170974, -76.84725450664456048 ) ) ;
#86488=CARTESIAN_POINT ( 'NONE',  ( 22.00356870069427018, 76.00000000002543743, -76.77734984627505810 ) ) ;
#86494=CYLINDRICAL_SURFACE ( 'NONE', #170425, 0.5000000000000004441 ) ;
#86503=DIRECTION ( 'NONE',  ( 0.000000000000000000, 0.000000000000000000, -1.000000000000000000 ) ) ;
#86518=CARTESIAN_POINT ( 'NONE',  ( -21.08078803292166725, 75.92081401285399522, -75.85612044896146244 ) ) ;
#86519=DIRECTION ( 'NONE',  ( 0.000000000000000000, 0.000000000000000000, 1.000000000000000000 ) ) ;
#86522=ADVANCED_FACE ( 'NONE', ( #67529 ), #248746, .T. ) ;
#86564=CARTESIAN_POINT ( 'NONE',  ( 23.14999999999999503, 69.35000000001156195, -57.37310748452436826 ) ) ;
#86574=ORIENTED_EDGE ( 'NONE', *, *, #201003, .T. ) ;
#86585=VERTEX_POINT ( 'NONE', #88351 ) ;
#86586=CARTESIAN_POINT ( 'NONE',  ( 23.14999999999999503, 69.45000000001149942, -48.37310748452436826 ) ) ;
#86649=ORIENTED_EDGE ( 'NONE', *, *, #100628, .T. ) ;
#86679=CARTESIAN_POINT ( 'NONE',  ( 18.49999999999999645, 74.36282728704118483, -57.94095411905231430 ) ) ;
#86702=CARTESIAN_POINT ( 'NONE',  ( -22.59999999999999787, 76.00000000001165290, -69.52310748452431710 ) ) ;
#86714=CIRCLE ( 'NONE', #132537, 0.09999999999999939493 ) ;
#86726=EDGE_LOOP ( 'NONE', ( #229614, #226558, #8822, #232597, #148053, #165167, #102882, #185174, #122730, #52478 ) ) ;
#86743=CARTESIAN_POINT ( 'NONE',  ( 21.13461538461538680, 67.11458296203711882, -57.27310748452438816 ) ) ;
#86789=CARTESIAN_POINT ( 'NONE',  ( -23.15000000000000213, 85.00000000001149658, -45.91707660717669626 ) ) ;
#86808=CARTESIAN_POINT ( 'NONE',  ( 20.04142135623731136, 64.25000000001148237, -44.87310748452440379 ) ) ;
#86864=CARTESIAN_POINT ( 'NONE',  ( -18.54118089899631983, 85.46353763185970820, -62.47452988665613560 ) ) ;
#86887=CARTESIAN_POINT ( 'NONE',  ( 23.14999999999998437, 76.00000000001165290, -69.52310748452431710 ) ) ;
#86898=AXIS2_PLACEMENT_3D ( 'NONE', #141760, #204298, #240884 ) ;
#86905=EDGE_LOOP ( 'NONE', ( #231850, #11359, #177184, #222698 ) ) ;
#86908=ADVANCED_FACE ( 'NONE', ( #24268 ), #168368, .T. ) ;
#86945=ORIENTED_EDGE ( 'NONE', *, *, #186548, .T. ) ;
#86948=VERTEX_POINT ( 'NONE', #58215 ) ;
#86955=CARTESIAN_POINT ( 'NONE',  ( -21.05000000000000071, 87.48912529308769592, -66.52310748452423184 ) ) ;
#86958=DIRECTION ( 'NONE',  ( 1.000000000000000000, 7.304098846218135653E-16, 5.311601492717085047E-30 ) ) ;
#86960=DIRECTION ( 'NONE',  ( 0.000000000000000000, 0.6728971962617172897, -0.7397360091702445128 ) ) ;
#86987=CARTESIAN_POINT ( 'NONE',  ( 20.94999999999999929, 76.00000000001142553, -36.02310748452432421 ) ) ;
#86993=ORIENTED_EDGE ( 'NONE', *, *, #183914, .T. ) ;
#86997=CARTESIAN_POINT ( 'NONE',  ( -18.50000000000000000, 66.85000000001173248, -81.27310748452438816 ) ) ;
#87056=DIRECTION ( 'NONE',  ( 2.978066053179066272E-16, 1.000000000000000000, 7.147358527629759053E-15 ) ) ;
#87064=ORIENTED_EDGE ( 'NONE', *, *, #191823, .F. ) ;
#87072=CARTESIAN_POINT ( 'NONE',  ( 23.24999999999997513, 64.35000000001146248, -43.03791325517834565 ) ) ;
#87115=DIRECTION ( 'NONE',  ( 3.616040088954490704E-32, 7.105427357601001859E-15, -1.000000000000000000 ) ) ;
#87140=CIRCLE ( 'NONE', #253537, 0.1000000000000028644 ) ;
#87161=CARTESIAN_POINT ( 'NONE',  ( 18.59999999999999076, 65.79142135624879018, -44.87310748452438958 ) ) ;
#87162=EDGE_CURVE ( 'NONE', #251301, #137039, #197344, .T. ) ;
#87186=CARTESIAN_POINT ( 'NONE',  ( -20.54999999999999716, 76.00000000001142553, -36.02310748452432421 ) ) ;
#87195=DIRECTION ( 'NONE',  ( 1.000000000000000000, 0.000000000000000000, 0.000000000000000000 ) ) ;
#87199=CARTESIAN_POINT ( 'NONE',  ( 18.59999999999999432, 77.16270174994961906, -61.42310748452431568 ) ) ;
#87233=CARTESIAN_POINT ( 'NONE',  ( -21.05000000000000071, 64.35000000001161879, -62.73924182154625129 ) ) ;
#87261=LINE ( 'NONE', #166859, #63346 ) ;
#87280=DIRECTION ( 'NONE',  ( 0.000000000000000000, -1.000000000000000000, -6.982962677686265922E-15 ) ) ;
#87299=EDGE_CURVE ( 'NONE', #235880, #182847, #216987, .T. ) ;
#87333=ORIENTED_EDGE ( 'NONE', *, *, #209519, .F. ) ;
#87359=CARTESIAN_POINT ( 'NONE',  ( 23.24999999999999645, 79.90000000001141700, -36.02310748452429578 ) ) ;
#87385=AXIS2_PLACEMENT_3D ( 'NONE', #257452, #80116, #78854 ) ;
#87393=VERTEX_POINT ( 'NONE', #66920 ) ;
#87409=AXIS2_PLACEMENT_3D ( 'NONE', #65158, #149861, #104274 ) ;
#87412=AXIS2_PLACEMENT_3D ( 'NONE', #183363, #46389, #107658 ) ;
#87419=CARTESIAN_POINT ( 'NONE',  ( 23.15000000000000213, 85.50000000001149658, -45.91707660717669626 ) ) ;
#87426=EDGE_CURVE ( 'NONE', #47971, #228818, #85157, .T. ) ;
#87460=CIRCLE ( 'NONE', #120822, 0.1000000000000028644 ) ;
#87467=CIRCLE ( 'NONE', #124906, 0.1000000000000028644 ) ;
#87491=ORIENTED_EDGE ( 'NONE', *, *, #52682, .T. ) ;
#87492=VERTEX_POINT ( 'NONE', #30384 ) ;
#87495=CARTESIAN_POINT ( 'NONE',  ( 18.49999999999999289, 65.50857864377418593, -44.67310748452439384 ) ) ;
#87540=DIRECTION ( 'NONE',  ( -1.000000000000000000, 0.000000000000000000, 0.000000000000000000 ) ) ;
#87545=DIRECTION ( 'NONE',  ( 1.000000000000000000, 0.000000000000000000, 0.000000000000000000 ) ) ;
#87565=AXIS2_PLACEMENT_3D ( 'NONE', #122755, #204, #241408 ) ;
#87566=TOROIDAL_SURFACE ( 'NONE', #112535, 11.65000000000000036, 0.1000000000000000056 ) ;
#87577=CARTESIAN_POINT ( 'NONE',  ( 21.04999999999999716, 76.03753606329739512, -75.85537975845998915 ) ) ;
#87596=ORIENTED_EDGE ( 'NONE', *, *, #57661, .F. ) ;
#87598=LINE ( 'NONE', #216210, #67355 ) ;
#87613=AXIS2_PLACEMENT_3D ( 'NONE', #127552, #70172, #89689 ) ;
#87660=VERTEX_POINT ( 'NONE', #219264 ) ;
#87685=B_SPLINE_CURVE_WITH_KNOTS ( 'NONE', 3,
 ( #168887, #30640, #248381, #151878 ),
 .UNSPECIFIED., .F., .F.,
 ( 4, 4 ),
 ( 0.000000000000000000, 0.0002118541922231799543 ),
 .UNSPECIFIED. ) ;
#87707=TOROIDAL_SURFACE ( 'NONE', #233501, 0.2000000000000000111, 0.1000000000000000056 ) ;
#87708=ADVANCED_FACE ( 'NONE', ( #86151 ), #142298, .T. ) ;
#87712=ORIENTED_EDGE ( 'NONE', *, *, #125617, .T. ) ;
#87716=CARTESIAN_POINT ( 'NONE',  ( -18.59999999999999787, 64.40000000001161595, -62.59490425424885274 ) ) ;
#87729=CARTESIAN_POINT ( 'NONE',  ( 20.95262331984758575, 65.49584273722187788, -61.96221915493101307 ) ) ;
#87739=DIRECTION ( 'NONE',  ( 0.000000000000000000, -6.467318590049456648E-15, 1.000000000000000000 ) ) ;
#87766=VERTEX_POINT ( 'NONE', #24952 ) ;
#87815=CARTESIAN_POINT ( 'NONE',  ( -23.15000000000000213, 76.00000000001156764, -56.74810748452433273 ) ) ;
#87821=ADVANCED_FACE ( 'NONE', ( #26228 ), #206137, .F. ) ;
#87838=CARTESIAN_POINT ( 'NONE',  ( 20.94999999999999929, 71.00000000001151079, -48.42837350343745584 ) ) ;
#87840=DIRECTION ( 'NONE',  ( -0.000000000000000000, 6.982962677686266711E-15, -1.000000000000000000 ) ) ;
#87845=DIRECTION ( 'NONE',  ( 0.000000000000000000, -7.429790795770647916E-15, 1.000000000000000000 ) ) ;
#87846=EDGE_LOOP ( 'NONE', ( #205090, #48170, #161409, #198601 ) ) ;
#87850=EDGE_CURVE ( 'NONE', #44347, #72194, #156726, .T. ) ;
#87860=DIRECTION ( 'NONE',  ( -1.000000000000000000, 0.000000000000000000, -0.000000000000000000 ) ) ;
#87875=ORIENTED_EDGE ( 'NONE', *, *, #178998, .F. ) ;
#87890=DIRECTION ( 'NONE',  ( -0.000000000000000000, 6.982962677686266711E-15, -1.000000000000000000 ) ) ;
#87898=ORIENTED_EDGE ( 'NONE', *, *, #215880, .F. ) ;
#87906=PLANE ( 'NONE',  #126632 ) ;
#87920=EDGE_CURVE ( 'NONE', #152615, #195996, #244154, .T. ) ;
#87958=DIRECTION ( 'NONE',  ( -1.000000000000000000, 0.000000000000000000, -0.000000000000000000 ) ) ;
#87960=DIRECTION ( 'NONE',  ( -1.000000000000000000, -0.000000000000000000, -0.000000000000000000 ) ) ;
#87977=DIRECTION ( 'NONE',  ( -0.000000000000000000, 0.8660254037844424824, 0.4999999999999934497 ) ) ;
#88002=VECTOR ( 'NONE', #74202, 1000.000000000000000 ) ;
#88013=CARTESIAN_POINT ( 'NONE',  ( 23.14999999999999858, 69.35000000001156195, -57.17310748452436542 ) ) ;
#88014=DIRECTION ( 'NONE',  ( 0.000000000000000000, 0.000000000000000000, 1.000000000000000000 ) ) ;
#88022=CARTESIAN_POINT ( 'NONE',  ( -18.50000000000000000, 77.36242903720467723, -28.13422623660311217 ) ) ;
#88040=ORIENTED_EDGE ( 'NONE', *, *, #143188, .F. ) ;
#88049=CARTESIAN_POINT ( 'NONE',  ( -23.15000000000000213, 76.00000000001165290, -69.52310748452431710 ) ) ;
#88051=ADVANCED_FACE ( 'NONE', ( #46405 ), #89386, .F. ) ;
#88059=AXIS2_PLACEMENT_3D ( 'NONE', #140781, #102911, #243732 ) ;
#88063=DIRECTION ( 'NONE',  ( 0.000000000000000000, 0.000000000000000000, 1.000000000000000000 ) ) ;
#88082=DIRECTION ( 'NONE',  ( 0.000000000000000000, 0.000000000000000000, 1.000000000000000000 ) ) ;
#88137=CARTESIAN_POINT ( 'NONE',  ( -18.46902351632713746, 85.50947011869244818, -62.53665355026694073 ) ) ;
#88139=VERTEX_POINT ( 'NONE', #208085 ) ;
#88143=CARTESIAN_POINT ( 'NONE',  ( 20.94999999999999929, 65.27628289530404970, -57.37310748452439668 ) ) ;
#88172=CARTESIAN_POINT ( 'NONE',  ( 20.94999999999999929, 64.36312671090679771, -42.84486669784945434 ) ) ;
#88178=CIRCLE ( 'NONE', #138092, 0.1000000000000028644 ) ;
#88187=CYLINDRICAL_SURFACE ( 'NONE', #145253, 0.09999999999999939493 ) ;
#88198=CARTESIAN_POINT ( 'NONE',  ( -22.39999999999999858, 76.00000000001165290, -69.52310748452431710 ) ) ;
#88207=EDGE_CURVE ( 'NONE', #175419, #76430, #11123, .T. ) ;
#88208=( BOUNDED_SURFACE ( )  B_SPLINE_SURFACE ( 3, 2, ( 
 ( #174737, #73059, #152589 ),
 ( #252925, #58566, #216370 ),
 ( #195556, #153893, #116013 ),
 ( #114711, #55991, #156445 ),
 ( #136831, #215092, #232109 ),
 ( #14356, #92563, #57277 ) ),
 .UNSPECIFIED., .F., .F., .F. ) 
 B_SPLINE_SURFACE_WITH_KNOTS ( ( 4, 2, 4 ),
 ( 3, 3 ),
 ( 0.0001300404313046710908, 0.0003183318589266704419, 0.0005066232865486697658 ),
 ( 0.000000000000000000, 1.000000000000000000 ),
 .UNSPECIFIED. ) 
 GEOMETRIC_REPRESENTATION_ITEM ( )  RATIONAL_B_SPLINE_SURFACE ( (
 ( 1.000000000000000000, 0.7071067811865597852, 1.000000000000000000),
 ( 1.000000000000000000, 0.7625113560540824897, 1.000000000000000000),
 ( 1.000000000000000000, 0.8126073484687461601, 1.000000000000000000),
 ( 1.000000000000000000, 0.8923049332733758998, 1.000000000000000000),
 ( 1.000000000000000000, 0.9231914937768594953, 1.000000000000000000),
 ( 1.000000000000000000, 0.9238795325112947321, 1.000000000000000000) ) ) 
 REPRESENTATION_ITEM ( '' )  SURFACE ( )  );
#88241=DIRECTION ( 'NONE',  ( -1.000000000000000000, -0.000000000000000000, -0.000000000000000000 ) ) ;
#88246=AXIS2_PLACEMENT_3D ( 'NONE', #2431, #123692, #40336 ) ;
#88291=ORIENTED_EDGE ( 'NONE', *, *, #54244, .F. ) ;
#88293=DIRECTION ( 'NONE',  ( 1.000000000000000000, 0.000000000000000000, 0.000000000000000000 ) ) ;
#88303=VERTEX_POINT ( 'NONE', #201337 ) ;
#88338=CIRCLE ( 'NONE', #196689, 4.150000000000001243 ) ;
#88345=AXIS2_PLACEMENT_3D ( 'NONE', #129918, #71268, #252431 ) ;
#88351=CARTESIAN_POINT ( 'NONE',  ( 18.52928932188133970, 65.72071067813013201, -44.87310748452439668 ) ) ;
#88392=CARTESIAN_POINT ( 'NONE',  ( 18.59999999999999076, 77.14957036958705316, -28.20719500002235236 ) ) ;
#88399=B_SPLINE_CURVE_WITH_KNOTS ( 'NONE', 3,
 ( #83594, #23692, #184011, #201021, #225676, #43230 ),
 .UNSPECIFIED., .F., .F.,
 ( 4, 2, 4 ),
 ( 0.000000000000000000, 0.0001497467027049268525, 0.0002994934054098537051 ),
 .UNSPECIFIED. ) ;
#88431=CARTESIAN_POINT ( 'NONE',  ( -20.54999999999999716, 68.75000000001151079, -48.27310748452437394 ) ) ;
#88432=TOROIDAL_SURFACE ( 'NONE', #155139, 1.900000000000002576, 0.1000000000000000056 ) ;
#88459=ADVANCED_FACE ( 'NONE', ( #83907 ), #163497, .T. ) ;
#88477=VERTEX_POINT ( 'NONE', #223451 ) ;
#88500=LINE ( 'NONE', #105490, #91371 ) ;
#88511=CARTESIAN_POINT ( 'NONE',  ( 23.15000000000000213, 87.39257802171711376, -39.09705706435617856 ) ) ;
#88519=DIRECTION ( 'NONE',  ( 0.000000000000000000, 6.982962677686266711E-15, -1.000000000000000000 ) ) ;
#88538=VERTEX_POINT ( 'NONE', #154253 ) ;
#88562=FACE_OUTER_BOUND ( 'NONE', #72888, .T. ) ;
#88576=VERTEX_POINT ( 'NONE', #214182 ) ;
#88589=FACE_OUTER_BOUND ( 'NONE', #128284, .T. ) ;
#88620=EDGE_LOOP ( 'NONE', ( #5064, #29695, #236619 ) ) ;
#88645=DIRECTION ( 'NONE',  ( 1.000000000000000000, 0.000000000000000000, 0.000000000000000000 ) ) ;
#88660=DIRECTION ( 'NONE',  ( 0.000000000000000000, -7.116814260417668513E-15, 1.000000000000000000 ) ) ;
#88697=DIRECTION ( 'NONE',  ( -0.000000000000000000, -0.6132151058540604716, 0.7899159663865477077 ) ) ;
#88707=DIRECTION ( 'NONE',  ( -0.000000000000000000, 1.000000000000000000, 6.982962677686266711E-15 ) ) ;
#88726=AXIS2_PLACEMENT_3D ( 'NONE', #55543, #136365, #114272 ) ;
#88798=CARTESIAN_POINT ( 'NONE',  ( -18.59999999999999787, 68.97833521811131163, -32.38954208262708079 ) ) ;
#88837=DIRECTION ( 'NONE',  ( -0.7071067811865475727, 0.7071067811865475727, 4.937700262164531476E-15 ) ) ;
#88852=EDGE_CURVE ( 'NONE', #213807, #89961, #96323, .T. ) ;
#88880=DIRECTION ( 'NONE',  ( 0.000000000000000000, 1.000000000000000000, 1.387778780781444413E-14 ) ) ;
#88905=EDGE_CURVE ( 'NONE', #21530, #90111, #34768, .T. ) ;
#88910=CIRCLE ( 'NONE', #34997, 0.1000000000000052097 ) ;
#88919=CARTESIAN_POINT ( 'NONE',  ( -20.94999999999999929, 87.65000000001163016, -66.62310748452424036 ) ) ;
#88958=ORIENTED_EDGE ( 'NONE', *, *, #191934, .T. ) ;
#88980=CARTESIAN_POINT ( 'NONE',  ( 18.49999999999999645, 70.05000000001165006, -59.21740517948951066 ) ) ;
#88990=TOROIDAL_SURFACE ( 'NONE', #143152, 11.65000000000000036, 0.1000000000000000056 ) ;
#88995=VERTEX_POINT ( 'NONE', #200578 ) ;
#89068=CARTESIAN_POINT ( 'NONE',  ( 20.95512820512820440, 65.37615131629972609, -61.85819391543678591 ) ) ;
#89083=B_SPLINE_CURVE_WITH_KNOTS ( 'NONE', 3,
 ( #8641, #169037, #88137, #248531, #86864, #167740, #110302, #231548 ),
 .UNSPECIFIED., .F., .F.,
 ( 4, 2, 2, 4 ),
 ( 0.000000000000000000, 0.0001049670497870057353, 0.0002099340995740114706, 0.0004198681991480003898 ),
 .UNSPECIFIED. ) ;
#89090=DIRECTION ( 'NONE',  ( 0.000000000000000000, 0.000000000000000000, -1.000000000000000000 ) ) ;
#89114=CIRCLE ( 'NONE', #143459, 0.1999999999999987899 ) ;
#89140=ORIENTED_EDGE ( 'NONE', *, *, #166328, .T. ) ;
#89158=LINE ( 'NONE', #27948, #231066 ) ;
#89195=CARTESIAN_POINT ( 'NONE',  ( 21.09696443733127325, 65.27599011609309798, -57.28832995747617218 ) ) ;
#89227=ORIENTED_EDGE ( 'NONE', *, *, #168780, .T. ) ;
#89250=CARTESIAN_POINT ( 'NONE',  ( 21.04116576186320842, 65.37533692126021378, -57.19452571589663847 ) ) ;
#89286=CARTESIAN_POINT ( 'NONE',  ( -22.50000000000000000, 75.90000000001172964, -81.17267829206912211 ) ) ;
#89289=DIRECTION ( 'NONE',  ( -1.000000000000000000, 0.000000000000000000, 0.000000000000000000 ) ) ;
#89290=VERTEX_POINT ( 'NONE', #75380 ) ;
#89313=ORIENTED_EDGE ( 'NONE', *, *, #250555, .T. ) ;
#89321=VERTEX_POINT ( 'NONE', #94901 ) ;
#89350=DIRECTION ( 'NONE',  ( 0.000000000000000000, 0.000000000000000000, 1.000000000000000000 ) ) ;
#89354=EDGE_LOOP ( 'NONE', ( #173316, #185481, #107007, #222425 ) ) ;
#89355=ORIENTED_EDGE ( 'NONE', *, *, #235771, .T. ) ;
#89367=CARTESIAN_POINT ( 'NONE',  ( -20.64999999999999858, 71.75000000001156764, -57.27310748452435263 ) ) ;
#89385=ADVANCED_FACE ( 'NONE', ( #173223 ), #126503, .T. ) ;
#89386=CYLINDRICAL_SURFACE ( 'NONE', #173497, 0.1000000000000028644 ) ;
#89397=ORIENTED_EDGE ( 'NONE', *, *, #135283, .F. ) ;
#89437=CARTESIAN_POINT ( 'NONE',  ( 21.05000000000000071, 70.15000000001163016, -59.39061026024639034 ) ) ;
#89462=DIRECTION ( 'NONE',  ( 0.000000000000000000, -6.853228547068871147E-15, 1.000000000000000000 ) ) ;
#89463=AXIS2_PLACEMENT_3D ( 'NONE', #173064, #76471, #73951 ) ;
#89467=EDGE_CURVE ( 'NONE', #116008, #47209, #230755, .T. ) ;
#89472=CARTESIAN_POINT ( 'NONE',  ( -18.59999999999999787, 70.05000000001165006, -59.21740517948951066 ) ) ;
#89474=CARTESIAN_POINT ( 'NONE',  ( 21.02374657821574644, 64.39999999919136542, -42.95131071432642500 ) ) ;
#89478=ADVANCED_FACE ( 'NONE', ( #200435 ), #180877, .T. ) ;
#89498=CARTESIAN_POINT ( 'NONE',  ( -21.33487959338958362, 69.27444184810046579, -69.52310748452435973 ) ) ;
#89544=DIRECTION ( 'NONE',  ( -1.000000000000000000, 0.000000000000000000, -0.000000000000000000 ) ) ;
#89545=AXIS2_PLACEMENT_3D ( 'NONE', #46897, #245122, #66483 ) ;
#89555=AXIS2_PLACEMENT_3D ( 'NONE', #210728, #255909, #248565 ) ;
#89556=CIRCLE ( 'NONE', #152139, 0.1000000000000028644 ) ;
#89557=DIRECTION ( 'NONE',  ( 0.000000000000000000, -6.240597636138643358E-14, -1.000000000000000000 ) ) ;
#89563=EDGE_LOOP ( 'NONE', ( #7160, #101283, #194411, #143055 ) ) ;
#89643=EDGE_CURVE ( 'NONE', #186334, #73251, #230950, .T. ) ;
#89651=ORIENTED_EDGE ( 'NONE', *, *, #127357, .F. ) ;
#89654=ORIENTED_EDGE ( 'NONE', *, *, #158322, .T. ) ;
#89659=CARTESIAN_POINT ( 'NONE',  ( -20.99142135623731420, 64.40000000001147384, -42.95131071479990226 ) ) ;
#89663=( NAMED_UNIT ( * ) SI_UNIT ( $, .STERADIAN. ) SOLID_ANGLE_UNIT ( ) );
#89672=DIRECTION ( 'NONE',  ( 0.000000000000000000, -1.000000000000000000, -6.982962677686265922E-15 ) ) ;
#89689=DIRECTION ( 'NONE',  ( -1.000000000000000000, 0.000000000000000000, 0.000000000000000000 ) ) ;
#89694=ORIENTED_EDGE ( 'NONE', *, *, #498, .T. ) ;
#89706=VERTEX_POINT ( 'NONE', #179002 ) ;
#89728=EDGE_CURVE ( 'NONE', #136766, #96347, #105992, .T. ) ;
#89752=DIRECTION ( 'NONE',  ( 0.000000000000000000, 0.000000000000000000, 1.000000000000000000 ) ) ;
#89787=DIRECTION ( 'NONE',  ( 1.000000000000000000, 0.000000000000000000, 0.000000000000000000 ) ) ;
#89798=AXIS2_PLACEMENT_3D ( 'NONE', #225615, #46985, #126550 ) ;
#89808=CARTESIAN_POINT ( 'NONE',  ( -20.64999999999999858, 85.00000000001149658, -45.41707660717669626 ) ) ;
#89829=ORIENTED_EDGE ( 'NONE', *, *, #160278, .T. ) ;
#89856=CARTESIAN_POINT ( 'NONE',  ( -21.14999999999999858, 76.10000000001170406, -75.77310748452431710 ) ) ;
#89859=CARTESIAN_POINT ( 'NONE',  ( -18.59999999999999787, 68.97833521811131163, -32.18954208262707795 ) ) ;
#89869=DIRECTION ( 'NONE',  ( 1.000000000000000000, -2.952720810173289112E-16, -2.061873921506763405E-30 ) ) ;
#89873=VERTEX_POINT ( 'NONE', #23773 ) ;
#89911=DIRECTION ( 'NONE',  ( 0.000000000000000000, 6.938893903907234689E-15, -1.000000000000000000 ) ) ;
#89961=VERTEX_POINT ( 'NONE', #52263 ) ;
#89975=DIRECTION ( 'NONE',  ( 2.952720810173289112E-16, 1.000000000000000000, 6.308085367188367561E-15 ) ) ;
#89976=CIRCLE ( 'NONE', #235717, 0.1999999999999987899 ) ;
#89993=CARTESIAN_POINT ( 'NONE',  ( -22.39999999999999858, 76.00000000001169553, -75.77310748452431710 ) ) ;
#90076=AXIS2_PLACEMENT_3D ( 'NONE', #115589, #96015, #175584 ) ;
#90089=FACE_OUTER_BOUND ( 'NONE', #32458, .T. ) ;
#90093=VERTEX_POINT ( 'NONE', #136951 ) ;
#90111=VERTEX_POINT ( 'NONE', #176110 ) ;
#90114=ORIENTED_EDGE ( 'NONE', *, *, #145117, .T. ) ;
#90117=AXIS2_PLACEMENT_3D ( 'NONE', #256314, #77726, #37357 ) ;
#90156=ORIENTED_EDGE ( 'NONE', *, *, #225162, .T. ) ;
#90180=CARTESIAN_POINT ( 'NONE',  ( -20.00857864376270001, 66.85000000001156195, -57.17310748452438673 ) ) ;
#90182=ORIENTED_EDGE ( 'NONE', *, *, #109317, .T. ) ;
#90243=DIRECTION ( 'NONE',  ( 1.000000000000000000, 0.000000000000000000, 0.000000000000000000 ) ) ;
#90247=ORIENTED_EDGE ( 'NONE', *, *, #147667, .F. ) ;
#90262=CARTESIAN_POINT ( 'NONE',  ( -23.25000000000000000, 68.97833521811131163, -32.18954208262707795 ) ) ;
#90275=AXIS2_PLACEMENT_3D ( 'NONE', #29645, #247365, #148279 ) ;
#90308=DIRECTION ( 'NONE',  ( -1.000000000000000000, 0.000000000000000000, -0.000000000000000000 ) ) ;
#90315=CYLINDRICAL_SURFACE ( 'NONE', #232930, 7.900000000000000355 ) ;
#90336=TOROIDAL_SURFACE ( 'NONE', #94615, 11.65000000000000036, 0.1000000000000000056 ) ;
#90353=CARTESIAN_POINT ( 'NONE',  ( 20.94999999999999574, 77.16270174994961906, -61.42310748452431568 ) ) ;
#90370=CARTESIAN_POINT ( 'NONE',  ( 22.57320508075687115, 64.25000000001165290, -69.52310748452440237 ) ) ;
#90378=CARTESIAN_POINT ( 'NONE',  ( 21.05000000000000071, 87.48912529308749697, -39.12310748452424747 ) ) ;
#90402=DIRECTION ( 'NONE',  ( 0.000000000000000000, 6.467318590049456648E-15, -1.000000000000000000 ) ) ;
#90415=CIRCLE ( 'NONE', #202838, 0.09999999999999939493 ) ;
#90425=CARTESIAN_POINT ( 'NONE',  ( 20.94999999999999929, 64.35000000001146248, -42.80697314750249660 ) ) ;
#90477=CARTESIAN_POINT ( 'NONE',  ( 21.13507111622889667, 65.28231661301319377, -57.27393889816360684 ) ) ;
#90498=TOROIDAL_SURFACE ( 'NONE', #123848, 2.100000000000002309, 0.1000000000000000056 ) ;
#90513=ORIENTED_EDGE ( 'NONE', *, *, #107044, .F. ) ;
#90529=EDGE_CURVE ( 'NONE', #40138, #91949, #97410, .T. ) ;
#90553=VERTEX_POINT ( 'NONE', #97484 ) ;
#90573=DIRECTION ( 'NONE',  ( 0.000000000000000000, 1.000000000000000000, 1.156482317317864980E-14 ) ) ;
#90588=ORIENTED_EDGE ( 'NONE', *, *, #161485, .F. ) ;
#90590=FACE_OUTER_BOUND ( 'NONE', #235139, .T. ) ;
#90608=DIRECTION ( 'NONE',  ( 1.000000000000000000, 7.304098846218105085E-16, 4.217023435051677501E-16 ) ) ;
#90614=AXIS2_PLACEMENT_3D ( 'NONE', #138220, #59965, #196925 ) ;
#90617=DIRECTION ( 'NONE',  ( -1.000000000000000000, 0.000000000000000000, 0.000000000000000000 ) ) ;
#90625=ORIENTED_EDGE ( 'NONE', *, *, #235756, .F. ) ;
#90644=LINE ( 'NONE', #145491, #108745 ) ;
#90657=CARTESIAN_POINT ( 'NONE',  ( -18.59999999999999787, 66.75000000001151079, -48.27310748452438816 ) ) ;
#90665=VERTEX_POINT ( 'NONE', #200474 ) ;
#90733=CARTESIAN_POINT ( 'NONE',  ( 20.04142135623730070, 64.25000000001151079, -48.17310748452440805 ) ) ;
#90748=ORIENTED_EDGE ( 'NONE', *, *, #153013, .T. ) ;
#90761=FACE_OUTER_BOUND ( 'NONE', #66063, .T. ) ;
#90763=ORIENTED_EDGE ( 'NONE', *, *, #88905, .F. ) ;
#90790=TOROIDAL_SURFACE ( 'NONE', #182594, 11.90000000000000213, 0.1000000000000000056 ) ;
#90811=CARTESIAN_POINT ( 'NONE',  ( 18.59999999999998366, 76.00000000001142553, -36.02310748452432421 ) ) ;
#90847=FACE_OUTER_BOUND ( 'NONE', #56709, .T. ) ;
#90858=DIRECTION ( 'NONE',  ( 0.000000000000000000, 0.9915357197604849349, -0.1298341882520056834 ) ) ;
#90866=AXIS2_PLACEMENT_3D ( 'NONE', #209638, #132676, #173129 ) ;
#90894=DIRECTION ( 'NONE',  ( 0.000000000000000000, 0.4930308989875575865, 0.8700118002898125091 ) ) ;
#90895=CARTESIAN_POINT ( 'NONE',  ( 21.05000000000000071, 76.00000000001165290, -69.52310748452431710 ) ) ;
#90900=ORIENTED_EDGE ( 'NONE', *, *, #152044, .F. ) ;
#90906=LINE ( 'NONE', #72657, #243410 ) ;
#90914=ORIENTED_EDGE ( 'NONE', *, *, #256288, .T. ) ;
#90931=DIRECTION ( 'NONE',  ( 0.000000000000000000, -7.147358527629762208E-15, 1.000000000000000000 ) ) ;
#90940=CIRCLE ( 'NONE', #145095, 0.1000000000000052097 ) ;
#90978=ORIENTED_EDGE ( 'NONE', *, *, #131986, .F. ) ;
#90991=DIRECTION ( 'NONE',  ( 0.000000000000000000, 0.4999999999999689138, 0.8660254037844565822 ) ) ;
#90995=ORIENTED_EDGE ( 'NONE', *, *, #112856, .F. ) ;
#91048=CARTESIAN_POINT ( 'NONE',  ( 18.49999999999999289, 68.87972903831379767, -32.36354444268504693 ) ) ;
#91055=ORIENTED_EDGE ( 'NONE', *, *, #31803, .F. ) ;
#91098=DIRECTION ( 'NONE',  ( 0.000000000000000000, -6.982962677686266711E-15, 1.000000000000000000 ) ) ;
#91123=DIRECTION ( 'NONE',  ( 1.000000000000000000, -0.000000000000000000, 0.000000000000000000 ) ) ;
#91133=VERTEX_POINT ( 'NONE', #129624 ) ;
#91136=CARTESIAN_POINT ( 'NONE',  ( -20.64999999999999858, 73.60000000001157616, -56.29848556176223440 ) ) ;
#91147=DIRECTION ( 'NONE',  ( 1.000000000000000000, 0.000000000000000000, 0.000000000000000000 ) ) ;
#91149=ORIENTED_EDGE ( 'NONE', *, *, #77941, .F. ) ;
#91152=EDGE_LOOP ( 'NONE', ( #177800, #217399, #217359, #84525 ) ) ;
#91161=VERTEX_POINT ( 'NONE', #127050 ) ;
#91209=CARTESIAN_POINT ( 'NONE',  ( -23.25000000000000000, 77.83585931145498193, -24.41866831572578533 ) ) ;
#91212=EDGE_CURVE ( 'NONE', #60425, #165019, #14839, .T. ) ;
#91218=CARTESIAN_POINT ( 'NONE',  ( 20.94999999999999574, 74.83729825007360148, -61.42310748452432989 ) ) ;
#91253=DIRECTION ( 'NONE',  ( 1.000000000000000000, -2.952720810173289112E-16, -2.061873921506763405E-30 ) ) ;
#91267=CARTESIAN_POINT ( 'NONE',  ( 18.59999999999999076, 76.00000000001142553, -36.02310748452432421 ) ) ;
#91278=CARTESIAN_POINT ( 'NONE',  ( -23.25000000000000000, 64.25000000001146816, -43.03791325517834565 ) ) ;
#91281=DIRECTION ( 'NONE',  ( 0.000000000000000000, 0.000000000000000000, 1.000000000000000000 ) ) ;
#91283=CARTESIAN_POINT ( 'NONE',  ( 20.84999999999999787, 64.25000000001146816, -42.94225473048309993 ) ) ;
#91347=EDGE_CURVE ( 'NONE', #12734, #66731, #122910, .T. ) ;
#91371=VECTOR ( 'NONE', #6418, 1000.000000000000000 ) ;
#91395=FACE_OUTER_BOUND ( 'NONE', #83545, .T. ) ;
#91440=DIRECTION ( 'NONE',  ( -0.7071067811865474617, 0.7071067811865474617, 4.937700262164531476E-15 ) ) ;
#91447=DIRECTION ( 'NONE',  ( 0.000000000000000000, -6.467318590049456648E-15, 1.000000000000000000 ) ) ;
#91450=DIRECTION ( 'NONE',  ( 0.000000000000000000, -1.000000000000000000, -8.717686153663073805E-15 ) ) ;
#91480=DIRECTION ( 'NONE',  ( 0.000000000000000000, 0.000000000000000000, 1.000000000000000000 ) ) ;
#91484=CIRCLE ( 'NONE', #104111, 0.5000000000000004441 ) ;
#91529=CARTESIAN_POINT ( 'NONE',  ( 21.14999999999999858, 76.00000000001165290, -69.42310748452432279 ) ) ;
#91530=ORIENTED_EDGE ( 'NONE', *, *, #136993, .T. ) ;
#91542=CARTESIAN_POINT ( 'NONE',  ( -20.94999999999999929, 74.16465844978715438, -57.96795619196134908 ) ) ;
#91553=DIRECTION ( 'NONE',  ( 0.000000000000000000, 0.000000000000000000, 1.000000000000000000 ) ) ;
#91562=CARTESIAN_POINT ( 'NONE',  ( -18.59999999999999787, 74.16465844978715438, -57.96795619196135618 ) ) ;
#91565=LINE ( 'NONE', #188100, #225068 ) ;
#91570=VECTOR ( 'NONE', #100902, 1000.000000000000114 ) ;
#91619=CIRCLE ( 'NONE', #137391, 0.1000000000000028644 ) ;
#91644=( BOUNDED_SURFACE ( )  B_SPLINE_SURFACE ( 3, 2, ( 
 ( #211103, #32507, #112018 ),
 ( #191566, #252777, #153753 ),
 ( #172017, #54585, #36333 ),
 ( #217494, #174604, #115853 ),
 ( #175844, #214948, #993 ),
 ( #234502, #195414, #238353 ),
 ( #216218, #256587, #257872 ),
 ( #75471, #213667, #194128 ),
 ( #77990, #79262, #19315 ),
 ( #16769, #197940, #98811 ) ),
 .UNSPECIFIED., .F., .F., .T. ) 
 B_SPLINE_SURFACE_WITH_KNOTS ( ( 4, 2, 2, 2, 4 ),
 ( 3, 3 ),
 ( 0.0001836757140119196091, 0.0004000170051583634982, 0.0005081876507315854835, 0.0005622729735181964490, 0.0006163582963048074145 ),
 ( 0.000000000000000000, 1.000000000000000000 ),
 .UNSPECIFIED. ) 
 GEOMETRIC_REPRESENTATION_ITEM ( )  RATIONAL_B_SPLINE_SURFACE ( (
 ( 1.000000000000000000, 0.7071067811865079378, 1.000000000000000000),
 ( 1.000000000000000000, 0.6461995200025473229, 1.000000000000000000),
 ( 1.000000000000000000, 0.5776453529555616306, 1.000000000000000000),
 ( 1.000000000000000000, 0.4585233068348677499, 1.000000000000000000),
 ( 1.000000000000000000, 0.4154092989938408254, 1.000000000000000000),
 ( 1.000000000000000000, 0.3550093145837127095, 1.000000000000000000),
 ( 1.000000000000000000, 0.3354498651688673228, 1.000000000000000000),
 ( 1.000000000000000000, 0.3060347992253271698, 1.000000000000000000),
 ( 1.000000000000000000, 0.2963555829628214955, 1.000000000000000000),
 ( 1.000000000000000000, 0.2966190024561043415, 1.000000000000000000) ) ) 
 REPRESENTATION_ITEM ( '' )  SURFACE ( )  );
#91647=DIRECTION ( 'NONE',  ( 2.952720810173289112E-16, 1.000000000000000000, 6.938893903907229955E-15 ) ) ;
#91653=CARTESIAN_POINT ( 'NONE',  ( 21.97500000000000497, 66.25000000001151079, -48.27310748452438816 ) ) ;
#91685=EDGE_CURVE ( 'NONE', #49235, #185953, #59996, .T. ) ;
#91695=DIRECTION ( 'NONE',  ( 1.000000000000000000, -6.938893903907222067E-15, -4.845403715540888588E-29 ) ) ;
#91712=DIRECTION ( 'NONE',  ( 0.000000000000000000, 0.000000000000000000, -1.000000000000000000 ) ) ;
#91749=AXIS2_PLACEMENT_3D ( 'NONE', #123797, #224161, #6402 ) ;
#91760=CIRCLE ( 'NONE', #179264, 11.90000000000000746 ) ;
#91769=AXIS2_PLACEMENT_3D ( 'NONE', #77180, #220556, #117598 ) ;
#91776=CARTESIAN_POINT ( 'NONE',  ( 21.14261333020286671, 65.28430735075666291, -57.27310748452418920 ) ) ;
#91779=DIRECTION ( 'NONE',  ( 1.000000000000000000, 0.000000000000000000, 0.000000000000000000 ) ) ;
#91786=EDGE_CURVE ( 'NONE', #31422, #89321, #14824, .T. ) ;
#91791=DIRECTION ( 'NONE',  ( -2.952720810173289112E-16, -1.000000000000000000, -6.982962677686266711E-15 ) ) ;
#91826=CIRCLE ( 'NONE', #237581, 11.90000000000000746 ) ;
#91830=EDGE_CURVE ( 'NONE', #148964, #8048, #246067, .T. ) ;
#91833=CARTESIAN_POINT ( 'NONE',  ( 21.13461538461538680, 65.38541703798603066, -57.17310748452440095 ) ) ;
#91846=ORIENTED_EDGE ( 'NONE', *, *, #39743, .T. ) ;
#91859=TOROIDAL_SURFACE ( 'NONE', #245991, 0.2000000000000000111, 0.1000000000000000056 ) ;
#91877=EDGE_CURVE ( 'NONE', #238989, #160578, #248015, .T. ) ;
#91883=FACE_OUTER_BOUND ( 'NONE', #121413, .T. ) ;
#91896=CIRCLE ( 'NONE', #212555, 0.1000000000000028644 ) ;
#91901=CARTESIAN_POINT ( 'NONE',  ( 18.49999999999999645, 76.00000000001142553, -36.02310748452432421 ) ) ;
#91902=ORIENTED_EDGE ( 'NONE', *, *, #209470, .T. ) ;
#91916=AXIS2_PLACEMENT_3D ( 'NONE', #197271, #346, #142427 ) ;
#91925=VECTOR ( 'NONE', #184854, 1000.000000000000000 ) ;
#91938=AXIS2_PLACEMENT_3D ( 'NONE', #195570, #235946, #157759 ) ;
#91940=CARTESIAN_POINT ( 'NONE',  ( -23.15000000000000213, 64.35000000001156195, -57.37310748452440379 ) ) ;
#91949=VERTEX_POINT ( 'NONE', #36011 ) ;
#91954=ORIENTED_EDGE ( 'NONE', *, *, #234133, .T. ) ;
#92019=ORIENTED_EDGE ( 'NONE', *, *, #33803, .F. ) ;
#92023=DIRECTION ( 'NONE',  ( -1.000000000000000000, -0.000000000000000000, -0.000000000000000000 ) ) ;
#92039=CIRCLE ( 'NONE', #125380, 0.1000000000000028644 ) ;
#92040=VERTEX_POINT ( 'NONE', #154689 ) ;
#92086=DIRECTION ( 'NONE',  ( 0.000000000000000000, -6.938893903907234689E-15, 1.000000000000000000 ) ) ;
#92088=CARTESIAN_POINT ( 'NONE',  ( -18.59999999999999787, 64.35000000001157616, -57.27310748452440237 ) ) ;
#92157=ORIENTED_EDGE ( 'NONE', *, *, #98698, .F. ) ;
#92184=ORIENTED_EDGE ( 'NONE', *, *, #55941, .T. ) ;
#92224=EDGE_LOOP ( 'NONE', ( #27771, #9343, #82576, #140669 ) ) ;
#92238=EDGE_LOOP ( 'NONE', ( #87596, #114809, #218846, #79519 ) ) ;
#92243=SPHERICAL_SURFACE ( 'NONE', #188148, 0.1000000000000000056 ) ;
#92244=CARTESIAN_POINT ( 'NONE',  ( 23.15000000000000213, 87.75000000001156764, -57.27310748452423894 ) ) ;
#92262=EDGE_CURVE ( 'NONE', #6238, #122696, #210783, .T. ) ;
#92311=EDGE_LOOP ( 'NONE', ( #207379, #55857, #16815, #254562 ) ) ;
#92313=DIRECTION ( 'NONE',  ( -1.000000000000000000, -3.469446951953635015E-14, -2.422701857770461054E-28 ) ) ;
#92345=CARTESIAN_POINT ( 'NONE',  ( 21.05000000000000071, 87.65000000001144542, -38.92310748452424463 ) ) ;
#92351=LINE ( 'NONE', #96192, #95405 ) ;
#92354=CARTESIAN_POINT ( 'NONE',  ( 23.15000000000000213, 87.48912529308749697, -39.12310748452424747 ) ) ;
#92392=DIRECTION ( 'NONE',  ( -0.000000000000000000, 1.000000000000000000, 6.982962677686267499E-15 ) ) ;
#92410=DIRECTION ( 'NONE',  ( 0.000000000000000000, -6.938893903907222067E-15, 1.000000000000000000 ) ) ;
#92426=ORIENTED_EDGE ( 'NONE', *, *, #37688, .F. ) ;
#92431=VECTOR ( 'NONE', #74263, 1000.000000000000000 ) ;
#92449=DIRECTION ( 'NONE',  ( 0.000000000000000000, -0.008583690987162452199, 0.9999631594459053030 ) ) ;
#92453=ORIENTED_EDGE ( 'NONE', *, *, #78306, .F. ) ;
#92474=AXIS2_PLACEMENT_3D ( 'NONE', #160957, #5689, #43567 ) ;
#92481=ORIENTED_EDGE ( 'NONE', *, *, #4383, .F. ) ;
#92482=FACE_OUTER_BOUND ( 'NONE', #152895, .T. ) ;
#92558=CYLINDRICAL_SURFACE ( 'NONE', #28999, 0.09999999999999939493 ) ;
#92561=VERTEX_POINT ( 'NONE', #119087 ) ;
#92563=CARTESIAN_POINT ( 'NONE',  ( -21.04999999999999716, 69.70076908991939035, -69.62154498452471785 ) ) ;
#92590=B_SPLINE_CURVE_WITH_KNOTS ( 'NONE', 3,
 ( #215964, #255038, #218521, #99853, #195169, #79008, #197688, #116883, #34811, #157323 ),
 .UNSPECIFIED., .F., .F.,
 ( 4, 2, 2, 2, 4 ),
 ( 0.000000000000000000, 0.0001660831991682299249, 0.0002491247987523412147, 0.0002906455985444013454, 0.0003321663983364614762 ),
 .UNSPECIFIED. ) ;
#92605=ADVANCED_FACE ( 'NONE', ( #219443 ), #56808, .F. ) ;
#92612=CIRCLE ( 'NONE', #84372, 11.74999999999999645 ) ;
#92637=DIRECTION ( 'NONE',  ( -1.000000000000000000, -0.000000000000000000, -0.000000000000000000 ) ) ;
#92669=VERTEX_POINT ( 'NONE', #244145 ) ;
#92690=AXIS2_PLACEMENT_3D ( 'NONE', #68517, #148052, #81009 ) ;
#92720=CARTESIAN_POINT ( 'NONE',  ( -18.59999999999999787, 74.83729825007360148, -61.42310748452432989 ) ) ;
#92746=ORIENTED_EDGE ( 'NONE', *, *, #143887, .T. ) ;
#92759=DIRECTION ( 'NONE',  ( 1.000000000000000000, 0.000000000000000000, 0.000000000000000000 ) ) ;
#92761=ADVANCED_FACE ( 'NONE', ( #141955 ), #6957, .T. ) ;
#92787=AXIS2_PLACEMENT_3D ( 'NONE', #1627, #238984, #40805 ) ;
#92796=DIRECTION ( 'NONE',  ( 0.000000000000000000, -6.417474130781252121E-15, 1.000000000000000000 ) ) ;
#92800=ORIENTED_EDGE ( 'NONE', *, *, #33865, .F. ) ;
#92818=VERTEX_POINT ( 'NONE', #19458 ) ;
#92833=DIRECTION ( 'NONE',  ( 0.000000000000000000, 0.000000000000000000, -1.000000000000000000 ) ) ;
#92847=DIRECTION ( 'NONE',  ( 1.000000000000000000, 0.000000000000000000, 0.000000000000000000 ) ) ;
#92866=ORIENTED_EDGE ( 'NONE', *, *, #50047, .T. ) ;
#92881=DIRECTION ( 'NONE',  ( 0.000000000000000000, -6.982962677686266711E-15, 1.000000000000000000 ) ) ;
#92882=DIRECTION ( 'NONE',  ( 0.000000000000000000, 6.982962677686267499E-15, -1.000000000000000000 ) ) ;
#92892=DIRECTION ( 'NONE',  ( -0.7071067811865474617, 0.7071067811865474617, 5.142139384388980375E-15 ) ) ;
#92900=DIRECTION ( 'NONE',  ( 0.000000000000000000, 0.000000000000000000, 1.000000000000000000 ) ) ;
#92901=ORIENTED_EDGE ( 'NONE', *, *, #4202, .F. ) ;
#92909=AXIS2_PLACEMENT_3D ( 'NONE', #80189, #239308, #138874 ) ;
#92936=DIRECTION ( 'NONE',  ( -0.000000000000000000, 6.982962677686266711E-15, -1.000000000000000000 ) ) ;
#92943=VERTEX_POINT ( 'NONE', #44159 ) ;
#92974=CARTESIAN_POINT ( 'NONE',  ( 20.94999999999999574, 87.65000000001163016, -66.62310748452424036 ) ) ;
#93009=ORIENTED_EDGE ( 'NONE', *, *, #41199, .T. ) ;
#93032=AXIS2_PLACEMENT_3D ( 'NONE', #216130, #60906, #196571 ) ;
#93046=CARTESIAN_POINT ( 'NONE',  ( 20.95512820512820085, 67.12384868372348024, -60.96447848938343839 ) ) ;
#93059=EDGE_LOOP ( 'NONE', ( #120938, #182381 ) ) ;
#93085=ORIENTED_EDGE ( 'NONE', *, *, #257400, .T. ) ;
#93100=ORIENTED_EDGE ( 'NONE', *, *, #86341, .T. ) ;
#93160=AXIS2_PLACEMENT_3D ( 'NONE', #196769, #80662, #220208 ) ;
#93162=EDGE_CURVE ( 'NONE', #221285, #160725, #12750, .T. ) ;
#93203=AXIS2_PLACEMENT_3D ( 'NONE', #64449, #12201, #111282 ) ;
#93217=ORIENTED_EDGE ( 'NONE', *, *, #16764, .T. ) ;
#93271=ORIENTED_EDGE ( 'NONE', *, *, #108341, .F. ) ;
#93320=CARTESIAN_POINT ( 'NONE',  ( -21.05000000000000071, 76.00000000001165290, -69.52310748452431710 ) ) ;
#93326=EDGE_CURVE ( 'NONE', #154564, #148964, #78049, .T. ) ;
#93355=DIRECTION ( 'NONE',  ( 0.000000000000000000, 0.8700118002898393765, -0.4930308989875104575 ) ) ;
#93358=CARTESIAN_POINT ( 'NONE',  ( -21.70464131381649509, 68.90464198104380955, -69.52310748452435973 ) ) ;
#93396=VERTEX_POINT ( 'NONE', #26870 ) ;
#93410=CARTESIAN_POINT ( 'NONE',  ( 21.97500000000000497, 66.25000000001151079, -48.37310748452438958 ) ) ;
#93411=CARTESIAN_POINT ( 'NONE',  ( 21.00000000000000000, 66.25000000001151079, -48.37310748452438958 ) ) ;
#93424=VERTEX_POINT ( 'NONE', #23020 ) ;
#93426=EDGE_LOOP ( 'NONE', ( #76317, #213866, #158811, #91846 ) ) ;
#93439=EDGE_CURVE ( 'NONE', #87660, #17664, #253026, .T. ) ;
#93464=ORIENTED_EDGE ( 'NONE', *, *, #169887, .T. ) ;
#93473=ORIENTED_EDGE ( 'NONE', *, *, #169563, .T. ) ;
#93507=DIRECTION ( 'NONE',  ( 0.000000000000000000, 0.000000000000000000, 1.000000000000000000 ) ) ;
#93511=ORIENTED_EDGE ( 'NONE', *, *, #66504, .T. ) ;
#93542=CARTESIAN_POINT ( 'NONE',  ( 21.05000000000000071, 76.00000000001156764, -57.37310748452432563 ) ) ;
#93604=CARTESIAN_POINT ( 'NONE',  ( -21.06715728752538652, 64.25000000001161027, -62.50830171387038803 ) ) ;
#93605=CARTESIAN_POINT ( 'NONE',  ( 18.49999999999999645, 74.13328508995425636, -57.77043223824233564 ) ) ;
#93631=FACE_OUTER_BOUND ( 'NONE', #187948, .T. ) ;
#93648=ADVANCED_FACE ( 'NONE', ( #157073 ), #132422, .T. ) ;
#93657=CIRCLE ( 'NONE', #176883, 0.09999999999999520384 ) ;
#93675=FACE_OUTER_BOUND ( 'NONE', #149456, .T. ) ;
#93680=ORIENTED_EDGE ( 'NONE', *, *, #15541, .T. ) ;
#93682=DIRECTION ( 'NONE',  ( 1.000000000000000000, 0.000000000000000000, 0.000000000000000000 ) ) ;
#93683=CIRCLE ( 'NONE', #239428, 0.09999999999999939493 ) ;
#93726=CARTESIAN_POINT ( 'NONE',  ( -22.49999999999999645, 64.25043287652226809, -69.62396585362311896 ) ) ;
#93733=ORIENTED_EDGE ( 'NONE', *, *, #191823, .T. ) ;
#93735=EDGE_CURVE ( 'NONE', #125917, #44661, #161469, .T. ) ;
#93764=DIRECTION ( 'NONE',  ( -0.000000000000000000, -6.982962677686266711E-15, 1.000000000000000000 ) ) ;
#93767=DIRECTION ( 'NONE',  ( 1.000000000000000000, 0.000000000000000000, 0.000000000000000000 ) ) ;
#93772=ORIENTED_EDGE ( 'NONE', *, *, #178854, .F. ) ;
#93796=DIRECTION ( 'NONE',  ( 1.875376730785737719E-16, 1.000000000000000000, 6.982962677686266711E-15 ) ) ;
#93837=CARTESIAN_POINT ( 'NONE',  ( -20.85000000000000142, 68.97833521811131163, -32.18954208262707795 ) ) ;
#93844=CIRCLE ( 'NONE', #122899, 0.1000000000000028644 ) ;
#93855=VECTOR ( 'NONE', #218195, 1000.000000000000000 ) ;
#93878=LINE ( 'NONE', #113443, #182789 ) ;
#93881=CYLINDRICAL_SURFACE ( 'NONE', #162516, 11.74999999999999645 ) ;
#93891=CIRCLE ( 'NONE', #164824, 0.1000000000000028644 ) ;
#93903=AXIS2_PLACEMENT_3D ( 'NONE', #81977, #221503, #161575 ) ;
#93904=ORIENTED_EDGE ( 'NONE', *, *, #80925, .F. ) ;
#93923=EDGE_CURVE ( 'NONE', #206022, #231849, #165940, .T. ) ;
#93929=CARTESIAN_POINT ( 'NONE',  ( -20.64999999999999858, 68.75000000001151079, -48.27310748452437394 ) ) ;
#93959=CARTESIAN_POINT ( 'NONE',  ( 20.94999999999999574, 87.39257802171731271, -66.44915790469229933 ) ) ;
#93974=EDGE_LOOP ( 'NONE', ( #68323, #51784, #136272, #8608 ) ) ;
#94017=DIRECTION ( 'NONE',  ( -1.000000000000000000, -0.000000000000000000, -0.000000000000000000 ) ) ;
#94066=CIRCLE ( 'NONE', #194057, 0.1000000000000028644 ) ;
#94074=EDGE_CURVE ( 'NONE', #55596, #115794, #88399, .T. ) ;
#94081=CARTESIAN_POINT ( 'NONE',  ( 20.94999999999999929, 76.00000000001165290, -69.52310748452431710 ) ) ;
#94111=ORIENTED_EDGE ( 'NONE', *, *, #26784, .T. ) ;
#94136=CARTESIAN_POINT ( 'NONE',  ( 20.94999999999999929, 69.55000000001159322, -59.50608031408435039 ) ) ;
#94138=DIRECTION ( 'NONE',  ( 0.000000000000000000, 0.000000000000000000, -1.000000000000000000 ) ) ;
#94144=AXIS2_PLACEMENT_3D ( 'NONE', #93320, #209413, #15081 ) ;
#94150=VERTEX_POINT ( 'NONE', #126612 ) ;
#94169=DIRECTION ( 'NONE',  ( 1.000000000000000000, 0.000000000000000000, 0.000000000000000000 ) ) ;
#94196=AXIS2_PLACEMENT_3D ( 'NONE', #2281, #222608, #80524 ) ;
#94199=CARTESIAN_POINT ( 'NONE',  ( -20.64999999999999858, 73.50000000001151079, -49.24772940728643533 ) ) ;
#94200=DIRECTION ( 'NONE',  ( -0.000000000000000000, 6.982962677686266711E-15, -1.000000000000000000 ) ) ;
#94266=ORIENTED_EDGE ( 'NONE', *, *, #212262, .F. ) ;
#94274=CIRCLE ( 'NONE', #244114, 0.1000000000000052097 ) ;
#94311=EDGE_CURVE ( 'NONE', #158894, #37076, #124419, .T. ) ;
#94360=LINE ( 'NONE', #74849, #205633 ) ;
#94369=DIRECTION ( 'NONE',  ( 0.7071067811865487940, 4.851104656540973741E-15, -0.7071067811865463515 ) ) ;
#94383=CARTESIAN_POINT ( 'NONE',  ( 21.59780538579342135, 75.90102133041372667, -76.37019801446757583 ) ) ;
#94397=VERTEX_POINT ( 'NONE', #155200 ) ;
#94416=ORIENTED_EDGE ( 'NONE', *, *, #70326, .T. ) ;
#94421=CARTESIAN_POINT ( 'NONE',  ( -21.05000000000000071, 76.00000000001165290, -69.52310748452431710 ) ) ;
#94434=CARTESIAN_POINT ( 'NONE',  ( 21.05000000000000071, 76.10000000001170406, -76.06376443622556849 ) ) ;
#94486=ORIENTED_EDGE ( 'NONE', *, *, #112350, .F. ) ;
#94562=AXIS2_PLACEMENT_3D ( 'NONE', #150081, #250434, #28876 ) ;
#94580=VECTOR ( 'NONE', #75861, 1000.000000000000000 ) ;
#94585=ORIENTED_EDGE ( 'NONE', *, *, #210392, .T. ) ;
#94615=AXIS2_PLACEMENT_3D ( 'NONE', #146136, #24937, #180149 ) ;
#94630=EDGE_CURVE ( 'NONE', #55457, #87660, #20368, .T. ) ;
#94646=CARTESIAN_POINT ( 'NONE',  ( 21.00000000000000000, 66.25000000001151079, -48.27310748452438816 ) ) ;
#94670=EDGE_LOOP ( 'NONE', ( #22697, #173194, #25890, #92019 ) ) ;
#94728=AXIS2_PLACEMENT_3D ( 'NONE', #142706, #21510, #180571 ) ;
#94745=CARTESIAN_POINT ( 'NONE',  ( 23.14999999999999858, 71.00000000001151079, -47.92837350343745584 ) ) ;
#94760=VERTEX_POINT ( 'NONE', #5700 ) ;
#94811=TOROIDAL_SURFACE ( 'NONE', #240565, 0.2000000000000000111, 0.1000000000000000056 ) ;
#94877=CARTESIAN_POINT ( 'NONE',  ( -20.94999999999999929, 64.25000000001161027, -62.50830171387040934 ) ) ;
#94901=CARTESIAN_POINT ( 'NONE',  ( -20.64999999999999858, 76.00000000001141132, -34.02310748452431710 ) ) ;
#94919=ORIENTED_EDGE ( 'NONE', *, *, #145765, .T. ) ;
#94926=AXIS2_PLACEMENT_3D ( 'NONE', #105318, #85755, #87056 ) ;
#94929=EDGE_LOOP ( 'NONE', ( #5636, #242334, #58725, #71960 ) ) ;
#94963=EDGE_CURVE ( 'NONE', #92943, #202854, #153101, .T. ) ;
#94997=CARTESIAN_POINT ( 'NONE',  ( -21.37071067811865532, 67.92928932189285263, -48.27310748452438105 ) ) ;
#95007=LINE ( 'NONE', #173323, #244604 ) ;
#95061=VERTEX_POINT ( 'NONE', #36890 ) ;
#95063=DIRECTION ( 'NONE',  ( 0.000000000000000000, -0.1350103645451945777, 0.9908441862701590219 ) ) ;
#95092=TOROIDAL_SURFACE ( 'NONE', #11728, 2.100000000000002309, 0.1000000000000000056 ) ;
#95095=CARTESIAN_POINT ( 'NONE',  ( 23.24999999999999645, 72.10000000001141984, -36.02310748452435263 ) ) ;
#95098=ORIENTED_EDGE ( 'NONE', *, *, #143649, .T. ) ;
#95111=ORIENTED_EDGE ( 'NONE', *, *, #150744, .T. ) ;
#95127=DIRECTION ( 'NONE',  ( -1.000000000000000000, 0.000000000000000000, -0.000000000000000000 ) ) ;
#95147=FACE_OUTER_BOUND ( 'NONE', #76135, .T. ) ;
#95161=CYLINDRICAL_SURFACE ( 'NONE', #204457, 0.5000000000000004441 ) ;
#95179=CIRCLE ( 'NONE', #36773, 0.1000000000000028644 ) ;
#95228=ORIENTED_EDGE ( 'NONE', *, *, #33116, .T. ) ;
#95232=CARTESIAN_POINT ( 'NONE',  ( 21.09813707148777340, 69.61493789427515821, -69.55445898405388050 ) ) ;
#95239=ORIENTED_EDGE ( 'NONE', *, *, #57176, .T. ) ;
#95254=ADVANCED_FACE ( 'NONE', ( #185349 ), #125383, .T. ) ;
#95320=AXIS2_PLACEMENT_3D ( 'NONE', #164377, #147376, #144783 ) ;
#95340=VERTEX_POINT ( 'NONE', #129230 ) ;
#95372=EDGE_CURVE ( 'NONE', #196598, #59275, #178397, .T. ) ;
#95384=EDGE_CURVE ( 'NONE', #235467, #56908, #245203, .T. ) ;
#95405=VECTOR ( 'NONE', #171939, 1000.000000000000000 ) ;
#95408=CIRCLE ( 'NONE', #162063, 4.049999999999998046 ) ;
#95413=ORIENTED_EDGE ( 'NONE', *, *, #154904, .F. ) ;
#95429=CYLINDRICAL_SURFACE ( 'NONE', #36192, 0.09999999999999939493 ) ;
#95432=DIRECTION ( 'NONE',  ( -1.000000000000000000, 0.000000000000000000, -0.000000000000000000 ) ) ;
#95459=ORIENTED_EDGE ( 'NONE', *, *, #142470, .T. ) ;
#95480=EDGE_LOOP ( 'NONE', ( #95459, #191124, #243578, #177164 ) ) ;
#95482=VERTEX_POINT ( 'NONE', #136925 ) ;
#95486=AXIS2_PLACEMENT_3D ( 'NONE', #81308, #184289, #146434 ) ;
#95512=EDGE_CURVE ( 'NONE', #17744, #57945, #136860, .T. ) ;
#95568=DIRECTION ( 'NONE',  ( 0.000000000000000000, 0.000000000000000000, -1.000000000000000000 ) ) ;
#95601=CARTESIAN_POINT ( 'NONE',  ( -23.15000000000000213, 64.35000000001150511, -48.17310748452440805 ) ) ;
#95602=B_SPLINE_CURVE_WITH_KNOTS ( 'NONE', 3,
 ( #139555, #116177, #96570, #176159, #40518, #155322, #138267, #234825, #255618, #19639 ),
 .UNSPECIFIED., .F., .F.,
 ( 4, 2, 2, 2, 4 ),
 ( 0.000000000000000000, 3.990160268012894350E-05, 7.980320536025788699E-05, 0.0001596064107205239868, 0.0003192128214410228202 ),
 .UNSPECIFIED. ) ;
#95610=CARTESIAN_POINT ( 'NONE',  ( 20.95429402530582408, 67.12380584890942714, -61.00002078658653204 ) ) ;
#95645=AXIS2_PLACEMENT_3D ( 'NONE', #34575, #172833, #78790 ) ;
#95669=CIRCLE ( 'NONE', #99743, 0.1000000000000028644 ) ;
#95673=DIRECTION ( 'NONE',  ( 0.000000000000000000, 0.000000000000000000, 1.000000000000000000 ) ) ;
#95691=ORIENTED_EDGE ( 'NONE', *, *, #57052, .F. ) ;
#95713=CARTESIAN_POINT ( 'NONE',  ( 21.05000000000000071, 75.96798630682366138, -75.78195020806214188 ) ) ;
#95719=CIRCLE ( 'NONE', #70646, 4.099999999999999645 ) ;
#95730=VECTOR ( 'NONE', #220706, 1000.000000000000000 ) ;
#95761=EDGE_CURVE ( 'NONE', #211306, #187198, #111942, .T. ) ;
#95773=DIRECTION ( 'NONE',  ( 0.000000000000000000, -0.4999999999999689138, -0.8660254037844565822 ) ) ;
#95781=CYLINDRICAL_SURFACE ( 'NONE', #25209, 12.87499999999999822 ) ;
#95792=DIRECTION ( 'NONE',  ( 1.000000000000000000, -0.000000000000000000, -0.000000000000000000 ) ) ;
#95882=AXIS2_PLACEMENT_3D ( 'NONE', #208412, #230531, #171871 ) ;
#95902=CARTESIAN_POINT ( 'NONE',  ( 18.59999999999999432, 74.73821383144657204, -61.43660852097884373 ) ) ;
#95911=CARTESIAN_POINT ( 'NONE',  ( -18.59999999999999787, 77.16270174994961906, -61.42310748452431568 ) ) ;
#95956=EDGE_LOOP ( 'NONE', ( #71846, #96029, #134370 ) ) ;
#95967=FACE_OUTER_BOUND ( 'NONE', #93426, .T. ) ;
#95971=ORIENTED_EDGE ( 'NONE', *, *, #93326, .T. ) ;
#95999=VECTOR ( 'NONE', #46512, 1000.000000000000000 ) ;
#96015=DIRECTION ( 'NONE',  ( 0.000000000000000000, 0.8700118002898393765, -0.4930308989875104575 ) ) ;
#96029=ORIENTED_EDGE ( 'NONE', *, *, #149124, .T. ) ;
#96031=EDGE_CURVE ( 'NONE', #80057, #248144, #208456, .T. ) ;
#96078=EDGE_CURVE ( 'NONE', #40625, #116437, #49562, .T. ) ;
#96092=CARTESIAN_POINT ( 'NONE',  ( 23.14999999999999858, 71.22429906543206357, -47.87187558857031888 ) ) ;
#96112=EDGE_LOOP ( 'NONE', ( #7135, #67828, #188950, #37122 ) ) ;
#96120=ORIENTED_EDGE ( 'NONE', *, *, #238319, .T. ) ;
#96137=CARTESIAN_POINT ( 'NONE',  ( 21.05000000000000071, 87.48912529308769592, -66.62310748452424036 ) ) ;
#96169=CIRCLE ( 'NONE', #221071, 0.09999999999999939493 ) ;
#96170=ORIENTED_EDGE ( 'NONE', *, *, #65339, .T. ) ;
#96175=DIRECTION ( 'NONE',  ( 1.000000000000000000, 0.000000000000000000, 0.000000000000000000 ) ) ;
#96192=CARTESIAN_POINT ( 'NONE',  ( 21.05000000000000071, 70.50000000001151079, -48.42837350343745584 ) ) ;
#96202=ORIENTED_EDGE ( 'NONE', *, *, #24321, .F. ) ;
#96212=TOROIDAL_SURFACE ( 'NONE', #221109, 0.2000000000000000111, 0.1000000000000000056 ) ;
#96221=DIRECTION ( 'NONE',  ( -1.000000000000000000, -0.000000000000000000, -0.000000000000000000 ) ) ;
#96243=AXIS2_PLACEMENT_3D ( 'NONE', #46587, #44047, #123584 ) ;
#96273=CIRCLE ( 'NONE', #75477, 0.09999999999999939493 ) ;
#96280=ORIENTED_EDGE ( 'NONE', *, *, #35863, .T. ) ;
#96315=ORIENTED_EDGE ( 'NONE', *, *, #96078, .T. ) ;
#96317=CARTESIAN_POINT ( 'NONE',  ( -20.94999027547553894, 65.70673848566926267, -30.56382523348290547 ) ) ;
#96320=CARTESIAN_POINT ( 'NONE',  ( -21.14999999999999858, 64.35000000001166143, -69.42310748452440805 ) ) ;
#96323=LINE ( 'NONE', #135456, #26570 ) ;
#96347=VERTEX_POINT ( 'NONE', #111170 ) ;
#96379=DIRECTION ( 'NONE',  ( 1.000000000000000000, 0.000000000000000000, 0.000000000000000000 ) ) ;
#96411=CARTESIAN_POINT ( 'NONE',  ( -18.59999999999999787, 74.83729825007360148, -61.42310748452432989 ) ) ;
#96435=CIRCLE ( 'NONE', #567, 0.1000000000000028644 ) ;
#96472=CARTESIAN_POINT ( 'NONE',  ( 18.59999999999999787, 77.83585931145498193, -24.51866831572578675 ) ) ;
#96485=CARTESIAN_POINT ( 'NONE',  ( 20.94999999999999929, 65.70729864260954400, -30.56574559737246233 ) ) ;
#96488=DIRECTION ( 'NONE',  ( 0.000000000000000000, -6.853228547068871147E-15, 1.000000000000000000 ) ) ;
#96510=ORIENTED_EDGE ( 'NONE', *, *, #16887, .F. ) ;
#96517=DIRECTION ( 'NONE',  ( 1.000000000000000000, 0.000000000000000000, 0.000000000000000000 ) ) ;
#96547=VERTEX_POINT ( 'NONE', #143462 ) ;
#96570=CARTESIAN_POINT ( 'NONE',  ( -18.42554971533678199, 85.49715966944935985, -62.48328057097562294 ) ) ;
#96584=EDGE_LOOP ( 'NONE', ( #241796, #129392, #18703, #32064, #234004, #89829, #63681, #11, #103733, #98618, #54369 ) ) ;
#96586=AXIS2_PLACEMENT_3D ( 'NONE', #216676, #155465, #249702 ) ;
#96597=DIRECTION ( 'NONE',  ( 1.000000000000000000, -7.304098846218134667E-16, -5.100424963727256530E-30 ) ) ;
#96611=LINE ( 'NONE', #53668, #164147 ) ;
#96664=DIRECTION ( 'NONE',  ( 0.000000000000000000, 0.9908441862701605762, 0.1350103645451835310 ) ) ;
#96667=DIRECTION ( 'NONE',  ( 0.000000000000000000, 0.000000000000000000, 1.000000000000000000 ) ) ;
#96681=VERTEX_POINT ( 'NONE', #5210 ) ;
#96704=EDGE_CURVE ( 'NONE', #47933, #221530, #67779, .T. ) ;
#96708=DIRECTION ( 'NONE',  ( 0.000000000000000000, -6.982962677686266711E-15, 1.000000000000000000 ) ) ;
#96735=EDGE_CURVE ( 'NONE', #204082, #245148, #91619, .T. ) ;
#96766=CARTESIAN_POINT ( 'NONE',  ( 23.24999999999999645, 76.00000000001165290, -69.52310748452431710 ) ) ;
#96778=CARTESIAN_POINT ( 'NONE',  ( 23.24999999999999645, 70.40000000001174385, -81.27310748452435973 ) ) ;
#96813=ADVANCED_FACE ( 'NONE', ( #195458 ), #213706, .F. ) ;
#96827=FACE_OUTER_BOUND ( 'NONE', #133906, .T. ) ;
#96838=CARTESIAN_POINT ( 'NONE',  ( 20.04142135623730070, 64.35000000001150511, -48.17310748452440095 ) ) ;
#96849=DIRECTION ( 'NONE',  ( 0.000000000000000000, -1.000000000000000000, -6.982962677686265922E-15 ) ) ;
#96860=DIRECTION ( 'NONE',  ( 0.000000000000000000, -7.056502275159890043E-15, 1.000000000000000000 ) ) ;
#96862=LINE ( 'NONE', #215558, #31175 ) ;
#96872=CARTESIAN_POINT ( 'NONE',  ( 21.05000000000000071, 76.00000000001139711, -31.92310748452432279 ) ) ;
#96916=EDGE_LOOP ( 'NONE', ( #220202, #246098, #83354, #220218 ) ) ;
#96920=EDGE_CURVE ( 'NONE', #183881, #241131, #62587, .T. ) ;
#96924=CARTESIAN_POINT ( 'NONE',  ( 21.40925344232283223, 75.90104981139204199, -76.18162634391477184 ) ) ;
#96942=DIRECTION ( 'NONE',  ( -0.000000000000000000, 1.000000000000000000, 6.982962677686266711E-15 ) ) ;
#96966=CARTESIAN_POINT ( 'NONE',  ( 21.04999999999999716, 75.98528214348812071, -75.86783088861417923 ) ) ;
#97020=ORIENTED_EDGE ( 'NONE', *, *, #130371, .F. ) ;
#97027=CIRCLE ( 'NONE', #242815, 0.1000000000000028644 ) ;
#97052=CARTESIAN_POINT ( 'NONE',  ( 22.60000000000000142, 75.89914163091303578, -81.27267460801371612 ) ) ;
#97086=ORIENTED_EDGE ( 'NONE', *, *, #238737, .F. ) ;
#97104=VERTEX_POINT ( 'NONE', #129989 ) ;
#97117=CARTESIAN_POINT ( 'NONE',  ( -23.25000000000000000, 64.35000000001156195, -57.37310748452439668 ) ) ;
#97119=ORIENTED_EDGE ( 'NONE', *, *, #156256, .F. ) ;
#97120=LINE ( 'NONE', #138821, #226170 ) ;
#97140=ORIENTED_EDGE ( 'NONE', *, *, #52212, .T. ) ;
#97164=FACE_OUTER_BOUND ( 'NONE', #180454, .T. ) ;
#97174=DIRECTION ( 'NONE',  ( 0.000000000000000000, -0.1568667991644355497, -0.9876197685951332295 ) ) ;
#97186=EDGE_CURVE ( 'NONE', #105103, #173457, #30949, .T. ) ;
#97208=EDGE_LOOP ( 'NONE', ( #44724, #240881, #104456, #105859, #245766, #19622, #181755, #73446, #14292, #244970 ) ) ;
#97210=CARTESIAN_POINT ( 'NONE',  ( -21.05000000000000071, 64.40000000001147384, -42.95131071479990936 ) ) ;
#97314=DIRECTION ( 'NONE',  ( -1.000000000000000000, 0.000000000000000000, 0.000000000000000000 ) ) ;
#97324=VECTOR ( 'NONE', #55193, 1000.000000000000000 ) ;
#97325=EDGE_CURVE ( 'NONE', #175273, #39343, #71815, .T. ) ;
#97341=EDGE_CURVE ( 'NONE', #167581, #166958, #75888, .T. ) ;
#97344=CARTESIAN_POINT ( 'NONE',  ( -18.59999999999999787, 77.83585931145498193, -24.51866831572578675 ) ) ;
#97361=ORIENTED_EDGE ( 'NONE', *, *, #126659, .T. ) ;
#97369=AXIS2_PLACEMENT_3D ( 'NONE', #144428, #105293, #56737 ) ;
#97393=( BOUNDED_SURFACE ( )  B_SPLINE_SURFACE ( 3, 2, ( 
 ( #224733, #102197, #3111 ),
 ( #46102, #86488, #81352 ),
 ( #121815, #166096, #164783 ),
 ( #146477, #104766, #47378 ) ),
 .UNSPECIFIED., .F., .F., .T. ) 
 B_SPLINE_SURFACE_WITH_KNOTS ( ( 4, 4 ),
 ( 3, 3 ),
 ( 1.734723475976807094E-18, 0.001979672783031534173 ),
 ( 0.000000000000000000, 1.000000000000000000 ),
 .UNSPECIFIED. ) 
 GEOMETRIC_REPRESENTATION_ITEM ( )  RATIONAL_B_SPLINE_SURFACE ( (
 ( 1.000000000000000000, 0.7103081912008384347, 1.000000000000000000),
 ( 1.000000000000000000, 0.7104998333558379953, 1.000000000000000000),
 ( 1.000000000000000000, 0.7107238315755348701, 1.000000000000000000),
 ( 1.000000000000000000, 0.7110073749539290722, 1.000000000000000000) ) ) 
 REPRESENTATION_ITEM ( '' )  SURFACE ( )  );
#97399=SPHERICAL_SURFACE ( 'NONE', #79456, 0.1000000000000000056 ) ;
#97406=CARTESIAN_POINT ( 'NONE',  ( -23.15000000000000213, 64.25000000001165290, -69.52310748452440237 ) ) ;
#97410=CIRCLE ( 'NONE', #26544, 0.09999999999999958922 ) ;
#97417=AXIS2_PLACEMENT_3D ( 'NONE', #139547, #157900, #194432 ) ;
#97430=AXIS2_PLACEMENT_3D ( 'NONE', #23101, #257781, #102580 ) ;
#97437=DIRECTION ( 'NONE',  ( -1.000000000000000000, 0.000000000000000000, 0.000000000000000000 ) ) ;
#97439=CARTESIAN_POINT ( 'NONE',  ( -20.64999999999999858, 76.00000000001142553, -36.02310748452432421 ) ) ;
#97470=ORIENTED_EDGE ( 'NONE', *, *, #152130, .T. ) ;
#97483=CARTESIAN_POINT ( 'NONE',  ( 20.94999999999999929, 76.00000000001156764, -56.64810748452432421 ) ) ;
#97484=CARTESIAN_POINT ( 'NONE',  ( 21.05000000000000071, 87.39257802171711376, -39.09705706435617856 ) ) ;
#97503=LINE ( 'NONE', #216184, #193701 ) ;
#97526=CARTESIAN_POINT ( 'NONE',  ( -21.05000000000000071, 75.96636726467806966, -75.78192467920580100 ) ) ;
#97545=DIRECTION ( 'NONE',  ( 0.000000000000000000, 0.4999999999999689138, -0.8660254037844565822 ) ) ;
#97552=AXIS2_PLACEMENT_3D ( 'NONE', #124486, #240568, #244411 ) ;
#97584=EDGE_CURVE ( 'NONE', #251642, #113738, #152841, .T. ) ;
#97602=VECTOR ( 'NONE', #40004, 1000.000000000000000 ) ;
#97628=ORIENTED_EDGE ( 'NONE', *, *, #213063, .F. ) ;
#97640=FACE_OUTER_BOUND ( 'NONE', #221497, .T. ) ;
#97683=DIRECTION ( 'NONE',  ( -3.265361837132813093E-16, -1.000000000000000000, -6.938893903907229955E-15 ) ) ;
#97691=VERTEX_POINT ( 'NONE', #100497 ) ;
#97734=VERTEX_POINT ( 'NONE', #130351 ) ;
#97762=CARTESIAN_POINT ( 'NONE',  ( 18.56579813702275317, 65.66974365629616273, -30.43601455626050623 ) ) ;
#97765=EDGE_LOOP ( 'NONE', ( #237790, #131656, #188585, #16980 ) ) ;
#97767=DIRECTION ( 'NONE',  ( 1.000000000000000000, -0.000000000000000000, 0.000000000000000000 ) ) ;
#97775=ADVANCED_FACE ( 'NONE', ( #110796 ), #190360, .T. ) ;
#97821=VERTEX_POINT ( 'NONE', #146065 ) ;
#97835=EDGE_CURVE ( 'NONE', #47640, #100678, #104962, .T. ) ;
#97848=VERTEX_POINT ( 'NONE', #246460 ) ;
#97860=CARTESIAN_POINT ( 'NONE',  ( -23.15000000000000213, 64.25000000001158185, -57.27310748452440237 ) ) ;
#97864=VERTEX_POINT ( 'NONE', #228193 ) ;
#97932=ORIENTED_EDGE ( 'NONE', *, *, #35265, .T. ) ;
#97967=ADVANCED_FACE ( 'NONE', ( #14297 ), #213750, .F. ) ;
#97972=EDGE_CURVE ( 'NONE', #88303, #233233, #134317, .T. ) ;
#97985=CARTESIAN_POINT ( 'NONE',  ( -20.94999999999999929, 74.26374286841418382, -57.95445515550683524 ) ) ;
#97991=CARTESIAN_POINT ( 'NONE',  ( -23.25000000000000000, 85.00000000001149658, -45.91707660717669626 ) ) ;
#98003=VERTEX_POINT ( 'NONE', #257962 ) ;
#98004=CARTESIAN_POINT ( 'NONE',  ( -20.94999999999999929, 76.00000000001139711, -32.02310748452432421 ) ) ;
#98034=DIRECTION ( 'NONE',  ( 1.000000000000000000, 0.000000000000000000, 0.000000000000000000 ) ) ;
#98060=AXIS2_PLACEMENT_3D ( 'NONE', #222596, #124818, #221319 ) ;
#98067=CARTESIAN_POINT ( 'NONE',  ( 23.15000000000000213, 87.65000000001172964, -81.27310748452423184 ) ) ;
#98073=STYLED_ITEM ( 'NONE', ( #107965 ), #48300 ) ;
#98131=CARTESIAN_POINT ( 'NONE',  ( -20.64999999999999858, 68.85000000001156195, -57.17310748452437252 ) ) ;
#98142=VERTEX_POINT ( 'NONE', #102762 ) ;
#98143=DIRECTION ( 'NONE',  ( 1.000000000000000000, 0.000000000000000000, 0.000000000000000000 ) ) ;
#98176=AXIS2_PLACEMENT_3D ( 'NONE', #134257, #70492, #213816 ) ;
#98191=ORIENTED_EDGE ( 'NONE', *, *, #24683, .F. ) ;
#98208=FACE_OUTER_BOUND ( 'NONE', #107136, .T. ) ;
#98228=CARTESIAN_POINT ( 'NONE',  ( 18.39999999999999858, 85.40000000001174385, -81.27310748452426026 ) ) ;
#98231=EDGE_CURVE ( 'NONE', #220609, #92818, #51276, .T. ) ;
#98291=DIRECTION ( 'NONE',  ( 0.000000000000000000, -1.000000000000000000, 0.000000000000000000 ) ) ;
#98325=ORIENTED_EDGE ( 'NONE', *, *, #156256, .T. ) ;
#98334=CIRCLE ( 'NONE', #244121, 0.1000000000000028644 ) ;
#98342=CIRCLE ( 'NONE', #210637, 0.1000000000000028644 ) ;
#98348=DIRECTION ( 'NONE',  ( -2.578261006436899437E-14, -0.1350103645451973811, 0.9908441862701586889 ) ) ;
#98379=EDGE_LOOP ( 'NONE', ( #202661, #146635, #33216, #190793 ) ) ;
#98399=EDGE_LOOP ( 'NONE', ( #27182, #51773, #229091, #103805 ) ) ;
#98413=DIRECTION ( 'NONE',  ( -0.000000000000000000, -1.000000000000000000, -6.982962677686266711E-15 ) ) ;
#98418=ORIENTED_EDGE ( 'NONE', *, *, #244181, .T. ) ;
#98430=CIRCLE ( 'NONE', #206819, 0.09999999999999939493 ) ;
#98435=CARTESIAN_POINT ( 'NONE',  ( -18.50000000000000000, 64.35000000001150511, -48.17310748452440095 ) ) ;
#98451=CARTESIAN_POINT ( 'NONE',  ( -20.00857864376270001, 66.85000000001156195, -57.27310748452438816 ) ) ;
#98485=AXIS2_PLACEMENT_3D ( 'NONE', #146647, #12326, #248343 ) ;
#98500=CARTESIAN_POINT ( 'NONE',  ( 21.07954763557399502, 69.67070900997433114, -69.58898340314273412 ) ) ;
#98531=ADVANCED_FACE ( 'NONE', ( #58191 ), #19082, .T. ) ;
#98547=FACE_OUTER_BOUND ( 'NONE', #16788, .T. ) ;
#98584=FACE_OUTER_BOUND ( 'NONE', #208921, .T. ) ;
#98618=ORIENTED_EDGE ( 'NONE', *, *, #237634, .T. ) ;
#98626=DIRECTION ( 'NONE',  ( 0.000000000000000000, -6.467318590049456648E-15, 1.000000000000000000 ) ) ;
#98642=ORIENTED_EDGE ( 'NONE', *, *, #234133, .F. ) ;
#98644=CARTESIAN_POINT ( 'NONE',  ( -23.25000000000000000, 85.60000000001159037, -59.62913836187181005 ) ) ;
#98646=DIRECTION ( 'NONE',  ( 1.000000000000000000, 0.000000000000000000, 0.000000000000000000 ) ) ;
#98669=ORIENTED_EDGE ( 'NONE', *, *, #29422, .T. ) ;
#98698=EDGE_CURVE ( 'NONE', #233017, #146658, #204127, .T. ) ;
#98721=B_SPLINE_CURVE_WITH_KNOTS ( 'NONE', 3,
 ( #82624, #160932, #220876, #240454, #61823, #121805, #102187, #181769 ),
 .UNSPECIFIED., .F., .F.,
 ( 4, 2, 2, 4 ),
 ( 0.000000000000000000, 0.0002181133598169061188, 0.0003271700397253531610, 0.0004362267196338002031 ),
 .UNSPECIFIED. ) ;
#98767=CARTESIAN_POINT ( 'NONE',  ( -21.00250684356851849, 64.25000000001161027, -62.50830171576457417 ) ) ;
#98776=ADVANCED_FACE ( 'NONE', ( #73652 ), #50187, .T. ) ;
#98802=FACE_OUTER_BOUND ( 'NONE', #116657, .T. ) ;
#98811=CARTESIAN_POINT ( 'NONE',  ( -18.39999999999999858, 85.68240343348777799, -29.36626410711147983 ) ) ;
#98819=EDGE_LOOP ( 'NONE', ( #225054, #97086, #121415, #50618 ) ) ;
#98825=UNCERTAINTY_MEASURE_WITH_UNIT (LENGTH_MEASURE( 1.000000000000000082E-05 ), #203409, 'distance_accuracy_value', 'NONE');
#98853=CARTESIAN_POINT ( 'NONE',  ( 21.05000000000000426, 69.58617371119866846, -69.43736654749098136 ) ) ;
#98869=CARTESIAN_POINT ( 'NONE',  ( -20.89878130938411616, 65.67252876774480796, -30.44570419949946327 ) ) ;
#98878=CARTESIAN_POINT ( 'NONE',  ( 23.25000000000000000, 87.65000000001165859, -69.52310748452424605 ) ) ;
#98900=ORIENTED_EDGE ( 'NONE', *, *, #83790, .T. ) ;
#98905=CARTESIAN_POINT ( 'NONE',  ( 23.24999999999999289, 64.35000000001164722, -69.42310748452440805 ) ) ;
#98951=CARTESIAN_POINT ( 'NONE',  ( -22.50485643085238863, 76.07878633908894983, -81.27290242369674900 ) ) ;
#98986=AXIS2_PLACEMENT_3D ( 'NONE', #173948, #194768, #35699 ) ;
#98996=ORIENTED_EDGE ( 'NONE', *, *, #250555, .F. ) ;
#99011=AXIS2_PLACEMENT_3D ( 'NONE', #144462, #225280, #45385 ) ;
#99047=DIRECTION ( 'NONE',  ( 1.000000000000000000, -0.000000000000000000, 0.000000000000000000 ) ) ;
#99048=CARTESIAN_POINT ( 'NONE',  ( 20.87600722750343252, 65.66887361445283489, -30.43298459182692994 ) ) ;
#99050=DIRECTION ( 'NONE',  ( -0.000000000000000000, 6.982962677686266711E-15, -1.000000000000000000 ) ) ;
#99056=CARTESIAN_POINT ( 'NONE',  ( 21.07933241753356768, 69.67135405163190853, -69.61648707494366306 ) ) ;
#99062=EDGE_LOOP ( 'NONE', ( #182554, #165325, #187729, #227468 ) ) ;
#99077=LINE ( 'NONE', #2557, #26885 ) ;
#99094=ORIENTED_EDGE ( 'NONE', *, *, #99864, .F. ) ;
#99103=EDGE_LOOP ( 'NONE', ( #113055, #171101, #227287, #146707 ) ) ;
#99170=ADVANCED_FACE ( 'NONE', ( #79400 ), #166862, .F. ) ;
#99171=AXIS2_PLACEMENT_3D ( 'NONE', #90180, #44663, #164612 ) ;
#99172=AXIS2_PLACEMENT_3D ( 'NONE', #43208, #103154, #58881 ) ;
#99185=EDGE_CURVE ( 'NONE', #251754, #34877, #225056, .T. ) ;
#99204=ORIENTED_EDGE ( 'NONE', *, *, #160699, .F. ) ;
#99214=DIRECTION ( 'NONE',  ( -1.000000000000000000, 0.000000000000000000, 0.000000000000000000 ) ) ;
#99316=TOROIDAL_SURFACE ( 'NONE', #245099, 11.70000000000000107, 0.1000000000000000056 ) ;
#99320=CARTESIAN_POINT ( 'NONE',  ( 20.94999999999999929, 71.00000000001151079, -48.02837350343745015 ) ) ;
#99343=DIRECTION ( 'NONE',  ( 0.000000000000000000, 2.775557561562812086E-13, -1.000000000000000000 ) ) ;
#99408=EDGE_LOOP ( 'NONE', ( #173601, #183617, #74368, #205406 ) ) ;
#99461=DIRECTION ( 'NONE',  ( 0.000000000000000000, -0.9915357197604804940, 0.1298341882520397950 ) ) ;
#99468=CARTESIAN_POINT ( 'NONE',  ( -18.50000000000001066, 85.42130820975074812, -62.28074427047331341 ) ) ;
#99530=ORIENTED_EDGE ( 'NONE', *, *, #146312, .F. ) ;
#99560=ORIENTED_EDGE ( 'NONE', *, *, #152130, .F. ) ;
#99563=ADVANCED_FACE ( 'NONE', ( #84177 ), #29660, .T. ) ;
#99570=AXIS2_PLACEMENT_3D ( 'NONE', #154591, #30787, #50302 ) ;
#99576=LINE ( 'NONE', #237837, #39605 ) ;
#99581=DIRECTION ( 'NONE',  ( 1.000000000000000000, 0.000000000000000000, 0.000000000000000000 ) ) ;
#99583=DIRECTION ( 'NONE',  ( 1.000000000000000000, -0.000000000000000000, 0.000000000000000000 ) ) ;
#99643=DIRECTION ( 'NONE',  ( -0.7071067811865475727, 0.7071067811865475727, 4.937700262164531476E-15 ) ) ;
#99649=CIRCLE ( 'NONE', #245444, 0.1000000000000028644 ) ;
#99651=CARTESIAN_POINT ( 'NONE',  ( -21.29999999999995808, 76.00000000001162448, -65.47310748452431994 ) ) ;
#99652=CIRCLE ( 'NONE', #220324, 0.3999999999999975797 ) ;
#99666=CARTESIAN_POINT ( 'NONE',  ( 21.05281448260627641, 67.22398984147393719, -57.34954957271295939 ) ) ;
#99678=AXIS2_PLACEMENT_3D ( 'NONE', #244719, #84320, #246028 ) ;
#99693=ADVANCED_FACE ( 'NONE', ( #239475 ), #38033, .T. ) ;
#99698=CARTESIAN_POINT ( 'NONE',  ( -20.54999999999999716, 85.50000000001149658, -45.91707660717669626 ) ) ;
#99699=EDGE_CURVE ( 'NONE', #29497, #117921, #146155, .T. ) ;
#99708=ORIENTED_EDGE ( 'NONE', *, *, #55893, .F. ) ;
#99714=LINE ( 'NONE', #159727, #113342 ) ;
#99736=VECTOR ( 'NONE', #84184, 1000.000000000000000 ) ;
#99743=AXIS2_PLACEMENT_3D ( 'NONE', #194890, #154496, #117891 ) ;
#99760=VERTEX_POINT ( 'NONE', #11129 ) ;
#99767=EDGE_CURVE ( 'NONE', #66731, #84841, #90644, .T. ) ;
#99772=ORIENTED_EDGE ( 'NONE', *, *, #66029, .F. ) ;
#99807=DIRECTION ( 'NONE',  ( -1.000000000000000000, 0.000000000000000000, 0.000000000000000000 ) ) ;
#99839=ADVANCED_FACE ( 'NONE', ( #187216 ), #17177, .T. ) ;
#99853=CARTESIAN_POINT ( 'NONE',  ( 18.47688499308725696, 85.46485595029550097, -29.32175973138686587 ) ) ;
#99864=EDGE_CURVE ( 'NONE', #223391, #167778, #246118, .T. ) ;
#99888=CARTESIAN_POINT ( 'NONE',  ( 20.94999999999999574, 77.16270174994961906, -61.42310748452431568 ) ) ;
#99913=EDGE_CURVE ( 'NONE', #2960, #162902, #96435, .T. ) ;
#99916=ORIENTED_EDGE ( 'NONE', *, *, #66169, .F. ) ;
#99936=FACE_OUTER_BOUND ( 'NONE', #22190, .T. ) ;
#99946=EDGE_CURVE ( 'NONE', #165812, #86432, #175574, .T. ) ;
#99964=ORIENTED_EDGE ( 'NONE', *, *, #159570, .F. ) ;
#99969=ADVANCED_FACE ( 'NONE', ( #31994 ), #111511, .T. ) ;
#99975=CARTESIAN_POINT ( 'NONE',  ( 21.14999999999999858, 65.28660755661168480, -57.27310748452439526 ) ) ;
#99982=CARTESIAN_POINT ( 'NONE',  ( 20.74625933824083646, 67.11708647892730539, -60.96793646040334380 ) ) ;
#99984=AXIS2_PLACEMENT_3D ( 'NONE', #174104, #22390, #253578 ) ;
#99987=PLANE ( 'NONE',  #220853 ) ;
#99994=EDGE_CURVE ( 'NONE', #215272, #208753, #176638, .T. ) ;
#100002=EDGE_CURVE ( 'NONE', #172217, #235108, #100510, .T. ) ;
#100006=CARTESIAN_POINT ( 'NONE',  ( 18.59999999999999076, 65.75000000001149658, -44.77310748452439526 ) ) ;
#100014=VECTOR ( 'NONE', #327, 1000.000000000000000 ) ;
#100058=CARTESIAN_POINT ( 'NONE',  ( -22.39999999999999858, 75.90000000001165859, -69.52310748452431710 ) ) ;
#100106=FACE_OUTER_BOUND ( 'NONE', #119312, .T. ) ;
#100123=EDGE_LOOP ( 'NONE', ( #221221, #103490, #10070, #1598 ) ) ;
#100137=ADVANCED_FACE ( 'NONE', ( #18818 ), #125489, .T. ) ;
#100160=AXIS2_PLACEMENT_3D ( 'NONE', #170889, #31363, #66602 ) ;
#100246=LINE ( 'NONE', #1153, #171665 ) ;
#100291=CARTESIAN_POINT ( 'NONE',  ( -22.39999999999999858, 76.00000000001170974, -77.31388708289772183 ) ) ;
#100316=VERTEX_POINT ( 'NONE', #31424 ) ;
#100326=CARTESIAN_POINT ( 'NONE',  ( -21.05000000000000071, 87.29603075034691528, -66.47520832486038955 ) ) ;
#100329=DIRECTION ( 'NONE',  ( 0.000000000000000000, 0.9887567792719329507, 0.1495327102803732933 ) ) ;
#100334=CARTESIAN_POINT ( 'NONE',  ( 18.52643265882457868, 65.68026841930851845, -30.47257401318894665 ) ) ;
#100341=CARTESIAN_POINT ( 'NONE',  ( 20.84999999999999432, 77.16412189325258453, -28.10825939895270764 ) ) ;
#100350=VERTEX_POINT ( 'NONE', #86191 ) ;
#100358=CARTESIAN_POINT ( 'NONE',  ( 18.33683296300380405, 85.51114997114433436, -29.11740007181401424 ) ) ;
#100361=( BOUNDED_SURFACE ( )  B_SPLINE_SURFACE ( 3, 2, ( 
 ( #59017, #16106, #172640 ),
 ( #194743, #235133, #112619 ),
 ( #133461, #192171, #95610 ),
 ( #156906, #257202, #93046 ) ),
 .UNSPECIFIED., .F., .F., .F. ) 
 B_SPLINE_SURFACE_WITH_KNOTS ( ( 4, 4 ),
 ( 3, 3 ),
 ( 0.0002700421466196708999, 0.0004789321604330827272 ),
 ( 0.000000000000000000, 1.000000000000000000 ),
 .UNSPECIFIED. ) 
 GEOMETRIC_REPRESENTATION_ITEM ( )  RATIONAL_B_SPLINE_SURFACE ( (
 ( 1.000000000000000000, 0.7071067811865475727, 1.000000000000000000),
 ( 1.000000000000000000, 0.7163411249511302259, 1.000000000000000000),
 ( 1.000000000000000000, 0.7221957104842335884, 1.000000000000000000),
 ( 1.000000000000000000, 0.7250110520819756932, 1.000000000000000000) ) ) 
 REPRESENTATION_ITEM ( '' )  SURFACE ( )  );
#100363=CARTESIAN_POINT ( 'NONE',  ( -21.53699400379686324, 69.21228820681083960, -69.52310748452437394 ) ) ;
#100406=CARTESIAN_POINT ( 'NONE',  ( -18.50000000000000000, 77.83534155023598089, -57.96795619196132776 ) ) ;
#100407=CARTESIAN_POINT ( 'NONE',  ( -1.739115166359751801E-14, 64.35000000001151932, -48.17310748452440095 ) ) ;
#100429=DIRECTION ( 'NONE',  ( -1.000000000000000000, -0.000000000000000000, -0.000000000000000000 ) ) ;
#100433=ORIENTED_EDGE ( 'NONE', *, *, #15828, .T. ) ;
#100456=EDGE_LOOP ( 'NONE', ( #171079, #92157, #27611, #27442 ) ) ;
#100462=AXIS2_PLACEMENT_3D ( 'NONE', #185742, #142738, #7091 ) ;
#100472=COLOUR_RGB ( '', 0.66274510, 0.83137255, 0.94901961) ;
#100478=LINE ( 'NONE', #82194, #24847 ) ;
#100497=CARTESIAN_POINT ( 'NONE',  ( -20.94999999999999929, 70.15000000001148805, -46.15560470880229360 ) ) ;
#100499=SPHERICAL_SURFACE ( 'NONE', #106471, 0.1000000000000000056 ) ;
#100510=CIRCLE ( 'NONE', #104603, 0.09999999999999939493 ) ;
#100513=ORIENTED_EDGE ( 'NONE', *, *, #252822, .F. ) ;
#100531=EDGE_LOOP ( 'NONE', ( #3122, #248632 ) ) ;
#100564=CARTESIAN_POINT ( 'NONE',  ( -23.15000000000000213, 76.00000000001149658, -47.82310748452432847 ) ) ;
#100586=CARTESIAN_POINT ( 'NONE',  ( -18.50000000000000000, 65.70711192142317714, -30.56510546851221477 ) ) ;
#100600=ORIENTED_EDGE ( 'NONE', *, *, #142996, .F. ) ;
#100603=DIRECTION ( 'NONE',  ( 0.000000000000000000, -0.1298341882519953583, -0.9915357197604861561 ) ) ;
#100620=CARTESIAN_POINT ( 'NONE',  ( -18.59999999999999787, 77.16270174994961906, -61.42310748452431568 ) ) ;
#100628=EDGE_CURVE ( 'NONE', #2004, #87393, #254963, .T. ) ;
#100633=DIRECTION ( 'NONE',  ( 0.000000000000000000, 0.000000000000000000, 1.000000000000000000 ) ) ;
#100636=DIRECTION ( 'NONE',  ( 0.000000000000000000, 0.000000000000000000, -1.000000000000000000 ) ) ;
#100667=DIRECTION ( 'NONE',  ( 0.000000000000000000, -6.467318590049456648E-15, 1.000000000000000000 ) ) ;
#100670=CARTESIAN_POINT ( 'NONE',  ( -20.64999999999999858, 76.00000000001142553, -36.02310748452432421 ) ) ;
#100678=VERTEX_POINT ( 'NONE', #51559 ) ;
#100723=DIRECTION ( 'NONE',  ( -0.1538461538461484146, -0.9880948137434723000, 0.000000000000000000 ) ) ;
#100726=ORIENTED_EDGE ( 'NONE', *, *, #162371, .F. ) ;
#100737=CARTESIAN_POINT ( 'NONE',  ( -18.40000000000000568, 85.50000000001162448, -62.52374538734409981 ) ) ;
#100757=ORIENTED_EDGE ( 'NONE', *, *, #228281, .T. ) ;
#100777=SPHERICAL_SURFACE ( 'NONE', #161423, 0.1000000000000000056 ) ;
#100780=VECTOR ( 'NONE', #36746, 1000.000000000000227 ) ;
#100794=ORIENTED_EDGE ( 'NONE', *, *, #172059, .F. ) ;
#100797=DIRECTION ( 'NONE',  ( 0.000000000000000000, -0.6728971962616412394, -0.7397360091703134577 ) ) ;
#100803=AXIS2_PLACEMENT_3D ( 'NONE', #14736, #207803, #12168 ) ;
#100835=DIRECTION ( 'NONE',  ( 0.000000000000000000, -5.956132106358135699E-15, 1.000000000000000000 ) ) ;
#100846=EDGE_CURVE ( 'NONE', #137039, #119848, #105140, .T. ) ;
#100853=CARTESIAN_POINT ( 'NONE',  ( -18.50000000000000000, 85.40000000001138858, -29.10844914155459762 ) ) ;
#100863=CYLINDRICAL_SURFACE ( 'NONE', #238885, 0.09999999999999867328 ) ;
#100885=DIRECTION ( 'NONE',  ( 1.000000000000000000, 0.000000000000000000, 0.000000000000000000 ) ) ;
#100891=CARTESIAN_POINT ( 'NONE',  ( 20.95052659398289308, 65.52017563223169816, -61.94786872865878991 ) ) ;
#100901=CIRCLE ( 'NONE', #80060, 0.5000000000000004441 ) ;
#100902=DIRECTION ( 'NONE',  ( -0.000000000000000000, 0.1350103645451945777, -0.9908441862701590219 ) ) ;
#100910=EDGE_LOOP ( 'NONE', ( #98418, #169335, #236560, #9134 ) ) ;
#100916=CARTESIAN_POINT ( 'NONE',  ( 20.94999999999999574, 74.16465844978715438, -57.96795619196135618 ) ) ;
#100921=ORIENTED_EDGE ( 'NONE', *, *, #39399, .T. ) ;
#100928=PLANE ( 'NONE',  #117360 ) ;
#100961=CIRCLE ( 'NONE', #21920, 0.09999999999999939493 ) ;
#100978=LINE ( 'NONE', #256181, #131573 ) ;
#100987=ORIENTED_EDGE ( 'NONE', *, *, #175817, .T. ) ;
#101007=DIRECTION ( 'NONE',  ( 0.000000000000000000, 0.000000000000000000, 1.000000000000000000 ) ) ;
#101012=CARTESIAN_POINT ( 'NONE',  ( 23.14999999999998437, 87.75000000001165290, -69.52310748452424605 ) ) ;
#101026=CARTESIAN_POINT ( 'NONE',  ( -21.05000000000000071, 87.75000000001143974, -39.12310748452424747 ) ) ;
#101061=DIRECTION ( 'NONE',  ( 1.000000000000000000, 0.000000000000000000, 0.000000000000000000 ) ) ;
#101066=AXIS2_PLACEMENT_3D ( 'NONE', #91267, #125565, #245527 ) ;
#101076=ORIENTED_EDGE ( 'NONE', *, *, #184894, .F. ) ;
#101078=CARTESIAN_POINT ( 'NONE',  ( -23.25000000000000000, 76.00000000001165290, -69.52310748452431710 ) ) ;
#101114=AXIS2_PLACEMENT_3D ( 'NONE', #6183, #106555, #85689 ) ;
#101132=VERTEX_POINT ( 'NONE', #75998 ) ;
#101134=ORIENTED_EDGE ( 'NONE', *, *, #41818, .F. ) ;
#101137=CARTESIAN_POINT ( 'NONE',  ( -21.14999999999999858, 87.65000000001165859, -69.52310748452424605 ) ) ;
#101150=CIRCLE ( 'NONE', #226083, 0.1000000000000028644 ) ;
#101152=DIRECTION ( 'NONE',  ( 1.000000000000000000, 0.000000000000000000, 0.000000000000000000 ) ) ;
#101154=ORIENTED_EDGE ( 'NONE', *, *, #108831, .F. ) ;
#101168=( BOUNDED_CURVE ( )  B_SPLINE_CURVE ( 3, ( #61469, #241400, #62753, #142280 ),
 .UNSPECIFIED., .F., .F. ) 
 B_SPLINE_CURVE_WITH_KNOTS ( ( 4, 4 ),
 ( 3.141592653589793116, 4.712388980384689674 ),
 .UNSPECIFIED. ) 
 CURVE ( )  GEOMETRIC_REPRESENTATION_ITEM ( )  RATIONAL_B_SPLINE_CURVE ( ( 1.000000000000000000, 0.8047378541243649375, 0.8047378541243649375, 1.000000000000000000 ) ) 
 REPRESENTATION_ITEM ( '' )  );
#101208=DIRECTION ( 'NONE',  ( 0.000000000000000000, -1.000000000000000000, 0.000000000000000000 ) ) ;
#101246=CARTESIAN_POINT ( 'NONE',  ( 20.12518398540832010, 66.02491127934389681, -61.52643923205447862 ) ) ;
#101253=DIRECTION ( 'NONE',  ( -1.000000000000000000, -0.000000000000000000, -0.000000000000000000 ) ) ;
#101281=CARTESIAN_POINT ( 'NONE',  ( -21.05000000000000071, 69.74168394267961446, -69.58880909484646793 ) ) ;
#101283=ORIENTED_EDGE ( 'NONE', *, *, #67135, .F. ) ;
#101333=ADVANCED_FACE ( 'NONE', ( #65413 ), #161976, .T. ) ;
#101391=AXIS2_PLACEMENT_3D ( 'NONE', #147553, #131838, #49734 ) ;
#101400=ORIENTED_EDGE ( 'NONE', *, *, #142811, .F. ) ;
#101405=DIRECTION ( 'NONE',  ( 0.7071067811865474617, -0.7071067811865474617, -4.937700262164531476E-15 ) ) ;
#101422=AXIS2_PLACEMENT_3D ( 'NONE', #117737, #159447, #115175 ) ;
#101458=CARTESIAN_POINT ( 'NONE',  ( -21.14999999999999858, 64.35000000001166143, -69.42310748452440805 ) ) ;
#101464=VECTOR ( 'NONE', #160370, 1000.000000000000000 ) ;
#101465=EDGE_CURVE ( 'NONE', #116437, #121217, #107105, .T. ) ;
#101515=DIRECTION ( 'NONE',  ( 1.000000000000000000, -3.265361837132813093E-16, -2.280189983783949500E-30 ) ) ;
#101517=CARTESIAN_POINT ( 'NONE',  ( -20.64999999999999858, 68.75000000001158185, -57.27310748452437394 ) ) ;
#101601=CARTESIAN_POINT ( 'NONE',  ( 20.94999027547553894, 65.70673848566926267, -30.56382523348290547 ) ) ;
#101605=LINE ( 'NONE', #121256, #101464 ) ;
#101623=ORIENTED_EDGE ( 'NONE', *, *, #17888, .T. ) ;
#101680=CYLINDRICAL_SURFACE ( 'NONE', #43591, 11.79999999999999716 ) ;
#101690=VERTEX_POINT ( 'NONE', #203343 ) ;
#101698=VERTEX_POINT ( 'NONE', #84621 ) ;
#101724=ORIENTED_EDGE ( 'NONE', *, *, #54153, .T. ) ;
#101769=CARTESIAN_POINT ( 'NONE',  ( -20.64999999999999858, 84.73084112150681335, -45.62118220350859588 ) ) ;
#101771=VERTEX_POINT ( 'NONE', #188908 ) ;
#101776=ORIENTED_EDGE ( 'NONE', *, *, #213058, .F. ) ;
#101778=DIRECTION ( 'NONE',  ( 1.000000000000000000, 0.000000000000000000, 0.000000000000000000 ) ) ;
#101779=ORIENTED_EDGE ( 'NONE', *, *, #257701, .F. ) ;
#101805=DIRECTION ( 'NONE',  ( 3.616040088954490704E-32, 7.105427357601001859E-15, -1.000000000000000000 ) ) ;
#101808=CARTESIAN_POINT ( 'NONE',  ( 20.94999999999999929, 87.48912529308749697, -38.92310748452424463 ) ) ;
#101826=ORIENTED_EDGE ( 'NONE', *, *, #171915, .F. ) ;
#101845=VECTOR ( 'NONE', #68933, 1000.000000000000114 ) ;
#101856=AXIS2_PLACEMENT_3D ( 'NONE', #14223, #175857, #35086 ) ;
#101891=DIRECTION ( 'NONE',  ( 0.000000000000000000, -0.1350103645451945777, 0.9908441862701591329 ) ) ;
#102028=CIRCLE ( 'NONE', #56244, 0.1000000000000028644 ) ;
#102039=EDGE_CURVE ( 'NONE', #92040, #2004, #77929, .T. ) ;
#102057=VERTEX_POINT ( 'NONE', #222560 ) ;
#102060=ORIENTED_EDGE ( 'NONE', *, *, #203559, .T. ) ;
#102074=VERTEX_POINT ( 'NONE', #239590 ) ;
#102095=FACE_OUTER_BOUND ( 'NONE', #58633, .T. ) ;
#102096=ORIENTED_EDGE ( 'NONE', *, *, #71889, .F. ) ;
#102166=DIRECTION ( 'NONE',  ( 1.000000000000000000, 0.000000000000000000, 0.000000000000000000 ) ) ;
#102187=CARTESIAN_POINT ( 'NONE',  ( 18.43709777086140278, 85.68240343348777799, -29.36626410711147273 ) ) ;
#102188=CARTESIAN_POINT ( 'NONE',  ( 21.05000000000000071, 64.35000000001164722, -69.42310748452440805 ) ) ;
#102197=CARTESIAN_POINT ( 'NONE',  ( 22.47007471830798053, 76.00000000001169553, -77.24381813645078410 ) ) ;
#102212=DIRECTION ( 'NONE',  ( 0.000000000000000000, 0.000000000000000000, 1.000000000000000000 ) ) ;
#102241=CARTESIAN_POINT ( 'NONE',  ( 20.94999999999999929, 85.40000000001158753, -59.62913836187181715 ) ) ;
#102249=AXIS2_PLACEMENT_3D ( 'NONE', #38718, #118245, #84187 ) ;
#102258=ORIENTED_EDGE ( 'NONE', *, *, #104750, .T. ) ;
#102266=CARTESIAN_POINT ( 'NONE',  ( -21.05000000000000071, 62.00000000001146105, -41.45020001490689765 ) ) ;
#102298=DIRECTION ( 'NONE',  ( 0.000000000000000000, 0.1455152366551500653, 0.9893560106964507384 ) ) ;
#102302=FACE_OUTER_BOUND ( 'NONE', #57519, .T. ) ;
#102309=CARTESIAN_POINT ( 'NONE',  ( 21.05000000000000071, 65.27628289530413497, -69.52310748452438816 ) ) ;
#102319=CIRCLE ( 'NONE', #156568, 12.87499999999999822 ) ;
#102333=CIRCLE ( 'NONE', #231018, 0.09999999999999939493 ) ;
#102370=VERTEX_POINT ( 'NONE', #232879 ) ;
#102382=DIRECTION ( 'NONE',  ( 0.000000000000000000, -0.9915357197604892647, 0.1298341882519715440 ) ) ;
#102417=DIRECTION ( 'NONE',  ( 0.000000000000000000, -0.9908441862701610203, 0.1350103645451807555 ) ) ;
#102502=CARTESIAN_POINT ( 'NONE',  ( -21.13614978966382196, 69.50089529817788048, -69.52310748452437394 ) ) ;
#102527=ORIENTED_EDGE ( 'NONE', *, *, #65009, .F. ) ;
#102535=ORIENTED_EDGE ( 'NONE', *, *, #81872, .T. ) ;
#102578=DIRECTION ( 'NONE',  ( 1.000000000000000000, 0.000000000000000000, 0.000000000000000000 ) ) ;
#102580=DIRECTION ( 'NONE',  ( 0.000000000000000000, -0.1495327102803180597, -0.9887567792719412774 ) ) ;
#102605=AXIS2_PLACEMENT_3D ( 'NONE', #17160, #135783, #18417 ) ;
#102616=EDGE_CURVE ( 'NONE', #221113, #92818, #148863, .T. ) ;
#102633=CARTESIAN_POINT ( 'NONE',  ( 18.59999999999996945, 65.66751761918619934, -30.42826094061123854 ) ) ;
#102641=LINE ( 'NONE', #186066, #210235 ) ;
#102648=CIRCLE ( 'NONE', #32159, 0.1999999999999987899 ) ;
#102656=CARTESIAN_POINT ( 'NONE',  ( 18.49999999999999289, 65.79142135624879018, -44.87310748452439668 ) ) ;
#102659=CARTESIAN_POINT ( 'NONE',  ( -23.25000000000000000, 64.25000000001158185, -57.37310748452440379 ) ) ;
#102695=LINE ( 'NONE', #63591, #242770 ) ;
#102713=EDGE_CURVE ( 'NONE', #122621, #210362, #254342, .T. ) ;
#102735=DIRECTION ( 'NONE',  ( 1.441126678808781001E-14, -0.9876197685951241256, -0.1568667991644932258 ) ) ;
#102762=CARTESIAN_POINT ( 'NONE',  ( -20.94999999999999929, 87.48912529308769592, -66.52310748452423184 ) ) ;
#102783=SPHERICAL_SURFACE ( 'NONE', #119216, 0.1000000000000000056 ) ;
#102787=CARTESIAN_POINT ( 'NONE',  ( -18.59999999999999787, 66.85000000001156195, -57.17310748452438673 ) ) ;
#102788=CARTESIAN_POINT ( 'NONE',  ( 21.05000000000000071, 76.10000000001170406, -76.06376443622556849 ) ) ;
#102799=EDGE_CURVE ( 'NONE', #196143, #35500, #117427, .T. ) ;
#102841=CARTESIAN_POINT ( 'NONE',  ( 20.85000000000000142, 77.26327546522863088, -28.12124281777790813 ) ) ;
#102882=ORIENTED_EDGE ( 'NONE', *, *, #43636, .F. ) ;
#102894=DIRECTION ( 'NONE',  ( 0.000000000000000000, -7.056502275159890043E-15, 1.000000000000000000 ) ) ;
#102911=DIRECTION ( 'NONE',  ( -1.000000000000000000, 0.000000000000000000, -0.000000000000000000 ) ) ;
#102930=CARTESIAN_POINT ( 'NONE',  ( 18.54271179734060127, 85.62408429011018995, -29.28214263182405830 ) ) ;
#102939=CARTESIAN_POINT ( 'NONE',  ( -21.46681500593007641, 69.14248884062448042, -69.52310748452435973 ) ) ;
#102947=EDGE_CURVE ( 'NONE', #98142, #166990, #204644, .T. ) ;
#102987=AXIS2_PLACEMENT_3D ( 'NONE', #250596, #188071, #150243 ) ;
#102988=DIRECTION ( 'NONE',  ( 0.000000000000000000, -6.769652589177784668E-15, 1.000000000000000000 ) ) ;
#102996=ORIENTED_EDGE ( 'NONE', *, *, #168433, .T. ) ;
#103032=CARTESIAN_POINT ( 'NONE',  ( 23.14999999999999858, 76.00000000001142553, -36.02310748452432421 ) ) ;
#103049=DIRECTION ( 'NONE',  ( 1.000000000000000000, 0.000000000000000000, 0.000000000000000000 ) ) ;
#103052=( BOUNDED_SURFACE ( )  B_SPLINE_SURFACE ( 3, 2, ( 
 ( #118386, #38852, #256540 ),
 ( #177093, #17980, #36292 ),
 ( #213617, #76670, #197900 ),
 ( #134074, #156250, #173270 ),
 ( #174557, #233214, #98767 ),
 ( #115811, #19274, #218735 ) ),
 .UNSPECIFIED., .F., .F., .T. ) 
 B_SPLINE_SURFACE_WITH_KNOTS ( ( 4, 2, 4 ),
 ( 3, 3 ),
 ( 1.570796326794895448, 2.356194490192343505, 3.141592653589791784 ),
 ( 0.000000000000000000, 1.000000000000000000 ),
 .UNSPECIFIED. ) 
 GEOMETRIC_REPRESENTATION_ITEM ( )  RATIONAL_B_SPLINE_SURFACE ( (
 ( 1.000000000000000000, 0.7071067811865475727, 1.000000000000000000),
 ( 1.000000000000000000, 0.6611148371776105481, 1.000000000000000000),
 ( 1.000000000000000000, 0.6092287576700083918, 1.000000000000000000),
 ( 1.000000000000000000, 0.5278258667053740139, 1.000000000000000000),
 ( 1.000000000000000000, 0.4993418825337004874, 1.000000000000000000),
 ( 1.000000000000000000, 0.5000000000000154321, 1.000000000000000000) ) ) 
 REPRESENTATION_ITEM ( '' )  SURFACE ( )  );
#103078=VECTOR ( 'NONE', #235345, 1000.000000000000000 ) ;
#103126=DIRECTION ( 'NONE',  ( 1.000000000000000000, 0.000000000000000000, 0.000000000000000000 ) ) ;
#103152=EDGE_CURVE ( 'NONE', #199664, #121900, #137937, .T. ) ;
#103154=DIRECTION ( 'NONE',  ( -1.000000000000000000, 0.000000000000000000, 0.000000000000000000 ) ) ;
#103184=FACE_OUTER_BOUND ( 'NONE', #76818, .T. ) ;
#103195=AXIS2_PLACEMENT_3D ( 'NONE', #107129, #68008, #45877 ) ;
#103200=ORIENTED_EDGE ( 'NONE', *, *, #31243, .F. ) ;
#103202=CARTESIAN_POINT ( 'NONE',  ( 22.59999999999999432, 75.89914163091302157, -81.27267460801373034 ) ) ;
#103252=DIRECTION ( 'NONE',  ( 1.836970198721029934E-16, 1.000000000000000000, 6.982962677686266711E-15 ) ) ;
#103256=CARTESIAN_POINT ( 'NONE',  ( -23.25000000000000000, 85.60000000001149090, -45.91707660717669626 ) ) ;
#103285=DIRECTION ( 'NONE',  ( -1.000000000000000000, 7.304098846218134667E-16, 5.100424963727256530E-30 ) ) ;
#103292=EDGE_CURVE ( 'NONE', #64683, #138152, #193979, .T. ) ;
#103308=CARTESIAN_POINT ( 'NONE',  ( 21.06277459767440163, 67.12713756174332502, -57.31910829216806746 ) ) ;
#103320=AXIS2_PLACEMENT_3D ( 'NONE', #215459, #214188, #99343 ) ;
#103330=TOROIDAL_SURFACE ( 'NONE', #132578, 1.900000000000002576, 0.1000000000000000056 ) ;
#103339=ORIENTED_EDGE ( 'NONE', *, *, #213206, .F. ) ;
#103349=CIRCLE ( 'NONE', #20001, 0.09999999999999939493 ) ;
#103369=ORIENTED_EDGE ( 'NONE', *, *, #81730, .F. ) ;
#103391=ORIENTED_EDGE ( 'NONE', *, *, #161467, .F. ) ;
#103463=DIRECTION ( 'NONE',  ( 1.000000000000000000, 0.000000000000000000, 0.000000000000000000 ) ) ;
#103476=CIRCLE ( 'NONE', #149316, 0.1000000000000028644 ) ;
#103486=VECTOR ( 'NONE', #83647, 1000.000000000000000 ) ;
#103490=ORIENTED_EDGE ( 'NONE', *, *, #2040, .F. ) ;
#103552=CYLINDRICAL_SURFACE ( 'NONE', #217486, 0.5000000000000004441 ) ;
#103608=EDGE_CURVE ( 'NONE', #88576, #47933, #102333, .T. ) ;
#103632=CIRCLE ( 'NONE', #153608, 12.87499999999999822 ) ;
#103636=ORIENTED_EDGE ( 'NONE', *, *, #160789, .T. ) ;
#103661=CARTESIAN_POINT ( 'NONE',  ( -20.85000000000000142, 64.35000000001147669, -42.80697314750250371 ) ) ;
#103681=SPHERICAL_SURFACE ( 'NONE', #60904, 0.1000000000000000056 ) ;
#103684=AXIS2_PLACEMENT_3D ( 'NONE', #92720, #154044, #233546 ) ;
#103694=FACE_OUTER_BOUND ( 'NONE', #240315, .T. ) ;
#103712=ORIENTED_EDGE ( 'NONE', *, *, #40244, .F. ) ;
#103716=ORIENTED_EDGE ( 'NONE', *, *, #27236, .T. ) ;
#103733=ORIENTED_EDGE ( 'NONE', *, *, #248371, .T. ) ;
#103737=CARTESIAN_POINT ( 'NONE',  ( -18.59999999999999787, 76.00000000001142553, -36.02310748452432421 ) ) ;
#103744=AXIS2_PLACEMENT_3D ( 'NONE', #88143, #244670, #184701 ) ;
#103782=DIRECTION ( 'NONE',  ( 0.000000000000000000, -1.000000000000000000, -7.272083257015735086E-15 ) ) ;
#103796=CARTESIAN_POINT ( 'NONE',  ( 19.94784844284953707, 64.28691006698250021, -44.82090876722581640 ) ) ;
#103797=ORIENTED_EDGE ( 'NONE', *, *, #24531, .T. ) ;
#103798=EDGE_CURVE ( 'NONE', #224378, #106650, #73377, .T. ) ;
#103801=DIRECTION ( 'NONE',  ( -1.000000000000000000, -0.000000000000000000, -0.000000000000000000 ) ) ;
#103802=DIRECTION ( 'NONE',  ( -0.000000000000000000, 1.000000000000000000, 6.982962677686266711E-15 ) ) ;
#103805=ORIENTED_EDGE ( 'NONE', *, *, #19281, .F. ) ;
#103839=EDGE_CURVE ( 'NONE', #198094, #84743, #202332, .T. ) ;
#103846=ORIENTED_EDGE ( 'NONE', *, *, #100846, .F. ) ;
#103852=AXIS2_PLACEMENT_3D ( 'NONE', #167946, #110500, #247448 ) ;
#103876=CARTESIAN_POINT ( 'NONE',  ( -21.05000000000000071, 76.00000000001165290, -69.52310748452431710 ) ) ;
#103886=ADVANCED_FACE ( 'NONE', ( #175232 ), #250851, .T. ) ;
#103900=DIRECTION ( 'NONE',  ( 1.000000000000000000, 0.000000000000000000, 0.000000000000000000 ) ) ;
#103909=DIRECTION ( 'NONE',  ( 0.000000000000000000, 0.000000000000000000, 1.000000000000000000 ) ) ;
#103941=CARTESIAN_POINT ( 'NONE',  ( -21.56666275994539816, 76.00000000001169553, -76.48047589141765457 ) ) ;
#103948=EDGE_LOOP ( 'NONE', ( #36931, #41349, #184923, #144401 ) ) ;
#104019=FACE_OUTER_BOUND ( 'NONE', #204436, .T. ) ;
#104020=AXIS2_PLACEMENT_3D ( 'NONE', #114826, #213929, #172285 ) ;
#104021=ORIENTED_EDGE ( 'NONE', *, *, #10172, .F. ) ;
#104049=SPHERICAL_SURFACE ( 'NONE', #78180, 0.1000000000000000056 ) ;
#104076=FACE_OUTER_BOUND ( 'NONE', #152212, .T. ) ;
#104082=DIRECTION ( 'NONE',  ( -0.000000000000000000, -6.982962677686266711E-15, 1.000000000000000000 ) ) ;
#104096=CARTESIAN_POINT ( 'NONE',  ( 22.14074124539698829, 68.60992214896791097, -69.62216038036844168 ) ) ;
#104111=AXIS2_PLACEMENT_3D ( 'NONE', #143046, #221296, #67381 ) ;
#104118=ORIENTED_EDGE ( 'NONE', *, *, #91347, .T. ) ;
#104132=CIRCLE ( 'NONE', #174941, 0.09999999999999939493 ) ;
#104136=TOROIDAL_SURFACE ( 'NONE', #195760, 7.791421356237316687, 0.1000000000000000056 ) ;
#104141=AXIS2_PLACEMENT_3D ( 'NONE', #161299, #122159, #183418 ) ;
#104166=CYLINDRICAL_SURFACE ( 'NONE', #62050, 3.999999999999996447 ) ;
#104185=CARTESIAN_POINT ( 'NONE',  ( -23.15000000000000213, 71.75000000001156764, -57.17310748452435121 ) ) ;
#104238=FACE_OUTER_BOUND ( 'NONE', #206929, .T. ) ;
#104254=CIRCLE ( 'NONE', #95882, 12.87499999999999822 ) ;
#104270=CARTESIAN_POINT ( 'NONE',  ( 18.58703555224997928, 85.40633674080056892, -62.39816284327772422 ) ) ;
#104274=DIRECTION ( 'NONE',  ( 0.000000000000000000, 0.000000000000000000, -1.000000000000000000 ) ) ;
#104279=ORIENTED_EDGE ( 'NONE', *, *, #50887, .F. ) ;
#104290=DIRECTION ( 'NONE',  ( 1.000000000000000000, -7.304098846218135653E-16, -5.100424963727256530E-30 ) ) ;
#104308=AXIS2_PLACEMENT_3D ( 'NONE', #207424, #69207, #107006 ) ;
#104334=LINE ( 'NONE', #27436, #8079 ) ;
#104345=ORIENTED_EDGE ( 'NONE', *, *, #118512, .T. ) ;
#104352=CARTESIAN_POINT ( 'NONE',  ( 20.85000000000000142, 87.65000000001141700, -36.02310748452423894 ) ) ;
#104354=EDGE_LOOP ( 'NONE', ( #222774, #85735, #215588, #25956 ) ) ;
#104373=AXIS2_PLACEMENT_3D ( 'NONE', #77311, #74805, #56457 ) ;
#104387=LINE ( 'NONE', #166999, #20163 ) ;
#104398=ORIENTED_EDGE ( 'NONE', *, *, #170301, .F. ) ;
#104449=EDGE_LOOP ( 'NONE', ( #8434, #86257, #10749, #74928 ) ) ;
#104456=ORIENTED_EDGE ( 'NONE', *, *, #236818, .T. ) ;
#104457=CARTESIAN_POINT ( 'NONE',  ( -20.64999999999999858, 74.00000000001151079, -49.24772940728643533 ) ) ;
#104467=CARTESIAN_POINT ( 'NONE',  ( 22.39999999999999503, 76.00000000001170974, -77.27310748452433131 ) ) ;
#104476=CARTESIAN_POINT ( 'NONE',  ( 22.49999999999999645, 75.89914163091300736, -81.27267460801373034 ) ) ;
#104555=DIRECTION ( 'NONE',  ( -1.000000000000000000, 0.000000000000000000, -0.000000000000000000 ) ) ;
#104603=AXIS2_PLACEMENT_3D ( 'NONE', #63078, #39703, #237873 ) ;
#104615=FACE_OUTER_BOUND ( 'NONE', #98399, .T. ) ;
#104620=EDGE_CURVE ( 'NONE', #20936, #26458, #193761, .T. ) ;
#104625=CIRCLE ( 'NONE', #208896, 0.1999999999999987899 ) ;
#104641=ORIENTED_EDGE ( 'NONE', *, *, #59246, .F. ) ;
#104688=ORIENTED_EDGE ( 'NONE', *, *, #35863, .F. ) ;
#104697=CARTESIAN_POINT ( 'NONE',  ( 21.33487959338958717, 69.27444184810046579, -69.52310748452435973 ) ) ;
#104699=CARTESIAN_POINT ( 'NONE',  ( 20.94999999999999929, 65.52661458509871295, -61.94445302027585143 ) ) ;
#104708=ADVANCED_FACE ( 'NONE', ( #254735 ), #76138, .T. ) ;
#104711=ORIENTED_EDGE ( 'NONE', *, *, #213651, .F. ) ;
#104712=FACE_OUTER_BOUND ( 'NONE', #11930, .T. ) ;
#104715=CARTESIAN_POINT ( 'NONE',  ( -23.25000000000000000, 76.00000000001141132, -33.92310748452431568 ) ) ;
#104718=CARTESIAN_POINT ( 'NONE',  ( 23.24999999999999289, 64.25000000001172396, -81.27310748452440237 ) ) ;
#104745=DIRECTION ( 'NONE',  ( -1.000000000000000000, 2.952720810173289112E-16, 2.061873921506763405E-30 ) ) ;
#104750=EDGE_CURVE ( 'NONE', #62040, #218484, #102319, .T. ) ;
#104766=CARTESIAN_POINT ( 'NONE',  ( 21.07016717457011623, 76.00000000001170974, -75.84404832262522689 ) ) ;
#104774=ADVANCED_FACE ( 'NONE', ( #102095 ), #164905, .T. ) ;
#104818=FACE_OUTER_BOUND ( 'NONE', #14658, .T. ) ;
#104821=DIRECTION ( 'NONE',  ( -0.000000000000000000, -0.8660254037844420383, 0.4999999999999943379 ) ) ;
#104824=ORIENTED_EDGE ( 'NONE', *, *, #88207, .F. ) ;
#104827=ORIENTED_EDGE ( 'NONE', *, *, #158598, .F. ) ;
#104832=FACE_OUTER_BOUND ( 'NONE', #111222, .T. ) ;
#104844=DIRECTION ( 'NONE',  ( 1.000000000000000000, 0.000000000000000000, 0.000000000000000000 ) ) ;
#104845=CARTESIAN_POINT ( 'NONE',  ( 20.94999999999999929, 77.83534155023599510, -57.96795619196132776 ) ) ;
#104863=CYLINDRICAL_SURFACE ( 'NONE', #97552, 0.09999999999999939493 ) ;
#104877=CARTESIAN_POINT ( 'NONE',  ( -18.59999999999999787, 102.4393534156124730, -51.38159887701667827 ) ) ;
#104889=DIRECTION ( 'NONE',  ( 2.952720810173289112E-16, 1.000000000000000000, 6.530723674265620862E-15 ) ) ;
#104896=CARTESIAN_POINT ( 'NONE',  ( -22.57320508075687115, 64.25000000001165290, -69.52310748452440237 ) ) ;
#104943=ORIENTED_EDGE ( 'NONE', *, *, #14358, .F. ) ;
#104944=EDGE_CURVE ( 'NONE', #168638, #50336, #189378, .T. ) ;
#104959=CARTESIAN_POINT ( 'NONE',  ( -23.15000000000000213, 73.40000000001151648, -49.24772940728643533 ) ) ;
#104962=( BOUNDED_CURVE ( )  B_SPLINE_CURVE ( 3, ( #207351, #149952, #126518, #151228 ),
 .UNSPECIFIED., .F., .F. ) 
 B_SPLINE_CURVE_WITH_KNOTS ( ( 4, 4 ),
 ( 4.712388980384689674, 6.231880751915386263 ),
 .UNSPECIFIED. ) 
 CURVE ( )  GEOMETRIC_REPRESENTATION_ITEM ( )  RATIONAL_B_SPLINE_CURVE ( ( 1.000000000000000000, 0.8166740347213228279, 0.8166740347213228279, 1.000000000000000000 ) ) 
 REPRESENTATION_ITEM ( '' )  );
#104966=EDGE_CURVE ( 'NONE', #239369, #42405, #233006, .T. ) ;
#104978=DIRECTION ( 'NONE',  ( 1.734723475976817507E-14, -6.982962677686266711E-15, 1.000000000000000000 ) ) ;
#104986=EDGE_CURVE ( 'NONE', #180491, #51613, #56257, .T. ) ;
#104987=AXIS2_PLACEMENT_3D ( 'NONE', #171758, #196413, #752 ) ;
#104997=ORIENTED_EDGE ( 'NONE', *, *, #119874, .T. ) ;
#105008=CIRCLE ( 'NONE', #42508, 0.6000000000000033085 ) ;
#105071=CIRCLE ( 'NONE', #84391, 2.000000000000001776 ) ;
#105103=VERTEX_POINT ( 'NONE', #117532 ) ;
#105119=CARTESIAN_POINT ( 'NONE',  ( 20.94999999999999574, 65.37642973952880254, -62.03116228129384524 ) ) ;
#105135=ADVANCED_FACE ( 'NONE', ( #177548 ), #256989, .T. ) ;
#105140=CIRCLE ( 'NONE', #171681, 0.6000000000000033085 ) ;
#105143=CARTESIAN_POINT ( 'NONE',  ( -20.94999999999999929, 88.41227409416113403, -39.02310748452423894 ) ) ;
#105151=CARTESIAN_POINT ( 'NONE',  ( 20.85000000000000142, 64.25000000001146816, -42.80697314750249660 ) ) ;
#105154=ORIENTED_EDGE ( 'NONE', *, *, #245461, .F. ) ;
#105159=VERTEX_POINT ( 'NONE', #125242 ) ;
#105177=CARTESIAN_POINT ( 'NONE',  ( 23.14999999999999503, 64.25000000001146816, -43.03791325517834565 ) ) ;
#105186=AXIS2_PLACEMENT_3D ( 'NONE', #245074, #147254, #106833 ) ;
#105198=ORIENTED_EDGE ( 'NONE', *, *, #29422, .F. ) ;
#105238=ORIENTED_EDGE ( 'NONE', *, *, #154083, .F. ) ;
#105293=DIRECTION ( 'NONE',  ( 1.000000000000000000, 0.000000000000000000, 0.000000000000000000 ) ) ;
#105300=CARTESIAN_POINT ( 'NONE',  ( 23.24999999999999289, 69.55000000001173532, -81.27310748452437394 ) ) ;
#105318=CARTESIAN_POINT ( 'NONE',  ( 23.24999999999999645, 76.00000000001165290, -69.52310748452431710 ) ) ;
#105364=CARTESIAN_POINT ( 'NONE',  ( 22.32929514600007792, 68.42135243463518179, -69.62218316263829365 ) ) ;
#105367=ORIENTED_EDGE ( 'NONE', *, *, #182773, .T. ) ;
#105380=AXIS2_PLACEMENT_3D ( 'NONE', #109009, #92023, #152029 ) ;
#105443=ORIENTED_EDGE ( 'NONE', *, *, #249582, .F. ) ;
#105471=FACE_OUTER_BOUND ( 'NONE', #234592, .T. ) ;
#105485=CARTESIAN_POINT ( 'NONE',  ( 18.50000000000000355, 85.40000000001137437, -29.14106563635156988 ) ) ;
#105490=CARTESIAN_POINT ( 'NONE',  ( 20.94999999999999929, 76.00000000001145395, -40.02310748452431710 ) ) ;
#105496=DIRECTION ( 'NONE',  ( 0.000000000000000000, -7.272083257015735086E-15, 1.000000000000000000 ) ) ;
#105503=CARTESIAN_POINT ( 'NONE',  ( 18.59999999999999076, 69.55000000001150795, -48.27310748452436684 ) ) ;
#105541=CARTESIAN_POINT ( 'NONE',  ( -20.64999999999999858, 76.00000000001141132, -34.12310748452431852 ) ) ;
#105546=DIRECTION ( 'NONE',  ( 0.000000000000000000, 0.000000000000000000, -1.000000000000000000 ) ) ;
#105554=DIRECTION ( 'NONE',  ( 0.000000000000000000, 0.000000000000000000, 1.000000000000000000 ) ) ;
#105557=DIRECTION ( 'NONE',  ( 0.000000000000000000, 6.982962677686266711E-15, -1.000000000000000000 ) ) ;
#105591=ADVANCED_FACE ( 'NONE', ( #42826 ), #122366, .T. ) ;
#105597=ADVANCED_FACE ( 'NONE', ( #83196 ), #150590, .F. ) ;
#105606=LINE ( 'NONE', #69095, #110575 ) ;
#105651=FACE_OUTER_BOUND ( 'NONE', #38620, .T. ) ;
#105657=AXIS2_PLACEMENT_3D ( 'NONE', #196239, #215791, #60573 ) ;
#105658=FACE_BOUND ( 'NONE', #149716, .T. ) ;
#105701=CARTESIAN_POINT ( 'NONE',  ( 21.05000000000000071, 87.29603075034691528, -66.47520832486038955 ) ) ;
#105722=ADVANCED_FACE ( 'NONE', ( #90590 ), #148529, .F. ) ;
#105726=CARTESIAN_POINT ( 'NONE',  ( -18.51697539158857353, 65.68434038414308418, -30.48668807260655456 ) ) ;
#105727=ADVANCED_FACE ( 'NONE', ( #91883 ), #73714, .T. ) ;
#105746=AXIS2_PLACEMENT_3D ( 'NONE', #221147, #182044, #162492 ) ;
#105748=CIRCLE ( 'NONE', #226365, 0.09999999999999938105 ) ;
#105759=LINE ( 'NONE', #184036, #249284 ) ;
#105771=DIRECTION ( 'NONE',  ( -0.000000000000000000, -6.982962677686266711E-15, 1.000000000000000000 ) ) ;
#105827=DIRECTION ( 'NONE',  ( 1.000000000000000000, 0.000000000000000000, 0.000000000000000000 ) ) ;
#105843=CIRCLE ( 'NONE', #222349, 0.1000000000000028644 ) ;
#105844=CIRCLE ( 'NONE', #197433, 3.900000000000000799 ) ;
#105856=AXIS2_PLACEMENT_3D ( 'NONE', #155940, #213302, #195059 ) ;
#105859=ORIENTED_EDGE ( 'NONE', *, *, #66843, .T. ) ;
#105871=LINE ( 'NONE', #45924, #188172 ) ;
#105901=CARTESIAN_POINT ( 'NONE',  ( -22.50000000000000000, 75.90000000001170122, -77.31388708289772183 ) ) ;
#105927=ORIENTED_EDGE ( 'NONE', *, *, #169940, .T. ) ;
#105932=VECTOR ( 'NONE', #59173, 1000.000000000000000 ) ;
#105979=FACE_OUTER_BOUND ( 'NONE', #117377, .T. ) ;
#105992=CIRCLE ( 'NONE', #122617, 4.049999999999998046 ) ;
#105993=CARTESIAN_POINT ( 'NONE',  ( -22.50000000000000000, 76.00000000001165290, -69.52310748452431710 ) ) ;
#106002=ORIENTED_EDGE ( 'NONE', *, *, #174492, .T. ) ;
#106033=EDGE_LOOP ( 'NONE', ( #28708, #61716, #224329, #201309 ) ) ;
#106063=DIRECTION ( 'NONE',  ( 1.000000000000000000, 0.000000000000000000, 0.000000000000000000 ) ) ;
#106079=CIRCLE ( 'NONE', #18633, 7.900000000000003908 ) ;
#106109=AXIS2_PLACEMENT_3D ( 'NONE', #112254, #251744, #212633 ) ;
#106127=CYLINDRICAL_SURFACE ( 'NONE', #165150, 0.1000000000000028644 ) ;
#106166=DIRECTION ( 'NONE',  ( -1.000000000000000000, 2.952720810173289112E-16, 2.061873921506763405E-30 ) ) ;
#106200=PLANE ( 'NONE',  #6382 ) ;
#106243=VERTEX_POINT ( 'NONE', #97985 ) ;
#106268=( GEOMETRIC_REPRESENTATION_CONTEXT ( 3 ) GLOBAL_UNCERTAINTY_ASSIGNED_CONTEXT ( ( #188595 ) ) GLOBAL_UNIT_ASSIGNED_CONTEXT ( ( #156740, #238818, #89663 ) ) REPRESENTATION_CONTEXT ( 'NONE', 'WORKASPACE' ) );
#106274=CARTESIAN_POINT ( 'NONE',  ( 23.25000000000000000, 87.65000000001172964, -81.27310748452423184 ) ) ;
#106286=AXIS2_PLACEMENT_3D ( 'NONE', #86887, #188574, #126026 ) ;
#106304=CARTESIAN_POINT ( 'NONE',  ( 21.15000000000000213, 67.21339244341145047, -57.27310748452438105 ) ) ;
#106313=DIRECTION ( 'NONE',  ( 1.000000000000000000, 0.000000000000000000, 0.000000000000000000 ) ) ;
#106332=DIRECTION ( 'NONE',  ( 0.000000000000000000, 1.000000000000000000, 7.272083257015735086E-15 ) ) ;
#106337=EDGE_LOOP ( 'NONE', ( #61266, #46971, #4138, #188085 ) ) ;
#106355=DIRECTION ( 'NONE',  ( 1.000000000000000000, 0.000000000000000000, 0.000000000000000000 ) ) ;
#106367=CARTESIAN_POINT ( 'NONE',  ( 20.04142135391667168, 64.25000000001148237, -44.82060061889435332 ) ) ;
#106374=ORIENTED_EDGE ( 'NONE', *, *, #84568, .T. ) ;
#106384=DIRECTION ( 'NONE',  ( -1.000000000000000000, 0.000000000000000000, -0.000000000000000000 ) ) ;
#106395=CARTESIAN_POINT ( 'NONE',  ( 21.05000000000000071, 74.65091558138459504, -61.53660852097885225 ) ) ;
#106419=DIRECTION ( 'NONE',  ( 0.000000000000000000, -0.8660254037844377084, -0.5000000000000016653 ) ) ;
#106420=ADVANCED_FACE ( 'NONE', ( #70483 ), #240637, .T. ) ;
#106429=DIRECTION ( 'NONE',  ( -1.000000000000000000, 0.000000000000000000, -0.000000000000000000 ) ) ;
#106433=DIRECTION ( 'NONE',  ( -1.000000000000000000, 0.000000000000000000, 0.000000000000000000 ) ) ;
#106457=CIRCLE ( 'NONE', #152320, 0.4000000000000045186 ) ;
#106471=AXIS2_PLACEMENT_3D ( 'NONE', #180086, #155414, #54963 ) ;
#106479=DIRECTION ( 'NONE',  ( -0.000000000000000000, 1.000000000000000000, 6.982962677686266711E-15 ) ) ;
#106497=DIRECTION ( 'NONE',  ( -0.000000000000000000, -0.8660254037844377084, -0.5000000000000016653 ) ) ;
#106510=CARTESIAN_POINT ( 'NONE',  ( -21.14999999999999858, 76.00000000001169553, -76.06376443622556849 ) ) ;
#106554=DIRECTION ( 'NONE',  ( -1.000000000000000000, 1.836970198721029934E-16, 1.601412966608202925E-30 ) ) ;
#106555=DIRECTION ( 'NONE',  ( 4.504528286903032433E-15, 0.1298341882520054891, 0.9915357197604850459 ) ) ;
#106578=ADVANCED_FACE ( 'NONE', ( #22037 ), #174235, .T. ) ;
#106648=CARTESIAN_POINT ( 'NONE',  ( 23.15000000000000213, 87.48912529308749697, -39.12310748452424747 ) ) ;
#106650=VERTEX_POINT ( 'NONE', #32319 ) ;
#106666=CARTESIAN_POINT ( 'NONE',  ( 18.59999999999999076, 76.00000000001142553, -36.02310748452432421 ) ) ;
#106671=CIRCLE ( 'NONE', #252409, 0.2000000000000057288 ) ;
#106696=DIRECTION ( 'NONE',  ( 1.000000000000000000, 0.000000000000000000, 0.000000000000000000 ) ) ;
#106703=CARTESIAN_POINT ( 'NONE',  ( -23.15000000000000213, 73.50000000001151079, -49.24772940728643533 ) ) ;
#106712=LINE ( 'NONE', #222815, #197960 ) ;
#106743=AXIS2_PLACEMENT_3D ( 'NONE', #100620, #1545, #117655 ) ;
#106773=DIRECTION ( 'NONE',  ( 0.000000000000000000, -0.7397360091702802620, 0.6728971962616779878 ) ) ;
#106787=AXIS2_PLACEMENT_3D ( 'NONE', #55365, #95792, #54113 ) ;
#106798=PLANE ( 'NONE',  #124533 ) ;
#106823=CARTESIAN_POINT ( 'NONE',  ( -21.05000000000000071, 87.65000000001144542, -39.02310748452423894 ) ) ;
#106833=DIRECTION ( 'NONE',  ( 0.000000000000000000, 1.000000000000000000, 1.156482317317864980E-14 ) ) ;
#106844=CARTESIAN_POINT ( 'NONE',  ( 18.50000000000000355, 85.42145614550700827, -62.28112540050488377 ) ) ;
#106856=EDGE_CURVE ( 'NONE', #23444, #254970, #178315, .T. ) ;
#106879=CIRCLE ( 'NONE', #52706, 0.09999999999999939493 ) ;
#106901=CIRCLE ( 'NONE', #160912, 0.5000000000000004441 ) ;
#106910=DIRECTION ( 'NONE',  ( 0.000000000000000000, 0.4930308989875575865, 0.8700118002898125091 ) ) ;
#106911=CYLINDRICAL_SURFACE ( 'NONE', #70085, 3.999999999999996447 ) ;
#106939=EDGE_LOOP ( 'NONE', ( #161522, #214367, #13179 ) ) ;
#106947=LINE ( 'NONE', #228205, #186132 ) ;
#106961=VERTEX_POINT ( 'NONE', #204183 ) ;
#107006=DIRECTION ( 'NONE',  ( 0.000000000000000000, -7.124650136758311291E-15, 1.000000000000000000 ) ) ;
#107007=ORIENTED_EDGE ( 'NONE', *, *, #182500, .F. ) ;
#107040=CARTESIAN_POINT ( 'NONE',  ( -23.15000000000000213, 76.00000000001165290, -69.52310748452431710 ) ) ;
#107044=EDGE_CURVE ( 'NONE', #3677, #33572, #70173, .T. ) ;
#107062=AXIS2_PLACEMENT_3D ( 'NONE', #27214, #106696, #224081 ) ;
#107078=CARTESIAN_POINT ( 'NONE',  ( -23.25000000000000000, 76.00000000001165290, -69.52310748452431710 ) ) ;
#107099=TOROIDAL_SURFACE ( 'NONE', #102987, 11.65000000000000036, 0.1000000000000000056 ) ;
#107102=EDGE_CURVE ( 'NONE', #43818, #83438, #11904, .T. ) ;
#107105=LINE ( 'NONE', #186664, #55448 ) ;
#107107=AXIS2_PLACEMENT_3D ( 'NONE', #226553, #222710, #47927 ) ;
#107117=CARTESIAN_POINT ( 'NONE',  ( 18.59999999999999076, 64.35000000001141984, -36.02310748452440237 ) ) ;
#107119=DIRECTION ( 'NONE',  ( 8.673617379884087537E-15, 6.982962677686266711E-15, -1.000000000000000000 ) ) ;
#107129=CARTESIAN_POINT ( 'NONE',  ( -20.54999999999999716, 68.85000000001156195, -57.17310748452437252 ) ) ;
#107136=EDGE_LOOP ( 'NONE', ( #27506, #200203, #51623, #142654 ) ) ;
#107145=TOROIDAL_SURFACE ( 'NONE', #36260, 0.2000000000000000111, 0.1000000000000000056 ) ;
#107153=CYLINDRICAL_SURFACE ( 'NONE', #5957, 4.049999999999998046 ) ;
#107164=ADVANCED_FACE ( 'NONE', ( #15000 ), #95781, .T. ) ;
#107191=EDGE_CURVE ( 'NONE', #6351, #154564, #150115, .T. ) ;
#107226=CIRCLE ( 'NONE', #61450, 0.09999999999999939493 ) ;
#107237=CIRCLE ( 'NONE', #240518, 12.77499999999999503 ) ;
#107256=DIRECTION ( 'NONE',  ( 0.000000000000000000, 0.000000000000000000, -1.000000000000000000 ) ) ;
#107263=AXIS2_PLACEMENT_3D ( 'NONE', #65587, #6895, #147701 ) ;
#107266=DIRECTION ( 'NONE',  ( 0.000000000000000000, -7.272083257015735086E-15, 1.000000000000000000 ) ) ;
#107296=ORIENTED_EDGE ( 'NONE', *, *, #96031, .T. ) ;
#107300=ORIENTED_EDGE ( 'NONE', *, *, #33116, .F. ) ;
#107305=CARTESIAN_POINT ( 'NONE',  ( 21.05000000000000071, 65.43728505328265044, -62.06630537887970434 ) ) ;
#107312=DIRECTION ( 'NONE',  ( 0.000000000000000000, 7.026728003956683390E-15, -1.000000000000000000 ) ) ;
#107324=VECTOR ( 'NONE', #131096, 1000.000000000000000 ) ;
#107390=CARTESIAN_POINT ( 'NONE',  ( -21.08134388332232589, 75.92418108250473097, -75.85778806504229976 ) ) ;
#107415=TOROIDAL_SURFACE ( 'NONE', #24227, 0.2000000000000000111, 0.1000000000000000056 ) ;
#107430=CARTESIAN_POINT ( 'NONE',  ( 20.99142135623731065, 64.40000000001145963, -42.95131071479990226 ) ) ;
#107443=FACE_OUTER_BOUND ( 'NONE', #23860, .T. ) ;
#107446=ORIENTED_EDGE ( 'NONE', *, *, #41549, .T. ) ;
#107451=DIRECTION ( 'NONE',  ( 0.000000000000000000, -6.938893903907222067E-15, 1.000000000000000000 ) ) ;
#107464=CARTESIAN_POINT ( 'NONE',  ( 21.14999999999999858, 64.35000000001156195, -57.37310748452439668 ) ) ;
#107473=FACE_OUTER_BOUND ( 'NONE', #221079, .T. ) ;
#107480=CARTESIAN_POINT ( 'NONE',  ( -18.59999999999999787, 74.13328508995425636, -57.77043223824233564 ) ) ;
#107481=LINE ( 'NONE', #8398, #189307 ) ;
#107482=CARTESIAN_POINT ( 'NONE',  ( 21.07946286933444568, 75.92331615675530543, -75.85214480353204181 ) ) ;
#107486=DIRECTION ( 'NONE',  ( 0.000000000000000000, -0.4930308989875575865, -0.8700118002898125091 ) ) ;
#107541=CARTESIAN_POINT ( 'NONE',  ( -18.59999999999999787, 77.16412189325258453, -28.10825939895270764 ) ) ;
#107573=CARTESIAN_POINT ( 'NONE',  ( -22.42253884134832020, 75.99806764887642885, -81.17271318187276563 ) ) ;
#107600=ORIENTED_EDGE ( 'NONE', *, *, #160789, .F. ) ;
#107608=EDGE_LOOP ( 'NONE', ( #36485, #151319, #99560, #31201 ) ) ;
#107621=CARTESIAN_POINT ( 'NONE',  ( -20.54999999999999716, 85.40000000001148805, -45.91707660717669626 ) ) ;
#107654=CARTESIAN_POINT ( 'NONE',  ( -21.05000000000000071, 76.00000000001149658, -47.72310748452432705 ) ) ;
#107658=DIRECTION ( 'NONE',  ( 0.000000000000000000, 5.880418562633245778E-15, -1.000000000000000000 ) ) ;
#107680=CARTESIAN_POINT ( 'NONE',  ( -18.39999999999999858, 85.60000000001139142, -29.42291809330221142 ) ) ;
#107689=AXIS2_PLACEMENT_3D ( 'NONE', #194851, #192273, #175295 ) ;
#107695=LINE ( 'NONE', #165112, #12820 ) ;
#107709=AXIS2_PLACEMENT_3D ( 'NONE', #250891, #16174, #95673 ) ;
#107724=ADVANCED_FACE ( 'NONE', ( #11439 ), #87707, .F. ) ;
#107770=ORIENTED_EDGE ( 'NONE', *, *, #233109, .T. ) ;
#107790=DIRECTION ( 'NONE',  ( 0.000000000000000000, -7.034366652768089021E-15, 1.000000000000000000 ) ) ;
#107794=ORIENTED_EDGE ( 'NONE', *, *, #210765, .F. ) ;
#107815=CARTESIAN_POINT ( 'NONE',  ( -23.15000000000000213, 71.65000000001155911, -57.17310748452435121 ) ) ;
#107816=VECTOR ( 'NONE', #60477, 999.9999999999998863 ) ;
#107876=CIRCLE ( 'NONE', #178839, 0.5000000000000004441 ) ;
#107901=ORIENTED_EDGE ( 'NONE', *, *, #55049, .T. ) ;
#107914=ORIENTED_EDGE ( 'NONE', *, *, #111879, .F. ) ;
#107938=AXIS2_PLACEMENT_3D ( 'NONE', #155814, #38410, #235318 ) ;
#107965=PRESENTATION_STYLE_ASSIGNMENT (( #191383 ) ) ;
#107991=EDGE_CURVE ( 'NONE', #196598, #169810, #65954, .T. ) ;
#107996=DIRECTION ( 'NONE',  ( -4.408576920032447972E-17, -0.1350103645451946055, 0.9908441862701591329 ) ) ;
#108002=DIRECTION ( 'NONE',  ( 7.304098846218134667E-16, -1.000000000000000000, -6.982962677686267499E-15 ) ) ;
#108008=ADVANCED_FACE ( 'NONE', ( #8550 ), #2642, .T. ) ;
#108010=FACE_OUTER_BOUND ( 'NONE', #157984, .T. ) ;
#108069=EDGE_CURVE ( 'NONE', #246608, #116008, #244070, .T. ) ;
#108120=DIRECTION ( 'NONE',  ( 0.000000000000000000, 0.8777080977375072424, -0.4791956752371691608 ) ) ;
#108163=VECTOR ( 'NONE', #222540, 1000.000000000000000 ) ;
#108197=FACE_OUTER_BOUND ( 'NONE', #216294, .T. ) ;
#108212=CARTESIAN_POINT ( 'NONE',  ( 20.99999999999997868, 76.00000000001165290, -69.52310748452431710 ) ) ;
#108233=DIRECTION ( 'NONE',  ( 0.000000000000000000, -1.000000000000000000, -6.352154140967427193E-15 ) ) ;
#108287=ORIENTED_EDGE ( 'NONE', *, *, #73778, .T. ) ;
#108323=EDGE_CURVE ( 'NONE', #9118, #28771, #82600, .T. ) ;
#108337=VECTOR ( 'NONE', #94200, 1000.000000000000000 ) ;
#108341=EDGE_CURVE ( 'NONE', #182454, #212829, #106879, .T. ) ;
#108352=CIRCLE ( 'NONE', #174465, 11.65000000000000036 ) ;
#108369=CARTESIAN_POINT ( 'NONE',  ( 22.49999999999999645, 75.90000000001172964, -81.17267829206913632 ) ) ;
#108373=CARTESIAN_POINT ( 'NONE',  ( -21.05000000000000071, 64.40000000001147384, -42.95131071479990936 ) ) ;
#108385=DIRECTION ( 'NONE',  ( 0.000000000000000000, 0.000000000000000000, 1.000000000000000000 ) ) ;
#108397=EDGE_LOOP ( 'NONE', ( #92184, #47199, #134497, #31956 ) ) ;
#108403=VECTOR ( 'NONE', #125579, 1000.000000000000000 ) ;
#108436=EDGE_CURVE ( 'NONE', #8900, #78944, #185990, .T. ) ;
#108460=ORIENTED_EDGE ( 'NONE', *, *, #17254, .F. ) ;
#108464=DIRECTION ( 'NONE',  ( 1.000000000000000000, 0.000000000000000000, 0.000000000000000000 ) ) ;
#108468=EDGE_CURVE ( 'NONE', #221002, #42291, #12122, .T. ) ;
#108484=VERTEX_POINT ( 'NONE', #13388 ) ;
#108497=EDGE_LOOP ( 'NONE', ( #100757, #7271, #7757, #203973 ) ) ;
#108527=ORIENTED_EDGE ( 'NONE', *, *, #108468, .T. ) ;
#108529=AXIS2_PLACEMENT_3D ( 'NONE', #187775, #21331, #27444 ) ;
#108567=DIRECTION ( 'NONE',  ( 0.000000000000000000, 0.000000000000000000, 1.000000000000000000 ) ) ;
#108609=CIRCLE ( 'NONE', #62817, 0.09999999999999967248 ) ;
#108629=VERTEX_POINT ( 'NONE', #237245 ) ;
#108637=DIRECTION ( 'NONE',  ( 0.000000000000000000, -0.4999999999999689138, 0.8660254037844565822 ) ) ;
#108649=DIRECTION ( 'NONE',  ( 0.000000000000000000, -0.8660254037844468122, -0.4999999999999859557 ) ) ;
#108650=DIRECTION ( 'NONE',  ( 0.000000000000000000, 1.000000000000000000, 3.469446951953515108E-14 ) ) ;
#108663=ORIENTED_EDGE ( 'NONE', *, *, #255178, .T. ) ;
#108701=CARTESIAN_POINT ( 'NONE',  ( -23.15000000000000213, 74.00000000001156764, -56.29848556176223440 ) ) ;
#108721=ORIENTED_EDGE ( 'NONE', *, *, #132664, .F. ) ;
#108722=DIRECTION ( 'NONE',  ( 0.000000000000000000, -1.000000000000000000, -6.982962677686266711E-15 ) ) ;
#108731=DIRECTION ( 'NONE',  ( 1.000000000000000000, 0.000000000000000000, 0.000000000000000000 ) ) ;
#108745=VECTOR ( 'NONE', #45117, 1000.000000000000000 ) ;
#108749=ADVANCED_FACE ( 'NONE', ( #203246 ), #194587, .T. ) ;
#108815=CARTESIAN_POINT ( 'NONE',  ( 21.09551895715237535, 65.37856267284283263, -57.28598281862489472 ) ) ;
#108826=ORIENTED_EDGE ( 'NONE', *, *, #75336, .T. ) ;
#108828=ORIENTED_EDGE ( 'NONE', *, *, #209922, .T. ) ;
#108831=EDGE_CURVE ( 'NONE', #85045, #71888, #29482, .T. ) ;
#108836=ORIENTED_EDGE ( 'NONE', *, *, #148277, .F. ) ;
#108859=CIRCLE ( 'NONE', #241948, 0.1000000000000028644 ) ;
#108878=ORIENTED_EDGE ( 'NONE', *, *, #13720, .T. ) ;
#108898=LINE ( 'NONE', #170219, #47978 ) ;
#108911=CARTESIAN_POINT ( 'NONE',  ( -20.00857864376270001, 66.65000000001150227, -48.27310748452438816 ) ) ;
#108916=VERTEX_POINT ( 'NONE', #236929 ) ;
#108918=ORIENTED_EDGE ( 'NONE', *, *, #62307, .F. ) ;
#108922=DIRECTION ( 'NONE',  ( 1.000000000000000000, 0.000000000000000000, 0.000000000000000000 ) ) ;
#108941=DIRECTION ( 'NONE',  ( 0.000000000000000000, 0.000000000000000000, -1.000000000000000000 ) ) ;
#108960=DIRECTION ( 'NONE',  ( 0.000000000000000000, 0.000000000000000000, -1.000000000000000000 ) ) ;
#108965=AXIS2_PLACEMENT_3D ( 'NONE', #57981, #234065, #116688 ) ;
#108987=EDGE_CURVE ( 'NONE', #189246, #201514, #136437, .T. ) ;
#109006=CARTESIAN_POINT ( 'NONE',  ( 20.94999999999999574, 77.26178616857662007, -61.43660852097883662 ) ) ;
#109009=CARTESIAN_POINT ( 'NONE',  ( 20.85000000000000142, 76.00000000001142553, -36.02310748452432421 ) ) ;
#109036=DIRECTION ( 'NONE',  ( -0.000000000000000000, -0.01283462868040327436, 0.9999176327611370985 ) ) ;
#109040=CARTESIAN_POINT ( 'NONE',  ( 21.05315837417574443, 64.25000000264165578, -42.86475148229496313 ) ) ;
#109077=FACE_OUTER_BOUND ( 'NONE', #1136, .T. ) ;
#109080=CARTESIAN_POINT ( 'NONE',  ( -20.54999999999999716, 66.65000000001150227, -48.27310748452438816 ) ) ;
#109103=CARTESIAN_POINT ( 'NONE',  ( 21.30000000000002558, 76.00000000001168132, -73.57310748452432847 ) ) ;
#109108=CARTESIAN_POINT ( 'NONE',  ( -20.85000000000000142, 64.25000000001148237, -42.80697314750249660 ) ) ;
#109111=ORIENTED_EDGE ( 'NONE', *, *, #134739, .F. ) ;
#109151=AXIS2_PLACEMENT_3D ( 'NONE', #253352, #190855, #232541 ) ;
#109161=DIRECTION ( 'NONE',  ( 0.000000000000000000, -6.454785026890385471E-15, 1.000000000000000000 ) ) ;
#109204=VECTOR ( 'NONE', #121510, 1000.000000000000000 ) ;
#109219=AXIS2_PLACEMENT_3D ( 'NONE', #187267, #112846, #192384 ) ;
#109226=AXIS2_PLACEMENT_3D ( 'NONE', #80078, #141371, #220896 ) ;
#109269=ORIENTED_EDGE ( 'NONE', *, *, #131571, .T. ) ;
#109276=AXIS2_PLACEMENT_3D ( 'NONE', #84579, #122489, #123767 ) ;
#109284=DIRECTION ( 'NONE',  ( 0.000000000000000000, 0.000000000000000000, 1.000000000000000000 ) ) ;
#109317=EDGE_CURVE ( 'NONE', #81658, #212844, #194945, .T. ) ;
#109381=CARTESIAN_POINT ( 'NONE',  ( 22.49436431346199683, 75.93309647028948461, -81.17305843217778261 ) ) ;
#109398=DIRECTION ( 'NONE',  ( 1.000000000000000000, 0.000000000000000000, 0.000000000000000000 ) ) ;
#109414=ORIENTED_EDGE ( 'NONE', *, *, #166607, .T. ) ;
#109449=ORIENTED_EDGE ( 'NONE', *, *, #88207, .T. ) ;
#109506=ADVANCED_FACE ( 'NONE', ( #250733 ), #252018, .F. ) ;
#109521=ORIENTED_EDGE ( 'NONE', *, *, #152456, .T. ) ;
#109563=FACE_OUTER_BOUND ( 'NONE', #89354, .T. ) ;
#109577=DIRECTION ( 'NONE',  ( -0.000000000000000000, -0.1350103645451835865, -0.9908441862701606873 ) ) ;
#109629=FACE_OUTER_BOUND ( 'NONE', #129614, .T. ) ;
#109637=CARTESIAN_POINT ( 'NONE',  ( 23.14999999999999503, 64.35000000001173248, -81.27310748452440237 ) ) ;
#109641=AXIS2_PLACEMENT_3D ( 'NONE', #100407, #222934, #160441 ) ;
#109647=DIRECTION ( 'NONE',  ( -1.000000000000000000, 0.000000000000000000, 0.000000000000000000 ) ) ;
#109669=ORIENTED_EDGE ( 'NONE', *, *, #124949, .F. ) ;
#109674=ADVANCED_FACE ( 'NONE', ( #198467 ), #49167, .F. ) ;
#109682=DIRECTION ( 'NONE',  ( 0.000000000000000000, 6.982962677686266711E-15, -1.000000000000000000 ) ) ;
#109691=EDGE_CURVE ( 'NONE', #161130, #92943, #215749, .T. ) ;
#109699=CIRCLE ( 'NONE', #176368, 0.09999999999999939493 ) ;
#109702=CARTESIAN_POINT ( 'NONE',  ( -21.05000000000000071, 74.16465844978715438, -57.96795619196134908 ) ) ;
#109711=FACE_OUTER_BOUND ( 'NONE', #181654, .T. ) ;
#109722=DIRECTION ( 'NONE',  ( 1.000000000000000000, 0.000000000000000000, 0.000000000000000000 ) ) ;
#109733=CARTESIAN_POINT ( 'NONE',  ( -18.43707690579160641, 85.68240343348780641, -29.36626410711147273 ) ) ;
#109740=CIRCLE ( 'NONE', #247097, 0.1000000000000028644 ) ;
#109767=ORIENTED_EDGE ( 'NONE', *, *, #62432, .T. ) ;
#109805=DIRECTION ( 'NONE',  ( 0.000000000000000000, 0.000000000000000000, 1.000000000000000000 ) ) ;
#109814=ORIENTED_EDGE ( 'NONE', *, *, #189997, .F. ) ;
#109815=EDGE_CURVE ( 'NONE', #83134, #70064, #105759, .T. ) ;
#109825=CARTESIAN_POINT ( 'NONE',  ( 22.57320508075688537, 64.35000000001166143, -69.52310748452440237 ) ) ;
#109861=ORIENTED_EDGE ( 'NONE', *, *, #257859, .F. ) ;
#109864=CARTESIAN_POINT ( 'NONE',  ( 21.05000000000000071, 65.27628318601533408, -61.92870824864008483 ) ) ;
#109884=LINE ( 'NONE', #70803, #208129 ) ;
#109886=CYLINDRICAL_SURFACE ( 'NONE', #29898, 0.1000000000000028644 ) ;
#109888=EDGE_LOOP ( 'NONE', ( #237773, #128065, #85866, #34894 ) ) ;
#109940=ADVANCED_FACE ( 'NONE', ( #109629 ), #124381, .T. ) ;
#109979=DIRECTION ( 'NONE',  ( 1.000000000000000000, -0.000000000000000000, 0.000000000000000000 ) ) ;
#110010=ORIENTED_EDGE ( 'NONE', *, *, #208662, .T. ) ;
#110014=DIRECTION ( 'NONE',  ( -3.265361837132813093E-16, -1.000000000000000000, -6.982962677686266711E-15 ) ) ;
#110030=CARTESIAN_POINT ( 'NONE',  ( -23.15000000000000213, 64.25000000001151079, -48.17310748452440805 ) ) ;
#110038=PLANE ( 'NONE',  #190280 ) ;
#110074=EDGE_CURVE ( 'NONE', #121991, #88576, #74406, .T. ) ;
#110098=VERTEX_POINT ( 'NONE', #256792 ) ;
#110107=ORIENTED_EDGE ( 'NONE', *, *, #131432, .F. ) ;
#110116=EDGE_CURVE ( 'NONE', #124309, #152443, #153458, .T. ) ;
#110132=EDGE_CURVE ( 'NONE', #182847, #234718, #57884, .T. ) ;
#110140=DIRECTION ( 'NONE',  ( 7.304098846218134667E-16, 1.000000000000000000, 6.982962677686266711E-15 ) ) ;
#110173=EDGE_LOOP ( 'NONE', ( #99204, #254089, #26387, #164173 ) ) ;
#110191=CYLINDRICAL_SURFACE ( 'NONE', #146839, 0.1000000000000028644 ) ;
#110219=EDGE_CURVE ( 'NONE', #21500, #201700, #164184, .T. ) ;
#110228=DIRECTION ( 'NONE',  ( 1.000000000000000000, 0.000000000000000000, 0.000000000000000000 ) ) ;
#110232=AXIS2_PLACEMENT_3D ( 'NONE', #75414, #131499, #251450 ) ;
#110263=LINE ( 'NONE', #133685, #21245 ) ;
#110285=EDGE_CURVE ( 'NONE', #148530, #93424, #207783, .T. ) ;
#110287=CYLINDRICAL_SURFACE ( 'NONE', #99570, 0.1000000000000028644 ) ;
#110288=CARTESIAN_POINT ( 'NONE',  ( -20.54999999999999716, 85.50000000001159606, -59.62913836187181005 ) ) ;
#110299=ADVANCED_FACE ( 'NONE', ( #171584 ), #110287, .T. ) ;
#110302=CARTESIAN_POINT ( 'NONE',  ( -18.60000000000001563, 85.36424052760251868, -62.34285890268348140 ) ) ;
#110312=DIRECTION ( 'NONE',  ( 0.000000000000000000, -6.982962677686266711E-15, 1.000000000000000000 ) ) ;
#110314=LINE ( 'NONE', #189855, #45621 ) ;
#110335=EDGE_LOOP ( 'NONE', ( #156218, #61727, #84524, #241615, #132567, #51774, #162089 ) ) ;
#110341=CYLINDRICAL_SURFACE ( 'NONE', #67094, 0.1000000000000028644 ) ;
#110441=ORIENTED_EDGE ( 'NONE', *, *, #207451, .T. ) ;
#110443=DIRECTION ( 'NONE',  ( 0.000000000000000000, -0.8700118002898354908, 0.4930308989875170078 ) ) ;
#110457=FACE_OUTER_BOUND ( 'NONE', #78193, .T. ) ;
#110500=DIRECTION ( 'NONE',  ( 0.000000000000000000, -1.000000000000000000, -6.982962677686265922E-15 ) ) ;
#110545=DIRECTION ( 'NONE',  ( 1.000000000000000000, 0.000000000000000000, 0.000000000000000000 ) ) ;
#110575=VECTOR ( 'NONE', #93764, 1000.000000000000000 ) ;
#110576=VERTEX_POINT ( 'NONE', #4459 ) ;
#110577=DIRECTION ( 'NONE',  ( 1.000000000000000000, 0.000000000000000000, 0.000000000000000000 ) ) ;
#110641=ADVANCED_FACE ( 'NONE', ( #2725 ), #142250, .T. ) ;
#110736=CARTESIAN_POINT ( 'NONE',  ( -23.15000000000000213, 64.35000000001156195, -57.27310748452440237 ) ) ;
#110768=DIRECTION ( 'NONE',  ( 1.000000000000000000, 0.000000000000000000, 0.000000000000000000 ) ) ;
#110770=TOROIDAL_SURFACE ( 'NONE', #94196, 3.899999999999999467, 0.1000000000000000056 ) ;
#110788=AXIS2_PLACEMENT_3D ( 'NONE', #72637, #230405, #51738 ) ;
#110796=FACE_OUTER_BOUND ( 'NONE', #123622, .T. ) ;
#110840=ORIENTED_EDGE ( 'NONE', *, *, #71376, .T. ) ;
#110912=EDGE_CURVE ( 'NONE', #39343, #192913, #103476, .T. ) ;
#110930=CARTESIAN_POINT ( 'NONE',  ( 18.59999999999999432, 74.83729825007360148, -61.42310748452432989 ) ) ;
#110935=CARTESIAN_POINT ( 'NONE',  ( -18.59999999999999787, 72.08710075277812734, -58.04128451151338197 ) ) ;
#110946=DIRECTION ( 'NONE',  ( -0.000000000000000000, 1.000000000000000000, 7.525063763929033127E-15 ) ) ;
#110989=DIRECTION ( 'NONE',  ( 0.000000000000000000, -6.938893903907222067E-15, 1.000000000000000000 ) ) ;
#111003=DIRECTION ( 'NONE',  ( 1.000000000000000000, 0.000000000000000000, 0.000000000000000000 ) ) ;
#111012=CARTESIAN_POINT ( 'NONE',  ( 21.04999999999999716, 75.93429838968962997, -75.78142354185638396 ) ) ;
#111035=AXIS2_PLACEMENT_3D ( 'NONE', #239131, #117887, #98291 ) ;
#111059=AXIS2_PLACEMENT_3D ( 'NONE', #97344, #116949, #236889 ) ;
#111090=EDGE_CURVE ( 'NONE', #72671, #101771, #115996, .T. ) ;
#111095=CARTESIAN_POINT ( 'NONE',  ( 18.46858270002953262, 85.47420267472219280, -62.42108554982039692 ) ) ;
#111116=ORIENTED_EDGE ( 'NONE', *, *, #240079, .T. ) ;
#111145=AXIS2_PLACEMENT_3D ( 'NONE', #86987, #186119, #7476 ) ;
#111170=CARTESIAN_POINT ( 'NONE',  ( 23.14999999999998437, 76.00000000001162448, -65.47310748452431994 ) ) ;
#111217=ORIENTED_EDGE ( 'NONE', *, *, #32806, .T. ) ;
#111222=EDGE_LOOP ( 'NONE', ( #108287, #66250, #223328, #24640 ) ) ;
#111226=EDGE_CURVE ( 'NONE', #6238, #64945, #27498, .T. ) ;
#111234=VERTEX_POINT ( 'NONE', #129124 ) ;
#111282=DIRECTION ( 'NONE',  ( 0.000000000000000000, 0.000000000000000000, -1.000000000000000000 ) ) ;
#111318=CIRCLE ( 'NONE', #82229, 0.1000000000000028644 ) ;
#111332=TOROIDAL_SURFACE ( 'NONE', #198804, 0.2000000000000000111, 0.1000000000000000056 ) ;
#111338=DIRECTION ( 'NONE',  ( 0.000000000000000000, 0.000000000000000000, 1.000000000000000000 ) ) ;
#111343=CARTESIAN_POINT ( 'NONE',  ( 21.08750232978087524, 65.27513661400141132, -57.29424931152482259 ) ) ;
#111402=CARTESIAN_POINT ( 'NONE',  ( 21.12400247839512701, 65.27851195598117329, -57.27310748452440237 ) ) ;
#111453=DIRECTION ( 'NONE',  ( 1.000000000000000000, 0.000000000000000000, 0.000000000000000000 ) ) ;
#111511=SPHERICAL_SURFACE ( 'NONE', #208876, 0.1000000000000000056 ) ;
#111535=ORIENTED_EDGE ( 'NONE', *, *, #197010, .F. ) ;
#111549=EDGE_CURVE ( 'NONE', #231640, #181320, #238482, .T. ) ;
#111559=CARTESIAN_POINT ( 'NONE',  ( -20.94999999999999929, 76.00000000001142553, -36.02310748452432421 ) ) ;
#111569=CARTESIAN_POINT ( 'NONE',  ( 18.39999999999999858, 85.51932773110404185, -62.55013110796492271 ) ) ;
#111614=DIRECTION ( 'NONE',  ( -1.000000000000000000, -0.000000000000000000, -0.000000000000000000 ) ) ;
#111631=DIRECTION ( 'NONE',  ( 1.000000000000000000, 0.000000000000000000, 0.000000000000000000 ) ) ;
#111635=FACE_OUTER_BOUND ( 'NONE', #24113, .T. ) ;
#111679=DIRECTION ( 'NONE',  ( 1.000000000000000000, 0.000000000000000000, 0.000000000000000000 ) ) ;
#111747=DIRECTION ( 'NONE',  ( 0.000000000000000000, -1.000000000000000000, -6.982962677686266711E-15 ) ) ;
#111748=VECTOR ( 'NONE', #124545, 1000.000000000000000 ) ;
#111790=VERTEX_POINT ( 'NONE', #57909 ) ;
#111837=DIRECTION ( 'NONE',  ( 1.000000000000000000, -0.000000000000000000, 0.000000000000000000 ) ) ;
#111839=CARTESIAN_POINT ( 'NONE',  ( 23.14999999999999858, 72.10000000001141984, -36.02310748452435263 ) ) ;
#111866=DIRECTION ( 'NONE',  ( -1.000000000000000000, 3.265361837132813093E-16, 2.280189983783949500E-30 ) ) ;
#111879=EDGE_CURVE ( 'NONE', #186245, #27421, #137184, .T. ) ;
#111881=DIRECTION ( 'NONE',  ( 0.000000000000000000, -1.000000000000000000, -7.272083257015735086E-15 ) ) ;
#111930=CARTESIAN_POINT ( 'NONE',  ( 20.85000000000000142, 76.00000000001142553, -36.02310748452432421 ) ) ;
#111939=CARTESIAN_POINT ( 'NONE',  ( 21.14999999999999858, 69.45934304831041572, -69.42310748452437963 ) ) ;
#111942=LINE ( 'NONE', #149793, #145402 ) ;
#111954=DIRECTION ( 'NONE',  ( 1.000000000000000000, 0.000000000000000000, 0.000000000000000000 ) ) ;
#111960=CARTESIAN_POINT ( 'NONE',  ( 23.14999999999999858, 71.00000000001158185, -57.11784146561126363 ) ) ;
#111961=EDGE_CURVE ( 'NONE', #116304, #226817, #109884, .T. ) ;
#112018=CARTESIAN_POINT ( 'NONE',  ( -18.59999999999999787, 85.48068669529035901, -29.08199231576641353 ) ) ;
#112052=CARTESIAN_POINT ( 'NONE',  ( -18.59999999999999787, 74.83729825007360148, -61.42310748452432989 ) ) ;
#112058=DIRECTION ( 'NONE',  ( 0.000000000000000000, 0.000000000000000000, 1.000000000000000000 ) ) ;
#112061=ORIENTED_EDGE ( 'NONE', *, *, #14309, .F. ) ;
#112088=CARTESIAN_POINT ( 'NONE',  ( 21.05000000000000071, 76.00000000001165290, -69.52310748452431710 ) ) ;
#112107=ORIENTED_EDGE ( 'NONE', *, *, #185816, .F. ) ;
#112111=DIRECTION ( 'NONE',  ( 2.940209281316621016E-16, 1.000000000000000000, 7.056502275159890832E-15 ) ) ;
#112142=EDGE_CURVE ( 'NONE', #198388, #236713, #241435, .T. ) ;
#112172=CARTESIAN_POINT ( 'NONE',  ( 23.24999999999999289, 69.45000000001149942, -48.17310748452436542 ) ) ;
#112223=CARTESIAN_POINT ( 'NONE',  ( 22.49999999999999645, 64.35023708197972780, -69.61191746091132870 ) ) ;
#112238=CYLINDRICAL_SURFACE ( 'NONE', #78345, 0.09999999999999939493 ) ;
#112244=ORIENTED_EDGE ( 'NONE', *, *, #24736, .T. ) ;
#112250=CARTESIAN_POINT ( 'NONE',  ( -18.50000000000000000, 64.35000000001161879, -62.50830171387039513 ) ) ;
#112254=CARTESIAN_POINT ( 'NONE',  ( -23.25000000000000000, 76.10000000001174669, -81.17267829206912211 ) ) ;
#112286=VERTEX_POINT ( 'NONE', #5329 ) ;
#112319=ORIENTED_EDGE ( 'NONE', *, *, #20549, .T. ) ;
#112328=B_SPLINE_CURVE_WITH_KNOTS ( 'NONE', 3,
 ( #119959, #220321, #256806, #99048, #135619, #254277, #136917, #117362, #75682, #155237, #217718, #37845, #19552, #39126, #22131, #101601, #234736, #215170, #96485 ),
 .UNSPECIFIED., .F., .F.,
 ( 4, 3, 3, 3, 3, 3, 4 ),
 ( 1.430489624538199204E-17, 2.646747978908941165E-05, 5.271166642128824757E-05, 9.008788829885143402E-05, 0.0001426648776561019298, 0.0001897378458659829863, 0.0001917382627806356299 ),
 .UNSPECIFIED. ) ;
#112350=EDGE_CURVE ( 'NONE', #77589, #6871, #245890, .T. ) ;
#112373=FACE_OUTER_BOUND ( 'NONE', #16894, .T. ) ;
#112377=CIRCLE ( 'NONE', #16513, 0.1000000000000028644 ) ;
#112441=EDGE_CURVE ( 'NONE', #75472, #149751, #218069, .T. ) ;
#112442=EDGE_LOOP ( 'NONE', ( #112244, #236526, #90978 ) ) ;
#112472=DIRECTION ( 'NONE',  ( 0.000000000000000000, 0.000000000000000000, -1.000000000000000000 ) ) ;
#112474=EDGE_LOOP ( 'NONE', ( #45730, #16862, #10769, #63232 ) ) ;
#112485=DIRECTION ( 'NONE',  ( -0.000000000000000000, 1.000000000000000000, 6.352154140967427193E-15 ) ) ;
#112487=VECTOR ( 'NONE', #192995, 999.9999999999998863 ) ;
#112493=CARTESIAN_POINT ( 'NONE',  ( -20.00857864376270001, 66.65000000001157332, -57.17310748452438673 ) ) ;
#112515=CARTESIAN_POINT ( 'NONE',  ( -20.94999999999999929, 77.25000000001159606, -61.52310748452431710 ) ) ;
#112535=AXIS2_PLACEMENT_3D ( 'NONE', #62081, #256359, #158640 ) ;
#112543=FACE_OUTER_BOUND ( 'NONE', #12852, .T. ) ;
#112574=DIRECTION ( 'NONE',  ( -1.000000000000000000, 0.000000000000000000, -0.000000000000000000 ) ) ;
#112585=CYLINDRICAL_SURFACE ( 'NONE', #131448, 0.09999999999999939493 ) ;
#112591=DIRECTION ( 'NONE',  ( 0.000000000000000000, 0.000000000000000000, 1.000000000000000000 ) ) ;
#112602=AXIS2_PLACEMENT_3D ( 'NONE', #248581, #49087, #51630 ) ;
#112604=ADVANCED_FACE ( 'NONE', ( #14379 ), #93881, .T. ) ;
#112618=TOROIDAL_SURFACE ( 'NONE', #172, 7.800000000000000711, 0.1000000000000000056 ) ;
#112619=CARTESIAN_POINT ( 'NONE',  ( 20.95263205890653779, 67.10425989211756814, -61.03359907758274971 ) ) ;
#112680=VERTEX_POINT ( 'NONE', #106703 ) ;
#112727=CARTESIAN_POINT ( 'NONE',  ( 21.11825140030105530, 75.99279637937891607, -75.96851504994447168 ) ) ;
#112774=DIRECTION ( 'NONE',  ( 0.000000000000000000, -6.517943393102682774E-15, 1.000000000000000000 ) ) ;
#112792=VERTEX_POINT ( 'NONE', #113139 ) ;
#112794=AXIS2_PLACEMENT_3D ( 'NONE', #235640, #111866, #131411 ) ;
#112796=VECTOR ( 'NONE', #110545, 1000.000000000000000 ) ;
#112846=DIRECTION ( 'NONE',  ( 1.000000000000000000, 0.000000000000000000, 0.000000000000000000 ) ) ;
#112856=EDGE_CURVE ( 'NONE', #176023, #155495, #200101, .T. ) ;
#112863=CARTESIAN_POINT ( 'NONE',  ( 21.05000000000000071, 84.66355140188075268, -59.99900636645695329 ) ) ;
#112870=FACE_OUTER_BOUND ( 'NONE', #60639, .T. ) ;
#112884=DIRECTION ( 'NONE',  ( 0.000000000000000000, -6.454785026890510900E-15, 1.000000000000000000 ) ) ;
#112901=SPHERICAL_SURFACE ( 'NONE', #133442, 0.1000000000000000056 ) ;
#112912=ORIENTED_EDGE ( 'NONE', *, *, #36351, .T. ) ;
#112933=ORIENTED_EDGE ( 'NONE', *, *, #97341, .F. ) ;
#112943=FACE_OUTER_BOUND ( 'NONE', #202971, .T. ) ;
#112981=CARTESIAN_POINT ( 'NONE',  ( 18.49999999999999289, 65.79142135624879018, -44.75595019699900234 ) ) ;
#112991=DIRECTION ( 'NONE',  ( 0.000000000000000000, 0.000000000000000000, 1.000000000000000000 ) ) ;
#112992=DIRECTION ( 'NONE',  ( 0.000000000000000000, -1.000000000000000000, 6.938893903907030216E-14 ) ) ;
#113012=ORIENTED_EDGE ( 'NONE', *, *, #26052, .F. ) ;
#113020=VECTOR ( 'NONE', #201311, 1000.000000000000000 ) ;
#113049=ADVANCED_FACE ( 'NONE', ( #7301 ), #96212, .T. ) ;
#113055=ORIENTED_EDGE ( 'NONE', *, *, #48096, .T. ) ;
#113093=EDGE_CURVE ( 'NONE', #124432, #97848, #4623, .T. ) ;
#113097=DIRECTION ( 'NONE',  ( 0.000000000000000000, 0.000000000000000000, 1.000000000000000000 ) ) ;
#113109=DIRECTION ( 'NONE',  ( -1.000000000000000000, -0.000000000000000000, -0.000000000000000000 ) ) ;
#113139=CARTESIAN_POINT ( 'NONE',  ( -21.14999999999999858, 76.00000000001169553, -76.06376443622556849 ) ) ;
#113149=CIRCLE ( 'NONE', #171446, 0.1000000000000028644 ) ;
#113181=DIRECTION ( 'NONE',  ( -1.000000000000000000, -0.000000000000000000, -0.000000000000000000 ) ) ;
#113184=VERTEX_POINT ( 'NONE', #214485 ) ;
#113245=EDGE_CURVE ( 'NONE', #160781, #97691, #200463, .T. ) ;
#113286=DIRECTION ( 'NONE',  ( 1.000000000000000000, 0.000000000000000000, 0.000000000000000000 ) ) ;
#113342=VECTOR ( 'NONE', #239263, 1000.000000000000000 ) ;
#113349=VERTEX_POINT ( 'NONE', #80071 ) ;
#113356=( BOUNDED_SURFACE ( )  B_SPLINE_SURFACE ( 3, 2, ( 
 ( #108369, #104476, #103202 ),
 ( #62812, #184039, #9256 ),
 ( #4118, #5377, #124088 ),
 ( #142340, #84907, #164499 ) ),
 .UNSPECIFIED., .F., .F., .F. ) 
 B_SPLINE_SURFACE_WITH_KNOTS ( ( 4, 4 ),
 ( 3, 3 ),
 ( -1.028636811145622332E-17, 0.0003124336600439521472 ),
 ( 0.000000000000000000, 1.000000000000000000 ),
 .UNSPECIFIED. ) 
 GEOMETRIC_REPRESENTATION_ITEM ( )  RATIONAL_B_SPLINE_SURFACE ( (
 ( 1.000000000000000000, 0.7071067811865475727, 1.000000000000000000),
 ( 1.000000000000000000, 0.7089187706049935311, 1.000000000000000000),
 ( 1.000000000000000000, 0.7039288185051780777, 1.000000000000000000),
 ( 1.000000000000000000, 0.7040654476015839602, 1.000000000000000000) ) ) 
 REPRESENTATION_ITEM ( '' )  SURFACE ( )  );
#113383=EDGE_CURVE ( 'NONE', #182454, #221113, #251713, .T. ) ;
#113401=ORIENTED_EDGE ( 'NONE', *, *, #188775, .T. ) ;
#113437=DIRECTION ( 'NONE',  ( -0.000000000000000000, 6.982962677686266711E-15, -1.000000000000000000 ) ) ;
#113443=CARTESIAN_POINT ( 'NONE',  ( -20.94999999999999929, 87.48912529308749697, -39.02310748452423894 ) ) ;
#113448=CARTESIAN_POINT ( 'NONE',  ( 21.05000000000000071, 65.51556651036987944, -62.06630168303249206 ) ) ;
#113454=EDGE_CURVE ( 'NONE', #161516, #112286, #245305, .T. ) ;
#113533=PLANE ( 'NONE',  #219091 ) ;
#113668=ORIENTED_EDGE ( 'NONE', *, *, #7637, .T. ) ;
#113671=ORIENTED_EDGE ( 'NONE', *, *, #136570, .F. ) ;
#113686=B_SPLINE_CURVE_WITH_KNOTS ( 'NONE', 3,
 ( #142922, #21729, #42557, #162535, #62137, #197783, #102502, #81653 ),
 .UNSPECIFIED., .F., .F.,
 ( 4, 2, 2, 4 ),
 ( 0.000000000000000000, 6.534141206313191720E-05, 0.0001306828241262638344, 0.0002613656482524775245 ),
 .UNSPECIFIED. ) ;
#113693=ORIENTED_EDGE ( 'NONE', *, *, #103798, .T. ) ;
#113702=LINE ( 'NONE', #214089, #94580 ) ;
#113706=DIRECTION ( 'NONE',  ( 1.000000000000000000, 0.000000000000000000, 0.000000000000000000 ) ) ;
#113718=EDGE_CURVE ( 'NONE', #177733, #186334, #10240, .T. ) ;
#113738=VERTEX_POINT ( 'NONE', #91048 ) ;
#113741=DIRECTION ( 'NONE',  ( 2.259780016855445309E-14, -0.9875055080513764905, 0.1575844902526679359 ) ) ;
#113750=DIRECTION ( 'NONE',  ( 0.000000000000000000, 0.4999999999999689138, -0.8660254037844565822 ) ) ;
#113782=AXIS2_PLACEMENT_3D ( 'NONE', #138637, #235212, #116548 ) ;
#113786=ORIENTED_EDGE ( 'NONE', *, *, #241781, .T. ) ;
#113799=VECTOR ( 'NONE', #111954, 1000.000000000000000 ) ;
#113818=CARTESIAN_POINT ( 'NONE',  ( 23.25000000000000000, 85.00000000001149658, -45.91707660717670336 ) ) ;
#113858=VECTOR ( 'NONE', #29953, 1000.000000000000000 ) ;
#113865=CARTESIAN_POINT ( 'NONE',  ( -22.50047199487877947, 75.95509394809148773, -81.27315490344393822 ) ) ;
#113867=FACE_BOUND ( 'NONE', #93059, .T. ) ;
#113886=DIRECTION ( 'NONE',  ( 0.000000000000000000, -1.000000000000000000, -6.982962677686266711E-15 ) ) ;
#113911=CARTESIAN_POINT ( 'NONE',  ( 21.05000000000000071, 76.00000000001165290, -69.52310748452431710 ) ) ;
#113915=CARTESIAN_POINT ( 'NONE',  ( -21.44999999999999929, 68.65000000001157332, -57.17310748452437252 ) ) ;
#113945=VERTEX_POINT ( 'NONE', #255192 ) ;
#113950=CARTESIAN_POINT ( 'NONE',  ( 20.94999999999999929, 87.65000000001141700, -36.02310748452423894 ) ) ;
#113965=ORIENTED_EDGE ( 'NONE', *, *, #33865, .T. ) ;
#113966=ORIENTED_EDGE ( 'NONE', *, *, #188346, .F. ) ;
#113988=DIRECTION ( 'NONE',  ( -0.000000000000000000, -1.000000000000000000, -7.272083257015735086E-15 ) ) ;
#113994=CARTESIAN_POINT ( 'NONE',  ( 21.04999999999999716, 76.00000000001169553, -76.06376443622555428 ) ) ;
#114031=CIRCLE ( 'NONE', #218089, 0.1000000000000028644 ) ;
#114039=CYLINDRICAL_SURFACE ( 'NONE', #92690, 0.1000000000000052097 ) ;
#114048=CARTESIAN_POINT ( 'NONE',  ( -20.54999999999999716, 74.00000000001151079, -49.24772940728643533 ) ) ;
#114050=APPLICATION_CONTEXT ( 'automotive_design' ) ;
#114072=ORIENTED_EDGE ( 'NONE', *, *, #33729, .F. ) ;
#114075=CARTESIAN_POINT ( 'NONE',  ( -18.59999999999999787, 66.65000000001150227, -48.27310748452438816 ) ) ;
#114078=DIRECTION ( 'NONE',  ( -1.000000000000000000, 0.000000000000000000, 0.000000000000000000 ) ) ;
#114088=EDGE_CURVE ( 'NONE', #235880, #6238, #121580, .T. ) ;
#114093=DIRECTION ( 'NONE',  ( 2.952720810173289112E-16, 1.000000000000000000, -6.088138035986627436E-46 ) ) ;
#114158=ORIENTED_EDGE ( 'NONE', *, *, #215880, .T. ) ;
#114159=CARTESIAN_POINT ( 'NONE',  ( -18.50000000000000000, 66.65000000001150227, -48.17310748452438673 ) ) ;
#114163=CARTESIAN_POINT ( 'NONE',  ( 22.39999999999999858, 75.90000000001170122, -77.31388708289770761 ) ) ;
#114176=DIRECTION ( 'NONE',  ( 1.000000000000000000, 0.000000000000000000, 0.000000000000000000 ) ) ;
#114180=EDGE_CURVE ( 'NONE', #4242, #150112, #162589, .T. ) ;
#114215=AXIS2_PLACEMENT_3D ( 'NONE', #2731, #39336, #58842 ) ;
#114221=CIRCLE ( 'NONE', #234438, 0.1000000000000055705 ) ;
#114223=CARTESIAN_POINT ( 'NONE',  ( -20.85000000000000142, 68.97833521811131163, -32.18954208262707795 ) ) ;
#114247=ORIENTED_EDGE ( 'NONE', *, *, #91347, .F. ) ;
#114253=CYLINDRICAL_SURFACE ( 'NONE', #203470, 0.09999999999999939493 ) ;
#114257=CARTESIAN_POINT ( 'NONE',  ( -20.85000000106584750, 64.25000000001148237, -42.86760282805085609 ) ) ;
#114271=DIRECTION ( 'NONE',  ( 4.408576920032447355E-17, 0.1350103645451807555, 0.9908441862701610203 ) ) ;
#114272=DIRECTION ( 'NONE',  ( 0.000000000000000000, 1.000000000000000000, 1.387778780781444413E-14 ) ) ;
#114296=AXIS2_PLACEMENT_3D ( 'NONE', #62406, #196763, #118549 ) ;
#114319=CIRCLE ( 'NONE', #251864, 0.09999999999999939493 ) ;
#114323=DIRECTION ( 'NONE',  ( -1.000000000000000000, 0.000000000000000000, -0.000000000000000000 ) ) ;
#114334=CIRCLE ( 'NONE', #130905, 0.1000000000000017680 ) ;
#114338=EDGE_LOOP ( 'NONE', ( #183209, #241750, #245296, #33776, #49748 ) ) ;
#114383=ORIENTED_EDGE ( 'NONE', *, *, #177728, .F. ) ;
#114390=CARTESIAN_POINT ( 'NONE',  ( -21.05000000000000071, 61.95000000001162022, -64.00941241376342816 ) ) ;
#114419=CARTESIAN_POINT ( 'NONE',  ( 23.24999999999999289, 64.25000000001165290, -69.42310748452440805 ) ) ;
#114457=ORIENTED_EDGE ( 'NONE', *, *, #226797, .F. ) ;
#114481=FACE_OUTER_BOUND ( 'NONE', #5047, .T. ) ;
#114508=DIRECTION ( 'NONE',  ( 2.952720810173289112E-16, 1.000000000000000000, 9.912705577010238578E-15 ) ) ;
#114517=CARTESIAN_POINT ( 'NONE',  ( 18.59999999999999787, 85.40000000001137437, -29.14106563635157698 ) ) ;
#114562=AXIS2_PLACEMENT_3D ( 'NONE', #132496, #215858, #212049 ) ;
#114577=CIRCLE ( 'NONE', #10530, 0.1000000000000028644 ) ;
#114584=LINE ( 'NONE', #59712, #80115 ) ;
#114598=AXIS2_PLACEMENT_3D ( 'NONE', #151835, #172707, #252178 ) ;
#114622=AXIS2_PLACEMENT_3D ( 'NONE', #91901, #231439, #171484 ) ;
#114636=CARTESIAN_POINT ( 'NONE',  ( 22.47071067811865319, 75.90090754530910999, -77.24318222902238062 ) ) ;
#114646=ORIENTED_EDGE ( 'NONE', *, *, #137362, .T. ) ;
#114671=VECTOR ( 'NONE', #185098, 1000.000000000000000 ) ;
#114684=DIRECTION ( 'NONE',  ( -1.000000000000000000, -0.000000000000000000, -0.000000000000000000 ) ) ;
#114698=CYLINDRICAL_SURFACE ( 'NONE', #144854, 0.09999999999999976963 ) ;
#114704=ORIENTED_EDGE ( 'NONE', *, *, #133098, .F. ) ;
#114711=CARTESIAN_POINT ( 'NONE',  ( -21.09107601085561257, 69.63612202465148471, -69.56241464924151785 ) ) ;
#114722=ORIENTED_EDGE ( 'NONE', *, *, #97584, .F. ) ;
#114727=DIRECTION ( 'NONE',  ( 0.000000000000000000, -0.8660254037844377084, -0.5000000000000016653 ) ) ;
#114772=CARTESIAN_POINT ( 'NONE',  ( 18.59999999999999076, 69.01799029515494510, -32.32695536626807353 ) ) ;
#114774=AXIS2_PLACEMENT_3D ( 'NONE', #221520, #63751, #184990 ) ;
#114784=DIRECTION ( 'NONE',  ( -0.000000000000000000, -1.000000000000000000, -6.982962677686266711E-15 ) ) ;
#114789=FACE_OUTER_BOUND ( 'NONE', #146657, .T. ) ;
#114792=CARTESIAN_POINT ( 'NONE',  ( 18.53317502108576420, 65.67736539654895012, -30.46251168765719797 ) ) ;
#114809=ORIENTED_EDGE ( 'NONE', *, *, #251342, .F. ) ;
#114821=CARTESIAN_POINT ( 'NONE',  ( 20.94999999999999929, 76.00000000001142553, -36.02310748452432421 ) ) ;
#114826=CARTESIAN_POINT ( 'NONE',  ( -20.85000000000000142, 77.83585931145498193, -24.51866831572578320 ) ) ;
#114850=AXIS2_PLACEMENT_3D ( 'NONE', #89472, #213274, #34673 ) ;
#114916=ORIENTED_EDGE ( 'NONE', *, *, #19353, .F. ) ;
#114948=CARTESIAN_POINT ( 'NONE',  ( 23.14999999999999147, 76.00000000001165290, -69.52310748452431710 ) ) ;
#114951=ORIENTED_EDGE ( 'NONE', *, *, #13192, .F. ) ;
#114996=VERTEX_POINT ( 'NONE', #32516 ) ;
#115093=CIRCLE ( 'NONE', #61106, 4.300000000000039790 ) ;
#115121=EDGE_LOOP ( 'NONE', ( #54378, #121957, #177369, #14861 ) ) ;
#115154=ORIENTED_EDGE ( 'NONE', *, *, #5172, .F. ) ;
#115168=CIRCLE ( 'NONE', #111059, 0.1000000000000060146 ) ;
#115175=DIRECTION ( 'NONE',  ( 0.000000000000000000, 0.000000000000000000, -1.000000000000000000 ) ) ;
#115177=DIRECTION ( 'NONE',  ( 0.000000000000000000, 0.000000000000000000, 1.000000000000000000 ) ) ;
#115186=DIRECTION ( 'NONE',  ( -1.000000000000000000, 0.000000000000000000, -0.000000000000000000 ) ) ;
#115202=LINE ( 'NONE', #130914, #132325 ) ;
#115206=DIRECTION ( 'NONE',  ( -1.000000000000000000, 0.000000000000000000, -0.000000000000000000 ) ) ;
#115211=CIRCLE ( 'NONE', #156934, 0.1000000000000028644 ) ;
#115239=CIRCLE ( 'NONE', #252603, 4.099999999999999645 ) ;
#115241=DIRECTION ( 'NONE',  ( 0.000000000000000000, 0.000000000000000000, -1.000000000000000000 ) ) ;
#115275=ORIENTED_EDGE ( 'NONE', *, *, #51399, .F. ) ;
#115307=EDGE_CURVE ( 'NONE', #86585, #56972, #94360, .T. ) ;
#115329=CIRCLE ( 'NONE', #2898, 0.09999999999999520384 ) ;
#115336=DIRECTION ( 'NONE',  ( -2.915501640297152804E-16, -1.000000000000000000, -6.997203936713167125E-15 ) ) ;
#115360=CARTESIAN_POINT ( 'NONE',  ( -21.59142135623730852, 68.15000000001155911, -57.17310748452437963 ) ) ;
#115444=ORIENTED_EDGE ( 'NONE', *, *, #104944, .T. ) ;
#115457=VERTEX_POINT ( 'NONE', #169803 ) ;
#115466=CIRCLE ( 'NONE', #190322, 0.1000000000000028644 ) ;
#115581=ADVANCED_FACE ( 'NONE', ( #248000 ), #230026, .T. ) ;
#115585=CARTESIAN_POINT ( 'NONE',  ( 23.15000000000000213, 85.60000000001159037, -59.62913836187181005 ) ) ;
#115589=CARTESIAN_POINT ( 'NONE',  ( -20.85000000000000142, 68.87972903831379767, -32.36354444268504693 ) ) ;
#115597=ORIENTED_EDGE ( 'NONE', *, *, #223462, .T. ) ;
#115599=AXIS2_PLACEMENT_3D ( 'NONE', #32598, #91253, #70436 ) ;
#115604=ORIENTED_EDGE ( 'NONE', *, *, #108831, .T. ) ;
#115630=CARTESIAN_POINT ( 'NONE',  ( 21.05000000000000071, 76.00000000001142553, -36.02310748452432421 ) ) ;
#115640=CARTESIAN_POINT ( 'NONE',  ( -20.64999999999999858, 74.07476635515175190, -56.79286395139820343 ) ) ;
#115695=DIRECTION ( 'NONE',  ( 0.000000000000000000, -6.982962677686266711E-15, 1.000000000000000000 ) ) ;
#115707=VERTEX_POINT ( 'NONE', #54923 ) ;
#115716=DIRECTION ( 'NONE',  ( 1.000000000000000000, -0.000000000000000000, 0.000000000000000000 ) ) ;
#115721=DIRECTION ( 'NONE',  ( 1.000000000000000000, 0.000000000000000000, 0.000000000000000000 ) ) ;
#115733=CARTESIAN_POINT ( 'NONE',  ( 20.97565083910961548, 65.52538259873279003, -61.94516430793584760 ) ) ;
#115751=DIRECTION ( 'NONE',  ( -0.9880948137434723000, -0.1538461538461483591, -1.074301950413233512E-15 ) ) ;
#115769=VECTOR ( 'NONE', #151918, 1000.000000000000000 ) ;
#115794=VERTEX_POINT ( 'NONE', #41831 ) ;
#115798=CARTESIAN_POINT ( 'NONE',  ( -20.94999999999999929, 74.83729825007360148, -61.42310748452432989 ) ) ;
#115811=CARTESIAN_POINT ( 'NONE',  ( -20.94999999999999929, 64.40000000001161595, -62.59490425424883853 ) ) ;
#115821=DIRECTION ( 'NONE',  ( -1.000000000000000000, -0.000000000000000000, -0.000000000000000000 ) ) ;
#115841=TOROIDAL_SURFACE ( 'NONE', #220074, 0.4000000000000012990, 0.1000000000000000056 ) ;
#115853=CARTESIAN_POINT ( 'NONE',  ( -18.54260524012588007, 85.62421939008508787, -29.28233443875340924 ) ) ;
#115862=CARTESIAN_POINT ( 'NONE',  ( -22.59066674512259709, 64.25000000001163869, -69.55361160815476751 ) ) ;
#115871=EDGE_CURVE ( 'NONE', #72194, #124432, #172002, .T. ) ;
#115890=LINE ( 'NONE', #173344, #22219 ) ;
#115898=LINE ( 'NONE', #1042, #236275 ) ;
#115924=DIRECTION ( 'NONE',  ( -0.000000000000000000, 0.9908441862701591329, 0.1350103645451946055 ) ) ;
#115950=CIRCLE ( 'NONE', #174245, 0.1000000000000028644 ) ;
#115960=CARTESIAN_POINT ( 'NONE',  ( -23.25000000000000000, 64.35000000001150511, -48.17310748452440805 ) ) ;
#115975=ORIENTED_EDGE ( 'NONE', *, *, #207433, .T. ) ;
#115978=ORIENTED_EDGE ( 'NONE', *, *, #90529, .F. ) ;
#115996=CIRCLE ( 'NONE', #253347, 3.999999999999996447 ) ;
#116008=VERTEX_POINT ( 'NONE', #251546 ) ;
#116012=EDGE_LOOP ( 'NONE', ( #249720, #253386, #117456, #80966, #216661 ) ) ;
#116013=CARTESIAN_POINT ( 'NONE',  ( -21.05000000000000071, 69.58633726514248963, -69.43751462116246387 ) ) ;
#116025=CARTESIAN_POINT ( 'NONE',  ( -20.54999999999999716, 74.00000000001156764, -56.29848556176223440 ) ) ;
#116026=DIRECTION ( 'NONE',  ( 1.000000000000000000, 0.000000000000000000, 0.000000000000000000 ) ) ;
#116039=EDGE_LOOP ( 'NONE', ( #253359, #4372, #33416 ) ) ;
#116157=EDGE_LOOP ( 'NONE', ( #188722, #69234, #104943, #93271 ) ) ;
#116161=CARTESIAN_POINT ( 'NONE',  ( 20.94999999999999574, 87.75000000001162448, -66.42310748452423752 ) ) ;
#116163=DIRECTION ( 'NONE',  ( 1.000000000000000000, -0.000000000000000000, 0.000000000000000000 ) ) ;
#116173=DIRECTION ( 'NONE',  ( 0.000000000000000000, -2.775557561562888827E-14, 1.000000000000000000 ) ) ;
#116177=CARTESIAN_POINT ( 'NONE',  ( -18.41353343127311248, 85.50000000001161027, -62.49103808782458458 ) ) ;
#116211=DIRECTION ( 'NONE',  ( 1.000000000000000000, 0.000000000000000000, -0.000000000000000000 ) ) ;
#116254=ORIENTED_EDGE ( 'NONE', *, *, #69680, .T. ) ;
#116304=VERTEX_POINT ( 'NONE', #67465 ) ;
#116329=ORIENTED_EDGE ( 'NONE', *, *, #140919, .F. ) ;
#116330=DIRECTION ( 'NONE',  ( 0.000000000000000000, 0.000000000000000000, -1.000000000000000000 ) ) ;
#116333=DIRECTION ( 'NONE',  ( 0.000000000000000000, 0.000000000000000000, 1.000000000000000000 ) ) ;
#116350=CIRCLE ( 'NONE', #66449, 0.1999999999999987899 ) ;
#116353=ORIENTED_EDGE ( 'NONE', *, *, #36559, .T. ) ;
#116359=AXIS2_PLACEMENT_3D ( 'NONE', #24574, #162794, #200626 ) ;
#116369=DIRECTION ( 'NONE',  ( -1.000000000000000000, 7.304098846218134667E-16, 5.100424963727256530E-30 ) ) ;
#116419=AXIS2_PLACEMENT_3D ( 'NONE', #57882, #194869, #78731 ) ;
#116437=VERTEX_POINT ( 'NONE', #76448 ) ;
#116443=DIRECTION ( 'NONE',  ( -0.7071067811865214825, -0.7071067811865735520, 0.000000000000000000 ) ) ;
#116445=DIRECTION ( 'NONE',  ( -1.836970198721029934E-16, -1.000000000000000000, -6.982962677686266711E-15 ) ) ;
#116448=CARTESIAN_POINT ( 'NONE',  ( 20.04142135623730070, 64.35000000001150511, -48.17310748452440095 ) ) ;
#116476=CARTESIAN_POINT ( 'NONE',  ( -20.94999999999999929, 76.00000000001145395, -40.02310748452431710 ) ) ;
#116484=CARTESIAN_POINT ( 'NONE',  ( 18.49999999999998934, 69.45000000001158469, -59.50608031408435039 ) ) ;
#116488=ORIENTED_EDGE ( 'NONE', *, *, #147322, .T. ) ;
#116501=CARTESIAN_POINT ( 'NONE',  ( -18.51555513499745942, 85.35265705451639917, -62.32793758882646529 ) ) ;
#116511=CARTESIAN_POINT ( 'NONE',  ( -23.15000000000000213, 87.75000000001173817, -81.27310748452423184 ) ) ;
#116515=DIRECTION ( 'NONE',  ( 0.000000000000000000, 6.982962677686266711E-15, -1.000000000000000000 ) ) ;
#116521=VERTEX_POINT ( 'NONE', #219812 ) ;
#116546=DIRECTION ( 'NONE',  ( 0.000000000000000000, 0.000000000000000000, 1.000000000000000000 ) ) ;
#116548=DIRECTION ( 'NONE',  ( 0.000000000000000000, 0.000000000000000000, -1.000000000000000000 ) ) ;
#116576=FACE_OUTER_BOUND ( 'NONE', #47700, .T. ) ;
#116591=DIRECTION ( 'NONE',  ( -0.000000000000000000, -1.000000000000000000, -6.982962677686266711E-15 ) ) ;
#116613=DIRECTION ( 'NONE',  ( 0.000000000000000000, 0.000000000000000000, -1.000000000000000000 ) ) ;
#116620=CIRCLE ( 'NONE', #229254, 0.1000000000000028644 ) ;
#116657=EDGE_LOOP ( 'NONE', ( #249998, #41208, #36556, #171173 ) ) ;
#116688=DIRECTION ( 'NONE',  ( 0.000000000000000000, 0.000000000000000000, 1.000000000000000000 ) ) ;
#116693=EDGE_LOOP ( 'NONE', ( #122452, #192606, #234712, #132270 ) ) ;
#116700=CYLINDRICAL_SURFACE ( 'NONE', #75843, 0.1000000000000028644 ) ;
#116701=VECTOR ( 'NONE', #235301, 1000.000000000000114 ) ;
#116709=CYLINDRICAL_SURFACE ( 'NONE', #105657, 0.09999999999999939493 ) ;
#116721=LINE ( 'NONE', #196257, #2817 ) ;
#116724=ADVANCED_FACE ( 'NONE', ( #103694 ), #9815, .T. ) ;
#116733=VECTOR ( 'NONE', #14548, 1000.000000000000000 ) ;
#116766=PLANE ( 'NONE',  #7920 ) ;
#116785=DIRECTION ( 'NONE',  ( 1.000000000000000000, 0.000000000000000000, 0.000000000000000000 ) ) ;
#116786=DIRECTION ( 'NONE',  ( -1.000000000000000000, 0.000000000000000000, -0.000000000000000000 ) ) ;
#116791=DIRECTION ( 'NONE',  ( -1.000000000000000000, -0.000000000000000000, -0.000000000000000000 ) ) ;
#116801=AXIS2_PLACEMENT_3D ( 'NONE', #179223, #119234, #83899 ) ;
#116803=EDGE_CURVE ( 'NONE', #224921, #182454, #138958, .T. ) ;
#116827=CARTESIAN_POINT ( 'NONE',  ( -21.05000000000000071, 64.25000000001148237, -43.03791325517834565 ) ) ;
#116834=CARTESIAN_POINT ( 'NONE',  ( 21.05000000000000071, 69.74115287693250309, -69.55486583757952701 ) ) ;
#116860=ADVANCED_FACE ( 'NONE', ( #194845 ), #228820, .F. ) ;
#116865=ADVANCED_FACE ( 'NONE', ( #249664 ), #73616, .F. ) ;
#116883=CARTESIAN_POINT ( 'NONE',  ( 18.42636655943172030, 85.49694431578203080, -29.41402691336874753 ) ) ;
#116898=AXIS2_PLACEMENT_3D ( 'NONE', #27126, #166639, #7525 ) ;
#116902=ORIENTED_EDGE ( 'NONE', *, *, #183091, .T. ) ;
#116910=ORIENTED_EDGE ( 'NONE', *, *, #241190, .T. ) ;
#116940=CARTESIAN_POINT ( 'NONE',  ( -22.50000000000000000, 64.35000000001166143, -69.52310748452438816 ) ) ;
#116949=DIRECTION ( 'NONE',  ( -3.890533409366484652E-14, 0.1298341882520054891, 0.9915357197604850459 ) ) ;
#116961=DIRECTION ( 'NONE',  ( 0.000000000000000000, -0.3738317757008748909, -0.9274965247785733613 ) ) ;
#116973=CARTESIAN_POINT ( 'NONE',  ( -23.25000000000000000, 77.83585931145498193, -24.51866831572578675 ) ) ;
#117001=EDGE_CURVE ( 'NONE', #88576, #256296, #105843, .T. ) ;
#117016=CARTESIAN_POINT ( 'NONE',  ( 20.22894356738409272, 66.72150177717388431, -61.25458457828101189 ) ) ;
#117054=DIRECTION ( 'NONE',  ( -1.000000000000000000, 1.836970198721029934E-16, 1.282749433769087757E-30 ) ) ;
#117065=DIRECTION ( 'NONE',  ( 0.000000000000000000, 0.000000000000000000, 1.000000000000000000 ) ) ;
#117069=ORIENTED_EDGE ( 'NONE', *, *, #121225, .F. ) ;
#117076=CIRCLE ( 'NONE', #137895, 0.1000000000000055705 ) ;
#117099=CARTESIAN_POINT ( 'NONE',  ( -21.14999999999999858, 76.00000000001165290, -69.52310748452431710 ) ) ;
#117107=CARTESIAN_POINT ( 'NONE',  ( -22.59999999999999787, 75.89914163091303578, -81.27267460801371612 ) ) ;
#117112=VECTOR ( 'NONE', #212432, 1000.000000000000000 ) ;
#117117=ADVANCED_FACE ( 'NONE', ( #190361 ), #147362, .T. ) ;
#117121=ADVANCED_FACE ( 'NONE', ( #11725 ), #228194, .T. ) ;
#117142=PLANE ( 'NONE',  #38901 ) ;
#117152=FACE_OUTER_BOUND ( 'NONE', #176556, .T. ) ;
#117254=LINE ( 'NONE', #216339, #47362 ) ;
#117289=DIRECTION ( 'NONE',  ( 0.000000000000000000, -7.086529944415893080E-15, 1.000000000000000000 ) ) ;
#117293=CARTESIAN_POINT ( 'NONE',  ( -20.54999999999999716, 71.65000000001154490, -52.77310748452435263 ) ) ;
#117304=DIRECTION ( 'NONE',  ( -1.000000000000000000, 0.000000000000000000, -0.000000000000000000 ) ) ;
#117328=DIRECTION ( 'NONE',  ( -1.000000000000000000, -0.000000000000000000, -0.000000000000000000 ) ) ;
#117360=AXIS2_PLACEMENT_3D ( 'NONE', #180531, #91695, #226031 ) ;
#117361=DIRECTION ( 'NONE',  ( 0.000000000000000000, 6.982962677686266711E-15, -1.000000000000000000 ) ) ;
#117362=CARTESIAN_POINT ( 'NONE',  ( 20.90851465518106167, 65.67467670974367877, -30.45317318268843820 ) ) ;
#117365=CYLINDRICAL_SURFACE ( 'NONE', #251353, 4.049999999999998046 ) ;
#117370=CARTESIAN_POINT ( 'NONE',  ( 21.07971444708685738, 69.67020791838511684, -69.61093092084226441 ) ) ;
#117375=ADVANCED_FACE ( 'NONE', ( #83192 ), #2385, .T. ) ;
#117377=EDGE_LOOP ( 'NONE', ( #16796, #254740, #62679 ) ) ;
#117381=DIRECTION ( 'NONE',  ( 1.000000000000000000, 0.000000000000000000, 0.000000000000000000 ) ) ;
#117384=CARTESIAN_POINT ( 'NONE',  ( 18.46932045258645161, 85.67068520027710576, -29.34924711152760324 ) ) ;
#117397=AXIS2_PLACEMENT_3D ( 'NONE', #30130, #92637, #173527 ) ;
#117408=TOROIDAL_SURFACE ( 'NONE', #4933, 11.65000000000000036, 0.1000000000000000056 ) ;
#117424=CIRCLE ( 'NONE', #225720, 3.999999999999996447 ) ;
#117427=LINE ( 'NONE', #17059, #185406 ) ;
#117456=ORIENTED_EDGE ( 'NONE', *, *, #142338, .F. ) ;
#117505=CIRCLE ( 'NONE', #150817, 4.049999999999998046 ) ;
#117518=ORIENTED_EDGE ( 'NONE', *, *, #157447, .T. ) ;
#117532=CARTESIAN_POINT ( 'NONE',  ( -18.50000000000000000, 68.87972903831381188, -32.36354444268503983 ) ) ;
#117551=AXIS2_PLACEMENT_3D ( 'NONE', #201084, #84953, #82389 ) ;
#117567=VERTEX_POINT ( 'NONE', #246156 ) ;
#117571=CARTESIAN_POINT ( 'NONE',  ( -23.25000000000000000, 76.00000000001168132, -73.67310748452432279 ) ) ;
#117589=VERTEX_POINT ( 'NONE', #51779 ) ;
#117598=DIRECTION ( 'NONE',  ( -1.000000000000000000, 0.000000000000000000, 0.000000000000000000 ) ) ;
#117613=ORIENTED_EDGE ( 'NONE', *, *, #133033, .T. ) ;
#117620=DIRECTION ( 'NONE',  ( 1.000000000000000000, 0.000000000000000000, 0.000000000000000000 ) ) ;
#117621=VECTOR ( 'NONE', #228971, 1000.000000000000000 ) ;
#117633=LINE ( 'NONE', #160643, #161184 ) ;
#117655=DIRECTION ( 'NONE',  ( 0.000000000000000000, 0.000000000000000000, 1.000000000000000000 ) ) ;
#117667=DIRECTION ( 'NONE',  ( -0.000000000000000000, 1.000000000000000000, 6.982962677686267499E-15 ) ) ;
#117731=SPHERICAL_SURFACE ( 'NONE', #29897, 0.1000000000000000056 ) ;
#117735=CARTESIAN_POINT ( 'NONE',  ( 19.99999999999998934, 64.35000000001150511, -48.27310748452440237 ) ) ;
#117737=CARTESIAN_POINT ( 'NONE',  ( -22.39999999999999858, 76.00000000001165290, -69.62310748452432563 ) ) ;
#117746=FACE_OUTER_BOUND ( 'NONE', #241927, .T. ) ;
#117774=CIRCLE ( 'NONE', #251033, 0.09999999999999520384 ) ;
#117833=ORIENTED_EDGE ( 'NONE', *, *, #114088, .F. ) ;
#117841=CARTESIAN_POINT ( 'NONE',  ( -20.54999999999999716, 87.75000000001156764, -57.17310748452423752 ) ) ;
#117847=PLANE ( 'NONE',  #252575 ) ;
#117855=VERTEX_POINT ( 'NONE', #178193 ) ;
#117887=DIRECTION ( 'NONE',  ( 1.000000000000000000, 7.304098846218133681E-16, 5.100424963727255128E-30 ) ) ;
#117891=DIRECTION ( 'NONE',  ( 0.000000000000000000, 0.000000000000000000, 1.000000000000000000 ) ) ;
#117921=VERTEX_POINT ( 'NONE', #4639 ) ;
#117935=AXIS2_PLACEMENT_3D ( 'NONE', #177846, #164683, #125549 ) ;
#117939=ADVANCED_FACE ( 'NONE', ( #26824 ), #51648, .F. ) ;
#117976=CARTESIAN_POINT ( 'NONE',  ( 21.08832698747859169, 67.22463560659436155, -57.29439001806023413 ) ) ;
#118002=DIRECTION ( 'NONE',  ( 0.000000000000000000, 1.000000000000000000, 8.717686153663073805E-15 ) ) ;
#118005=CARTESIAN_POINT ( 'NONE',  ( -21.05000000000000071, 69.70000000001164153, -69.42310748452436542 ) ) ;
#118007=CIRCLE ( 'NONE', #43196, 0.1000000000000026007 ) ;
#118043=VECTOR ( 'NONE', #112485, 1000.000000000000000 ) ;
#118046=DIRECTION ( 'NONE',  ( -1.000000000000000000, 0.000000000000000000, -0.000000000000000000 ) ) ;
#118054=CARTESIAN_POINT ( 'NONE',  ( -20.94999999999999929, 64.35000000001141984, -36.02310748452440237 ) ) ;
#118075=AXIS2_PLACEMENT_3D ( 'NONE', #107078, #167100, #64114 ) ;
#118144=AXIS2_PLACEMENT_3D ( 'NONE', #132917, #110768, #70400 ) ;
#118151=VERTEX_POINT ( 'NONE', #128037 ) ;
#118199=ORIENTED_EDGE ( 'NONE', *, *, #125511, .T. ) ;
#118211=DIRECTION ( 'NONE',  ( 0.000000000000000000, -0.9998779222360104635, -0.01562499999996343723 ) ) ;
#118213=AXIS2_PLACEMENT_3D ( 'NONE', #120074, #116211, #37961 ) ;
#118217=CYLINDRICAL_SURFACE ( 'NONE', #35055, 0.1000000000000028644 ) ;
#118218=EDGE_LOOP ( 'NONE', ( #58444, #221666, #71311, #188113 ) ) ;
#118245=DIRECTION ( 'NONE',  ( 1.000000000000000000, 0.000000000000000000, 0.000000000000000000 ) ) ;
#118252=EDGE_LOOP ( 'NONE', ( #241337, #44804, #132843, #179957, #48365, #105367, #197003 ) ) ;
#118254=DIRECTION ( 'NONE',  ( -1.000000000000000000, 0.000000000000000000, 0.000000000000000000 ) ) ;
#118286=ADVANCED_FACE ( 'NONE', ( #1105 ), #120703, .T. ) ;
#118293=FACE_OUTER_BOUND ( 'NONE', #39352, .T. ) ;
#118323=CIRCLE ( 'NONE', #164303, 0.09999999999999939493 ) ;
#118331=EDGE_LOOP ( 'NONE', ( #79359, #149459, #40080, #150120 ) ) ;
#118343=CARTESIAN_POINT ( 'NONE',  ( -20.54999999999999716, 84.66355140188063899, -45.54720860259156723 ) ) ;
#118386=CARTESIAN_POINT ( 'NONE',  ( -21.05000000000000071, 64.35000000001161879, -62.73924182154625129 ) ) ;
#118394=AXIS2_PLACEMENT_3D ( 'NONE', #128346, #72230, #33134 ) ;
#118407=VECTOR ( 'NONE', #157518, 1000.000000000000000 ) ;
#118411=AXIS2_PLACEMENT_3D ( 'NONE', #96411, #13069, #213811 ) ;
#118474=CARTESIAN_POINT ( 'NONE',  ( 21.05000000000000071, 69.52293297888689949, -69.42310748452439384 ) ) ;
#118481=EDGE_CURVE ( 'NONE', #105103, #247138, #37308, .T. ) ;
#118488=EDGE_CURVE ( 'NONE', #196986, #215272, #174904, .T. ) ;
#118512=EDGE_CURVE ( 'NONE', #248655, #176779, #54035, .T. ) ;
#118524=ORIENTED_EDGE ( 'NONE', *, *, #40939, .F. ) ;
#118532=DIRECTION ( 'NONE',  ( 2.952720810173289112E-16, 1.000000000000000000, 6.467318590049456648E-15 ) ) ;
#118542=CARTESIAN_POINT ( 'NONE',  ( -18.50000000000000000, 64.35000000001166143, -69.42310748452440805 ) ) ;
#118544=ORIENTED_EDGE ( 'NONE', *, *, #132534, .F. ) ;
#118549=DIRECTION ( 'NONE',  ( -1.000000000000000000, 0.000000000000000000, 0.000000000000000000 ) ) ;
#118570=VECTOR ( 'NONE', #83630, 1000.000000000000000 ) ;
#118575=EDGE_LOOP ( 'NONE', ( #224166, #21896, #196743, #133397 ) ) ;
#118586=EDGE_CURVE ( 'NONE', #216178, #138795, #95719, .T. ) ;
#118593=CARTESIAN_POINT ( 'NONE',  ( -20.54999999999999716, 74.00000000001151079, -49.24772940728643533 ) ) ;
#118645=AXIS2_PLACEMENT_3D ( 'NONE', #162037, #223256, #185432 ) ;
#118726=DIRECTION ( 'NONE',  ( -2.952720810173289112E-16, -1.000000000000000000, -6.982962677686266711E-15 ) ) ;
#118763=VERTEX_POINT ( 'NONE', #142561 ) ;
#118768=DIRECTION ( 'NONE',  ( 0.000000000000000000, -0.4999999999999689138, 0.8660254037844565822 ) ) ;
#118793=EDGE_CURVE ( 'NONE', #84743, #91161, #245765, .T. ) ;
#118794=EDGE_CURVE ( 'NONE', #176232, #203476, #185557, .T. ) ;
#118830=EDGE_CURVE ( 'NONE', #230638, #91161, #254117, .T. ) ;
#118864=EDGE_CURVE ( 'NONE', #223901, #183793, #208956, .T. ) ;
#118890=DIRECTION ( 'NONE',  ( 1.000000000000000000, 0.000000000000000000, 0.000000000000000000 ) ) ;
#118895=CARTESIAN_POINT ( 'NONE',  ( -20.64999999999999858, 68.85000000001156195, -57.17310748452437252 ) ) ;
#118905=LINE ( 'NONE', #19805, #187080 ) ;
#118994=VERTEX_POINT ( 'NONE', #155467 ) ;
#119028=EDGE_LOOP ( 'NONE', ( #182651, #64738, #77267, #92481 ) ) ;
#119049=CARTESIAN_POINT ( 'NONE',  ( 21.09546886439543556, 67.12144688699666517, -57.28601363396898449 ) ) ;
#119087=CARTESIAN_POINT ( 'NONE',  ( 23.25000000000000000, 85.60000000001150511, -45.91707660717669626 ) ) ;
#119095=ADVANCED_FACE ( 'NONE', ( #40659 ), #180137, .F. ) ;
#119104=EDGE_CURVE ( 'NONE', #46909, #56627, #221784, .T. ) ;
#119130=DIRECTION ( 'NONE',  ( 0.000000000000000000, 0.000000000000000000, -1.000000000000000000 ) ) ;
#119136=B_SPLINE_CURVE_WITH_KNOTS ( 'NONE', 3,
 ( #57185, #237137, #199302, #96317, #42785, #217547, #38947, #138012, #40246, #2353, #160193, #136734, #98869, #197994, #218836, #181026, #200571, #175904, #62355 ),
 .UNSPECIFIED., .F., .F.,
 ( 4, 3, 3, 3, 3, 3, 4 ),
 ( -2.000416914656542534E-06, 0.000000000000000000, 4.714008503744896491E-05, 9.979203887777595382E-05, 0.0001372215519229517651, 0.0001635031576220978653, 0.0001900083748504165226 ),
 .UNSPECIFIED. ) ;
#119137=AXIS2_PLACEMENT_3D ( 'NONE', #166231, #245739, #67098 ) ;
#119150=DIRECTION ( 'NONE',  ( 3.469446951953635015E-14, 6.982962677686266711E-15, -1.000000000000000000 ) ) ;
#119155=ADVANCED_FACE ( 'NONE', ( #247798 ), #187851, .T. ) ;
#119165=CONICAL_SURFACE ( 'NONE', #219107, 4.049999999999998046, 0.7853981633974604915 ) ;
#119180=EDGE_CURVE ( 'NONE', #47775, #156378, #150114, .T. ) ;
#119190=DIRECTION ( 'NONE',  ( 0.000000000000000000, -1.000000000000000000, -6.982962677686265922E-15 ) ) ;
#119207=EDGE_LOOP ( 'NONE', ( #125796, #92800, #149061, #255277 ) ) ;
#119214=ORIENTED_EDGE ( 'NONE', *, *, #197799, .F. ) ;
#119216=AXIS2_PLACEMENT_3D ( 'NONE', #182366, #4966, #158971 ) ;
#119228=ADVANCED_FACE ( 'NONE', ( #52153 ), #46022, .T. ) ;
#119234=DIRECTION ( 'NONE',  ( -0.000000000000000000, -6.982962677686266711E-15, 1.000000000000000000 ) ) ;
#119242=ADVANCED_FACE ( 'NONE', ( #95147 ), #88208, .T. ) ;
#119277=FACE_OUTER_BOUND ( 'NONE', #257320, .T. ) ;
#119281=DIRECTION ( 'NONE',  ( 0.000000000000000000, 0.000000000000000000, 1.000000000000000000 ) ) ;
#119289=AXIS2_PLACEMENT_3D ( 'NONE', #14808, #248252, #110014 ) ;
#119312=EDGE_LOOP ( 'NONE', ( #91055, #40275, #160285, #254343 ) ) ;
#119343=CARTESIAN_POINT ( 'NONE',  ( -20.64999999999999858, 68.85000000001156195, -57.27310748452436684 ) ) ;
#119347=CARTESIAN_POINT ( 'NONE',  ( 23.25000000000000000, 87.75000000001173817, -81.27310748452423184 ) ) ;
#119350=FACE_OUTER_BOUND ( 'NONE', #212979, .T. ) ;
#119404=DIRECTION ( 'NONE',  ( -4.336808689942052446E-15, 0.8660254037844445918, 0.4999999999999896194 ) ) ;
#119410=CARTESIAN_POINT ( 'NONE',  ( 20.85000000000000142, 77.13501884592155022, -28.30613060109199353 ) ) ;
#119426=ORIENTED_EDGE ( 'NONE', *, *, #47582, .F. ) ;
#119431=AXIS2_PLACEMENT_3D ( 'NONE', #39639, #119150, #198674 ) ;
#119458=CARTESIAN_POINT ( 'NONE',  ( 22.47071067811865319, 76.00000000001165290, -69.52310748452431710 ) ) ;
#119471=ORIENTED_EDGE ( 'NONE', *, *, #158622, .F. ) ;
#119497=VERTEX_POINT ( 'NONE', #81963 ) ;
#119511=AXIS2_PLACEMENT_3D ( 'NONE', #195520, #239755, #215053 ) ;
#119524=DIRECTION ( 'NONE',  ( -1.000000000000000000, -7.304098846218135653E-16, -4.639676173203994055E-30 ) ) ;
#119531=CIRCLE ( 'NONE', #94562, 11.80000000000000426 ) ;
#119542=VECTOR ( 'NONE', #98143, 1000.000000000000000 ) ;
#119594=VERTEX_POINT ( 'NONE', #88392 ) ;
#119609=CARTESIAN_POINT ( 'NONE',  ( -23.25000000000000000, 76.00000000001142553, -36.02310748452432421 ) ) ;
#119641=CARTESIAN_POINT ( 'NONE',  ( 20.85000000000000142, 77.83585931145498193, -24.51866831572578320 ) ) ;
#119647=EDGE_CURVE ( 'NONE', #211829, #33150, #25388, .T. ) ;
#119661=CARTESIAN_POINT ( 'NONE',  ( 18.59999999999998366, 76.00000000001142553, -36.02310748452432421 ) ) ;
#119687=AXIS2_PLACEMENT_3D ( 'NONE', #172596, #52584, #95568 ) ;
#119714=DIRECTION ( 'NONE',  ( -1.000000000000000000, 0.000000000000000000, 0.000000000000000000 ) ) ;
#119762=CARTESIAN_POINT ( 'NONE',  ( 21.04999999999999716, 69.69554417806399726, -69.50207200798423912 ) ) ;
#119782=AXIS2_PLACEMENT_3D ( 'NONE', #107480, #44946, #184444 ) ;
#119841=CARTESIAN_POINT ( 'NONE',  ( -20.12071067811865888, 66.67928932189292368, -57.17310748452438673 ) ) ;
#119848=VERTEX_POINT ( 'NONE', #98644 ) ;
#119874=EDGE_CURVE ( 'NONE', #160781, #171007, #201633, .T. ) ;
#119921=AXIS2_PLACEMENT_3D ( 'NONE', #134673, #16066, #194702 ) ;
#119927=AXIS2_PLACEMENT_3D ( 'NONE', #212179, #192603, #231739 ) ;
#119932=CARTESIAN_POINT ( 'NONE',  ( -22.50000000000000000, 76.00000000001165290, -69.62310748452432563 ) ) ;
#119958=LINE ( 'NONE', #199481, #45424 ) ;
#119959=CARTESIAN_POINT ( 'NONE',  ( 20.84999999999998721, 65.66751761918619934, -30.42826094061123854 ) ) ;
#119974=AXIS2_PLACEMENT_3D ( 'NONE', #246114, #24513, #205679 ) ;
#119986=CARTESIAN_POINT ( 'NONE',  ( 18.40916198585728836, 85.50000000001136868, -29.42291785270129623 ) ) ;
#119993=AXIS2_PLACEMENT_3D ( 'NONE', #147871, #48748, #221596 ) ;
#120042=ORIENTED_EDGE ( 'NONE', *, *, #134585, .T. ) ;
#120044=SURFACE_STYLE_USAGE ( .BOTH. , #44339 ) ;
#120048=CARTESIAN_POINT ( 'NONE',  ( 23.14999999999999858, 76.00000000001141132, -34.02310748452431710 ) ) ;
#120051=ADVANCED_FACE ( 'NONE', ( #79748 ), #172830, .F. ) ;
#120074=CARTESIAN_POINT ( 'NONE',  ( -18.39999999999999858, 85.60000000001139142, -29.42291809330221142 ) ) ;
#120081=CIRCLE ( 'NONE', #207551, 0.1000000000000028644 ) ;
#120086=VERTEX_POINT ( 'NONE', #141044 ) ;
#120097=EDGE_CURVE ( 'NONE', #46294, #173457, #146106, .T. ) ;
#120128=DIRECTION ( 'NONE',  ( 0.000000000000000000, -0.6728971962617172897, 0.7397360091702445128 ) ) ;
#120129=AXIS2_PLACEMENT_3D ( 'NONE', #244130, #64225, #227143 ) ;
#120147=EDGE_LOOP ( 'NONE', ( #152954, #127177, #77855, #36905 ) ) ;
#120182=EDGE_LOOP ( 'NONE', ( #125021, #174784 ) ) ;
#120187=DIRECTION ( 'NONE',  ( 0.000000000000000000, -6.853228547068871147E-15, 1.000000000000000000 ) ) ;
#120205=CARTESIAN_POINT ( 'NONE',  ( -20.64999999999999858, 76.00000000001143974, -37.92310748452432989 ) ) ;
#120276=FACE_OUTER_BOUND ( 'NONE', #122882, .T. ) ;
#120302=ORIENTED_EDGE ( 'NONE', *, *, #122800, .T. ) ;
#120345=ORIENTED_EDGE ( 'NONE', *, *, #235756, .T. ) ;
#120360=CARTESIAN_POINT ( 'NONE',  ( 20.02499999999999858, 66.25000000001151079, -48.27310748452438816 ) ) ;
#120406=EDGE_CURVE ( 'NONE', #32328, #40297, #67420, .T. ) ;
#120427=ORIENTED_EDGE ( 'NONE', *, *, #250348, .F. ) ;
#120445=DIRECTION ( 'NONE',  ( -1.000000000000000000, -0.000000000000000000, 0.000000000000000000 ) ) ;
#120447=ORIENTED_EDGE ( 'NONE', *, *, #152740, .T. ) ;
#120449=CIRCLE ( 'NONE', #107938, 0.1000000000000028644 ) ;
#120452=ADVANCED_FACE ( 'NONE', ( #173496 ), #138139, .T. ) ;
#120476=DIRECTION ( 'NONE',  ( 0.000000000000000000, 0.000000000000000000, 1.000000000000000000 ) ) ;
#120513=CARTESIAN_POINT ( 'NONE',  ( -20.00857864376270001, 66.85000000001150511, -48.27310748452438816 ) ) ;
#120543=CARTESIAN_POINT ( 'NONE',  ( 22.48660254037844197, 64.35000000001164722, -69.57310748452439952 ) ) ;
#120578=SPHERICAL_SURFACE ( 'NONE', #25276, 0.1000000000000000056 ) ;
#120587=DIRECTION ( 'NONE',  ( 0.000000000000000000, 7.056502275159894776E-15, -1.000000000000000000 ) ) ;
#120588=EDGE_CURVE ( 'NONE', #55457, #85029, #129942, .T. ) ;
#120635=ORIENTED_EDGE ( 'NONE', *, *, #186719, .T. ) ;
#120650=DIRECTION ( 'NONE',  ( -1.000000000000000000, 2.952720810173289112E-16, 2.061873921506763405E-30 ) ) ;
#120662=ADVANCED_FACE ( 'NONE', ( #49329 ), #88432, .F. ) ;
#120703=TOROIDAL_SURFACE ( 'NONE', #3969, 0.6000000000000013101, 0.1000000000000000056 ) ;
#120721=ORIENTED_EDGE ( 'NONE', *, *, #122278, .T. ) ;
#120730=DIRECTION ( 'NONE',  ( 0.000000000000000000, 1.000000000000000000, 0.000000000000000000 ) ) ;
#120798=CARTESIAN_POINT ( 'NONE',  ( -23.15000000000000213, 64.25000000001145395, -39.12310748452440379 ) ) ;
#120801=EDGE_LOOP ( 'NONE', ( #177944, #230086, #180710, #234823 ) ) ;
#120822=AXIS2_PLACEMENT_3D ( 'NONE', #256845, #177399, #78252 ) ;
#120827=B_SPLINE_CURVE_WITH_KNOTS ( 'NONE', 3,
 ( #30229, #109733, #15481, #77985, #234496, #237076, #55834, #214940 ),
 .UNSPECIFIED., .F., .F.,
 ( 4, 2, 2, 4 ),
 ( 0.000000000000000000, 0.0001094981963948513511, 0.0002189963927897027021, 0.0004379927855794011216 ),
 .UNSPECIFIED. ) ;
#120830=CIRCLE ( 'NONE', #245699, 0.5000000000000004441 ) ;
#120836=DIRECTION ( 'NONE',  ( -1.000000000000000000, 0.000000000000000000, -0.000000000000000000 ) ) ;
#120838=DIRECTION ( 'NONE',  ( 0.000000000000000000, -1.000000000000000000, -6.352154140967427193E-15 ) ) ;
#120848=VERTEX_POINT ( 'NONE', #99975 ) ;
#120875=CYLINDRICAL_SURFACE ( 'NONE', #61547, 0.1000000000000028644 ) ;
#120896=CARTESIAN_POINT ( 'NONE',  ( 20.13684514580103624, 66.50414460725895083, -61.38007579883958442 ) ) ;
#120938=ORIENTED_EDGE ( 'NONE', *, *, #166481, .T. ) ;
#120944=DIRECTION ( 'NONE',  ( 0.000000000000000000, 2.081668171172181135E-13, -1.000000000000000000 ) ) ;
#120956=DIRECTION ( 'NONE',  ( -1.000000000000000000, -7.304098846218163263E-16, 4.217023435051627211E-16 ) ) ;
#121011=DIRECTION ( 'NONE',  ( 0.000000000000000000, -1.000000000000000000, -6.982962677686265922E-15 ) ) ;
#121024=DIRECTION ( 'NONE',  ( 0.000000000000000000, 0.000000000000000000, -1.000000000000000000 ) ) ;
#121075=LINE ( 'NONE', #182316, #91925 ) ;
#121084=VERTEX_POINT ( 'NONE', #111569 ) ;
#121097=CARTESIAN_POINT ( 'NONE',  ( 21.05000000000000071, 87.48912529308749697, -38.92310748452424463 ) ) ;
#121099=ORIENTED_EDGE ( 'NONE', *, *, #16551, .F. ) ;
#121121=AXIS2_PLACEMENT_3D ( 'NONE', #22407, #101891, #2802 ) ;
#121123=CARTESIAN_POINT ( 'NONE',  ( 22.39999999999999503, 76.10000000001174669, -81.17267829206912211 ) ) ;
#121160=FACE_OUTER_BOUND ( 'NONE', #227852, .T. ) ;
#121185=CARTESIAN_POINT ( 'NONE',  ( -21.05000000000000071, 74.63912941281955682, -61.45010955743337178 ) ) ;
#121197=ORIENTED_EDGE ( 'NONE', *, *, #62428, .F. ) ;
#121212=CARTESIAN_POINT ( 'NONE',  ( -21.05000000000000071, 69.74218538953553548, -69.62089777583315708 ) ) ;
#121217=VERTEX_POINT ( 'NONE', #251059 ) ;
#121225=EDGE_CURVE ( 'NONE', #171894, #90093, #34501, .T. ) ;
#121227=DIRECTION ( 'NONE',  ( 0.000000000000000000, 0.8660254037844420383, -0.4999999999999943379 ) ) ;
#121256=CARTESIAN_POINT ( 'NONE',  ( 23.24999999999997513, 64.25000000001146816, -43.03791325517834565 ) ) ;
#121264=EDGE_CURVE ( 'NONE', #221530, #177661, #55282, .T. ) ;
#121265=AXIS2_PLACEMENT_3D ( 'NONE', #43839, #123375, #98626 ) ;
#121319=CARTESIAN_POINT ( 'NONE',  ( 23.25000000000000000, 85.00000000001159606, -59.62913836187181715 ) ) ;
#121413=EDGE_LOOP ( 'NONE', ( #123765, #58705, #36806, #236587 ) ) ;
#121415=ORIENTED_EDGE ( 'NONE', *, *, #87850, .F. ) ;
#121416=LINE ( 'NONE', #1412, #152857 ) ;
#121432=VERTEX_POINT ( 'NONE', #167410 ) ;
#121449=CARTESIAN_POINT ( 'NONE',  ( -23.15000000000000213, 76.00000000001142553, -36.02310748452432421 ) ) ;
#121480=DIRECTION ( 'NONE',  ( -1.836970198721029934E-16, -1.000000000000000000, -6.982962677686266711E-15 ) ) ;
#121510=DIRECTION ( 'NONE',  ( -1.000000000000000000, 0.000000000000000000, -0.000000000000000000 ) ) ;
#121517=ADVANCED_FACE ( 'NONE', ( #254599 ), #155564, .T. ) ;
#121519=AXIS2_PLACEMENT_3D ( 'NONE', #176010, #75625, #116026 ) ;
#121580=CIRCLE ( 'NONE', #9112, 0.1000000000000028644 ) ;
#121590=DIRECTION ( 'NONE',  ( 0.000000000000000000, 6.982962677686266711E-15, -1.000000000000000000 ) ) ;
#121594=TOROIDAL_SURFACE ( 'NONE', #96586, 11.65000000000000036, 0.1000000000000000056 ) ;
#121615=FACE_OUTER_BOUND ( 'NONE', #235043, .T. ) ;
#121657=DIRECTION ( 'NONE',  ( 1.000000000000000000, 0.000000000000000000, 0.000000000000000000 ) ) ;
#121665=ORIENTED_EDGE ( 'NONE', *, *, #220452, .F. ) ;
#121688=EDGE_LOOP ( 'NONE', ( #79662, #3337, #41598, #159145 ) ) ;
#121691=DIRECTION ( 'NONE',  ( 0.000000000000000000, 6.982962677686266711E-15, -1.000000000000000000 ) ) ;
#121692=DIRECTION ( 'NONE',  ( 0.000000000000000000, 0.5000000000000729417, 0.8660254037843965191 ) ) ;
#121715=EDGE_LOOP ( 'NONE', ( #248721, #110441, #73386, #241967 ) ) ;
#121755=AXIS2_PLACEMENT_3D ( 'NONE', #138101, #178565, #139382 ) ;
#121767=FACE_OUTER_BOUND ( 'NONE', #184868, .T. ) ;
#121805=CARTESIAN_POINT ( 'NONE',  ( 18.47149038651511432, 85.67145715801805750, -29.35032114978585227 ) ) ;
#121815=CARTESIAN_POINT ( 'NONE',  ( 21.46681500598040415, 76.00000000001170974, -76.38061864395039890 ) ) ;
#121839=CARTESIAN_POINT ( 'NONE',  ( -21.07928932188134041, 75.90110485435729970, -75.85162414091762173 ) ) ;
#121852=EDGE_CURVE ( 'NONE', #13038, #196986, #126418, .T. ) ;
#121853=AXIS2_PLACEMENT_3D ( 'NONE', #151760, #14820, #115177 ) ;
#121870=CYLINDRICAL_SURFACE ( 'NONE', #4008, 0.1000000000000028644 ) ;
#121899=ADVANCED_FACE ( 'NONE', ( #245695 ), #27968, .T. ) ;
#121900=VERTEX_POINT ( 'NONE', #127029 ) ;
#121914=AXIS2_PLACEMENT_3D ( 'NONE', #71143, #193640, #55366 ) ;
#121932=ORIENTED_EDGE ( 'NONE', *, *, #162515, .T. ) ;
#121934=CARTESIAN_POINT ( 'NONE',  ( -21.05000000000000071, 76.00000000001142553, -36.02310748452432421 ) ) ;
#121953=ORIENTED_EDGE ( 'NONE', *, *, #237634, .F. ) ;
#121957=ORIENTED_EDGE ( 'NONE', *, *, #136993, .F. ) ;
#121981=ORIENTED_EDGE ( 'NONE', *, *, #36091, .F. ) ;
#121990=DIRECTION ( 'NONE',  ( -1.000000000000000000, 0.000000000000000000, 0.000000000000000000 ) ) ;
#121991=VERTEX_POINT ( 'NONE', #110030 ) ;
#122004=DIRECTION ( 'NONE',  ( -1.000000000000000000, 0.000000000000000000, 0.000000000000000000 ) ) ;
#122013=CARTESIAN_POINT ( 'NONE',  ( -22.49756042579671700, 75.92195366299456794, -81.17297244562665526 ) ) ;
#122033=ADVANCED_FACE ( 'NONE', ( #199865 ), #154349, .F. ) ;
#122035=CIRCLE ( 'NONE', #217873, 0.09999999999999820144 ) ;
#122046=ORIENTED_EDGE ( 'NONE', *, *, #190468, .T. ) ;
#122059=VECTOR ( 'NONE', #246041, 1000.000000000000000 ) ;
#122062=CARTESIAN_POINT ( 'NONE',  ( 18.49999999999999645, 74.83729825007360148, -61.42310748452432989 ) ) ;
#122102=CARTESIAN_POINT ( 'NONE',  ( 21.05000000000000071, 70.60000000001151932, -48.42837350343745584 ) ) ;
#122139=EDGE_LOOP ( 'NONE', ( #187641, #102535 ) ) ;
#122159=DIRECTION ( 'NONE',  ( -1.000000000000000000, 0.000000000000000000, -0.000000000000000000 ) ) ;
#122192=TOROIDAL_SURFACE ( 'NONE', #230318, 0.9750000000000019762, 0.1000000000000000056 ) ;
#122199=EDGE_LOOP ( 'NONE', ( #53139, #6448, #181942, #178198 ) ) ;
#122231=CARTESIAN_POINT ( 'NONE',  ( -18.50000000000000000, 70.65875701002008213, -79.32975769101238939 ) ) ;
#122236=ORIENTED_EDGE ( 'NONE', *, *, #191910, .T. ) ;
#122258=ADVANCED_FACE ( 'NONE', ( #109711 ), #107153, .F. ) ;
#122267=CARTESIAN_POINT ( 'NONE',  ( -23.15000000000000213, 76.00000000001141132, -34.02310748452431710 ) ) ;
#122278=EDGE_CURVE ( 'NONE', #130839, #245547, #20933, .T. ) ;
#122334=AXIS2_PLACEMENT_3D ( 'NONE', #107815, #127385, #85645 ) ;
#122357=DIRECTION ( 'NONE',  ( -0.000000000000000000, 1.000000000000000000, 6.352154140967427193E-15 ) ) ;
#122359=ORIENTED_EDGE ( 'NONE', *, *, #88852, .T. ) ;
#122366=CYLINDRICAL_SURFACE ( 'NONE', #152834, 7.900000000000000355 ) ;
#122370=ORIENTED_EDGE ( 'NONE', *, *, #151440, .F. ) ;
#122374=FACE_OUTER_BOUND ( 'NONE', #45051, .T. ) ;
#122410=CARTESIAN_POINT ( 'NONE',  ( 21.76363531954645936, 68.98706345213993529, -69.62210935882382046 ) ) ;
#122452=ORIENTED_EDGE ( 'NONE', *, *, #252051, .T. ) ;
#122481=CARTESIAN_POINT ( 'NONE',  ( -18.50000000000000000, 77.68707439010330518, -82.33768045106596389 ) ) ;
#122489=DIRECTION ( 'NONE',  ( 0.000000000000000000, -6.982962677686266711E-15, 1.000000000000000000 ) ) ;
#122495=ADVANCED_FACE ( 'NONE', ( #82123 ), #101680, .F. ) ;
#122539=CARTESIAN_POINT ( 'NONE',  ( -21.00023020733438628, 69.60913075474394418, -69.52310748452435973 ) ) ;
#122545=CARTESIAN_POINT ( 'NONE',  ( -21.05000000000000071, 76.00000000001168132, -73.82310748452428584 ) ) ;
#122570=CIRCLE ( 'NONE', #51591, 12.87499999999999822 ) ;
#122579=CARTESIAN_POINT ( 'NONE',  ( -23.15000000000000213, 74.00000000001151079, -49.24772940728643533 ) ) ;
#122586=ADVANCED_FACE ( 'NONE', ( #185106 ), #142122, .T. ) ;
#122588=AXIS2_PLACEMENT_3D ( 'NONE', #78457, #172488, #52465 ) ;
#122601=VERTEX_POINT ( 'NONE', #43037 ) ;
#122611=AXIS2_PLACEMENT_3D ( 'NONE', #126987, #164839, #142673 ) ;
#122617=AXIS2_PLACEMENT_3D ( 'NONE', #311, #79832, #12523 ) ;
#122621=VERTEX_POINT ( 'NONE', #9035 ) ;
#122696=VERTEX_POINT ( 'NONE', #187695 ) ;
#122730=ORIENTED_EDGE ( 'NONE', *, *, #189806, .T. ) ;
#122741=CARTESIAN_POINT ( 'NONE',  ( 20.94999999999999929, 76.00000000001142553, -36.02310748452432421 ) ) ;
#122742=AXIS2_PLACEMENT_3D ( 'NONE', #130888, #133465, #229991 ) ;
#122755=CARTESIAN_POINT ( 'NONE',  ( 20.94999999999999929, 76.00000000001165290, -69.52310748452431710 ) ) ;
#122757=ORIENTED_EDGE ( 'NONE', *, *, #74740, .F. ) ;
#122762=CARTESIAN_POINT ( 'NONE',  ( 19.58285714285715073, 65.61500148966017321, -61.89342281713445004 ) ) ;
#122788=LINE ( 'NONE', #81046, #232806 ) ;
#122800=EDGE_CURVE ( 'NONE', #139895, #199876, #56025, .T. ) ;
#122801=DIRECTION ( 'NONE',  ( 0.5000000000001141309, -6.047423072554455661E-15, 0.8660254037843729824 ) ) ;
#122818=ORIENTED_EDGE ( 'NONE', *, *, #99946, .F. ) ;
#122835=CARTESIAN_POINT ( 'NONE',  ( -21.05000000000000071, 77.85102823015243700, -57.86919421510181394 ) ) ;
#122882=EDGE_LOOP ( 'NONE', ( #197044, #71573, #92453, #209621 ) ) ;
#122899=AXIS2_PLACEMENT_3D ( 'NONE', #92354, #171943, #231895 ) ;
#122904=CARTESIAN_POINT ( 'NONE',  ( -18.50000000000000000, 76.00000000001142553, -36.02310748452432421 ) ) ;
#122910=LINE ( 'NONE', #79883, #176951 ) ;
#122922=CARTESIAN_POINT ( 'NONE',  ( -18.42637059832564361, 85.49694546190107758, -29.41403017472442727 ) ) ;
#122969=EDGE_LOOP ( 'NONE', ( #202850, #59738, #68070, #55521, #242880, #222124 ) ) ;
#122978=ADVANCED_FACE ( 'NONE', ( #28000 ), #38932, .T. ) ;
#122980=EDGE_LOOP ( 'NONE', ( #37016, #199838, #117833, #190598 ) ) ;
#123014=ORIENTED_EDGE ( 'NONE', *, *, #227116, .F. ) ;
#123015=TOROIDAL_SURFACE ( 'NONE', #10594, 0.2000000000000000111, 0.1000000000000000056 ) ;
#123019=EDGE_CURVE ( 'NONE', #189058, #112680, #192193, .T. ) ;
#123039=DIRECTION ( 'NONE',  ( 0.000000000000000000, 0.000000000000000000, 1.000000000000000000 ) ) ;
#123060=EDGE_CURVE ( 'NONE', #198432, #65850, #14849, .T. ) ;
#123084=CARTESIAN_POINT ( 'NONE',  ( 20.95035502843362707, 65.52236167323513882, -61.94680777578801667 ) ) ;
#123091=VECTOR ( 'NONE', #116163, 1000.000000000000000 ) ;
#123098=ORIENTED_EDGE ( 'NONE', *, *, #177768, .F. ) ;
#123107=EDGE_CURVE ( 'NONE', #41808, #30729, #33146, .T. ) ;
#123123=CARTESIAN_POINT ( 'NONE',  ( 21.07964655665547582, 67.22511038503301961, -57.30119090156032513 ) ) ;
#123155=ORIENTED_EDGE ( 'NONE', *, *, #185225, .F. ) ;
#123163=ORIENTED_EDGE ( 'NONE', *, *, #103292, .T. ) ;
#123302=CARTESIAN_POINT ( 'NONE',  ( 20.94999999999999574, 74.73821383144657204, -61.43660852097884373 ) ) ;
#123322=EDGE_CURVE ( 'NONE', #241487, #20464, #239015, .T. ) ;
#123375=DIRECTION ( 'NONE',  ( 1.000000000000000000, 0.000000000000000000, 0.000000000000000000 ) ) ;
#123441=FACE_OUTER_BOUND ( 'NONE', #41183, .T. ) ;
#123467=CARTESIAN_POINT ( 'NONE',  ( 18.59999999999999076, 64.35000000001147669, -44.77310748452440237 ) ) ;
#123485=DIRECTION ( 'NONE',  ( 1.000000000000000000, 0.000000000000000000, 0.000000000000000000 ) ) ;
#123491=CIRCLE ( 'NONE', #102605, 4.000000000000003553 ) ;
#123493=DIRECTION ( 'NONE',  ( 0.000000000000000000, 0.000000000000000000, 1.000000000000000000 ) ) ;
#123529=CIRCLE ( 'NONE', #77521, 11.75000000000000000 ) ;
#123530=AXIS2_PLACEMENT_3D ( 'NONE', #8549, #9825, #151935 ) ;
#123532=CIRCLE ( 'NONE', #235959, 0.2000000000000057288 ) ;
#123545=EDGE_CURVE ( 'NONE', #239074, #8048, #18438, .T. ) ;
#123584=DIRECTION ( 'NONE',  ( 0.000000000000000000, -0.9908441862701605762, -0.1350103645451835310 ) ) ;
#123604=AXIS2_PLACEMENT_3D ( 'NONE', #165412, #210952, #50562 ) ;
#123606=EDGE_LOOP ( 'NONE', ( #239695, #197026, #29558, #153609 ) ) ;
#123609=DIRECTION ( 'NONE',  ( 0.000000000000000000, 1.000000000000000000, 1.387778780781444413E-14 ) ) ;
#123622=EDGE_LOOP ( 'NONE', ( #187800, #123832, #88291, #64813 ) ) ;
#123640=EDGE_LOOP ( 'NONE', ( #61135, #132904, #216084, #44681 ) ) ;
#123644=VECTOR ( 'NONE', #190765, 1000.000000000000000 ) ;
#123650=DIRECTION ( 'NONE',  ( 1.000000000000000000, -7.304098846218133681E-16, -4.639676173203992654E-30 ) ) ;
#123673=DIRECTION ( 'NONE',  ( 0.000000000000000000, 0.9999631594459055250, 0.008583690987131395445 ) ) ;
#123692=DIRECTION ( 'NONE',  ( 1.000000000000000000, 0.000000000000000000, 0.000000000000000000 ) ) ;
#123698=DIRECTION ( 'NONE',  ( -3.265361837132813093E-16, -1.000000000000000000, -7.026728003956683390E-15 ) ) ;
#123704=AXIS2_PLACEMENT_3D ( 'NONE', #113818, #53855, #172571 ) ;
#123720=DIRECTION ( 'NONE',  ( 1.000000000000000000, 0.000000000000000000, 0.000000000000000000 ) ) ;
#123735=EDGE_CURVE ( 'NONE', #136422, #149532, #10057, .T. ) ;
#123743=DIRECTION ( 'NONE',  ( 0.000000000000000000, 0.000000000000000000, -1.000000000000000000 ) ) ;
#123755=DIRECTION ( 'NONE',  ( 0.000000000000000000, 0.000000000000000000, 1.000000000000000000 ) ) ;
#123765=ORIENTED_EDGE ( 'NONE', *, *, #242913, .F. ) ;
#123767=DIRECTION ( 'NONE',  ( -1.000000000000000000, 0.000000000000000000, 0.000000000000000000 ) ) ;
#123793=PRODUCT_DEFINITION_FORMATION_WITH_SPECIFIED_SOURCE ( 'ANY', '', #26382, .NOT_KNOWN. ) ;
#123797=CARTESIAN_POINT ( 'NONE',  ( 23.15000000000000213, 87.65000000001165859, -69.52310748452424605 ) ) ;
#123817=CARTESIAN_POINT ( 'NONE',  ( -21.93340585972066137, 68.67585297715831416, -69.52310748452435973 ) ) ;
#123826=CARTESIAN_POINT ( 'NONE',  ( -20.54999999999999716, 76.00000000001141132, -34.02310748452431710 ) ) ;
#123832=ORIENTED_EDGE ( 'NONE', *, *, #223017, .F. ) ;
#123835=DIRECTION ( 'NONE',  ( -1.000000000000000000, 0.000000000000000000, 0.000000000000000000 ) ) ;
#123848=AXIS2_PLACEMENT_3D ( 'NONE', #151264, #230807, #89975 ) ;
#123855=ORIENTED_EDGE ( 'NONE', *, *, #17070, .F. ) ;
#123866=DIRECTION ( 'NONE',  ( 0.000000000000000000, -6.853228547068871147E-15, 1.000000000000000000 ) ) ;
#123887=CYLINDRICAL_SURFACE ( 'NONE', #13927, 0.1000000000000052097 ) ;
#123912=DIRECTION ( 'NONE',  ( 1.000000000000000000, 0.000000000000000000, 0.000000000000000000 ) ) ;
#123932=DIRECTION ( 'NONE',  ( 0.000000000000000000, -6.938893903907234689E-15, 1.000000000000000000 ) ) ;
#123941=ORIENTED_EDGE ( 'NONE', *, *, #74069, .T. ) ;
#123957=FACE_OUTER_BOUND ( 'NONE', #230919, .T. ) ;
#123988=CARTESIAN_POINT ( 'NONE',  ( -20.54999999999999716, 73.60000000001151932, -49.24772940728643533 ) ) ;
#123989=CARTESIAN_POINT ( 'NONE',  ( 20.85000000000000142, 77.83585931145498193, -24.51866831572578675 ) ) ;
#123992=CYLINDRICAL_SURFACE ( 'NONE', #248227, 0.8750000000000007772 ) ;
#124008=AXIS2_PLACEMENT_3D ( 'NONE', #3604, #21900, #45308 ) ;
#124025=CARTESIAN_POINT ( 'NONE',  ( -20.94999999999999929, 77.83534155023598089, -57.96795619196132776 ) ) ;
#124028=CARTESIAN_POINT ( 'NONE',  ( 20.94999999999999574, 87.65000000001163016, -66.62310748452424036 ) ) ;
#124031=FACE_OUTER_BOUND ( 'NONE', #72591, .T. ) ;
#124056=ORIENTED_EDGE ( 'NONE', *, *, #228179, .F. ) ;
#124081=CIRCLE ( 'NONE', #32527, 0.09999999999999939493 ) ;
#124088=CARTESIAN_POINT ( 'NONE',  ( 22.50927854361893310, 76.10085807353952703, -81.27267461055122055 ) ) ;
#124100=VECTOR ( 'NONE', #222482, 1000.000000000000000 ) ;
#124126=CIRCLE ( 'NONE', #228166, 0.1000000000000028644 ) ;
#124128=CARTESIAN_POINT ( 'NONE',  ( 21.05000000000000071, 76.00000000001156764, -57.37310748452432563 ) ) ;
#124266=DIRECTION ( 'NONE',  ( -1.000000000000000000, 0.000000000000000000, -0.000000000000000000 ) ) ;
#124309=VERTEX_POINT ( 'NONE', #34779 ) ;
#124314=CARTESIAN_POINT ( 'NONE',  ( 21.04999999999987637, 65.39167043205816299, -61.93142247122878530 ) ) ;
#124359=CARTESIAN_POINT ( 'NONE',  ( -20.85000000000000142, 76.00000000001142553, -36.02310748452432421 ) ) ;
#124364=ADVANCED_FACE ( 'NONE', ( #174309 ), #253773, .F. ) ;
#124366=DIRECTION ( 'NONE',  ( -1.000000000000000000, -0.000000000000000000, -0.000000000000000000 ) ) ;
#124372=ORIENTED_EDGE ( 'NONE', *, *, #40008, .F. ) ;
#124381=TOROIDAL_SURFACE ( 'NONE', #140950, 0.6000000000000004219, 0.1000000000000000056 ) ;
#124393=CARTESIAN_POINT ( 'NONE',  ( 20.85000000000000142, 77.83585931145498193, -24.41866831572578178 ) ) ;
#124411=DIRECTION ( 'NONE',  ( 0.000000000000000000, 0.000000000000000000, 1.000000000000000000 ) ) ;
#124419=CIRCLE ( 'NONE', #232748, 11.65000000000000036 ) ;
#124432=VERTEX_POINT ( 'NONE', #42442 ) ;
#124435=DIRECTION ( 'NONE',  ( 0.000000000000000000, 0.000000000000000000, 1.000000000000000000 ) ) ;
#124436=EDGE_CURVE ( 'NONE', #189565, #251301, #210352, .T. ) ;
#124457=CARTESIAN_POINT ( 'NONE',  ( -23.25000000000000000, 64.35000000001150511, -48.27310748452440237 ) ) ;
#124473=DIRECTION ( 'NONE',  ( -1.000000000000000000, 0.000000000000000000, -0.000000000000000000 ) ) ;
#124486=CARTESIAN_POINT ( 'NONE',  ( 21.14999999999999858, 64.35000000001173248, -81.27310748452440237 ) ) ;
#124492=CARTESIAN_POINT ( 'NONE',  ( 21.09610168723073187, 75.96641049312022176, -75.90206319974912219 ) ) ;
#124521=ORIENTED_EDGE ( 'NONE', *, *, #135832, .F. ) ;
#124533=AXIS2_PLACEMENT_3D ( 'NONE', #131504, #186364, #91098 ) ;
#124545=DIRECTION ( 'NONE',  ( 0.000000000000000000, -6.982962677686266711E-15, 1.000000000000000000 ) ) ;
#124551=ORIENTED_EDGE ( 'NONE', *, *, #238319, .F. ) ;
#124563=EDGE_LOOP ( 'NONE', ( #75583, #160625, #12382, #108918 ) ) ;
#124569=CARTESIAN_POINT ( 'NONE',  ( 23.25000000000000000, 64.25000000001151079, -48.17310748452440805 ) ) ;
#124573=AXIS2_PLACEMENT_3D ( 'NONE', #175712, #71478, #173174 ) ;
#124577=VERTEX_POINT ( 'NONE', #247050 ) ;
#124582=VERTEX_POINT ( 'NONE', #86679 ) ;
#124591=CARTESIAN_POINT ( 'NONE',  ( -22.47120815636973745, 75.97109617810785664, -81.17303947327782510 ) ) ;
#124664=LINE ( 'NONE', #67245, #180152 ) ;
#124679=CARTESIAN_POINT ( 'NONE',  ( 19.97071067695833690, 64.27928932305314902, -44.84685405172082540 ) ) ;
#124680=ORIENTED_EDGE ( 'NONE', *, *, #109815, .T. ) ;
#124689=ORIENTED_EDGE ( 'NONE', *, *, #149901, .F. ) ;
#124726=LINE ( 'NONE', #252332, #8488 ) ;
#124777=ORIENTED_EDGE ( 'NONE', *, *, #18115, .F. ) ;
#124778=CARTESIAN_POINT ( 'NONE',  ( 20.99749315643149217, 64.25000000001146816, -43.03791325328343476 ) ) ;
#124790=DIRECTION ( 'NONE',  ( 0.000000000000000000, 0.000000000000000000, 1.000000000000000000 ) ) ;
#124793=CARTESIAN_POINT ( 'NONE',  ( -23.25000000000000000, 71.75000000001151079, -48.37310748452435405 ) ) ;
#124818=DIRECTION ( 'NONE',  ( 1.000000000000000000, 0.000000000000000000, 0.000000000000000000 ) ) ;
#124835=AXIS2_PLACEMENT_3D ( 'NONE', #212259, #33657, #133978 ) ;
#124843=DIRECTION ( 'NONE',  ( -3.265361837132813093E-16, -1.000000000000000000, -6.982962677686266711E-15 ) ) ;
#124906=AXIS2_PLACEMENT_3D ( 'NONE', #251770, #87860, #193095 ) ;
#124942=DIRECTION ( 'NONE',  ( 1.000000000000000000, 0.000000000000000000, 0.000000000000000000 ) ) ;
#124948=CIRCLE ( 'NONE', #45830, 0.1000000000000028644 ) ;
#124949=EDGE_CURVE ( 'NONE', #147021, #186245, #181503, .T. ) ;
#124957=CARTESIAN_POINT ( 'NONE',  ( 21.14999999999999503, 76.10000000001174669, -81.17267829206912211 ) ) ;
#124959=DIRECTION ( 'NONE',  ( 0.000000000000000000, 0.000000000000000000, 1.000000000000000000 ) ) ;
#124963=DIRECTION ( 'NONE',  ( -4.801466763864314121E-15, 0.2605042016806606298, 0.9654727137038736640 ) ) ;
#124975=CARTESIAN_POINT ( 'NONE',  ( -23.25000000000000000, 87.65000000001144542, -39.02310748452423894 ) ) ;
#124990=DIRECTION ( 'NONE',  ( 0.000000000000000000, 0.000000000000000000, -1.000000000000000000 ) ) ;
#125003=ORIENTED_EDGE ( 'NONE', *, *, #200030, .T. ) ;
#125011=EDGE_LOOP ( 'NONE', ( #138427, #19253, #237565 ) ) ;
#125021=ORIENTED_EDGE ( 'NONE', *, *, #241375, .T. ) ;
#125022=CIRCLE ( 'NONE', #104141, 11.70000000000000284 ) ;
#125029=ORIENTED_EDGE ( 'NONE', *, *, #176001, .T. ) ;
#125042=ORIENTED_EDGE ( 'NONE', *, *, #118864, .T. ) ;
#125063=DIRECTION ( 'NONE',  ( 0.000000000000000000, 6.938893903907229955E-15, -1.000000000000000000 ) ) ;
#125089=VECTOR ( 'NONE', #194643, 1000.000000000000000 ) ;
#125144=LINE ( 'NONE', #24779, #246697 ) ;
#125146=DIRECTION ( 'NONE',  ( 0.000000000000000000, 7.056502275159894776E-15, -1.000000000000000000 ) ) ;
#125151=CARTESIAN_POINT ( 'NONE',  ( 23.24999999999999289, 80.15000000001165859, -69.52310748452430289 ) ) ;
#125155=EDGE_LOOP ( 'NONE', ( #188414, #160621, #132520, #235475 ) ) ;
#125187=CARTESIAN_POINT ( 'NONE',  ( -18.59999999999999787, 74.65925378207803931, -79.79596998994550461 ) ) ;
#125190=EDGE_CURVE ( 'NONE', #169291, #171894, #249848, .T. ) ;
#125192=DIRECTION ( 'NONE',  ( 2.694716079187273439E-16, 1.000000000000000000, 7.006261805886910842E-15 ) ) ;
#125198=DIRECTION ( 'NONE',  ( -0.000000000000000000, 1.000000000000000000, 6.982962677686266711E-15 ) ) ;
#125229=DIRECTION ( 'NONE',  ( -0.000000000000000000, -1.000000000000000000, -6.982962677686266711E-15 ) ) ;
#125234=ORIENTED_EDGE ( 'NONE', *, *, #78665, .T. ) ;
#125242=CARTESIAN_POINT ( 'NONE',  ( -18.59999999999999787, 66.75000000001151079, -48.37310748452438247 ) ) ;
#125244=EDGE_CURVE ( 'NONE', #233936, #201514, #81486, .T. ) ;
#125249=CIRCLE ( 'NONE', #175187, 0.09999999999999939493 ) ;
#125252=EDGE_CURVE ( 'NONE', #238213, #202854, #223164, .T. ) ;
#125272=DIRECTION ( 'NONE',  ( 0.000000000000000000, 1.000000000000000000, 6.982962677686266711E-15 ) ) ;
#125295=CARTESIAN_POINT ( 'NONE',  ( 21.00000000000000000, 66.25000000001158185, -57.17310748452438673 ) ) ;
#125310=ORIENTED_EDGE ( 'NONE', *, *, #213063, .T. ) ;
#125321=AXIS2_PLACEMENT_3D ( 'NONE', #4573, #223618, #68426 ) ;
#125380=AXIS2_PLACEMENT_3D ( 'NONE', #220905, #203926, #42293 ) ;
#125383=CYLINDRICAL_SURFACE ( 'NONE', #207436, 0.09999999999999939493 ) ;
#125418=CIRCLE ( 'NONE', #150364, 11.65000000000000036 ) ;
#125421=CARTESIAN_POINT ( 'NONE',  ( -18.50000000000000000, 85.40000000001138858, -29.14106563635158764 ) ) ;
#125426=ORIENTED_EDGE ( 'NONE', *, *, #111549, .T. ) ;
#125489=TOROIDAL_SURFACE ( 'NONE', #200504, 11.89999999999999858, 0.1000000000000000056 ) ;
#125501=EDGE_LOOP ( 'NONE', ( #42236, #89355, #113965, #60104, #135430, #152635, #162347, #44516 ) ) ;
#125511=EDGE_CURVE ( 'NONE', #40297, #729, #127505, .T. ) ;
#125513=ORIENTED_EDGE ( 'NONE', *, *, #30, .F. ) ;
#125549=DIRECTION ( 'NONE',  ( 0.000000000000000000, 6.577889128801591149E-15, -1.000000000000000000 ) ) ;
#125561=DIRECTION ( 'NONE',  ( 1.000000000000000000, 1.110223024625155531E-13, 0.000000000000000000 ) ) ;
#125565=DIRECTION ( 'NONE',  ( 1.000000000000000000, -3.265361837132813093E-16, -2.280189983783949500E-30 ) ) ;
#125567=ADVANCED_FACE ( 'NONE', ( #114789 ), #211327, .T. ) ;
#125579=DIRECTION ( 'NONE',  ( 0.000000000000000000, -7.109473446599835262E-15, 1.000000000000000000 ) ) ;
#125617=EDGE_CURVE ( 'NONE', #102370, #81005, #112328, .T. ) ;
#125639=FACE_OUTER_BOUND ( 'NONE', #256361, .T. ) ;
#125674=CARTESIAN_POINT ( 'NONE',  ( -21.11101077989000174, 75.98471473109741225, -75.94679221925045454 ) ) ;
#125679=DIRECTION ( 'NONE',  ( 1.000000000000000000, 0.000000000000000000, 0.000000000000000000 ) ) ;
#125728=AXIS2_PLACEMENT_3D ( 'NONE', #49999, #70881, #150404 ) ;
#125733=DIRECTION ( 'NONE',  ( 0.000000000000000000, 0.000000000000000000, -1.000000000000000000 ) ) ;
#125741=CARTESIAN_POINT ( 'NONE',  ( 20.94999999999999929, 69.35000000001151932, -48.27310748452436684 ) ) ;
#125773=DIRECTION ( 'NONE',  ( 0.000000000000000000, 6.982962677686266711E-15, -1.000000000000000000 ) ) ;
#125779=VECTOR ( 'NONE', #21882, 1000.000000000000000 ) ;
#125796=ORIENTED_EDGE ( 'NONE', *, *, #190774, .T. ) ;
#125797=AXIS2_PLACEMENT_3D ( 'NONE', #248263, #189585, #50054 ) ;
#125809=EDGE_CURVE ( 'NONE', #159302, #216065, #252752, .T. ) ;
#125879=DIRECTION ( 'NONE',  ( 1.000000000000000000, 0.000000000000000000, 0.000000000000000000 ) ) ;
#125881=ADVANCED_FACE ( 'NONE', ( #176715 ), #81850, .T. ) ;
#125884=ORIENTED_EDGE ( 'NONE', *, *, #224938, .F. ) ;
#125917=VERTEX_POINT ( 'NONE', #58007 ) ;
#125938=CARTESIAN_POINT ( 'NONE',  ( 19.86930884467584946, 64.31308993304044463, -44.78388484558566773 ) ) ;
#125951=EDGE_LOOP ( 'NONE', ( #30876, #98642, #63092, #6409 ) ) ;
#125965=CARTESIAN_POINT ( 'NONE',  ( 23.24999999999999645, 76.00000000001142553, -36.02310748452432421 ) ) ;
#125973=DIRECTION ( 'NONE',  ( -0.000000000000000000, 1.000000000000000000, 6.352154140967427193E-15 ) ) ;
#126026=DIRECTION ( 'NONE',  ( 2.952720810173289605E-16, 1.000000000000000000, 7.086529944415894657E-15 ) ) ;
#126035=CARTESIAN_POINT ( 'NONE',  ( 20.94999999999999929, 64.25000000001146816, -42.80697314750248950 ) ) ;
#126043=CYLINDRICAL_SURFACE ( 'NONE', #24205, 2.000000000000001776 ) ;
#126110=DIRECTION ( 'NONE',  ( 0.000000000000000000, 6.982962677686267499E-15, -1.000000000000000000 ) ) ;
#126163=CARTESIAN_POINT ( 'NONE',  ( -20.94999999999999929, 74.16465844978715438, -57.96795619196134908 ) ) ;
#126191=DIRECTION ( 'NONE',  ( 1.000000000000000000, 0.000000000000000000, 0.000000000000000000 ) ) ;
#126215=ORIENTED_EDGE ( 'NONE', *, *, #16887, .T. ) ;
#126223=DIRECTION ( 'NONE',  ( 1.000000000000000000, 0.000000000000000000, 0.000000000000000000 ) ) ;
#126228=ADVANCED_FACE ( 'NONE', ( #231256 ), #232130, .T. ) ;
#126256=CIRCLE ( 'NONE', #13834, 0.1999999999999987899 ) ;
#126283=DIRECTION ( 'NONE',  ( 0.000000000000000000, -1.000000000000000000, -6.982962677686265922E-15 ) ) ;
#126291=CARTESIAN_POINT ( 'NONE',  ( 21.05000000000000071, 76.00000000001142553, -36.02310748452432421 ) ) ;
#126418=CIRCLE ( 'NONE', #76522, 0.1000000000000028644 ) ;
#126430=CARTESIAN_POINT ( 'NONE',  ( 18.59999999999999787, 74.13328508995425636, -57.77043223824233564 ) ) ;
#126439=DIRECTION ( 'NONE',  ( 0.000000000000000000, 0.9908441862701605762, -0.1350103645451835310 ) ) ;
#126461=AXIS2_PLACEMENT_3D ( 'NONE', #76647, #156220, #58344 ) ;
#126476=ADVANCED_FACE ( 'NONE', ( #47127 ), #49720, .F. ) ;
#126491=CIRCLE ( 'NONE', #197395, 0.1000000000000043771 ) ;
#126503=TOROIDAL_SURFACE ( 'NONE', #159833, 7.800000000000000711, 0.1000000000000000056 ) ;
#126512=VERTEX_POINT ( 'NONE', #54837 ) ;
#126518=CARTESIAN_POINT ( 'NONE',  ( 20.46382478191414833, 65.40137955871422548, -61.84529301517892463 ) ) ;
#126542=EDGE_LOOP ( 'NONE', ( #206363, #58950, #237940, #141255 ) ) ;
#126550=DIRECTION ( 'NONE',  ( 1.000000000000000000, 0.000000000000000000, 0.000000000000000000 ) ) ;
#126559=AXIS2_PLACEMENT_3D ( 'NONE', #230093, #149300, #89289 ) ;
#126612=CARTESIAN_POINT ( 'NONE',  ( 20.94999999999999929, 71.14953271029195037, -57.48884007552268116 ) ) ;
#126622=AXIS2_PLACEMENT_3D ( 'NONE', #175341, #151925, #112774 ) ;
#126629=ORIENTED_EDGE ( 'NONE', *, *, #52203, .F. ) ;
#126632=AXIS2_PLACEMENT_3D ( 'NONE', #72237, #250844, #190919 ) ;
#126659=EDGE_CURVE ( 'NONE', #19568, #200, #28310, .T. ) ;
#126664=DIRECTION ( 'NONE',  ( 0.000000000000000000, -1.000000000000000000, 0.000000000000000000 ) ) ;
#126665=EDGE_CURVE ( 'NONE', #65850, #100316, #15665, .T. ) ;
#126667=ORIENTED_EDGE ( 'NONE', *, *, #244263, .F. ) ;
#126702=DIRECTION ( 'NONE',  ( -1.000000000000000000, -0.000000000000000000, -0.000000000000000000 ) ) ;
#126775=VERTEX_POINT ( 'NONE', #88511 ) ;
#126832=EDGE_LOOP ( 'NONE', ( #220073, #4983, #210430, #159984 ) ) ;
#126897=DIRECTION ( 'NONE',  ( 1.000000000000000000, -7.304098846218134667E-16, -5.100424963727256530E-30 ) ) ;
#126931=CARTESIAN_POINT ( 'NONE',  ( -21.53699400384554963, 76.00000000001170974, -76.31081927776580187 ) ) ;
#126957=ORIENTED_EDGE ( 'NONE', *, *, #17888, .F. ) ;
#126987=CARTESIAN_POINT ( 'NONE',  ( 18.59999999999999076, 76.00000000001142553, -36.02310748452432421 ) ) ;
#126999=FACE_OUTER_BOUND ( 'NONE', #148910, .T. ) ;
#127029=CARTESIAN_POINT ( 'NONE',  ( 21.05000000000000071, 85.50000000001159606, -59.62913836187181715 ) ) ;
#127050=CARTESIAN_POINT ( 'NONE',  ( -22.50000000000000000, 68.20922040163824818, -69.62310748452438247 ) ) ;
#127065=FACE_OUTER_BOUND ( 'NONE', #185190, .T. ) ;
#127083=DIRECTION ( 'NONE',  ( 0.000000000000000000, 6.982962677686266711E-15, -1.000000000000000000 ) ) ;
#127094=CIRCLE ( 'NONE', #114622, 11.64999999999999325 ) ;
#127096=AXIS2_PLACEMENT_3D ( 'NONE', #239883, #87195, #165484 ) ;
#127129=ORIENTED_EDGE ( 'NONE', *, *, #212927, .F. ) ;
#127143=COLOUR_RGB ( '', 0.66274510, 0.83137255, 0.94901961) ;
#127164=EDGE_CURVE ( 'NONE', #95340, #128522, #166333, .T. ) ;
#127170=TOROIDAL_SURFACE ( 'NONE', #89555, 0.9750000000000019762, 0.1000000000000000056 ) ;
#127177=ORIENTED_EDGE ( 'NONE', *, *, #64383, .T. ) ;
#127180=DIRECTION ( 'NONE',  ( 1.000000000000000000, -0.000000000000000000, 0.000000000000000000 ) ) ;
#127193=DIRECTION ( 'NONE',  ( 0.000000000000000000, 0.000000000000000000, 1.000000000000000000 ) ) ;
#127195=CARTESIAN_POINT ( 'NONE',  ( 18.59999999999999076, 65.79142135624879018, -44.77310748452439526 ) ) ;
#127198=EDGE_CURVE ( 'NONE', #185202, #189058, #91484, .T. ) ;
#127246=CARTESIAN_POINT ( 'NONE',  ( 18.59999999999997655, 76.00000000001136868, -28.12310748452432208 ) ) ;
#127273=FACE_OUTER_BOUND ( 'NONE', #96584, .T. ) ;
#127357=EDGE_CURVE ( 'NONE', #64016, #87492, #253955, .T. ) ;
#127374=AXIS2_PLACEMENT_3D ( 'NONE', #168415, #208783, #185357 ) ;
#127385=DIRECTION ( 'NONE',  ( 1.000000000000000000, 0.000000000000000000, 0.000000000000000000 ) ) ;
#127427=LINE ( 'NONE', #246101, #43767 ) ;
#127431=EDGE_LOOP ( 'NONE', ( #64253, #116329, #132483, #195763 ) ) ;
#127445=TOROIDAL_SURFACE ( 'NONE', #56669, 0.2000000000000000111, 0.1000000000000000056 ) ;
#127453=ORIENTED_EDGE ( 'NONE', *, *, #145765, .F. ) ;
#127464=EDGE_CURVE ( 'NONE', #127854, #216920, #258023, .T. ) ;
#127489=CARTESIAN_POINT ( 'NONE',  ( 18.59999999999999076, 74.16465844978715438, -57.86795619196135476 ) ) ;
#127505=CIRCLE ( 'NONE', #152662, 11.65000000000000036 ) ;
#127525=CARTESIAN_POINT ( 'NONE',  ( -21.05000000000000071, 64.40000000001147384, -42.95131071479990936 ) ) ;
#127539=CARTESIAN_POINT ( 'NONE',  ( 20.85000000000000142, 77.85161776048025217, -24.41991776492064758 ) ) ;
#127552=CARTESIAN_POINT ( 'NONE',  ( 20.94999999999999929, 67.22371710471912820, -60.96447848938343839 ) ) ;
#127564=ORIENTED_EDGE ( 'NONE', *, *, #2166, .T. ) ;
#127579=DIRECTION ( 'NONE',  ( 0.000000000000000000, 1.000000000000000000, 0.000000000000000000 ) ) ;
#127591=CARTESIAN_POINT ( 'NONE',  ( 23.14999999999999503, 64.35000000001156195, -57.37310748452439668 ) ) ;
#127598=AXIS2_PLACEMENT_3D ( 'NONE', #101769, #138341, #120128 ) ;
#127606=CARTESIAN_POINT ( 'NONE',  ( 18.49999999999999645, 77.36242903720467723, -28.13422623660311217 ) ) ;
#127650=ADVANCED_FACE ( 'NONE', ( #164583 ), #40569, .F. ) ;
#127655=AXIS2_PLACEMENT_3D ( 'NONE', #155171, #39059, #78147 ) ;
#127658=LINE ( 'NONE', #28611, #138086 ) ;
#127718=CARTESIAN_POINT ( 'NONE',  ( 18.49999999999998224, 85.32100840337292880, -62.28716923544642015 ) ) ;
#127721=DIRECTION ( 'NONE',  ( 0.000000000000000000, -1.000000000000000000, 0.000000000000000000 ) ) ;
#127722=DIRECTION ( 'NONE',  ( 1.000000000000000000, 0.000000000000000000, 0.000000000000000000 ) ) ;
#127781=VECTOR ( 'NONE', #224318, 1000.000000000000000 ) ;
#127785=VERTEX_POINT ( 'NONE', #18336 ) ;
#127823=ADVANCED_FACE ( 'NONE', ( #6466 ), #194877, .T. ) ;
#127854=VERTEX_POINT ( 'NONE', #49458 ) ;
#127869=EDGE_LOOP ( 'NONE', ( #206912, #33674, #69816, #59768 ) ) ;
#127884=B_SPLINE_CURVE_WITH_KNOTS ( 'NONE', 3,
 ( #163485, #141350, #123084, #100891, #142613, #42260, #183060, #201321, #22717, #3100, #83898, #82623, #243008, #64389, #223440, #44821, #70833, #249456, #166087, #49946, #86481, #89068 ),
 .UNSPECIFIED., .F., .F.,
 ( 4, 3, 3, 3, 3, 3, 3, 4 ),
 ( 0.000000000000000000, 7.307836821083771763E-06, 4.161455748548197731E-05, 7.576591810646988155E-05, 0.0001098090429817560448, 0.0001438003617351108854, 0.0001777914035423656264, 0.0002117966137403014628 ),
 .UNSPECIFIED. ) ;
#127915=AXIS2_PLACEMENT_3D ( 'NONE', #202131, #3931, #183846 ) ;
#127922=CARTESIAN_POINT ( 'NONE',  ( 22.48660254037844197, 64.35000000001164722, -69.57310748452439952 ) ) ;
#127934=CARTESIAN_POINT ( 'NONE',  ( 21.05000000000000071, 70.15000000001163016, -59.39061026024639744 ) ) ;
#127939=LINE ( 'NONE', #133074, #228423 ) ;
#127948=CARTESIAN_POINT ( 'NONE',  ( 18.59999999999999076, 74.25000000001156764, -57.85359592662268824 ) ) ;
#127989=TOROIDAL_SURFACE ( 'NONE', #186254, 3.899999999999999467, 0.1000000000000000056 ) ;
#127993=ADVANCED_FACE ( 'NONE', ( #231966 ), #207321, .F. ) ;
#128037=CARTESIAN_POINT ( 'NONE',  ( -23.25000000000000000, 76.00000000001143974, -38.12310748452432563 ) ) ;
#128057=ADVANCED_FACE ( 'NONE', ( #40190 ), #220084, .T. ) ;
#128065=ORIENTED_EDGE ( 'NONE', *, *, #120588, .T. ) ;
#128100=ORIENTED_EDGE ( 'NONE', *, *, #45311, .T. ) ;
#128102=ORIENTED_EDGE ( 'NONE', *, *, #157543, .T. ) ;
#128105=AXIS2_PLACEMENT_3D ( 'NONE', #98067, #177676, #199797 ) ;
#128134=DIRECTION ( 'NONE',  ( 1.000000000000000000, 0.000000000000000000, 0.000000000000000000 ) ) ;
#128137=CARTESIAN_POINT ( 'NONE',  ( -21.05000000000000071, 77.83534155023598089, -57.96795619196132776 ) ) ;
#128150=VECTOR ( 'NONE', #135161, 1000.000000000000114 ) ;
#128154=VERTEX_POINT ( 'NONE', #122267 ) ;
#128160=DIRECTION ( 'NONE',  ( -0.000000000000000000, -0.01283462868040327436, 0.9999176327611370985 ) ) ;
#128167=CARTESIAN_POINT ( 'NONE',  ( 23.15000000000000213, 87.65000000001144542, -39.12310748452424747 ) ) ;
#128219=ORIENTED_EDGE ( 'NONE', *, *, #120588, .F. ) ;
#128226=AXIS2_PLACEMENT_3D ( 'NONE', #138098, #40344, #136825 ) ;
#128235=EDGE_CURVE ( 'NONE', #38202, #98142, #67418, .T. ) ;
#128251=FACE_OUTER_BOUND ( 'NONE', #106939, .T. ) ;
#128273=ORIENTED_EDGE ( 'NONE', *, *, #31803, .T. ) ;
#128281=CIRCLE ( 'NONE', #153244, 11.65000000000000036 ) ;
#128284=EDGE_LOOP ( 'NONE', ( #242299, #242594, #54452, #72049 ) ) ;
#128301=ADVANCED_FACE ( 'NONE', ( #241756 ), #201349, .F. ) ;
#128306=ORIENTED_EDGE ( 'NONE', *, *, #217433, .T. ) ;
#128320=ORIENTED_EDGE ( 'NONE', *, *, #17075, .T. ) ;
#128345=CARTESIAN_POINT ( 'NONE',  ( 21.05000000000000071, 65.27628289530404970, -57.37310748452439668 ) ) ;
#128346=CARTESIAN_POINT ( 'NONE',  ( -21.44999999999999929, 68.65000000001150227, -48.27310748452437394 ) ) ;
#128353=DIRECTION ( 'NONE',  ( -1.000000000000000000, 0.000000000000000000, -0.000000000000000000 ) ) ;
#128362=CARTESIAN_POINT ( 'NONE',  ( -23.15000000000000213, 74.00000000001151079, -49.24772940728643533 ) ) ;
#128369=CARTESIAN_POINT ( 'NONE',  ( 18.59999999999999787, 77.83534155023598089, -57.96795619196132776 ) ) ;
#128390=CARTESIAN_POINT ( 'NONE',  ( -21.05000000000000071, 76.00000000001162448, -65.22310748452436258 ) ) ;
#128394=CARTESIAN_POINT ( 'NONE',  ( 21.06280952165552733, 65.37286769941061948, -57.31905359774562214 ) ) ;
#128419=DIRECTION ( 'NONE',  ( -1.000000000000000000, 2.952720810173289112E-16, 2.061873921506763405E-30 ) ) ;
#128430=CARTESIAN_POINT ( 'NONE',  ( -20.54999999999999716, 76.00000000001142553, -36.02310748452432421 ) ) ;
#128508=DIRECTION ( 'NONE',  ( -1.000000000000000000, 2.775557561562908012E-13, 0.000000000000000000 ) ) ;
#128522=VERTEX_POINT ( 'NONE', #183090 ) ;
#128530=CARTESIAN_POINT ( 'NONE',  ( -21.05000000000000071, 74.16465844978715438, -57.96795619196135618 ) ) ;
#128531=CARTESIAN_POINT ( 'NONE',  ( -21.14999999999999858, 87.75000000001165290, -69.52310748452424605 ) ) ;
#128558=CARTESIAN_POINT ( 'NONE',  ( 18.49999999999999645, 74.26374286841418382, -57.95445515550683524 ) ) ;
#128577=DIRECTION ( 'NONE',  ( 1.000000000000000000, 0.000000000000000000, 0.000000000000000000 ) ) ;
#128665=DIRECTION ( 'NONE',  ( 0.000000000000000000, 6.853228547068871147E-15, -1.000000000000000000 ) ) ;
#128711=CARTESIAN_POINT ( 'NONE',  ( -21.05000000000000071, 87.75000000001143974, -38.92310748452424463 ) ) ;
#128741=EDGE_CURVE ( 'NONE', #187198, #215216, #253442, .T. ) ;
#128743=LINE ( 'NONE', #12663, #209762 ) ;
#128750=DIRECTION ( 'NONE',  ( 0.000000000000000000, 0.6728971962616412394, 0.7397360091703134577 ) ) ;
#128793=CARTESIAN_POINT ( 'NONE',  ( 23.24999999999999645, 73.90000000001141700, -36.02310748452433842 ) ) ;
#128816=AXIS2_PLACEMENT_3D ( 'NONE', #114163, #11222, #212000 ) ;
#128820=EDGE_CURVE ( 'NONE', #212844, #251754, #32747, .T. ) ;
#128844=CARTESIAN_POINT ( 'NONE',  ( -23.25000000000000000, 77.85161776048025217, -24.41991776492064758 ) ) ;
#128852=ADVANCED_FACE ( 'NONE', ( #98208 ), #60398, .F. ) ;
#128884=SPHERICAL_SURFACE ( 'NONE', #144047, 0.1000000000000000056 ) ;
#128926=ORIENTED_EDGE ( 'NONE', *, *, #158339, .F. ) ;
#128935=DIRECTION ( 'NONE',  ( 0.000000000000000000, 0.000000000000000000, 1.000000000000000000 ) ) ;
#128966=CYLINDRICAL_SURFACE ( 'NONE', #131809, 0.09999999999999939493 ) ;
#128972=CARTESIAN_POINT ( 'NONE',  ( 22.48508240969612615, 75.95372358549481362, -81.17311821609789035 ) ) ;
#129015=AXIS2_PLACEMENT_3D ( 'NONE', #38672, #255089, #157368 ) ;
#129123=VECTOR ( 'NONE', #33790, 1000.000000000000114 ) ;
#129124=CARTESIAN_POINT ( 'NONE',  ( 23.14999999999999858, 64.40000000001145963, -42.95131071479990226 ) ) ;
#129138=CARTESIAN_POINT ( 'NONE',  ( 20.85000000000000142, 68.87972903831379767, -32.36354444268504693 ) ) ;
#129146=EDGE_LOOP ( 'NONE', ( #7076, #191325, #245217, #147332 ) ) ;
#129178=CIRCLE ( 'NONE', #162502, 0.2000000000000057288 ) ;
#129206=CARTESIAN_POINT ( 'NONE',  ( 22.49806830649814060, 64.35011034517256689, -69.60057180084992012 ) ) ;
#129230=CARTESIAN_POINT ( 'NONE',  ( -23.15000000000000213, 85.50000000001159606, -59.62913836187181005 ) ) ;
#129293=ORIENTED_EDGE ( 'NONE', *, *, #19012, .F. ) ;
#129298=CARTESIAN_POINT ( 'NONE',  ( 20.94999999999999929, 85.40000000001148805, -45.91707660717669626 ) ) ;
#129302=FACE_OUTER_BOUND ( 'NONE', #244139, .T. ) ;
#129316=DIRECTION ( 'NONE',  ( 1.000000000000000000, -0.000000000000000000, 0.000000000000000000 ) ) ;
#129348=EDGE_LOOP ( 'NONE', ( #112061, #179435, #251394, #187226, #120042, #113693 ) ) ;
#129353=DIRECTION ( 'NONE',  ( 0.000000000000000000, 0.000000000000000000, 1.000000000000000000 ) ) ;
#129362=AXIS2_PLACEMENT_3D ( 'NONE', #116973, #98646, #238185 ) ;
#129371=( BOUNDED_CURVE ( )  B_SPLINE_CURVE ( 3, ( #208675, #91283, #247776, #192948 ),
 .UNSPECIFIED., .F., .F. ) 
 B_SPLINE_CURVE_WITH_KNOTS ( ( 4, 4 ),
 ( 4.712388980384690562, 6.283185307179586232 ),
 .UNSPECIFIED. ) 
 CURVE ( )  GEOMETRIC_REPRESENTATION_ITEM ( )  RATIONAL_B_SPLINE_CURVE ( ( 1.000000000000000000, 0.8047378541243652705, 0.8047378541243652705, 1.000000000000000000 ) ) 
 REPRESENTATION_ITEM ( '' )  );
#129392=ORIENTED_EDGE ( 'NONE', *, *, #108069, .T. ) ;
#129424=CARTESIAN_POINT ( 'NONE',  ( 20.94999999999999929, 76.00000000001143974, -38.02310748452432421 ) ) ;
#129427=EDGE_LOOP ( 'NONE', ( #157970, #42804, #257397, #97, #218001 ) ) ;
#129465=CARTESIAN_POINT ( 'NONE',  ( -23.25000000000000000, 76.00000000001142553, -36.02310748452432421 ) ) ;
#129500=EDGE_CURVE ( 'NONE', #41312, #187599, #249176, .T. ) ;
#129532=ORIENTED_EDGE ( 'NONE', *, *, #133617, .T. ) ;
#129565=CARTESIAN_POINT ( 'NONE',  ( -18.59999999999999787, 77.16412189325258453, -28.10825939895270764 ) ) ;
#129577=ORIENTED_EDGE ( 'NONE', *, *, #169208, .F. ) ;
#129583=CARTESIAN_POINT ( 'NONE',  ( 21.14999999999999858, 87.65000000001164437, -69.52310748452424605 ) ) ;
#129614=EDGE_LOOP ( 'NONE', ( #197042, #158423, #24872, #208607 ) ) ;
#129624=CARTESIAN_POINT ( 'NONE',  ( -18.50000000000000000, 77.63717271298195044, -57.94095411905229298 ) ) ;
#129709=AXIS2_PLACEMENT_3D ( 'NONE', #28980, #9354, #88880 ) ;
#129794=EDGE_CURVE ( 'NONE', #17744, #86948, #24509, .T. ) ;
#129839=ORIENTED_EDGE ( 'NONE', *, *, #16108, .F. ) ;
#129846=LINE ( 'NONE', #89437, #243188 ) ;
#129860=DIRECTION ( 'NONE',  ( 1.000000000000000000, 0.000000000000000000, 0.000000000000000000 ) ) ;
#129881=ORIENTED_EDGE ( 'NONE', *, *, #256323, .F. ) ;
#129918=CARTESIAN_POINT ( 'NONE',  ( 20.94999999999999574, 87.65000000001161595, -66.42310748452423752 ) ) ;
#129922=SPHERICAL_SURFACE ( 'NONE', #14609, 0.1000000000000000056 ) ;
#129942=CIRCLE ( 'NONE', #204786, 0.1999999999999987899 ) ;
#129954=EDGE_CURVE ( 'NONE', #220391, #174834, #61912, .T. ) ;
#129980=CIRCLE ( 'NONE', #80072, 11.70000000000000284 ) ;
#129984=DIRECTION ( 'NONE',  ( 0.000000000000000000, 6.982962677686266711E-15, -1.000000000000000000 ) ) ;
#129989=CARTESIAN_POINT ( 'NONE',  ( -23.25000000000000000, 84.59626168225447884, -45.47323500167453858 ) ) ;
#130000=EDGE_CURVE ( 'NONE', #209151, #146391, #216938, .T. ) ;
#130030=ORIENTED_EDGE ( 'NONE', *, *, #50789, .F. ) ;
#130202=CARTESIAN_POINT ( 'NONE',  ( -21.64999999999999858, 68.65000000001150227, -48.27310748452437394 ) ) ;
#130214=EDGE_CURVE ( 'NONE', #96347, #208477, #166183, .T. ) ;
#130224=DIRECTION ( 'NONE',  ( 1.000000000000000000, 0.000000000000000000, 0.000000000000000000 ) ) ;
#130238=ADVANCED_FACE ( 'NONE', ( #147695 ), #48582, .F. ) ;
#130245=VERTEX_POINT ( 'NONE', #88980 ) ;
#130279=ADVANCED_FACE ( 'NONE', ( #173731 ), #52426, .T. ) ;
#130287=ORIENTED_EDGE ( 'NONE', *, *, #93439, .F. ) ;
#130333=CARTESIAN_POINT ( 'NONE',  ( -20.94999999999999929, 77.26178616857662007, -61.43660852097883662 ) ) ;
#130336=ORIENTED_EDGE ( 'NONE', *, *, #228380, .F. ) ;
#130351=CARTESIAN_POINT ( 'NONE',  ( -21.65000000000000213, 68.29142135624881860, -48.27310748452437394 ) ) ;
#130371=EDGE_CURVE ( 'NONE', #253401, #131663, #45332, .T. ) ;
#130413=CARTESIAN_POINT ( 'NONE',  ( 20.94999999999999574, 77.83534155023598089, -57.96795619196132776 ) ) ;
#130435=VECTOR ( 'NONE', #17677, 1000.000000000000000 ) ;
#130595=EDGE_CURVE ( 'NONE', #238186, #232528, #203739, .T. ) ;
#130617=DIRECTION ( 'NONE',  ( 0.000000000000000000, -1.000000000000000000, 0.000000000000000000 ) ) ;
#130619=EDGE_CURVE ( 'NONE', #88139, #96681, #52125, .T. ) ;
#130689=CARTESIAN_POINT ( 'NONE',  ( 23.14999999999999858, 71.18691588786205671, -57.58158972800053022 ) ) ;
#130703=ORIENTED_EDGE ( 'NONE', *, *, #209059, .T. ) ;
#130747=FACE_OUTER_BOUND ( 'NONE', #191368, .T. ) ;
#130762=DIRECTION ( 'NONE',  ( 0.000000000000000000, 1.000000000000000000, 6.982962677686266711E-15 ) ) ;
#130766=CIRCLE ( 'NONE', #93160, 0.1000000000000028644 ) ;
#130767=LINE ( 'NONE', #150348, #220758 ) ;
#130804=CARTESIAN_POINT ( 'NONE',  ( 18.59999999999999432, 74.83729825007360148, -61.42310748452432989 ) ) ;
#130839=VERTEX_POINT ( 'NONE', #102788 ) ;
#130857=EDGE_LOOP ( 'NONE', ( #119426, #251046, #15782, #247491 ) ) ;
#130861=ORIENTED_EDGE ( 'NONE', *, *, #83790, .F. ) ;
#130888=CARTESIAN_POINT ( 'NONE',  ( 21.05000000000000071, 76.00000000001165290, -69.52310748452431710 ) ) ;
#130897=EDGE_CURVE ( 'NONE', #29497, #196290, #199371, .T. ) ;
#130905=AXIS2_PLACEMENT_3D ( 'NONE', #243130, #46209, #102298 ) ;
#130914=CARTESIAN_POINT ( 'NONE',  ( 23.25000000000000000, 87.75000000001143974, -39.12310748452424747 ) ) ;
#130922=DIRECTION ( 'NONE',  ( 1.000000000000000000, 0.000000000000000000, 0.000000000000000000 ) ) ;
#130958=TOROIDAL_SURFACE ( 'NONE', #122611, 11.65000000000000036, 0.1000000000000000056 ) ;
#130960=CARTESIAN_POINT ( 'NONE',  ( 21.09793522318413395, 65.27537548979879034, -57.28381661354728038 ) ) ;
#130988=ADVANCED_FACE ( 'NONE', ( #104076 ), #148043, .T. ) ;
#131029=ORIENTED_EDGE ( 'NONE', *, *, #118793, .F. ) ;
#131030=CARTESIAN_POINT ( 'NONE',  ( -21.29999999999995808, 76.00000000001165290, -69.52310748452431710 ) ) ;
#131046=CIRCLE ( 'NONE', #51921, 11.79999999999999716 ) ;
#131096=DIRECTION ( 'NONE',  ( -1.000000000000000000, -0.000000000000000000, -0.000000000000000000 ) ) ;
#131113=LINE ( 'NONE', #30764, #217004 ) ;
#131139=LINE ( 'NONE', #110288, #218230 ) ;
#131152=CARTESIAN_POINT ( 'NONE',  ( -20.64999999999999858, 73.60000000001151932, -49.24772940728643533 ) ) ;
#131162=FACE_OUTER_BOUND ( 'NONE', #116012, .T. ) ;
#131190=EDGE_CURVE ( 'NONE', #195194, #60391, #8303, .T. ) ;
#131197=DIRECTION ( 'NONE',  ( 0.000000000000000000, -0.9654727137038715545, -0.2605042016806676242 ) ) ;
#131218=ORIENTED_EDGE ( 'NONE', *, *, #204945, .F. ) ;
#131225=CARTESIAN_POINT ( 'NONE',  ( 19.97071067811864609, 64.27928932189283273, -44.77310748452440237 ) ) ;
#131227=EDGE_CURVE ( 'NONE', #14506, #131663, #143864, .T. ) ;
#131300=CARTESIAN_POINT ( 'NONE',  ( -20.94999999999999929, 77.16270174994961906, -61.62310748452431142 ) ) ;
#131312=CARTESIAN_POINT ( 'NONE',  ( 18.49999999999998934, 56.14960075277809182, -67.24280442672311153 ) ) ;
#131317=DIRECTION ( 'NONE',  ( 1.000000000000000000, 0.000000000000000000, 0.000000000000000000 ) ) ;
#131348=ORIENTED_EDGE ( 'NONE', *, *, #15828, .F. ) ;
#131385=DIRECTION ( 'NONE',  ( 0.000000000000000000, 1.000000000000000000, 0.000000000000000000 ) ) ;
#131392=LINE ( 'NONE', #148404, #141826 ) ;
#131398=ORIENTED_EDGE ( 'NONE', *, *, #141405, .F. ) ;
#131411=DIRECTION ( 'NONE',  ( 0.000000000000000000, -1.000000000000000000, 0.000000000000000000 ) ) ;
#131416=VECTOR ( 'NONE', #14717, 999.9999999999998863 ) ;
#131417=AXIS2_PLACEMENT_3D ( 'NONE', #236161, #216598, #197019 ) ;
#131432=EDGE_CURVE ( 'NONE', #167581, #20467, #187572, .T. ) ;
#131444=DIRECTION ( 'NONE',  ( -3.469446951953515108E-14, 1.000000000000000000, 0.000000000000000000 ) ) ;
#131448=AXIS2_PLACEMENT_3D ( 'NONE', #13486, #250794, #173883 ) ;
#131496=AXIS2_PLACEMENT_3D ( 'NONE', #32169, #169126, #111679 ) ;
#131499=DIRECTION ( 'NONE',  ( 1.000000000000000000, -3.265361837132813093E-16, -2.280189983783949500E-30 ) ) ;
#131504=CARTESIAN_POINT ( 'NONE',  ( 20.94999999999999929, 85.00000000001149658, -45.91707660717670336 ) ) ;
#131527=CARTESIAN_POINT ( 'NONE',  ( 22.39999999999999503, 76.00000000001173817, -81.17267829206912211 ) ) ;
#131558=DIRECTION ( 'NONE',  ( 0.000000000000000000, -6.454785026890510900E-15, 1.000000000000000000 ) ) ;
#131564=FACE_OUTER_BOUND ( 'NONE', #43996, .T. ) ;
#131571=EDGE_CURVE ( 'NONE', #94150, #45697, #245801, .T. ) ;
#131573=VECTOR ( 'NONE', #98413, 1000.000000000000000 ) ;
#131578=ADVANCED_FACE ( 'NONE', ( #181441 ), #37725, .F. ) ;
#131597=CIRCLE ( 'NONE', #139953, 0.1000000000000028644 ) ;
#131649=ORIENTED_EDGE ( 'NONE', *, *, #125809, .T. ) ;
#131656=ORIENTED_EDGE ( 'NONE', *, *, #196119, .F. ) ;
#131657=ADVANCED_FACE ( 'NONE', ( #160606 ), #204269, .T. ) ;
#131663=VERTEX_POINT ( 'NONE', #49614 ) ;
#131675=DIRECTION ( 'NONE',  ( -1.000000000000000000, -7.304098846218164250E-16, 4.217023435051628197E-16 ) ) ;
#131720=DIRECTION ( 'NONE',  ( 0.000000000000000000, 0.000000000000000000, -1.000000000000000000 ) ) ;
#131737=EDGE_CURVE ( 'NONE', #233936, #87492, #216748, .T. ) ;
#131740=AXIS2_PLACEMENT_3D ( 'NONE', #63404, #103801, #237256 ) ;
#131748=AXIS2_PLACEMENT_3D ( 'NONE', #100058, #3544, #2252 ) ;
#131753=CARTESIAN_POINT ( 'NONE',  ( 18.49999999999999289, 69.55000000001150795, -48.37310748452436826 ) ) ;
#131762=CARTESIAN_POINT ( 'NONE',  ( 22.48970261584622321, 64.35000000001166143, -69.57847697274181087 ) ) ;
#131784=VERTEX_POINT ( 'NONE', #16921 ) ;
#131808=DIRECTION ( 'NONE',  ( 0.000000000000000000, 0.8660254037844420383, -0.4999999999999943379 ) ) ;
#131809=AXIS2_PLACEMENT_3D ( 'NONE', #105503, #88519, #185077 ) ;
#131821=EDGE_CURVE ( 'NONE', #211078, #198094, #108609, .T. ) ;
#131838=DIRECTION ( 'NONE',  ( -1.000000000000000000, 0.000000000000000000, -0.000000000000000000 ) ) ;
#131846=ORIENTED_EDGE ( 'NONE', *, *, #220452, .T. ) ;
#131853=ADVANCED_FACE ( 'NONE', ( #176009 ), #95161, .F. ) ;
#131856=CARTESIAN_POINT ( 'NONE',  ( 21.04999999999999716, 76.01681986839737704, -75.83053270408971969 ) ) ;
#131866=ORIENTED_EDGE ( 'NONE', *, *, #172144, .F. ) ;
#131873=CIRCLE ( 'NONE', #127598, 0.1000000000000067224 ) ;
#131935=ORIENTED_EDGE ( 'NONE', *, *, #231145, .T. ) ;
#131937=ORIENTED_EDGE ( 'NONE', *, *, #160132, .T. ) ;
#131941=DIRECTION ( 'NONE',  ( 2.952720810173289112E-16, 1.000000000000000000, 6.530723674265620862E-15 ) ) ;
#131960=AXIS2_PLACEMENT_3D ( 'NONE', #75061, #133711, #136253 ) ;
#131964=CIRCLE ( 'NONE', #69632, 12.97499999999999964 ) ;
#131967=TOROIDAL_SURFACE ( 'NONE', #165288, 4.099999999999999645, 0.1000000000000000056 ) ;
#131986=EDGE_CURVE ( 'NONE', #81658, #59275, #192024, .T. ) ;
#132037=ADVANCED_FACE ( 'NONE', ( #205810 ), #79371, .T. ) ;
#132046=CIRCLE ( 'NONE', #202769, 0.09999999999999939493 ) ;
#132096=CARTESIAN_POINT ( 'NONE',  ( -20.54999999999999716, 68.85000000001151932, -48.37310748452436826 ) ) ;
#132112=CYLINDRICAL_SURFACE ( 'NONE', #191170, 12.87499999999999822 ) ;
#132145=CARTESIAN_POINT ( 'NONE',  ( -20.64999999999999858, 74.00000000001156764, -56.29848556176223440 ) ) ;
#132160=ORIENTED_EDGE ( 'NONE', *, *, #21735, .F. ) ;
#132186=CARTESIAN_POINT ( 'NONE',  ( 21.07189867249812210, 65.27501972991842649, -57.31065604224765764 ) ) ;
#132211=DIRECTION ( 'NONE',  ( 1.000000000000000000, -3.265361837132813093E-16, -2.280189983783949500E-30 ) ) ;
#132231=AXIS2_PLACEMENT_3D ( 'NONE', #219711, #38525, #101007 ) ;
#132233=ORIENTED_EDGE ( 'NONE', *, *, #89728, .T. ) ;
#132258=ORIENTED_EDGE ( 'NONE', *, *, #140460, .T. ) ;
#132269=AXIS2_PLACEMENT_3D ( 'NONE', #125965, #68578, #6013 ) ;
#132270=ORIENTED_EDGE ( 'NONE', *, *, #172059, .T. ) ;
#132281=AXIS2_PLACEMENT_3D ( 'NONE', #257870, #121011, #156293 ) ;
#132312=AXIS2_PLACEMENT_3D ( 'NONE', #168720, #4441, #143954 ) ;
#132325=VECTOR ( 'NONE', #91791, 1000.000000000000000 ) ;
#132332=VECTOR ( 'NONE', #68169, 1000.000000000000000 ) ;
#132348=CIRCLE ( 'NONE', #211469, 0.9750000000000036415 ) ;
#132356=CIRCLE ( 'NONE', #78366, 0.1000000000000028644 ) ;
#132361=DIRECTION ( 'NONE',  ( -0.7071067811865127117, -0.7071067811865821007, 0.000000000000000000 ) ) ;
#132388=FACE_OUTER_BOUND ( 'NONE', #247046, .T. ) ;
#132422=TOROIDAL_SURFACE ( 'NONE', #3212, 0.6000000000000015321, 0.1000000000000000056 ) ;
#132483=ORIENTED_EDGE ( 'NONE', *, *, #240401, .F. ) ;
#132496=CARTESIAN_POINT ( 'NONE',  ( 21.14999999999999858, 64.35000000001164722, -69.42310748452440805 ) ) ;
#132511=EDGE_CURVE ( 'NONE', #230638, #82836, #167272, .T. ) ;
#132517=ADVANCED_FACE ( 'NONE', ( #121615 ), #117731, .F. ) ;
#132520=ORIENTED_EDGE ( 'NONE', *, *, #221537, .F. ) ;
#132521=DIRECTION ( 'NONE',  ( -0.000000000000000000, 6.982962677686266711E-15, -1.000000000000000000 ) ) ;
#132534=EDGE_CURVE ( 'NONE', #225338, #158894, #78596, .T. ) ;
#132537=AXIS2_PLACEMENT_3D ( 'NONE', #35326, #154007, #173570 ) ;
#132541=CARTESIAN_POINT ( 'NONE',  ( -20.94999999999999929, 64.36312671090738036, -42.84486669784926249 ) ) ;
#132559=CARTESIAN_POINT ( 'NONE',  ( -22.50000000000000000, 64.25000000001165290, -69.52310748452438816 ) ) ;
#132567=ORIENTED_EDGE ( 'NONE', *, *, #78594, .T. ) ;
#132578=AXIS2_PLACEMENT_3D ( 'NONE', #230698, #14229, #172034 ) ;
#132615=DIRECTION ( 'NONE',  ( -1.000000000000000000, 0.000000000000000000, -0.000000000000000000 ) ) ;
#132633=DIRECTION ( 'NONE',  ( -0.000000000000000000, 6.982962677686266711E-15, -1.000000000000000000 ) ) ;
#132661=CARTESIAN_POINT ( 'NONE',  ( -20.85000000000000142, 76.00000000001142553, -36.02310748452432421 ) ) ;
#132664=EDGE_CURVE ( 'NONE', #21197, #175346, #22508, .T. ) ;
#132676=DIRECTION ( 'NONE',  ( -1.000000000000000000, -0.000000000000000000, -0.000000000000000000 ) ) ;
#132697=AXIS2_PLACEMENT_3D ( 'NONE', #131152, #208149, #129860 ) ;
#132725=AXIS2_PLACEMENT_3D ( 'NONE', #140771, #100329, #23422 ) ;
#132817=ORIENTED_EDGE ( 'NONE', *, *, #185360, .T. ) ;
#132822=ORIENTED_EDGE ( 'NONE', *, *, #139069, .T. ) ;
#132826=LINE ( 'NONE', #152405, #80223 ) ;
#132843=ORIENTED_EDGE ( 'NONE', *, *, #241004, .T. ) ;
#132899=ORIENTED_EDGE ( 'NONE', *, *, #182170, .T. ) ;
#132900=ORIENTED_EDGE ( 'NONE', *, *, #140919, .T. ) ;
#132904=ORIENTED_EDGE ( 'NONE', *, *, #93439, .T. ) ;
#132917=CARTESIAN_POINT ( 'NONE',  ( 21.05000000000000071, 76.00000000001142553, -36.02310748452432421 ) ) ;
#132931=EDGE_CURVE ( 'NONE', #185202, #246608, #134086, .T. ) ;
#132963=DIRECTION ( 'NONE',  ( 0.000000000000000000, -1.000000000000000000, -6.982962677686265922E-15 ) ) ;
#132972=EDGE_LOOP ( 'NONE', ( #157925, #204151, #28665, #237437 ) ) ;
#133011=DIRECTION ( 'NONE',  ( 2.952720810173289112E-16, 1.000000000000000000, 6.982962677686266711E-15 ) ) ;
#133017=CARTESIAN_POINT ( 'NONE',  ( -21.05000000000000071, 61.95000000001162022, -64.00941241376342816 ) ) ;
#133033=EDGE_CURVE ( 'NONE', #211306, #234821, #204992, .T. ) ;
#133036=EDGE_CURVE ( 'NONE', #94760, #81005, #87261, .T. ) ;
#133074=CARTESIAN_POINT ( 'NONE',  ( -21.55000000000000426, 68.25000000001158185, -57.17310748452437963 ) ) ;
#133088=FACE_OUTER_BOUND ( 'NONE', #43074, .T. ) ;
#133098=EDGE_CURVE ( 'NONE', #187599, #215584, #105008, .T. ) ;
#133138=CARTESIAN_POINT ( 'NONE',  ( -21.05000000000000071, 76.00000000001162448, -66.62310748452433984 ) ) ;
#133148=DIRECTION ( 'NONE',  ( 0.000000000000000000, -7.172728831056617961E-15, 1.000000000000000000 ) ) ;
#133158=DIRECTION ( 'NONE',  ( 3.616040088954490704E-32, 7.105427357601001859E-15, -1.000000000000000000 ) ) ;
#133197=EDGE_CURVE ( 'NONE', #218147, #138152, #129980, .T. ) ;
#133256=ORIENTED_EDGE ( 'NONE', *, *, #241541, .F. ) ;
#133289=DIRECTION ( 'NONE',  ( -0.000000000000000000, 6.982962677686266711E-15, -1.000000000000000000 ) ) ;
#133327=EDGE_CURVE ( 'NONE', #82047, #241131, #195394, .T. ) ;
#133339=ADVANCED_FACE ( 'NONE', ( #16746 ), #252757, .F. ) ;
#133397=ORIENTED_EDGE ( 'NONE', *, *, #37735, .F. ) ;
#133416=ORIENTED_EDGE ( 'NONE', *, *, #95761, .T. ) ;
#133432=CIRCLE ( 'NONE', #87613, 0.09999999999999939493 ) ;
#133442=AXIS2_PLACEMENT_3D ( 'NONE', #69942, #245997, #210714 ) ;
#133461=CARTESIAN_POINT ( 'NONE',  ( 21.05000000000000071, 67.22371735104047730, -61.03551510600370023 ) ) ;
#133465=DIRECTION ( 'NONE',  ( 1.000000000000000000, 0.000000000000000000, 0.000000000000000000 ) ) ;
#133469=CARTESIAN_POINT ( 'NONE',  ( -21.05000000000000071, 77.36087058720364951, -61.45010955743335046 ) ) ;
#133492=ORIENTED_EDGE ( 'NONE', *, *, #257404, .F. ) ;
#133535=ORIENTED_EDGE ( 'NONE', *, *, #100002, .T. ) ;
#133550=ORIENTED_EDGE ( 'NONE', *, *, #34626, .F. ) ;
#133588=CARTESIAN_POINT ( 'NONE',  ( -23.25000000000000000, 73.40000000001151648, -49.24772940728643533 ) ) ;
#133598=EDGE_CURVE ( 'NONE', #196513, #117921, #72559, .T. ) ;
#133617=EDGE_CURVE ( 'NONE', #40138, #206496, #27028, .T. ) ;
#133627=AXIS2_PLACEMENT_3D ( 'NONE', #54139, #252334, #51545 ) ;
#133678=CARTESIAN_POINT ( 'NONE',  ( 20.94999999999999929, 85.40000000001148805, -45.91707660717669626 ) ) ;
#133685=CARTESIAN_POINT ( 'NONE',  ( -23.25000000000000000, 69.06610602788505560, -32.23746165015079868 ) ) ;
#133687=EDGE_LOOP ( 'NONE', ( #125042, #33832, #11853, #19867 ) ) ;
#133704=DIRECTION ( 'NONE',  ( 1.000000000000000000, 0.000000000000000000, 0.000000000000000000 ) ) ;
#133711=DIRECTION ( 'NONE',  ( -1.000000000000000000, 0.000000000000000000, -0.000000000000000000 ) ) ;
#133726=DIRECTION ( 'NONE',  ( 0.000000000000000000, 1.000000000000000000, 6.982962677686266711E-15 ) ) ;
#133738=CARTESIAN_POINT ( 'NONE',  ( -23.15000000000000213, 87.75000000001165290, -69.52310748452424605 ) ) ;
#133740=CARTESIAN_POINT ( 'NONE',  ( 22.39999999999999858, 68.20922040163827660, -69.62310748452438247 ) ) ;
#133790=CIRCLE ( 'NONE', #46478, 0.09999999999999799327 ) ;
#133794=ORIENTED_EDGE ( 'NONE', *, *, #150042, .F. ) ;
#133845=DIRECTION ( 'NONE',  ( -0.000000000000000000, 0.9875055080513808203, -0.1575844902526395142 ) ) ;
#133847=AXIS2_PLACEMENT_3D ( 'NONE', #232972, #133845, #213372 ) ;
#133873=VECTOR ( 'NONE', #118254, 1000.000000000000000 ) ;
#133880=LINE ( 'NONE', #231718, #20931 ) ;
#133906=EDGE_LOOP ( 'NONE', ( #219490, #75571, #16441, #242663 ) ) ;
#133973=ORIENTED_EDGE ( 'NONE', *, *, #81450, .F. ) ;
#133978=DIRECTION ( 'NONE',  ( 0.000000000000000000, 0.000000000000000000, 1.000000000000000000 ) ) ;
#134011=ORIENTED_EDGE ( 'NONE', *, *, #74069, .F. ) ;
#134050=ORIENTED_EDGE ( 'NONE', *, *, #69433, .T. ) ;
#134074=CARTESIAN_POINT ( 'NONE',  ( -21.00219873199078435, 64.39461131213502654, -62.61046005622981880 ) ) ;
#134086=CIRCLE ( 'NONE', #67452, 0.1000000000000028644 ) ;
#134087=AXIS2_PLACEMENT_3D ( 'NONE', #108701, #150416, #73460 ) ;
#134130=VECTOR ( 'NONE', #74528, 1000.000000000000000 ) ;
#134134=AXIS2_PLACEMENT_3D ( 'NONE', #6870, #228504, #150256 ) ;
#134152=CIRCLE ( 'NONE', #34424, 0.09999999999999938105 ) ;
#134198=FACE_OUTER_BOUND ( 'NONE', #151191, .T. ) ;
#134201=DIRECTION ( 'NONE',  ( 1.000000000000000000, -1.875376730785737719E-16, -1.309568571767809260E-30 ) ) ;
#134212=DIRECTION ( 'NONE',  ( 1.000000000000000000, 7.304098846218133681E-16, 4.639676173203992654E-30 ) ) ;
#134214=ORIENTED_EDGE ( 'NONE', *, *, #156228, .F. ) ;
#134250=CARTESIAN_POINT ( 'NONE',  ( 21.53752568617679586, 69.21319212550768896, -69.62208194579503129 ) ) ;
#134257=CARTESIAN_POINT ( 'NONE',  ( 23.14999999999999858, 70.40000000001150227, -48.42837350343745584 ) ) ;
#134275=CARTESIAN_POINT ( 'NONE',  ( -21.14999999999999858, 64.35000000001166143, -69.52310748452438816 ) ) ;
#134285=VERTEX_POINT ( 'NONE', #142158 ) ;
#134317=CIRCLE ( 'NONE', #21911, 12.97499999999999964 ) ;
#134358=VECTOR ( 'NONE', #204203, 1000.000000000000000 ) ;
#134359=PLANE ( 'NONE',  #152499 ) ;
#134370=ORIENTED_EDGE ( 'NONE', *, *, #135998, .F. ) ;
#134399=CARTESIAN_POINT ( 'NONE',  ( -18.50000000000000355, 77.26327546522863088, -28.12124281777790813 ) ) ;
#134427=CARTESIAN_POINT ( 'NONE',  ( 23.15000000000000213, 87.65000000001144542, -39.02310748452423894 ) ) ;
#134429=CARTESIAN_POINT ( 'NONE',  ( 20.04142135623730070, 64.25000000001148237, -44.87310748452440379 ) ) ;
#134468=VERTEX_POINT ( 'NONE', #37641 ) ;
#134493=DIRECTION ( 'NONE',  ( 0.000000000000000000, -6.982962677686266711E-15, 1.000000000000000000 ) ) ;
#134497=ORIENTED_EDGE ( 'NONE', *, *, #201590, .F. ) ;
#134555=ORIENTED_EDGE ( 'NONE', *, *, #23851, .F. ) ;
#134562=ORIENTED_EDGE ( 'NONE', *, *, #76155, .T. ) ;
#134585=EDGE_CURVE ( 'NONE', #112680, #224378, #100901, .T. ) ;
#134587=VERTEX_POINT ( 'NONE', #194151 ) ;
#134608=ORIENTED_EDGE ( 'NONE', *, *, #143887, .F. ) ;
#134626=DIRECTION ( 'NONE',  ( 0.000000000000000000, 1.000000000000000000, 6.982962677686267499E-15 ) ) ;
#134646=DIRECTION ( 'NONE',  ( -1.000000000000000000, 0.000000000000000000, -0.000000000000000000 ) ) ;
#134669=( BOUNDED_SURFACE ( )  B_SPLINE_SURFACE ( 3, 2, ( 
 ( #256025, #113994, #94434 ),
 ( #52737, #215654, #76151 ),
 ( #112727, #196120, #214387 ),
 ( #253504, #96966, #192276 ),
 ( #56563, #194853, #95713 ),
 ( #74912, #77422, #136103 ) ),
 .UNSPECIFIED., .F., .F., .F. ) 
 B_SPLINE_SURFACE_WITH_KNOTS ( ( 4, 2, 4 ),
 ( 3, 3 ),
 ( 0.0001300404313046550988, 0.0003183318589266533115, 0.0005066232865486515512 ),
 ( 0.000000000000000000, 1.000000000000000000 ),
 .UNSPECIFIED. ) 
 GEOMETRIC_REPRESENTATION_ITEM ( )  RATIONAL_B_SPLINE_SURFACE ( (
 ( 1.000000000000000000, 0.7071067811865597852, 1.000000000000000000),
 ( 1.000000000000000000, 0.7625113560543042013, 1.000000000000000000),
 ( 1.000000000000000000, 0.8126073484684787074, 1.000000000000000000),
 ( 1.000000000000000000, 0.8923049332736151529, 1.000000000000000000),
 ( 1.000000000000000000, 0.9231914937766685370, 1.000000000000000000),
 ( 1.000000000000000000, 0.9238795325112900692, 1.000000000000000000) ) ) 
 REPRESENTATION_ITEM ( '' )  SURFACE ( )  );
#134671=EDGE_CURVE ( 'NONE', #172794, #108629, #175997, .T. ) ;
#134673=CARTESIAN_POINT ( 'NONE',  ( -23.25000000000000000, 71.65000000001151648, -48.37310748452435405 ) ) ;
#134717=EDGE_CURVE ( 'NONE', #33150, #92669, #102695, .T. ) ;
#134737=DIRECTION ( 'NONE',  ( -1.000000000000000000, -0.000000000000000000, -0.000000000000000000 ) ) ;
#134739=EDGE_CURVE ( 'NONE', #33150, #117589, #246869, .T. ) ;
#134743=DIRECTION ( 'NONE',  ( 1.000000000000000000, 0.000000000000000000, 0.000000000000000000 ) ) ;
#134754=AXIS2_PLACEMENT_3D ( 'NONE', #127195, #84148, #171183 ) ;
#134760=CARTESIAN_POINT ( 'NONE',  ( 21.07928932188134397, 76.00000000001165290, -69.52310748452431710 ) ) ;
#134761=ORIENTED_EDGE ( 'NONE', *, *, #42597, .T. ) ;
#134781=CARTESIAN_POINT ( 'NONE',  ( 21.78635804494511419, 75.90099493450402690, -76.55876896967750156 ) ) ;
#134793=CIRCLE ( 'NONE', #22417, 0.6000000000000033085 ) ;
#134796=ORIENTED_EDGE ( 'NONE', *, *, #21057, .F. ) ;
#134801=EDGE_LOOP ( 'NONE', ( #69088, #227141, #139174, #34698 ) ) ;
#134832=ORIENTED_EDGE ( 'NONE', *, *, #65551, .T. ) ;
#134839=DIRECTION ( 'NONE',  ( 0.000000000000000000, 0.9915357197604862671, -0.1298341882519953583 ) ) ;
#134846=DIRECTION ( 'NONE',  ( -1.000000000000000000, -0.000000000000000000, -0.000000000000000000 ) ) ;
#134865=LINE ( 'NONE', #38369, #141108 ) ;
#134870=AXIS2_PLACEMENT_3D ( 'NONE', #165665, #88645, #27462 ) ;
#134886=EDGE_LOOP ( 'NONE', ( #655, #172870, #205212, #174762 ) ) ;
#134888=AXIS2_PLACEMENT_3D ( 'NONE', #128430, #168884, #150567 ) ;
#134899=ORIENTED_EDGE ( 'NONE', *, *, #210392, .F. ) ;
#134911=DIRECTION ( 'NONE',  ( 0.000000000000000000, -6.982962677686266711E-15, 1.000000000000000000 ) ) ;
#134942=LINE ( 'NONE', #155846, #103078 ) ;
#134951=DIRECTION ( 'NONE',  ( 0.000000000000000000, 0.000000000000000000, 1.000000000000000000 ) ) ;
#134968=CARTESIAN_POINT ( 'NONE',  ( -21.05000000000000071, 69.45934304831041572, -69.42310748452437963 ) ) ;
#135006=EDGE_LOOP ( 'NONE', ( #107794, #29579, #49558, #224771 ) ) ;
#135069=SHAPE_REPRESENTATION ( 'Injection Molded Chain Links 15', ( #2425 ), #106268 ) ;
#135099=DIRECTION ( 'NONE',  ( 0.000000000000000000, -0.9908441862701605762, -0.1350103645451835310 ) ) ;
#135111=ADVANCED_FACE ( 'NONE', ( #72294 ), #72287, .T. ) ;
#135112=CARTESIAN_POINT ( 'NONE',  ( -20.64999999999999858, 68.85000000001156195, -57.17310748452437252 ) ) ;
#135122=DIRECTION ( 'NONE',  ( -7.304098846218134667E-16, -1.000000000000000000, -6.982962677686267499E-15 ) ) ;
#135141=AXIS2_PLACEMENT_3D ( 'NONE', #13984, #173097, #90931 ) ;
#135160=DIRECTION ( 'NONE',  ( 0.000000000000000000, 0.000000000000000000, 1.000000000000000000 ) ) ;
#135161=DIRECTION ( 'NONE',  ( -0.000000000000000000, 0.8700118002898356018, -0.4930308989875170078 ) ) ;
#135162=TOROIDAL_SURFACE ( 'NONE', #64462, 4.099999999999999645, 0.1000000000000000056 ) ;
#135280=VECTOR ( 'NONE', #215172, 1000.000000000000000 ) ;
#135283=EDGE_CURVE ( 'NONE', #221285, #35500, #255376, .T. ) ;
#135284=ORIENTED_EDGE ( 'NONE', *, *, #232504, .F. ) ;
#135291=CARTESIAN_POINT ( 'NONE',  ( -20.54999999999999716, 85.00000000001149658, -45.91707660717669626 ) ) ;
#135299=FACE_OUTER_BOUND ( 'NONE', #215974, .T. ) ;
#135331=CARTESIAN_POINT ( 'NONE',  ( 20.94999999999999929, 87.65000000001141700, -36.02310748452425315 ) ) ;
#135334=CIRCLE ( 'NONE', #106286, 11.74999999999999645 ) ;
#135361=AXIS2_PLACEMENT_3D ( 'NONE', #93411, #153447, #54281 ) ;
#135364=CARTESIAN_POINT ( 'NONE',  ( -23.25000000000000000, 71.65000000001155911, -57.17310748452435121 ) ) ;
#135365=DIRECTION ( 'NONE',  ( 0.000000000000000000, 0.1455152366551500653, 0.9893560106964507384 ) ) ;
#135366=AXIS2_PLACEMENT_3D ( 'NONE', #119410, #219770, #20321 ) ;
#135368=CARTESIAN_POINT ( 'NONE',  ( -20.54999999999999716, 66.65000000001157332, -57.27310748452438816 ) ) ;
#135381=CARTESIAN_POINT ( 'NONE',  ( 21.05000000000000071, 76.00000000001142553, -36.02310748452432421 ) ) ;
#135389=CARTESIAN_POINT ( 'NONE',  ( -21.05000000000000071, 75.90220970870291239, -75.78092209500043452 ) ) ;
#135404=VECTOR ( 'NONE', #136032, 1000.000000000000000 ) ;
#135430=ORIENTED_EDGE ( 'NONE', *, *, #174793, .T. ) ;
#135446=EDGE_LOOP ( 'NONE', ( #82937, #176838, #172388 ) ) ;
#135454=CIRCLE ( 'NONE', #39646, 11.74999999999999645 ) ;
#135456=CARTESIAN_POINT ( 'NONE',  ( -20.94999999999999929, 68.96868720525620233, -32.41395654629707224 ) ) ;
#135458=ORIENTED_EDGE ( 'NONE', *, *, #76582, .F. ) ;
#135485=DIRECTION ( 'NONE',  ( 1.000000000000000000, 0.000000000000000000, 0.000000000000000000 ) ) ;
#135536=CARTESIAN_POINT ( 'NONE',  ( 22.47071067811864609, 68.27992525551361780, -69.62219993922697370 ) ) ;
#135548=EDGE_CURVE ( 'NONE', #106243, #251339, #255564, .T. ) ;
#135554=LINE ( 'NONE', #53470, #27552 ) ;
#135587=DIRECTION ( 'NONE',  ( 1.000000000000000000, 0.000000000000000000, 0.000000000000000000 ) ) ;
#135597=CIRCLE ( 'NONE', #10717, 0.09999999999999592548 ) ;
#135615=LINE ( 'NONE', #215164, #144316 ) ;
#135619=CARTESIAN_POINT ( 'NONE',  ( 20.88420186297724257, 65.66974365629616273, -30.43601455626050978 ) ) ;
#135677=EDGE_CURVE ( 'NONE', #206022, #238213, #19384, .T. ) ;
#135703=CIRCLE ( 'NONE', #23323, 11.80000000000000426 ) ;
#135710=ORIENTED_EDGE ( 'NONE', *, *, #213017, .F. ) ;
#135745=EDGE_CURVE ( 'NONE', #108629, #251339, #105748, .T. ) ;
#135772=FACE_OUTER_BOUND ( 'NONE', #194564, .T. ) ;
#135783=DIRECTION ( 'NONE',  ( -1.000000000000000000, 2.952720810173289112E-16, 2.061873921506763405E-30 ) ) ;
#135797=ORIENTED_EDGE ( 'NONE', *, *, #237285, .T. ) ;
#135808=ADVANCED_FACE ( 'NONE', ( #104019 ), #159765, .T. ) ;
#135830=CIRCLE ( 'NONE', #169194, 12.87499999999999822 ) ;
#135832=EDGE_CURVE ( 'NONE', #224073, #122696, #139061, .T. ) ;
#135855=DIRECTION ( 'NONE',  ( -1.000000000000000000, 2.952720810173289112E-16, 2.061873921506763405E-30 ) ) ;
#135943=CARTESIAN_POINT ( 'NONE',  ( 18.49999999999998934, 69.55000000001159322, -59.50608031408435039 ) ) ;
#135998=EDGE_CURVE ( 'NONE', #169291, #140287, #30978, .T. ) ;
#136001=ORIENTED_EDGE ( 'NONE', *, *, #252403, .F. ) ;
#136027=CARTESIAN_POINT ( 'NONE',  ( -18.49719636458555883, 85.44636535923967813, -62.45149361464103777 ) ) ;
#136032=DIRECTION ( 'NONE',  ( -3.265361837132813093E-16, -1.000000000000000000, -6.982962677686266711E-15 ) ) ;
#136036=DIRECTION ( 'NONE',  ( -1.000000000000000000, 3.265361837132813093E-16, 2.280189983783949500E-30 ) ) ;
#136037=ORIENTED_EDGE ( 'NONE', *, *, #119647, .F. ) ;
#136088=DIRECTION ( 'NONE',  ( 0.000000000000000000, -6.982962677686266711E-15, 1.000000000000000000 ) ) ;
#136103=CARTESIAN_POINT ( 'NONE',  ( 21.05000000000000071, 75.90220970870248607, -75.78092209500584886 ) ) ;
#136160=EDGE_CURVE ( 'NONE', #224073, #199876, #99077, .T. ) ;
#136169=CIRCLE ( 'NONE', #57070, 0.09999999999999971412 ) ;
#136171=DIRECTION ( 'NONE',  ( 0.000000000000000000, 0.000000000000000000, 1.000000000000000000 ) ) ;
#136191=FACE_OUTER_BOUND ( 'NONE', #89563, .T. ) ;
#136200=ORIENTED_EDGE ( 'NONE', *, *, #189492, .T. ) ;
#136228=DIRECTION ( 'NONE',  ( 0.000000000000000000, 0.000000000000000000, -1.000000000000000000 ) ) ;
#136244=CIRCLE ( 'NONE', #57141, 0.09999999999999939493 ) ;
#136252=DIRECTION ( 'NONE',  ( 0.000000000000000000, 0.000000000000000000, 1.000000000000000000 ) ) ;
#136253=DIRECTION ( 'NONE',  ( 0.000000000000000000, 0.000000000000000000, -1.000000000000000000 ) ) ;
#136259=ORIENTED_EDGE ( 'NONE', *, *, #4658, .T. ) ;
#136272=ORIENTED_EDGE ( 'NONE', *, *, #43336, .F. ) ;
#136296=FACE_OUTER_BOUND ( 'NONE', #57091, .T. ) ;
#136301=FACE_BOUND ( 'NONE', #125501, .T. ) ;
#136304=DIRECTION ( 'NONE',  ( -0.000000000000000000, 6.982962677686266711E-15, -1.000000000000000000 ) ) ;
#136329=CIRCLE ( 'NONE', #178079, 0.09999999999999939493 ) ;
#136352=AXIS2_PLACEMENT_3D ( 'NONE', #104877, #245721, #107486 ) ;
#136357=EDGE_CURVE ( 'NONE', #119594, #233017, #176896, .T. ) ;
#136365=DIRECTION ( 'NONE',  ( 1.000000000000000000, -2.952720810173289112E-16, -2.061873921506763405E-30 ) ) ;
#136380=ADVANCED_FACE ( 'NONE', ( #35015 ), #143557, .T. ) ;
#136392=CIRCLE ( 'NONE', #153626, 0.1000000000000028644 ) ;
#136416=TOROIDAL_SURFACE ( 'NONE', #223734, 12.77500000000000036, 0.1000000000000000056 ) ;
#136422=VERTEX_POINT ( 'NONE', #130202 ) ;
#136430=VERTEX_POINT ( 'NONE', #192770 ) ;
#136437=CIRCLE ( 'NONE', #211492, 0.1000000000000021289 ) ;
#136444=ORIENTED_EDGE ( 'NONE', *, *, #227686, .T. ) ;
#136473=ORIENTED_EDGE ( 'NONE', *, *, #128235, .F. ) ;
#136474=CARTESIAN_POINT ( 'NONE',  ( -22.50000000000000000, 76.00000000001173817, -81.17267829206912211 ) ) ;
#136490=ORIENTED_EDGE ( 'NONE', *, *, #70948, .T. ) ;
#136554=CIRCLE ( 'NONE', #24157, 0.1999999999999987899 ) ;
#136557=CARTESIAN_POINT ( 'NONE',  ( 20.11144452914042802, 66.06638914889163061, -61.63281403056953422 ) ) ;
#136570=EDGE_CURVE ( 'NONE', #153937, #256858, #31360, .T. ) ;
#136580=VERTEX_POINT ( 'NONE', #66079 ) ;
#136620=ORIENTED_EDGE ( 'NONE', *, *, #257612, .F. ) ;
#136629=DIRECTION ( 'NONE',  ( 0.000000000000000000, 0.5907332058517377193, -0.8068669527896954463 ) ) ;
#136659=DIRECTION ( 'NONE',  ( -7.304098846218134667E-16, 1.000000000000000000, 6.982962677686266711E-15 ) ) ;
#136695=DIRECTION ( 'NONE',  ( 0.000000000000000000, 0.1350103645451945777, -0.9908441862701591329 ) ) ;
#136730=VERTEX_POINT ( 'NONE', #24418 ) ;
#136734=CARTESIAN_POINT ( 'NONE',  ( -20.90851465518106167, 65.67467670974367877, -30.45317318268843820 ) ) ;
#136741=DIRECTION ( 'NONE',  ( 0.000000000000000000, 0.8700118002898356018, -0.4930308989875170078 ) ) ;
#136766=VERTEX_POINT ( 'NONE', #50341 ) ;
#136825=DIRECTION ( 'NONE',  ( 0.000000000000000000, -7.026728003956686545E-15, 1.000000000000000000 ) ) ;
#136827=EDGE_LOOP ( 'NONE', ( #223018, #2998, #35599, #123155 ) ) ;
#136831=CARTESIAN_POINT ( 'NONE',  ( -21.07954640115405809, 69.67071230398674686, -69.58911519166422011 ) ) ;
#136846=DIRECTION ( 'NONE',  ( 1.000000000000000000, 0.000000000000000000, 0.000000000000000000 ) ) ;
#136856=AXIS2_PLACEMENT_3D ( 'NONE', #23810, #163297, #165873 ) ;
#136859=ADVANCED_FACE ( 'NONE', ( #90761 ), #127170, .F. ) ;
#136860=CIRCLE ( 'NONE', #41207, 0.1000000000000000888 ) ;
#136886=FACE_OUTER_BOUND ( 'NONE', #87846, .T. ) ;
#136903=DIRECTION ( 'NONE',  ( 1.000000000000000000, 7.304098846218134667E-16, 5.100424963727256530E-30 ) ) ;
#136917=CARTESIAN_POINT ( 'NONE',  ( 20.89878130938411616, 65.67252876774480796, -30.44570419949946327 ) ) ;
#136925=CARTESIAN_POINT ( 'NONE',  ( 21.07928932188134397, 75.90110485435729970, -75.85162414091763594 ) ) ;
#136942=CARTESIAN_POINT ( 'NONE',  ( 18.43630871534874416, 85.67980087481434737, -29.36247541654018889 ) ) ;
#136944=DIRECTION ( 'NONE',  ( -0.000000000000000000, 6.982962677686266711E-15, -1.000000000000000000 ) ) ;
#136951=CARTESIAN_POINT ( 'NONE',  ( -22.39999999999999858, 76.00000000001173817, -81.17267829206912211 ) ) ;
#136993=EDGE_CURVE ( 'NONE', #89321, #31422, #152138, .T. ) ;
#137035=ORIENTED_EDGE ( 'NONE', *, *, #189092, .T. ) ;
#137039=VERTEX_POINT ( 'NONE', #79864 ) ;
#137086=VERTEX_POINT ( 'NONE', #86283 ) ;
#137124=DIRECTION ( 'NONE',  ( 0.000000000000000000, -6.982962677686266711E-15, 1.000000000000000000 ) ) ;
#137149=ORIENTED_EDGE ( 'NONE', *, *, #121264, .F. ) ;
#137153=CYLINDRICAL_SURFACE ( 'NONE', #140408, 0.1000000000000028644 ) ;
#137184=CIRCLE ( 'NONE', #95486, 0.09999999999999971412 ) ;
#137229=ORIENTED_EDGE ( 'NONE', *, *, #51226, .T. ) ;
#137245=EDGE_CURVE ( 'NONE', #56627, #13982, #57437, .T. ) ;
#137247=CARTESIAN_POINT ( 'NONE',  ( 20.94999999999999929, 87.39257802171711376, -39.09705706435617856 ) ) ;
#137284=DIRECTION ( 'NONE',  ( 0.7070776581709139474, 0.7071359030027652981, 2.946958787807621248E-14 ) ) ;
#137362=EDGE_CURVE ( 'NONE', #8048, #102057, #198241, .T. ) ;
#137384=EDGE_CURVE ( 'NONE', #193842, #91133, #150897, .T. ) ;
#137391=AXIS2_PLACEMENT_3D ( 'NONE', #173352, #252824, #112058 ) ;
#137408=B_SPLINE_CURVE_WITH_KNOTS ( 'NONE', 3,
 ( #20171, #222183, #159682, #99666, #163524, #162261, #239207, #60556, #123123, #117976, #21467, #240493, #63121, #24035, #59236, #197502 ),
 .UNSPECIFIED., .F., .F.,
 ( 4, 3, 3, 3, 3, 4 ),
 ( 0.000000000000000000, 2.372700795694236445E-05, 5.739057815866932760E-05, 9.073899019179894126E-05, 0.0001243544287365692729, 0.0001585386695601185094 ),
 .UNSPECIFIED. ) ;
#137409=DIRECTION ( 'NONE',  ( 0.000000000000000000, -0.4930308989875170078, -0.8700118002898356018 ) ) ;
#137455=DIRECTION ( 'NONE',  ( 0.000000000000000000, -0.5000000000000209832, 0.8660254037844264952 ) ) ;
#137463=ORIENTED_EDGE ( 'NONE', *, *, #133327, .F. ) ;
#137517=EDGE_CURVE ( 'NONE', #142182, #153937, #100961, .T. ) ;
#137522=EDGE_CURVE ( 'NONE', #51183, #136580, #105071, .T. ) ;
#137523=CARTESIAN_POINT ( 'NONE',  ( 18.49999999999999289, 64.35000000001147669, -44.67310748452440095 ) ) ;
#137566=VECTOR ( 'NONE', #110443, 1000.000000000000227 ) ;
#137574=CARTESIAN_POINT ( 'NONE',  ( 20.94999999999999929, 69.35000000001156195, -57.37310748452436826 ) ) ;
#137610=DIRECTION ( 'NONE',  ( -0.000000000000000000, -6.982962677686266711E-15, 1.000000000000000000 ) ) ;
#137622=ORIENTED_EDGE ( 'NONE', *, *, #122278, .F. ) ;
#137669=ORIENTED_EDGE ( 'NONE', *, *, #249582, .T. ) ;
#137733=DIRECTION ( 'NONE',  ( 1.000000000000000000, 0.000000000000000000, 0.000000000000000000 ) ) ;
#137739=ORIENTED_EDGE ( 'NONE', *, *, #142811, .T. ) ;
#137773=EDGE_CURVE ( 'NONE', #112792, #198094, #225703, .T. ) ;
#137795=CARTESIAN_POINT ( 'NONE',  ( -20.94999999999999929, 70.10000000001149090, -46.24220724918073699 ) ) ;
#137797=CARTESIAN_POINT ( 'NONE',  ( -21.65000000000000213, 68.29142135624888965, -57.27310748452437394 ) ) ;
#137827=CARTESIAN_POINT ( 'NONE',  ( -23.15000000000000213, 64.35000000001150511, -48.17310748452440095 ) ) ;
#137840=CARTESIAN_POINT ( 'NONE',  ( 20.74897398619119215, 65.40430697834514717, -61.84379602826854239 ) ) ;
#137859=ORIENTED_EDGE ( 'NONE', *, *, #212927, .T. ) ;
#137895=AXIS2_PLACEMENT_3D ( 'NONE', #29493, #251053, #72450 ) ;
#137909=DIRECTION ( 'NONE',  ( 0.000000000000000000, -6.982962677686266711E-15, 1.000000000000000000 ) ) ;
#137914=FACE_OUTER_BOUND ( 'NONE', #249752, .T. ) ;
#137937=LINE ( 'NONE', #237058, #43748 ) ;
#137961=DIRECTION ( 'NONE',  ( 1.000000000000000000, 0.000000000000000000, 0.000000000000000000 ) ) ;
#138000=ORIENTED_EDGE ( 'NONE', *, *, #166607, .F. ) ;
#138012=CARTESIAN_POINT ( 'NONE',  ( -20.93975676684922504, 65.68895814178191017, -30.50265578621382190 ) ) ;
#138014=DIRECTION ( 'NONE',  ( 0.000000000000000000, 1.000000000000000000, 6.352154140967427193E-15 ) ) ;
#138040=ORIENTED_EDGE ( 'NONE', *, *, #111226, .T. ) ;
#138054=CYLINDRICAL_SURFACE ( 'NONE', #24164, 11.75000000000000000 ) ;
#138078=DIRECTION ( 'NONE',  ( -0.7071067811865127117, -0.7071067811865821007, 0.000000000000000000 ) ) ;
#138086=VECTOR ( 'NONE', #67674, 1000.000000000000000 ) ;
#138092=AXIS2_PLACEMENT_3D ( 'NONE', #186567, #88707, #168320 ) ;
#138098=CARTESIAN_POINT ( 'NONE',  ( 20.85000000000000142, 76.00000000001142553, -36.02310748452432421 ) ) ;
#138101=CARTESIAN_POINT ( 'NONE',  ( -20.54999999999999716, 85.00000000001149658, -45.91707660717669626 ) ) ;
#138134=( BOUNDED_SURFACE ( )  B_SPLINE_SURFACE ( 3, 2, ( 
 ( #220355, #161675, #242457 ),
 ( #123817, #65112, #2560 ),
 ( #102939, #100363, #182522 ),
 ( #122539, #40463, #5105 ) ),
 .UNSPECIFIED., .F., .F., .F. ) 
 B_SPLINE_SURFACE_WITH_KNOTS ( ( 4, 4 ),
 ( 3, 3 ),
 ( 0.04058434257139457990, 0.04256401539001584966 ),
 ( 0.000000000000000000, 1.000000000000000000 ),
 .UNSPECIFIED. ) 
 GEOMETRIC_REPRESENTATION_ITEM ( )  RATIONAL_B_SPLINE_SURFACE ( (
 ( 1.000000000000000000, 0.7103081912008383236, 1.000000000000000000),
 ( 1.000000000000000000, 0.7104998333555154755, 1.000000000000000000),
 ( 1.000000000000000000, 0.7107238315755263214, 1.000000000000000000),
 ( 1.000000000000000000, 0.7110073749539205235, 1.000000000000000000) ) ) 
 REPRESENTATION_ITEM ( '' )  SURFACE ( )  );
#138139=CYLINDRICAL_SURFACE ( 'NONE', #188239, 0.1000000000000064587 ) ;
#138152=VERTEX_POINT ( 'NONE', #243164 ) ;
#138180=FACE_OUTER_BOUND ( 'NONE', #29436, .T. ) ;
#138182=CARTESIAN_POINT ( 'NONE',  ( -20.54999999999999716, 71.75000000001156764, -57.27310748452435263 ) ) ;
#138187=CARTESIAN_POINT ( 'NONE',  ( 21.08078803292165659, 69.66698703557453598, -69.60229347168214531 ) ) ;
#138220=CARTESIAN_POINT ( 'NONE',  ( 20.94999999999999929, 85.00000000001149658, -45.91707660717670336 ) ) ;
#138267=CARTESIAN_POINT ( 'NONE',  ( -18.47653818581421348, 85.46528038777458391, -62.39714666838443691 ) ) ;
#138274=CARTESIAN_POINT ( 'NONE',  ( 21.14999999999999503, 87.75000000001173817, -81.27310748452423184 ) ) ;
#138341=DIRECTION ( 'NONE',  ( 9.044546369203337730E-15, 0.7397360091702647189, 0.6728971962616949742 ) ) ;
#138352=CARTESIAN_POINT ( 'NONE',  ( 18.59999999999999076, 65.79142135624880439, -48.17310748452439384 ) ) ;
#138421=EDGE_CURVE ( 'NONE', #152525, #229077, #179076, .T. ) ;
#138427=ORIENTED_EDGE ( 'NONE', *, *, #117001, .T. ) ;
#138465=EDGE_CURVE ( 'NONE', #85964, #128522, #240309, .T. ) ;
#138518=ADVANCED_FACE ( 'NONE', ( #149893 ), #61662, .T. ) ;
#138542=EDGE_LOOP ( 'NONE', ( #211414, #197506, #197219, #131937 ) ) ;
#138562=AXIS2_PLACEMENT_3D ( 'NONE', #57854, #14919, #171448 ) ;
#138587=CARTESIAN_POINT ( 'NONE',  ( -18.59999999999999787, 64.35000000001161879, -62.50830171387040934 ) ) ;
#138624=ORIENTED_EDGE ( 'NONE', *, *, #112856, .T. ) ;
#138625=PLANE ( 'NONE',  #173020 ) ;
#138637=CARTESIAN_POINT ( 'NONE',  ( 23.14999999999999503, 64.35000000001156195, -57.37310748452439668 ) ) ;
#138640=DIRECTION ( 'NONE',  ( 0.000000000000000000, -0.9274965247785555977, 0.3738317757009190223 ) ) ;
#138673=VECTOR ( 'NONE', #93682, 1000.000000000000000 ) ;
#138723=ORIENTED_EDGE ( 'NONE', *, *, #74709, .T. ) ;
#138773=ORIENTED_EDGE ( 'NONE', *, *, #140460, .F. ) ;
#138788=DIRECTION ( 'NONE',  ( -1.000000000000000000, -0.000000000000000000, -0.000000000000000000 ) ) ;
#138789=FACE_OUTER_BOUND ( 'NONE', #81795, .T. ) ;
#138795=VERTEX_POINT ( 'NONE', #240961 ) ;
#138821=CARTESIAN_POINT ( 'NONE',  ( 21.87500000000000355, 66.25000000001151079, -48.27310748452438816 ) ) ;
#138854=ORIENTED_EDGE ( 'NONE', *, *, #149109, .T. ) ;
#138858=VERTEX_POINT ( 'NONE', #68745 ) ;
#138859=DIRECTION ( 'NONE',  ( -0.000000000000000000, -1.000000000000000000, -6.982962677686266711E-15 ) ) ;
#138865=DIRECTION ( 'NONE',  ( 0.000000000000000000, 6.982962677686266711E-15, -1.000000000000000000 ) ) ;
#138869=ORIENTED_EDGE ( 'NONE', *, *, #48096, .F. ) ;
#138874=DIRECTION ( 'NONE',  ( 0.000000000000000000, -6.769652589177784668E-15, 1.000000000000000000 ) ) ;
#138875=DIRECTION ( 'NONE',  ( 0.000000000000000000, 0.000000000000000000, -1.000000000000000000 ) ) ;
#138915=AXIS2_PLACEMENT_3D ( 'NONE', #58830, #160554, #241365 ) ;
#138933=EDGE_CURVE ( 'NONE', #9118, #233017, #80702, .T. ) ;
#138958=CIRCLE ( 'NONE', #26590, 11.65000000000000036 ) ;
#138969=DIRECTION ( 'NONE',  ( 0.000000000000000000, -7.189901751995769991E-15, 1.000000000000000000 ) ) ;
#139032=AXIS2_PLACEMENT_3D ( 'NONE', #107464, #249563, #52622 ) ;
#139055=ORIENTED_EDGE ( 'NONE', *, *, #42570, .T. ) ;
#139061=CIRCLE ( 'NONE', #26693, 0.09999999999999939493 ) ;
#139069=EDGE_CURVE ( 'NONE', #13982, #202471, #67861, .T. ) ;
#139080=VECTOR ( 'NONE', #73191, 1000.000000000000000 ) ;
#139091=DIRECTION ( 'NONE',  ( 0.000000000000000000, 6.982962677686266711E-15, -1.000000000000000000 ) ) ;
#139102=CARTESIAN_POINT ( 'NONE',  ( 20.21567752745066215, 65.80188589877963068, -61.64048713687273562 ) ) ;
#139141=B_SPLINE_CURVE_WITH_KNOTS ( 'NONE', 3,
 ( #245257, #147431, #224386, #189126, #66615, #226967, #70499, #86137, #65317, #24939 ),
 .UNSPECIFIED., .F., .F.,
 ( 4, 3, 3, 4 ),
 ( 0.000000000000000000, 3.394313611811022212E-05, 6.779740500700426732E-05, 0.0001049857339142650257 ),
 .UNSPECIFIED. ) ;
#139149=EDGE_CURVE ( 'NONE', #122601, #175419, #76220, .T. ) ;
#139174=ORIENTED_EDGE ( 'NONE', *, *, #11343, .F. ) ;
#139193=DIRECTION ( 'NONE',  ( -1.000000000000000000, -0.000000000000000000, -0.000000000000000000 ) ) ;
#139208=VERTEX_POINT ( 'NONE', #37331 ) ;
#139233=AXIS2_PLACEMENT_3D ( 'NONE', #55950, #132963, #251609 ) ;
#139246=DIRECTION ( 'NONE',  ( 1.000000000000000000, 0.000000000000000000, 0.000000000000000000 ) ) ;
#139271=EDGE_CURVE ( 'NONE', #158894, #46909, #114221, .T. ) ;
#139291=CIRCLE ( 'NONE', #185113, 0.1000000000000014488 ) ;
#139294=DIRECTION ( 'NONE',  ( 0.000000000000000000, -1.000000000000000000, -6.982962677686266711E-15 ) ) ;
#139311=ORIENTED_EDGE ( 'NONE', *, *, #42913, .F. ) ;
#139332=FACE_OUTER_BOUND ( 'NONE', #25212, .T. ) ;
#139355=DIRECTION ( 'NONE',  ( 0.7071067811865475727, -0.7071067811865475727, -5.142139384388981164E-15 ) ) ;
#139366=EDGE_LOOP ( 'NONE', ( #66658, #255916, #174975, #169252 ) ) ;
#139382=DIRECTION ( 'NONE',  ( 0.000000000000000000, 0.000000000000000000, -1.000000000000000000 ) ) ;
#139397=CYLINDRICAL_SURFACE ( 'NONE', #93903, 0.1000000000000028644 ) ;
#139410=CARTESIAN_POINT ( 'NONE',  ( -20.85000000000000142, 68.97833521811131163, -32.28954208262708647 ) ) ;
#139473=CARTESIAN_POINT ( 'NONE',  ( 18.59999999999996945, 65.66751761918619934, -30.42826094061123854 ) ) ;
#139511=CARTESIAN_POINT ( 'NONE',  ( 22.39999999999999503, 64.35000000001164722, -69.42310748452440805 ) ) ;
#139513=AXIS2_PLACEMENT_3D ( 'NONE', #189447, #245569, #70804 ) ;
#139547=CARTESIAN_POINT ( 'NONE',  ( -20.00857864376270001, 66.85000000001150511, -48.37310748452438247 ) ) ;
#139554=CYLINDRICAL_SURFACE ( 'NONE', #65529, 11.79999999999999716 ) ;
#139555=CARTESIAN_POINT ( 'NONE',  ( -18.39999999999999858, 85.50000000001161027, -62.49103808782458458 ) ) ;
#139559=LINE ( 'NONE', #17086, #243123 ) ;
#139595=EDGE_CURVE ( 'NONE', #178236, #147021, #184551, .T. ) ;
#139597=FACE_OUTER_BOUND ( 'NONE', #239979, .T. ) ;
#139598=ORIENTED_EDGE ( 'NONE', *, *, #158339, .T. ) ;
#139616=AXIS2_PLACEMENT_3D ( 'NONE', #164563, #1614, #163283 ) ;
#139676=ORIENTED_EDGE ( 'NONE', *, *, #195180, .T. ) ;
#139690=EDGE_CURVE ( 'NONE', #41808, #208701, #222133, .T. ) ;
#139702=DIRECTION ( 'NONE',  ( 0.000000000000000000, 1.000000000000000000, 6.982962677686266711E-15 ) ) ;
#139773=AXIS2_PLACEMENT_3D ( 'NONE', #208433, #248832, #70212 ) ;
#139793=LINE ( 'NONE', #122835, #103486 ) ;
#139804=AXIS2_PLACEMENT_3D ( 'NONE', #229157, #186175, #50479 ) ;
#139822=ORIENTED_EDGE ( 'NONE', *, *, #217354, .T. ) ;
#139831=DIRECTION ( 'NONE',  ( 1.000000000000000000, -2.952720810173289112E-16, -2.061873921506763405E-30 ) ) ;
#139895=VERTEX_POINT ( 'NONE', #184126 ) ;
#139911=ORIENTED_EDGE ( 'NONE', *, *, #1896, .T. ) ;
#139924=DIRECTION ( 'NONE',  ( 0.000000000000000000, 6.982962677686266711E-15, -1.000000000000000000 ) ) ;
#139944=ORIENTED_EDGE ( 'NONE', *, *, #210765, .T. ) ;
#139953=AXIS2_PLACEMENT_3D ( 'NONE', #40072, #180842, #158735 ) ;
#139974=CARTESIAN_POINT ( 'NONE',  ( 21.05000000000000071, 71.00000000001151079, -48.42837350343745584 ) ) ;
#139983=ADVANCED_FACE ( 'NONE', ( #129302 ), #208837, .T. ) ;
#139997=CARTESIAN_POINT ( 'NONE',  ( -20.05000000000000426, 66.75000000001158185, -57.17310748452438673 ) ) ;
#140034=CARTESIAN_POINT ( 'NONE',  ( -23.25000000000000000, 64.25000000001151079, -48.17310748452440805 ) ) ;
#140043=CARTESIAN_POINT ( 'NONE',  ( 20.85000000000000142, 77.36242903720467723, -28.13422623660311217 ) ) ;
#140044=CARTESIAN_POINT ( 'NONE',  ( 18.59999999999999076, 69.55000000001159322, -59.50608031408435039 ) ) ;
#140056=CARTESIAN_POINT ( 'NONE',  ( 22.59066674512251183, 64.25000000001163869, -69.55361160815502330 ) ) ;
#140093=CARTESIAN_POINT ( 'NONE',  ( 20.85000000000000142, 87.75000000001142553, -38.92310748452424463 ) ) ;
#140099=DIRECTION ( 'NONE',  ( 0.000000000000000000, 0.000000000000000000, 1.000000000000000000 ) ) ;
#140149=EDGE_CURVE ( 'NONE', #166958, #181320, #180851, .T. ) ;
#140153=VECTOR ( 'NONE', #206486, 1000.000000000000000 ) ;
#140164=FACE_BOUND ( 'NONE', #100531, .T. ) ;
#140165=TOROIDAL_SURFACE ( 'NONE', #215205, 4.149999999999999467, 0.1000000000000000056 ) ;
#140169=LINE ( 'NONE', #102309, #9833 ) ;
#140228=CARTESIAN_POINT ( 'NONE',  ( -23.25000000000000000, 87.75000000001165290, -69.52310748452424605 ) ) ;
#140235=DIRECTION ( 'NONE',  ( 0.000000000000000000, 0.000000000000000000, 1.000000000000000000 ) ) ;
#140240=ORIENTED_EDGE ( 'NONE', *, *, #40186, .T. ) ;
#140242=DIRECTION ( 'NONE',  ( -1.000000000000000000, 0.000000000000000000, -0.000000000000000000 ) ) ;
#140254=CARTESIAN_POINT ( 'NONE',  ( 22.39999999999999503, 64.35000000001164722, -69.62310748452439668 ) ) ;
#140287=VERTEX_POINT ( 'NONE', #66452 ) ;
#140351=CARTESIAN_POINT ( 'NONE',  ( 20.04142135623730070, 64.35000000001147669, -44.87310748452440379 ) ) ;
#140356=AXIS2_PLACEMENT_3D ( 'NONE', #166203, #171354, #187041 ) ;
#140376=ORIENTED_EDGE ( 'NONE', *, *, #118794, .T. ) ;
#140389=DIRECTION ( 'NONE',  ( 0.000000000000000000, 0.000000000000000000, -1.000000000000000000 ) ) ;
#140408=AXIS2_PLACEMENT_3D ( 'NONE', #159308, #139702, #60173 ) ;
#140412=CARTESIAN_POINT ( 'NONE',  ( 20.77526135991769607, 67.06799098339034515, -61.05453894179962049 ) ) ;
#140435=CARTESIAN_POINT ( 'NONE',  ( -21.05000000000000071, 75.90220970870291239, -75.78092209500044873 ) ) ;
#140460=EDGE_CURVE ( 'NONE', #194241, #177733, #47730, .T. ) ;
#140469=CIRCLE ( 'NONE', #215499, 0.1000000000000028644 ) ;
#140501=ORIENTED_EDGE ( 'NONE', *, *, #137522, .T. ) ;
#140502=ORIENTED_EDGE ( 'NONE', *, *, #138421, .T. ) ;
#140513=DIRECTION ( 'NONE',  ( 0.000000000000000000, 7.086529944415894657E-15, -1.000000000000000000 ) ) ;
#140548=DIRECTION ( 'NONE',  ( -1.000000000000000000, 2.952720810173289112E-16, 2.061873921506763405E-30 ) ) ;
#140564=CARTESIAN_POINT ( 'NONE',  ( -20.54999999999999716, 66.65000000001150227, -48.37310748452438958 ) ) ;
#140574=ORIENTED_EDGE ( 'NONE', *, *, #126665, .F. ) ;
#140581=ORIENTED_EDGE ( 'NONE', *, *, #192727, .T. ) ;
#140592=LINE ( 'NONE', #23254, #253214 ) ;
#140618=EDGE_LOOP ( 'NONE', ( #137035, #250300, #246428, #138869, #200228 ) ) ;
#140643=EDGE_CURVE ( 'NONE', #6026, #64921, #18530, .T. ) ;
#140669=ORIENTED_EDGE ( 'NONE', *, *, #17254, .T. ) ;
#140712=AXIS2_PLACEMENT_3D ( 'NONE', #176611, #13665, #256062 ) ;
#140755=CIRCLE ( 'NONE', #28363, 0.1000000000000028644 ) ;
#140761=CARTESIAN_POINT ( 'NONE',  ( -18.59999999999999787, 74.75000000001159606, -61.52310748452433131 ) ) ;
#140771=CARTESIAN_POINT ( 'NONE',  ( -20.64999999999999858, 74.05981308412370367, -56.69398827347101388 ) ) ;
#140772=CARTESIAN_POINT ( 'NONE',  ( -20.64999999999999858, 68.85000000001156195, -57.27310748452436684 ) ) ;
#140777=DIRECTION ( 'NONE',  ( 1.000000000000000000, 0.000000000000000000, 0.000000000000000000 ) ) ;
#140781=CARTESIAN_POINT ( 'NONE',  ( -20.94999999999999929, 77.16412189325258453, -28.10825939895270764 ) ) ;
#140788=EDGE_CURVE ( 'NONE', #168638, #162902, #64500, .T. ) ;
#140794=AXIS2_PLACEMENT_3D ( 'NONE', #28505, #107996, #8896 ) ;
#140801=B_SPLINE_CURVE_WITH_KNOTS ( 'NONE', 3,
 ( #121839, #201359, #145226, #162257, #86518, #107390, #245630, #5701, #241763, #184354, #26600, #46132, #143945, #125674, #224762, #141379, #64426, #63118, #244329 ),
 .UNSPECIFIED., .F., .F.,
 ( 4, 3, 3, 3, 3, 3, 4 ),
 ( 0.000000000000000000, 1.655171619026205498E-05, 2.773500582849481967E-05, 5.941817267378896972E-05, 0.0001114174635873591685, 0.0001914169455916391949, 0.0002627181070750695150 ),
 .UNSPECIFIED. ) ;
#140806=EDGE_LOOP ( 'NONE', ( #230702, #44011, #121197, #248442 ) ) ;
#140829=ORIENTED_EDGE ( 'NONE', *, *, #36194, .F. ) ;
#140893=DIRECTION ( 'NONE',  ( 1.000000000000000000, 0.000000000000000000, 0.000000000000000000 ) ) ;
#140895=EDGE_CURVE ( 'NONE', #176023, #89706, #236439, .T. ) ;
#140918=ORIENTED_EDGE ( 'NONE', *, *, #57762, .F. ) ;
#140919=EDGE_CURVE ( 'NONE', #65120, #68194, #201165, .T. ) ;
#140932=CARTESIAN_POINT ( 'NONE',  ( 23.15000000000000213, 85.00000000001159606, -59.62913836187181715 ) ) ;
#140935=FACE_OUTER_BOUND ( 'NONE', #148923, .T. ) ;
#140950=AXIS2_PLACEMENT_3D ( 'NONE', #52217, #49666, #7986 ) ;
#140953=ORIENTED_EDGE ( 'NONE', *, *, #40244, .T. ) ;
#140974=ADVANCED_FACE ( 'NONE', ( #206313 ), #86324, .F. ) ;
#141018=FACE_OUTER_BOUND ( 'NONE', #188379, .T. ) ;
#141023=DIRECTION ( 'NONE',  ( 1.000000000000000000, 0.000000000000000000, 0.000000000000000000 ) ) ;
#141024=ORIENTED_EDGE ( 'NONE', *, *, #135998, .T. ) ;
#141044=CARTESIAN_POINT ( 'NONE',  ( -20.64999999999999858, 76.00000000001149658, -48.89810748452431710 ) ) ;
#141065=CARTESIAN_POINT ( 'NONE',  ( -23.25000000000000000, 70.05000000001149374, -46.32880978955918039 ) ) ;
#141088=CIRCLE ( 'NONE', #207741, 4.099999999999999645 ) ;
#141108=VECTOR ( 'NONE', #20095, 1000.000000000000000 ) ;
#141118=CARTESIAN_POINT ( 'NONE',  ( -20.94999999999999929, 64.40000000001147384, -42.95131071479990936 ) ) ;
#141188=EDGE_CURVE ( 'NONE', #253373, #248043, #114577, .T. ) ;
#141233=ORIENTED_EDGE ( 'NONE', *, *, #104966, .T. ) ;
#141255=ORIENTED_EDGE ( 'NONE', *, *, #219033, .F. ) ;
#141264=AXIS2_PLACEMENT_3D ( 'NONE', #153668, #184390, #223507 ) ;
#141301=CARTESIAN_POINT ( 'NONE',  ( 21.14999999999999858, 69.45934304831041572, -69.52310748452435973 ) ) ;
#141332=ORIENTED_EDGE ( 'NONE', *, *, #136160, .F. ) ;
#141336=EDGE_CURVE ( 'NONE', #201923, #30729, #35677, .T. ) ;
#141348=CARTESIAN_POINT ( 'NONE',  ( -21.30740335185486245, 75.90106547423584971, -76.07976540655232611 ) ) ;
#141350=CARTESIAN_POINT ( 'NONE',  ( 20.95017935633852346, 65.52451072038628865, -61.94566768713390559 ) ) ;
#141367=CARTESIAN_POINT ( 'NONE',  ( -18.50000000000000000, 70.05000000001165006, -59.21740517948951066 ) ) ;
#141368=AXIS2_PLACEMENT_3D ( 'NONE', #179302, #178009, #157170 ) ;
#141371=DIRECTION ( 'NONE',  ( 1.000000000000000000, -0.000000000000000000, 0.000000000000000000 ) ) ;
#141379=CARTESIAN_POINT ( 'NONE',  ( -21.12757541349819590, 75.99483878420197414, -75.99648805577588462 ) ) ;
#141394=CARTESIAN_POINT ( 'NONE',  ( 21.14999999999999858, 67.21339244341145047, -57.27310748452438105 ) ) ;
#141405=EDGE_CURVE ( 'NONE', #178434, #223761, #186451, .T. ) ;
#141473=EDGE_CURVE ( 'NONE', #149811, #183814, #164648, .T. ) ;
#141488=CIRCLE ( 'NONE', #249832, 0.1999999999999987899 ) ;
#141503=FACE_OUTER_BOUND ( 'NONE', #79660, .T. ) ;
#141505=CIRCLE ( 'NONE', #174897, 11.79999999999999716 ) ;
#141518=ORIENTED_EDGE ( 'NONE', *, *, #110285, .T. ) ;
#141526=CARTESIAN_POINT ( 'NONE',  ( -23.15000000000000213, 64.35000000001146248, -43.03791325517834565 ) ) ;
#141531=ORIENTED_EDGE ( 'NONE', *, *, #137517, .T. ) ;
#141545=CARTESIAN_POINT ( 'NONE',  ( -21.05000000000000071, 76.00000000001165290, -69.52310748452431710 ) ) ;
#141567=ORIENTED_EDGE ( 'NONE', *, *, #59576, .F. ) ;
#141579=ADVANCED_FACE ( 'NONE', ( #108197 ), #29962, .T. ) ;
#141609=DIRECTION ( 'NONE',  ( 0.000000000000000000, 7.086529944415894657E-15, -1.000000000000000000 ) ) ;
#141611=DIRECTION ( 'NONE',  ( -0.000000000000000000, 1.000000000000000000, 6.982962677686266711E-15 ) ) ;
#141630=DIRECTION ( 'NONE',  ( 0.000000000000000000, -7.172728831056617961E-15, 1.000000000000000000 ) ) ;
#141647=CARTESIAN_POINT ( 'NONE',  ( -20.54999999999999716, 76.00000000001142553, -36.02310748452432421 ) ) ;
#141662=CARTESIAN_POINT ( 'NONE',  ( 19.96984138294284250, 64.25000000001146816, -44.79853541332327893 ) ) ;
#141680=FACE_OUTER_BOUND ( 'NONE', #196641, .T. ) ;
#141685=FACE_OUTER_BOUND ( 'NONE', #166280, .T. ) ;
#141701=CARTESIAN_POINT ( 'NONE',  ( 20.86036036209904054, 65.37895722344063643, -61.85675906601803575 ) ) ;
#141705=CARTESIAN_POINT ( 'NONE',  ( 20.94999999999999929, 85.50000000001149658, -45.91707660717669626 ) ) ;
#141726=CARTESIAN_POINT ( 'NONE',  ( 20.94999999999999929, 68.97833521811131163, -32.18954208262707795 ) ) ;
#141760=CARTESIAN_POINT ( 'NONE',  ( -18.59999999999999787, 64.35000000001141984, -36.02310748452440237 ) ) ;
#141777=EDGE_CURVE ( 'NONE', #234494, #36355, #222668, .T. ) ;
#141786=DIRECTION ( 'NONE',  ( 1.000000000000000000, 0.000000000000000000, 0.000000000000000000 ) ) ;
#141794=ORIENTED_EDGE ( 'NONE', *, *, #3716, .F. ) ;
#141826=VECTOR ( 'NONE', #190097, 1000.000000000000000 ) ;
#141868=ORIENTED_EDGE ( 'NONE', *, *, #125511, .F. ) ;
#141955=FACE_OUTER_BOUND ( 'NONE', #51241, .T. ) ;
#141957=CARTESIAN_POINT ( 'NONE',  ( 22.37643362114956247, 68.37421000605328913, -69.62218885820576020 ) ) ;
#141976=CARTESIAN_POINT ( 'NONE',  ( -23.25000000000000000, 73.40000000001157332, -56.29848556176223440 ) ) ;
#142006=DIRECTION ( 'NONE',  ( 0.000000000000000000, -0.9999631594459053030, -0.008583690987162452199 ) ) ;
#142050=EDGE_LOOP ( 'NONE', ( #195038, #214556, #104398, #207866 ) ) ;
#142094=EDGE_LOOP ( 'NONE', ( #53451, #169804, #226807, #114072 ) ) ;
#142122=CYLINDRICAL_SURFACE ( 'NONE', #109641, 0.1000000000000028644 ) ;
#142123=CARTESIAN_POINT ( 'NONE',  ( 20.85000000000000142, 64.35000000001146248, -42.80697314750249660 ) ) ;
#142158=CARTESIAN_POINT ( 'NONE',  ( -18.59999999999999787, 64.25000000001142553, -36.02310748452440237 ) ) ;
#142182=VERTEX_POINT ( 'NONE', #222347 ) ;
#142201=DIRECTION ( 'NONE',  ( 2.952720810173289112E-16, 1.000000000000000000, 9.912705577010238578E-15 ) ) ;
#142217=DIRECTION ( 'NONE',  ( -1.000000000000000000, -0.000000000000000000, -0.000000000000000000 ) ) ;
#142243=DIRECTION ( 'NONE',  ( 0.000000000000000000, 1.000000000000000000, 0.000000000000000000 ) ) ;
#142250=PLANE ( 'NONE',  #3938 ) ;
#142251=DIRECTION ( 'NONE',  ( -1.000000000000000000, -0.000000000000000000, -0.000000000000000000 ) ) ;
#142260=VECTOR ( 'NONE', #174823, 1000.000000000000000 ) ;
#142280=CARTESIAN_POINT ( 'NONE',  ( -21.05000000000000071, 64.35000000001161879, -62.73924182154625129 ) ) ;
#142298=CYLINDRICAL_SURFACE ( 'NONE', #19124, 0.09999999999999939493 ) ;
#142316=ORIENTED_EDGE ( 'NONE', *, *, #205291, .T. ) ;
#142329=VECTOR ( 'NONE', #232182, 1000.000000000000000 ) ;
#142338=EDGE_CURVE ( 'NONE', #30032, #231849, #206698, .T. ) ;
#142340=CARTESIAN_POINT ( 'NONE',  ( 22.40000000000010516, 76.00000000001267608, -81.17267829206943475 ) ) ;
#142366=CARTESIAN_POINT ( 'NONE',  ( -20.94999999999999929, 77.83534155023598089, -57.86795619196132634 ) ) ;
#142375=EDGE_CURVE ( 'NONE', #187652, #5270, #123491, .T. ) ;
#142407=EDGE_CURVE ( 'NONE', #148706, #175005, #131873, .T. ) ;
#142415=ORIENTED_EDGE ( 'NONE', *, *, #37352, .F. ) ;
#142427=DIRECTION ( 'NONE',  ( 0.000000000000000000, -1.000000000000000000, 0.000000000000000000 ) ) ;
#142460=CARTESIAN_POINT ( 'NONE',  ( -18.39999999999999858, 85.50000000001138289, -29.42291809330221497 ) ) ;
#142470=EDGE_CURVE ( 'NONE', #257957, #85029, #27851, .T. ) ;
#142481=DIRECTION ( 'NONE',  ( 1.000000000000000000, 0.000000000000000000, 0.000000000000000000 ) ) ;
#142482=EDGE_LOOP ( 'NONE', ( #159083, #140829, #227580, #154798 ) ) ;
#142525=VERTEX_POINT ( 'NONE', #87359 ) ;
#142546=EDGE_CURVE ( 'NONE', #162078, #68363, #67812, .T. ) ;
#142552=VECTOR ( 'NONE', #134911, 1000.000000000000000 ) ;
#142561=CARTESIAN_POINT ( 'NONE',  ( -20.94999999999999929, 87.39257802171731271, -66.44915790469229933 ) ) ;
#142562=CARTESIAN_POINT ( 'NONE',  ( -21.05000000000000071, 88.41227409416111982, -38.92310748452423752 ) ) ;
#142571=DIRECTION ( 'NONE',  ( -1.000000000000000000, 0.000000000000000000, 0.000000000000000000 ) ) ;
#142583=CARTESIAN_POINT ( 'NONE',  ( -23.25000000000000000, 85.68240343348777799, -29.36626410711146562 ) ) ;
#142587=DIRECTION ( 'NONE',  ( 0.000000000000000000, -0.1350103645451807555, -0.9908441862701610203 ) ) ;
#142613=CARTESIAN_POINT ( 'NONE',  ( 20.95132126680579887, 65.51005012986480835, -61.95278294608986869 ) ) ;
#142618=DIRECTION ( 'NONE',  ( 0.000000000000000000, 0.4999999999999689138, -0.8660254037844565822 ) ) ;
#142644=SPHERICAL_SURFACE ( 'NONE', #168020, 0.1000000000000000056 ) ;
#142654=ORIENTED_EDGE ( 'NONE', *, *, #85648, .T. ) ;
#142655=CARTESIAN_POINT ( 'NONE',  ( -20.85000000000000142, 64.25000000001142553, -36.02310748452440237 ) ) ;
#142666=CIRCLE ( 'NONE', #246728, 0.09999999999999938105 ) ;
#142673=DIRECTION ( 'NONE',  ( -3.265361837132813093E-16, -1.000000000000000000, -7.086529944415894657E-15 ) ) ;
#142679=DIRECTION ( 'NONE',  ( 1.000000000000000000, 0.000000000000000000, 0.000000000000000000 ) ) ;
#142706=CARTESIAN_POINT ( 'NONE',  ( 23.14999999999999858, 76.00000000001142553, -36.02310748452432421 ) ) ;
#142709=ORIENTED_EDGE ( 'NONE', *, *, #69433, .F. ) ;
#142738=DIRECTION ( 'NONE',  ( 1.000000000000000000, 0.000000000000000000, 0.000000000000000000 ) ) ;
#142810=CIRCLE ( 'NONE', #9558, 7.720710678118678061 ) ;
#142811=EDGE_CURVE ( 'NONE', #64683, #178434, #190330, .T. ) ;
#142859=VERTEX_POINT ( 'NONE', #257953 ) ;
#142871=CARTESIAN_POINT ( 'NONE',  ( 23.25000000000000000, 87.48912529308749697, -39.12310748452424747 ) ) ;
#142873=CARTESIAN_POINT ( 'NONE',  ( 18.59999999999999432, 74.36282728704118483, -57.94095411905231430 ) ) ;
#142889=EDGE_LOOP ( 'NONE', ( #50263, #249934, #157659, #221672 ) ) ;
#142920=ORIENTED_EDGE ( 'NONE', *, *, #10280, .F. ) ;
#142922=CARTESIAN_POINT ( 'NONE',  ( -21.07928932188134041, 69.67148334361836248, -69.62200263017875557 ) ) ;
#142945=LINE ( 'NONE', #67285, #124100 ) ;
#142951=CYLINDRICAL_SURFACE ( 'NONE', #30964, 0.1000000000000028644 ) ;
#142969=CARTESIAN_POINT ( 'NONE',  ( 18.59999999999999787, 77.83585931145498193, -24.51866831572578675 ) ) ;
#142976=DIRECTION ( 'NONE',  ( 0.000000000000000000, 0.000000000000000000, 1.000000000000000000 ) ) ;
#142996=EDGE_CURVE ( 'NONE', #1074, #165183, #252841, .T. ) ;
#143009=EDGE_CURVE ( 'NONE', #90553, #178434, #3033, .T. ) ;
#143046=CARTESIAN_POINT ( 'NONE',  ( -20.64999999999999858, 74.00000000001151079, -49.24772940728643533 ) ) ;
#143048=CYLINDRICAL_SURFACE ( 'NONE', #131748, 0.09999999999999939493 ) ;
#143055=ORIENTED_EDGE ( 'NONE', *, *, #113454, .F. ) ;
#143080=CARTESIAN_POINT ( 'NONE',  ( 18.49999999999999289, 65.76093837589000657, -44.76871004992742087 ) ) ;
#143083=DIRECTION ( 'NONE',  ( -1.000000000000000000, -7.304098846218134667E-16, -5.311601492717084346E-30 ) ) ;
#143093=CARTESIAN_POINT ( 'NONE',  ( 23.15000000000000213, 84.59626168225447884, -45.47323500167454569 ) ) ;
#143098=AXIS2_PLACEMENT_3D ( 'NONE', #145360, #30585, #204052 ) ;
#143101=ORIENTED_EDGE ( 'NONE', *, *, #131986, .T. ) ;
#143108=CARTESIAN_POINT ( 'NONE',  ( -20.00857864376270001, 66.85000000001150511, -48.37310748452438247 ) ) ;
#143140=LINE ( 'NONE', #146993, #155454 ) ;
#143142=ORIENTED_EDGE ( 'NONE', *, *, #93923, .F. ) ;
#143145=DIRECTION ( 'NONE',  ( 3.265361837132813093E-16, 1.000000000000000000, 6.982962677686266711E-15 ) ) ;
#143152=AXIS2_PLACEMENT_3D ( 'NONE', #225809, #207580, #8088 ) ;
#143171=EDGE_LOOP ( 'NONE', ( #129577, #30946, #5943, #231679, #203237, #236104, #78319 ) ) ;
#143175=CARTESIAN_POINT ( 'NONE',  ( -21.05000000000000071, 87.48912529308749697, -39.02310748452423894 ) ) ;
#143180=DIRECTION ( 'NONE',  ( 0.000000000000000000, -7.116814260417668513E-15, 1.000000000000000000 ) ) ;
#143188=EDGE_CURVE ( 'NONE', #102370, #38899, #256340, .T. ) ;
#143215=DIRECTION ( 'NONE',  ( 0.000000000000000000, -1.000000000000000000, 0.000000000000000000 ) ) ;
#143222=ORIENTED_EDGE ( 'NONE', *, *, #227461, .T. ) ;
#143231=DIRECTION ( 'NONE',  ( -1.836970198721029934E-16, -1.000000000000000000, -6.982962677686266711E-15 ) ) ;
#143238=CARTESIAN_POINT ( 'NONE',  ( 21.30740335185486245, 69.44334207798367231, -69.62204201030021977 ) ) ;
#143288=CYLINDRICAL_SURFACE ( 'NONE', #114774, 0.1000000000000028644 ) ;
#143298=CARTESIAN_POINT ( 'NONE',  ( 21.14999999999999858, 75.90220970870291239, -75.78092209500044873 ) ) ;
#143302=DIRECTION ( 'NONE',  ( 0.000000000000000000, -0.8660254037844387076, 0.4999999999999998335 ) ) ;
#143341=DIRECTION ( 'NONE',  ( 1.000000000000000000, 0.000000000000000000, 0.000000000000000000 ) ) ;
#143358=CARTESIAN_POINT ( 'NONE',  ( 18.48197441911692707, 85.51795479471786621, -29.13289584231640461 ) ) ;
#143412=CARTESIAN_POINT ( 'NONE',  ( 21.30000000000002558, 76.00000000001165290, -69.52310748452431710 ) ) ;
#143425=DIRECTION ( 'NONE',  ( -0.000000000000000000, 0.9876197685951241256, 0.1568667991644932258 ) ) ;
#143455=DIRECTION ( 'NONE',  ( -1.000000000000000000, 2.952720810173289112E-16, 2.061873921506763405E-30 ) ) ;
#143459=AXIS2_PLACEMENT_3D ( 'NONE', #246918, #109979, #91712 ) ;
#143462=CARTESIAN_POINT ( 'NONE',  ( 20.94999999999999929, 76.00000000001141132, -34.12310748452431852 ) ) ;
#143467=ORIENTED_EDGE ( 'NONE', *, *, #12205, .T. ) ;
#143471=ORIENTED_EDGE ( 'NONE', *, *, #125252, .F. ) ;
#143518=CIRCLE ( 'NONE', #31145, 0.2000000000000057288 ) ;
#143534=CARTESIAN_POINT ( 'NONE',  ( 18.59999999999999432, 74.26374286841418382, -57.95445515550683524 ) ) ;
#143539=CIRCLE ( 'NONE', #218524, 0.1000000000000043771 ) ;
#143557=TOROIDAL_SURFACE ( 'NONE', #151964, 0.6000000000000013101, 0.1000000000000000056 ) ;
#143559=AXIS2_PLACEMENT_3D ( 'NONE', #196021, #74815, #154360 ) ;
#143565=ADVANCED_FACE ( 'NONE', ( #249690 ), #94811, .T. ) ;
#143567=ADVANCED_FACE ( 'NONE', ( #201206 ), #106911, .T. ) ;
#143574=DIRECTION ( 'NONE',  ( 1.000000000000000000, 0.000000000000000000, 0.000000000000000000 ) ) ;
#143599=CARTESIAN_POINT ( 'NONE',  ( -18.50211644919735576, 65.69792220476271893, -30.53355541284615171 ) ) ;
#143623=DIRECTION ( 'NONE',  ( 0.000000000000000000, 1.000000000000000000, 7.272083257015735086E-15 ) ) ;
#143624=ORIENTED_EDGE ( 'NONE', *, *, #237277, .F. ) ;
#143649=EDGE_CURVE ( 'NONE', #178423, #50215, #9109, .T. ) ;
#143695=FACE_OUTER_BOUND ( 'NONE', #216062, .T. ) ;
#143736=DIRECTION ( 'NONE',  ( 1.000000000000000000, 0.000000000000000000, 0.000000000000000000 ) ) ;
#143794=VECTOR ( 'NONE', #230543, 1000.000000000000000 ) ;
#143864=LINE ( 'NONE', #219547, #4185 ) ;
#143883=DIRECTION ( 'NONE',  ( 0.000000000000000000, -0.9908441862701610203, 0.1350103645451807555 ) ) ;
#143887=EDGE_CURVE ( 'NONE', #165812, #246837, #140592, .T. ) ;
#143945=CARTESIAN_POINT ( 'NONE',  ( -21.10320863425827298, 75.97497774878459609, -75.92338487098355415 ) ) ;
#143954=DIRECTION ( 'NONE',  ( 0.000000000000000000, -7.147358527629762208E-15, 1.000000000000000000 ) ) ;
#144025=CARTESIAN_POINT ( 'NONE',  ( -20.94999999999999929, 87.75000000001163869, -66.42310748452423752 ) ) ;
#144038=DIRECTION ( 'NONE',  ( 0.000000000000000000, 6.608470384673547079E-15, -1.000000000000000000 ) ) ;
#144047=AXIS2_PLACEMENT_3D ( 'NONE', #127591, #48044, #165442 ) ;
#144048=AXIS2_PLACEMENT_3D ( 'NONE', #195470, #139294, #16823 ) ;
#144063=LINE ( 'NONE', #41162, #56996 ) ;
#144077=ADVANCED_FACE ( 'NONE', ( #110457 ), #190005, .T. ) ;
#144086=VERTEX_POINT ( 'NONE', #170493 ) ;
#144094=DIRECTION ( 'NONE',  ( -1.000000000000000000, -0.000000000000000000, -0.000000000000000000 ) ) ;
#144113=CARTESIAN_POINT ( 'NONE',  ( -23.15000000000000213, 64.35000000001156195, -57.37310748452440379 ) ) ;
#144162=DIRECTION ( 'NONE',  ( 0.000000000000000000, 0.000000000000000000, -1.000000000000000000 ) ) ;
#144168=AXIS2_PLACEMENT_3D ( 'NONE', #192338, #172817, #155803 ) ;
#144214=CARTESIAN_POINT ( 'NONE',  ( 20.01093837587850288, 64.25000000001148237, -44.76871004992742797 ) ) ;
#144258=AXIS2_PLACEMENT_3D ( 'NONE', #173272, #194087, #231926 ) ;
#144269=CARTESIAN_POINT ( 'NONE',  ( -21.11833042828127915, 75.99289949095243912, -75.96875217837973082 ) ) ;
#144270=DIRECTION ( 'NONE',  ( -1.000000000000000000, -0.000000000000000000, 0.000000000000000000 ) ) ;
#144312=CARTESIAN_POINT ( 'NONE',  ( 21.05000000000000071, 87.29603075034673054, -39.07100664418810965 ) ) ;
#144316=VECTOR ( 'NONE', #53525, 1000.000000000000000 ) ;
#144341=ORIENTED_EDGE ( 'NONE', *, *, #97186, .F. ) ;
#144348=FACE_OUTER_BOUND ( 'NONE', #250874, .T. ) ;
#144385=AXIS2_PLACEMENT_3D ( 'NONE', #13641, #134839, #12380 ) ;
#144401=ORIENTED_EDGE ( 'NONE', *, *, #235307, .F. ) ;
#144412=EDGE_CURVE ( 'NONE', #212130, #155495, #210546, .T. ) ;
#144419=LINE ( 'NONE', #167896, #177291 ) ;
#144428=CARTESIAN_POINT ( 'NONE',  ( 21.14999999999999503, 76.00000000001165290, -69.52310748452431710 ) ) ;
#144432=AXIS2_PLACEMENT_3D ( 'NONE', #198416, #135855, #206 ) ;
#144462=CARTESIAN_POINT ( 'NONE',  ( -21.05000000000000071, 76.00000000001165290, -69.52310748452431710 ) ) ;
#144558=CARTESIAN_POINT ( 'NONE',  ( 23.14999999999999858, 71.00000000001158185, -57.11784146561126363 ) ) ;
#144573=VERTEX_POINT ( 'NONE', #81272 ) ;
#144580=ORIENTED_EDGE ( 'NONE', *, *, #248641, .T. ) ;
#144596=FACE_OUTER_BOUND ( 'NONE', #247038, .T. ) ;
#144629=EDGE_CURVE ( 'NONE', #33900, #125917, #179151, .T. ) ;
#144667=AXIS2_PLACEMENT_3D ( 'NONE', #64008, #125272, #182690 ) ;
#144689=CARTESIAN_POINT ( 'NONE',  ( 18.50000000000000000, 85.40000000001158753, -62.22584772486099070 ) ) ;
#144692=ORIENTED_EDGE ( 'NONE', *, *, #36194, .T. ) ;
#144720=EDGE_CURVE ( 'NONE', #160483, #82047, #244633, .T. ) ;
#144743=AXIS2_PLACEMENT_3D ( 'NONE', #213577, #49383, #230594 ) ;
#144760=CARTESIAN_POINT ( 'NONE',  ( 23.14999999999999503, 64.25000000001151079, -48.27310748452440237 ) ) ;
#144766=DIRECTION ( 'NONE',  ( -0.000000000000000000, -6.982962677686266711E-15, 1.000000000000000000 ) ) ;
#144768=ORIENTED_EDGE ( 'NONE', *, *, #94630, .F. ) ;
#144770=DIRECTION ( 'NONE',  ( 0.000000000000000000, 0.000000000000000000, 1.000000000000000000 ) ) ;
#144783=DIRECTION ( 'NONE',  ( 0.000000000000000000, -7.056502275159894776E-15, 1.000000000000000000 ) ) ;
#144785=ORIENTED_EDGE ( 'NONE', *, *, #174916, .T. ) ;
#144802=DIRECTION ( 'NONE',  ( 0.000000000000000000, 0.000000000000000000, 1.000000000000000000 ) ) ;
#144828=VERTEX_POINT ( 'NONE', #210254 ) ;
#144835=ORIENTED_EDGE ( 'NONE', *, *, #29131, .F. ) ;
#144854=AXIS2_PLACEMENT_3D ( 'NONE', #230820, #53444, #235916 ) ;
#144867=CIRCLE ( 'NONE', #40858, 0.1000000000000021289 ) ;
#144870=AXIS2_PLACEMENT_3D ( 'NONE', #124359, #5653, #205147 ) ;
#144908=AXIS2_PLACEMENT_3D ( 'NONE', #107680, #2151, #42574 ) ;
#144938=LINE ( 'NONE', #124128, #31698 ) ;
#144961=EDGE_LOOP ( 'NONE', ( #96315, #48596, #76092, #132233, #93772 ) ) ;
#145000=CIRCLE ( 'NONE', #211681, 0.1999999999999987899 ) ;
#145006=ORIENTED_EDGE ( 'NONE', *, *, #33971, .F. ) ;
#145030=CIRCLE ( 'NONE', #90866, 4.049999999999998046 ) ;
#145054=DIRECTION ( 'NONE',  ( -1.000000000000000000, 0.000000000000000000, 0.000000000000000000 ) ) ;
#145057=EDGE_LOOP ( 'NONE', ( #206551, #173687, #252590, #119214 ) ) ;
#145070=ORIENTED_EDGE ( 'NONE', *, *, #97835, .F. ) ;
#145095=AXIS2_PLACEMENT_3D ( 'NONE', #100916, #98348, #60542 ) ;
#145117=EDGE_CURVE ( 'NONE', #52116, #127854, #104387, .T. ) ;
#145209=ORIENTED_EDGE ( 'NONE', *, *, #228380, .T. ) ;
#145226=CARTESIAN_POINT ( 'NONE',  ( -21.07971444708686093, 75.91217656369386191, -75.85289956615088158 ) ) ;
#145253=AXIS2_PLACEMENT_3D ( 'NONE', #7389, #25686, #124790 ) ;
#145268=EDGE_CURVE ( 'NONE', #36755, #172698, #129371, .T. ) ;
#145312=CARTESIAN_POINT ( 'NONE',  ( 23.15000000000000213, 87.65000000001144542, -39.12310748452424747 ) ) ;
#145323=CARTESIAN_POINT ( 'NONE',  ( 20.85000000000000142, 69.06610602788505560, -32.23746165015079868 ) ) ;
#145360=CARTESIAN_POINT ( 'NONE',  ( 22.39999999999999858, 68.20922040163827660, -69.62310748452438247 ) ) ;
#145402=VECTOR ( 'NONE', #170668, 1000.000000000000000 ) ;
#145415=CARTESIAN_POINT ( 'NONE',  ( -22.39999999999999858, 76.00000000001173817, -81.17267829206912211 ) ) ;
#145435=DIRECTION ( 'NONE',  ( 2.952720810173289112E-16, 1.000000000000000000, 9.912705577010238578E-15 ) ) ;
#145452=ORIENTED_EDGE ( 'NONE', *, *, #246360, .T. ) ;
#145475=ORIENTED_EDGE ( 'NONE', *, *, #99864, .T. ) ;
#145491=CARTESIAN_POINT ( 'NONE',  ( 20.94999999999999574, 74.75000000001159606, -61.52310748452433131 ) ) ;
#145508=ORIENTED_EDGE ( 'NONE', *, *, #191934, .F. ) ;
#145513=ORIENTED_EDGE ( 'NONE', *, *, #222209, .T. ) ;
#145518=TOROIDAL_SURFACE ( 'NONE', #245497, 0.9750000000000019762, 0.1000000000000000056 ) ;
#145532=CARTESIAN_POINT ( 'NONE',  ( -18.59999999999999787, 76.00000000001142553, -36.02310748452432421 ) ) ;
#145560=AXIS2_PLACEMENT_3D ( 'NONE', #217287, #38677, #118211 ) ;
#145568=EDGE_CURVE ( 'NONE', #43098, #35500, #41212, .T. ) ;
#145599=ORIENTED_EDGE ( 'NONE', *, *, #171016, .F. ) ;
#145606=VERTEX_POINT ( 'NONE', #189740 ) ;
#145622=FACE_OUTER_BOUND ( 'NONE', #74522, .T. ) ;
#145668=ORIENTED_EDGE ( 'NONE', *, *, #197557, .F. ) ;
#145677=DIRECTION ( 'NONE',  ( 0.000000000000000000, -1.000000000000000000, 0.000000000000000000 ) ) ;
#145685=AXIS2_PLACEMENT_3D ( 'NONE', #214890, #16709, #20566 ) ;
#145687=DIRECTION ( 'NONE',  ( 1.000000000000000000, 0.000000000000000000, 0.000000000000000000 ) ) ;
#145712=CIRCLE ( 'NONE', #249792, 0.1000000000000028644 ) ;
#145717=CARTESIAN_POINT ( 'NONE',  ( -20.54999999999999716, 73.50000000001156764, -56.29848556176223440 ) ) ;
#145728=VECTOR ( 'NONE', #159726, 1000.000000000000000 ) ;
#145738=LINE ( 'NONE', #220163, #14502 ) ;
#145765=EDGE_CURVE ( 'NONE', #171007, #86432, #82587, .T. ) ;
#145829=ORIENTED_EDGE ( 'NONE', *, *, #190744, .F. ) ;
#145849=AXIS2_PLACEMENT_3D ( 'NONE', #47704, #166417, #225048 ) ;
#145917=CARTESIAN_POINT ( 'NONE',  ( 18.59999996954842771, 85.52320413787028031, -29.14006577260792596 ) ) ;
#145924=DIRECTION ( 'NONE',  ( -1.000000000000000000, 0.000000000000000000, 0.000000000000000000 ) ) ;
#145951=AXIS2_PLACEMENT_3D ( 'NONE', #125187, #186446, #48201 ) ;
#145975=CARTESIAN_POINT ( 'NONE',  ( 18.39999999999999858, 85.50000000001161027, -62.49103808782459879 ) ) ;
#145979=AXIS2_PLACEMENT_3D ( 'NONE', #226953, #88697, #48312 ) ;
#145988=CARTESIAN_POINT ( 'NONE',  ( -21.64999999999999858, 68.65000000001157332, -57.17310748452437252 ) ) ;
#145999=ADVANCED_FACE ( 'NONE', ( #55036 ), #90315, .T. ) ;
#146036=DIRECTION ( 'NONE',  ( 1.000000000000000000, 0.000000000000000000, 0.000000000000000000 ) ) ;
#146065=CARTESIAN_POINT ( 'NONE',  ( 23.14999999999999858, 70.50000000001151079, -48.42837350343745584 ) ) ;
#146106=B_SPLINE_CURVE_WITH_KNOTS ( 'NONE', 3,
 ( #82311, #40694, #84869, #220576, #203574, #21115, #83587, #64061, #43224, #2785, #105726, #182747, #242691, #143599, #146158, #202296, #161907, #100586, #22392 ),
 .UNSPECIFIED., .F., .F.,
 ( 4, 3, 3, 3, 3, 3, 4 ),
 ( 0.000000000000000000, 2.646747978908414649E-05, 5.271166642128387010E-05, 9.008788829884412921E-05, 0.0001426648776560982164, 0.0001897378458659780261, 0.0001917382627806345728 ),
 .UNSPECIFIED. ) ;
#146132=ORIENTED_EDGE ( 'NONE', *, *, #148277, .T. ) ;
#146136=CARTESIAN_POINT ( 'NONE',  ( -22.59999999999999787, 76.00000000001165290, -69.52310748452431710 ) ) ;
#146152=ORIENTED_EDGE ( 'NONE', *, *, #55266, .F. ) ;
#146155=CIRCLE ( 'NONE', #229566, 0.09999999999999939493 ) ;
#146158=CARTESIAN_POINT ( 'NONE',  ( -18.50016250449483479, 65.70233904876970144, -30.54874109119680625 ) ) ;
#146212=ORIENTED_EDGE ( 'NONE', *, *, #209059, .F. ) ;
#146241=EDGE_CURVE ( 'NONE', #64921, #178236, #44501, .T. ) ;
#146271=CARTESIAN_POINT ( 'NONE',  ( 20.94999999999999929, 70.10000000001149090, -46.24220724918073699 ) ) ;
#146273=EDGE_CURVE ( 'NONE', #98003, #111790, #124948, .T. ) ;
#146292=VERTEX_POINT ( 'NONE', #241415 ) ;
#146312=EDGE_CURVE ( 'NONE', #13982, #177501, #173482, .T. ) ;
#146343=ORIENTED_EDGE ( 'NONE', *, *, #34109, .T. ) ;
#146362=DIRECTION ( 'NONE',  ( 0.000000000000000000, 0.000000000000000000, 1.000000000000000000 ) ) ;
#146391=VERTEX_POINT ( 'NONE', #134275 ) ;
#146403=ORIENTED_EDGE ( 'NONE', *, *, #45311, .F. ) ;
#146414=CARTESIAN_POINT ( 'NONE',  ( 20.95429693346637734, 65.45669512011546942, -61.96222494621114407 ) ) ;
#146419=CARTESIAN_POINT ( 'NONE',  ( -23.15000000000000213, 87.48912529308749697, -39.12310748452424747 ) ) ;
#146421=FACE_OUTER_BOUND ( 'NONE', #244198, .T. ) ;
#146434=DIRECTION ( 'NONE',  ( 0.000000000000000000, -0.9654727137038715545, -0.2605042016806676242 ) ) ;
#146436=DIRECTION ( 'NONE',  ( 0.000000000000000000, -1.000000000000000000, 0.000000000000000000 ) ) ;
#146467=CYLINDRICAL_SURFACE ( 'NONE', #225347, 0.09999999999999939493 ) ;
#146477=CARTESIAN_POINT ( 'NONE',  ( 21.00023020733503643, 76.00000000001170974, -75.91397672979269373 ) ) ;
#146505=ADVANCED_FACE ( 'NONE', ( #254221 ), #37784, .F. ) ;
#146519=AXIS2_PLACEMENT_3D ( 'NONE', #36528, #153930, #176032 ) ;
#146551=CARTESIAN_POINT ( 'NONE',  ( -20.94999999999999929, 87.48912529308769592, -66.62310748452424036 ) ) ;
#146563=CARTESIAN_POINT ( 'NONE',  ( 20.94999999999999574, 67.07338541492450190, -61.05142446530125966 ) ) ;
#146595=CIRCLE ( 'NONE', #254881, 0.1000000000000000888 ) ;
#146621=CARTESIAN_POINT ( 'NONE',  ( 20.94999999999999929, 65.27628289530399286, -48.27310748452439526 ) ) ;
#146635=ORIENTED_EDGE ( 'NONE', *, *, #212325, .T. ) ;
#146647=CARTESIAN_POINT ( 'NONE',  ( -21.14999999999999858, 87.65000000001163016, -66.62310748452424036 ) ) ;
#146657=EDGE_LOOP ( 'NONE', ( #26546, #38208, #4999, #143471 ) ) ;
#146658=VERTEX_POINT ( 'NONE', #102841 ) ;
#146680=CARTESIAN_POINT ( 'NONE',  ( -22.48479450179659977, 75.95300841882485088, -81.17310593077593239 ) ) ;
#146685=DIRECTION ( 'NONE',  ( 0.000000000000000000, 0.4930308989875575865, 0.8700118002898125091 ) ) ;
#146707=ORIENTED_EDGE ( 'NONE', *, *, #63000, .T. ) ;
#146726=DIRECTION ( 'NONE',  ( -3.787827842127534447E-15, -0.7397360091702729346, -0.6728971962616859814 ) ) ;
#146773=AXIS2_PLACEMENT_3D ( 'NONE', #214959, #136695, #157601 ) ;
#146778=EDGE_CURVE ( 'NONE', #106650, #62040, #104254, .T. ) ;
#146794=CIRCLE ( 'NONE', #67708, 0.1000000000000028644 ) ;
#146810=EDGE_LOOP ( 'NONE', ( #223191, #45191, #14483, #67542 ) ) ;
#146817=ADVANCED_FACE ( 'NONE', ( #108010 ), #152292, .T. ) ;
#146839=AXIS2_PLACEMENT_3D ( 'NONE', #54075, #11111, #51480 ) ;
#146858=CARTESIAN_POINT ( 'NONE',  ( 21.30000000000002558, 76.00000000001165290, -69.52310748452431710 ) ) ;
#146871=CARTESIAN_POINT ( 'NONE',  ( 20.99551997958372596, 64.25000000001146816, -42.87144834683482486 ) ) ;
#146943=DIRECTION ( 'NONE',  ( 0.000000000000000000, -0.7397360091702647189, -0.6728971962616949742 ) ) ;
#146972=PLANE ( 'NONE',  #111145 ) ;
#146980=CARTESIAN_POINT ( 'NONE',  ( -20.64999999999999858, 68.85000000001151932, -48.37310748452436826 ) ) ;
#146992=EDGE_CURVE ( 'NONE', #246301, #147579, #216871, .T. ) ;
#146993=CARTESIAN_POINT ( 'NONE',  ( 20.12500000000000000, 66.25000000001151079, -48.27310748452438816 ) ) ;
#147021=VERTEX_POINT ( 'NONE', #232654 ) ;
#147038=FACE_OUTER_BOUND ( 'NONE', #97208, .T. ) ;
#147043=EDGE_LOOP ( 'NONE', ( #171793, #76381, #99772, #95413 ) ) ;
#147065=CARTESIAN_POINT ( 'NONE',  ( -20.95000000000000284, 64.37928932189282705, -42.89152413686537813 ) ) ;
#147121=DIRECTION ( 'NONE',  ( 0.000000000000000000, -1.000000000000000000, -6.982962677686265922E-15 ) ) ;
#147150=VERTEX_POINT ( 'NONE', #194818 ) ;
#147175=CARTESIAN_POINT ( 'NONE',  ( -20.94999999999999929, 87.48912529308749697, -38.92310748452424463 ) ) ;
#147214=SPHERICAL_SURFACE ( 'NONE', #46497, 0.1000000000000000056 ) ;
#147219=FACE_OUTER_BOUND ( 'NONE', #234805, .T. ) ;
#147224=CARTESIAN_POINT ( 'NONE',  ( 18.60000000000000142, 85.32100840337290037, -62.28716923544637041 ) ) ;
#147254=DIRECTION ( 'NONE',  ( -1.000000000000000000, 2.952720810173289112E-16, 2.061873921506763405E-30 ) ) ;
#147267=CARTESIAN_POINT ( 'NONE',  ( 18.46947024752519795, 85.50929715716780777, -62.53641803582647896 ) ) ;
#147268=CARTESIAN_POINT ( 'NONE',  ( 21.14999999999999858, 64.35000000001164722, -69.42310748452440805 ) ) ;
#147273=ORIENTED_EDGE ( 'NONE', *, *, #69682, .F. ) ;
#147285=DIRECTION ( 'NONE',  ( -5.603264701231743991E-32, -7.172728831056617961E-15, 1.000000000000000000 ) ) ;
#147286=DIRECTION ( 'NONE',  ( -4.408576920032448588E-17, -0.1350103645451807832, -0.9908441862701610203 ) ) ;
#147304=AXIS2_PLACEMENT_3D ( 'NONE', #204888, #30143, #8002 ) ;
#147322=EDGE_CURVE ( 'NONE', #36755, #119497, #62774, .T. ) ;
#147332=ORIENTED_EDGE ( 'NONE', *, *, #73181, .F. ) ;
#147357=LINE ( 'NONE', #69125, #74320 ) ;
#147358=EDGE_LOOP ( 'NONE', ( #132899, #134011, #29614, #234570 ) ) ;
#147362=CYLINDRICAL_SURFACE ( 'NONE', #134870, 12.87499999999999822 ) ;
#147376=DIRECTION ( 'NONE',  ( 1.000000000000000000, 0.000000000000000000, 0.000000000000000000 ) ) ;
#147403=ORIENTED_EDGE ( 'NONE', *, *, #59065, .F. ) ;
#147431=CARTESIAN_POINT ( 'NONE',  ( 20.95083306685154056, 67.08315735812139735, -61.04578263126603588 ) ) ;
#147551=CARTESIAN_POINT ( 'NONE',  ( -20.64999999999999858, 74.00000000001151079, -49.24772940728643533 ) ) ;
#147553=CARTESIAN_POINT ( 'NONE',  ( -21.05000000000000071, 76.00000000001142553, -36.02310748452432421 ) ) ;
#147561=LINE ( 'NONE', #14497, #139080 ) ;
#147579=VERTEX_POINT ( 'NONE', #70330 ) ;
#147606=CARTESIAN_POINT ( 'NONE',  ( -18.50000000000000355, 85.41908450282468834, -29.19319967749884626 ) ) ;
#147607=EDGE_LOOP ( 'NONE', ( #15203, #33680, #179960, #56887 ) ) ;
#147613=DIRECTION ( 'NONE',  ( 1.000000000000000000, 0.000000000000000000, 0.000000000000000000 ) ) ;
#147663=DIRECTION ( 'NONE',  ( -0.000000000000000000, -0.1350103645451718737, 0.9908441862701622416 ) ) ;
#147667=EDGE_CURVE ( 'NONE', #64945, #235108, #233245, .T. ) ;
#147695=FACE_OUTER_BOUND ( 'NONE', #65088, .T. ) ;
#147701=DIRECTION ( 'NONE',  ( 0.000000000000000000, 0.1568667991644355497, 0.9876197685951332295 ) ) ;
#147750=DIRECTION ( 'NONE',  ( 1.000000000000000000, -1.836970198721029934E-16, -1.282749433769087582E-30 ) ) ;
#147755=ADVANCED_FACE ( 'NONE', ( #243477 ), #110770, .T. ) ;
#147793=DIRECTION ( 'NONE',  ( 0.000000000000000000, 6.997203936713167125E-15, -1.000000000000000000 ) ) ;
#147805=CARTESIAN_POINT ( 'NONE',  ( -23.25000000000000000, 87.75000000001165290, -69.52310748452424605 ) ) ;
#147806=ADVANCED_FACE ( 'NONE', ( #144348 ), #51622, .T. ) ;
#147820=ORIENTED_EDGE ( 'NONE', *, *, #205563, .T. ) ;
#147833=ORIENTED_EDGE ( 'NONE', *, *, #1031, .F. ) ;
#147871=CARTESIAN_POINT ( 'NONE',  ( 22.39999999999999503, 64.25000000001165290, -69.62310748452439668 ) ) ;
#147887=FACE_OUTER_BOUND ( 'NONE', #228213, .T. ) ;
#147890=EDGE_CURVE ( 'NONE', #91949, #152443, #152503, .T. ) ;
#147896=VERTEX_POINT ( 'NONE', #210772 ) ;
#147918=CARTESIAN_POINT ( 'NONE',  ( 21.05000000000000071, 71.00000000001158185, -57.11784146561126363 ) ) ;
#147932=AXIS2_PLACEMENT_3D ( 'NONE', #104845, #1911, #202695 ) ;
#147956=CARTESIAN_POINT ( 'NONE',  ( 21.05000000000000071, 65.27628289530404970, -57.37310748452439668 ) ) ;
#147989=VECTOR ( 'NONE', #546, 1000.000000000000000 ) ;
#147992=MECHANICAL_DESIGN_GEOMETRIC_PRESENTATION_REPRESENTATION('',(#98073),#156408);
#148024=DIRECTION ( 'NONE',  ( 0.000000000000000000, -0.5000000000000016653, 0.8660254037844377084 ) ) ;
#148043=CYLINDRICAL_SURFACE ( 'NONE', #216574, 0.1000000000000028644 ) ;
#148052=DIRECTION ( 'NONE',  ( 0.000000000000000000, -0.1350103645451807555, -0.9908441862701609093 ) ) ;
#148053=ORIENTED_EDGE ( 'NONE', *, *, #52345, .F. ) ;
#148063=CIRCLE ( 'NONE', #56462, 0.1000000000000028644 ) ;
#148076=DIRECTION ( 'NONE',  ( 0.000000000000000000, 0.000000000000000000, 1.000000000000000000 ) ) ;
#148108=CARTESIAN_POINT ( 'NONE',  ( -20.85000000000000142, 77.16412189325258453, -28.10825939895270764 ) ) ;
#148113=AXIS2_PLACEMENT_3D ( 'NONE', #243022, #203899, #64399 ) ;
#148123=DIRECTION ( 'NONE',  ( 1.000000000000000000, 0.000000000000000000, 0.000000000000000000 ) ) ;
#148130=DIRECTION ( 'NONE',  ( -1.000000000000000000, 0.000000000000000000, 0.000000000000000000 ) ) ;
#148134=ORIENTED_EDGE ( 'NONE', *, *, #145117, .F. ) ;
#148213=CARTESIAN_POINT ( 'NONE',  ( -21.44999999999999929, 68.65000000001157332, -57.27310748452437394 ) ) ;
#148224=ORIENTED_EDGE ( 'NONE', *, *, #171915, .T. ) ;
#148234=AXIS2_PLACEMENT_3D ( 'NONE', #89856, #208553, #188973 ) ;
#148260=FACE_OUTER_BOUND ( 'NONE', #64205, .T. ) ;
#148272=EDGE_CURVE ( 'NONE', #234821, #81658, #166240, .T. ) ;
#148277=EDGE_CURVE ( 'NONE', #188373, #113738, #181877, .T. ) ;
#148279=DIRECTION ( 'NONE',  ( 1.000000000000000000, 0.000000000000000000, 0.000000000000000000 ) ) ;
#148289=ORIENTED_EDGE ( 'NONE', *, *, #237862, .F. ) ;
#148317=AXIS2_PLACEMENT_3D ( 'NONE', #9634, #104844, #107451 ) ;
#148404=CARTESIAN_POINT ( 'NONE',  ( 23.24999999999999289, 64.25000000001156764, -57.37310748452440379 ) ) ;
#148437=EDGE_LOOP ( 'NONE', ( #102060, #24458, #189778, #167463 ) ) ;
#148486=AXIS2_PLACEMENT_3D ( 'NONE', #221158, #106332, #242016 ) ;
#148529=TOROIDAL_SURFACE ( 'NONE', #23657, 0.4000000000000012990, 0.1000000000000000056 ) ;
#148530=VERTEX_POINT ( 'NONE', #240314 ) ;
#148552=ORIENTED_EDGE ( 'NONE', *, *, #244393, .T. ) ;
#148563=CARTESIAN_POINT ( 'NONE',  ( 18.41789779300691876, 85.50000000001161027, -62.49103781816362613 ) ) ;
#148590=EDGE_LOOP ( 'NONE', ( #22542, #24090, #6161, #128320, #82176 ) ) ;
#148615=ORIENTED_EDGE ( 'NONE', *, *, #7219, .T. ) ;
#148618=ORIENTED_EDGE ( 'NONE', *, *, #19012, .T. ) ;
#148661=CARTESIAN_POINT ( 'NONE',  ( -21.04999999999999716, 85.60000000001160458, -62.49103808782458458 ) ) ;
#148706=VERTEX_POINT ( 'NONE', #25763 ) ;
#148724=ORIENTED_EDGE ( 'NONE', *, *, #5008, .T. ) ;
#148740=DIRECTION ( 'NONE',  ( -1.000000000000000000, 0.000000000000000000, 0.000000000000000000 ) ) ;
#148747=ADVANCED_FACE ( 'NONE', ( #170459 ), #51713, .T. ) ;
#148784=ORIENTED_EDGE ( 'NONE', *, *, #206876, .T. ) ;
#148828=ADVANCED_FACE ( 'NONE', ( #212115, #33511 ), #146972, .T. ) ;
#148863=LINE ( 'NONE', #133138, #185222 ) ;
#148891=CARTESIAN_POINT ( 'NONE',  ( 18.59999999999999432, 74.83729825007360148, -61.42310748452432989 ) ) ;
#148900=LINE ( 'NONE', #10667, #47687 ) ;
#148910=EDGE_LOOP ( 'NONE', ( #229376, #255337, #199363, #122370 ) ) ;
#148911=SPHERICAL_SURFACE ( 'NONE', #54184, 0.1000000000000000056 ) ;
#148912=AXIS2_PLACEMENT_3D ( 'NONE', #178691, #82090, #195680 ) ;
#148923=EDGE_LOOP ( 'NONE', ( #194419, #137229, #614, #212533 ) ) ;
#148947=TOROIDAL_SURFACE ( 'NONE', #211295, 0.6000000000000017542, 0.1000000000000000056 ) ;
#148964=VERTEX_POINT ( 'NONE', #80252 ) ;
#148997=DIRECTION ( 'NONE',  ( 0.000000000000000000, 1.000000000000000000, 6.853228547068871147E-15 ) ) ;
#149022=CARTESIAN_POINT ( 'NONE',  ( -22.39999999999999858, 68.20922040163824818, -69.62310748452438247 ) ) ;
#149045=ADVANCED_FACE ( 'NONE', ( #240648 ), #111332, .T. ) ;
#149061=ORIENTED_EDGE ( 'NONE', *, *, #232758, .F. ) ;
#149097=CARTESIAN_POINT ( 'NONE',  ( -21.14999999999999858, 69.74218538953553548, -69.62089777583315708 ) ) ;
#149109=EDGE_CURVE ( 'NONE', #119848, #95340, #203083, .T. ) ;
#149124=EDGE_CURVE ( 'NONE', #224921, #140287, #236223, .T. ) ;
#149156=ORIENTED_EDGE ( 'NONE', *, *, #236818, .F. ) ;
#149167=CARTESIAN_POINT ( 'NONE',  ( -23.15000000000000213, 76.00000000001143974, -38.02310748452432421 ) ) ;
#149187=CIRCLE ( 'NONE', #186772, 0.1000000000000028644 ) ;
#149197=FACE_OUTER_BOUND ( 'NONE', #184897, .T. ) ;
#149202=CARTESIAN_POINT ( 'NONE',  ( 21.07888907270776002, 65.27493078649635549, -57.30191389769120747 ) ) ;
#149203=LINE ( 'NONE', #252124, #39297 ) ;
#149251=VECTOR ( 'NONE', #225281, 1000.000000000000000 ) ;
#149263=ORIENTED_EDGE ( 'NONE', *, *, #75747, .T. ) ;
#149278=ORIENTED_EDGE ( 'NONE', *, *, #58547, .F. ) ;
#149286=CARTESIAN_POINT ( 'NONE',  ( -21.44999999999999929, 68.85000000001156195, -57.17310748452437252 ) ) ;
#149293=AXIS2_PLACEMENT_3D ( 'NONE', #183182, #222259, #20251 ) ;
#149300=DIRECTION ( 'NONE',  ( -0.000000000000000000, -6.982962677686266711E-15, 1.000000000000000000 ) ) ;
#149316=AXIS2_PLACEMENT_3D ( 'NONE', #152564, #229508, #91281 ) ;
#149395=AXIS2_PLACEMENT_3D ( 'NONE', #119661, #195360, #158803 ) ;
#149402=ORIENTED_EDGE ( 'NONE', *, *, #111961, .T. ) ;
#149456=EDGE_LOOP ( 'NONE', ( #128306, #225403, #248563, #131218 ) ) ;
#149459=ORIENTED_EDGE ( 'NONE', *, *, #69070, .T. ) ;
#149474=VECTOR ( 'NONE', #245082, 1000.000000000000000 ) ;
#149514=CARTESIAN_POINT ( 'NONE',  ( -22.16821283564876666, 68.44102665923088580, -69.52310748452437394 ) ) ;
#149517=ORIENTED_EDGE ( 'NONE', *, *, #170301, .T. ) ;
#149530=DIRECTION ( 'NONE',  ( 0.000000000000000000, -1.000000000000000000, -6.982962677686265922E-15 ) ) ;
#149532=VERTEX_POINT ( 'NONE', #62989 ) ;
#149543=ADVANCED_FACE ( 'NONE', ( #181670 ), #74129, .F. ) ;
#149587=CARTESIAN_POINT ( 'NONE',  ( -20.64999999999999858, 76.00000000001155342, -56.54810748452432279 ) ) ;
#149594=PLANE ( 'NONE',  #26865 ) ;
#149641=CARTESIAN_POINT ( 'NONE',  ( -18.59999999999999787, 74.26374286841418382, -57.95445515550683524 ) ) ;
#149716=EDGE_LOOP ( 'NONE', ( #38268, #236558 ) ) ;
#149720=LINE ( 'NONE', #33647, #198722 ) ;
#149735=ORIENTED_EDGE ( 'NONE', *, *, #130595, .T. ) ;
#149744=ORIENTED_EDGE ( 'NONE', *, *, #41818, .T. ) ;
#149751=VERTEX_POINT ( 'NONE', #74589 ) ;
#149793=CARTESIAN_POINT ( 'NONE',  ( -23.25000000000000000, 64.25000000001165290, -69.52310748452440237 ) ) ;
#149811=VERTEX_POINT ( 'NONE', #35460 ) ;
#149855=CARTESIAN_POINT ( 'NONE',  ( 23.14999999999999858, 76.00000000001165290, -69.52310748452431710 ) ) ;
#149861=DIRECTION ( 'NONE',  ( 1.000000000000000000, -0.000000000000000000, 0.000000000000000000 ) ) ;
#149880=DIRECTION ( 'NONE',  ( 2.715809747126117987E-16, 1.000000000000000000, 1.032007703907924707E-14 ) ) ;
#149893=FACE_OUTER_BOUND ( 'NONE', #214217, .T. ) ;
#149901=EDGE_CURVE ( 'NONE', #84841, #182741, #121416, .T. ) ;
#149924=AXIS2_PLACEMENT_3D ( 'NONE', #149022, #128160, #30354 ) ;
#149925=CARTESIAN_POINT ( 'NONE',  ( -18.59999999999999787, 77.16270174994961906, -61.52310748452431710 ) ) ;
#149952=CARTESIAN_POINT ( 'NONE',  ( 20.12500000000000355, 65.75804927292892899, -61.66290375743827212 ) ) ;
#149973=DIRECTION ( 'NONE',  ( 1.000000000000000000, 0.000000000000000000, 0.000000000000000000 ) ) ;
#150012=ORIENTED_EDGE ( 'NONE', *, *, #142338, .T. ) ;
#150037=VECTOR ( 'NONE', #71567, 1000.000000000000000 ) ;
#150042=EDGE_CURVE ( 'NONE', #217695, #175273, #147357, .T. ) ;
#150050=DIRECTION ( 'NONE',  ( -1.000000000000000000, 0.000000000000000000, -0.000000000000000000 ) ) ;
#150063=ADVANCED_FACE ( 'NONE', ( #123957 ), #203486, .T. ) ;
#150069=EDGE_CURVE ( 'NONE', #144828, #112680, #164365, .T. ) ;
#150081=CARTESIAN_POINT ( 'NONE',  ( 20.94999999999999574, 76.00000000001165290, -69.52310748452431710 ) ) ;
#150100=ADVANCED_FACE ( 'NONE', ( #134198 ), #131967, .F. ) ;
#150112=VERTEX_POINT ( 'NONE', #254142 ) ;
#150114=CIRCLE ( 'NONE', #145979, 0.09999999999999907574 ) ;
#150115=CIRCLE ( 'NONE', #99984, 0.09999999999999939493 ) ;
#150120=ORIENTED_EDGE ( 'NONE', *, *, #3716, .T. ) ;
#150142=CARTESIAN_POINT ( 'NONE',  ( -21.59142135623730852, 68.15000000001150227, -48.37310748452437537 ) ) ;
#150196=ORIENTED_EDGE ( 'NONE', *, *, #173531, .T. ) ;
#150203=AXIS2_PLACEMENT_3D ( 'NONE', #203027, #2249, #42677 ) ;
#150221=CYLINDRICAL_SURFACE ( 'NONE', #10502, 0.1000000000000028644 ) ;
#150243=DIRECTION ( 'NONE',  ( 0.000000000000000000, 7.086529944415894657E-15, -1.000000000000000000 ) ) ;
#150256=DIRECTION ( 'NONE',  ( -3.469446951953515108E-14, -1.000000000000000000, 0.000000000000000000 ) ) ;
#150268=ORIENTED_EDGE ( 'NONE', *, *, #135677, .T. ) ;
#150270=EDGE_CURVE ( 'NONE', #194241, #114996, #19407, .T. ) ;
#150286=ORIENTED_EDGE ( 'NONE', *, *, #185225, .T. ) ;
#150308=CARTESIAN_POINT ( 'NONE',  ( -18.59999999999999787, 70.10000000001163301, -59.30400771986794695 ) ) ;
#150309=CARTESIAN_POINT ( 'NONE',  ( 20.85000000000000142, 77.83585931145498193, -24.51866831572578675 ) ) ;
#150348=CARTESIAN_POINT ( 'NONE',  ( 23.14999999999999503, 64.25000000001172396, -81.27310748452440237 ) ) ;
#150350=CARTESIAN_POINT ( 'NONE',  ( 23.24999999999999645, 71.22429906543206357, -47.87187558857032599 ) ) ;
#150361=ORIENTED_EDGE ( 'NONE', *, *, #629, .F. ) ;
#150364=AXIS2_PLACEMENT_3D ( 'NONE', #122904, #160766, #204970 ) ;
#150396=CARTESIAN_POINT ( 'NONE',  ( -18.59999999999999787, 76.00000000001165290, -69.52310748452431710 ) ) ;
#150404=DIRECTION ( 'NONE',  ( 1.000000000000000000, 0.000000000000000000, 0.000000000000000000 ) ) ;
#150416=DIRECTION ( 'NONE',  ( -1.000000000000000000, -0.000000000000000000, -0.000000000000000000 ) ) ;
#150428=EDGE_CURVE ( 'NONE', #218866, #189305, #257003, .T. ) ;
#150454=PLANE ( 'NONE',  #119289 ) ;
#150477=ORIENTED_EDGE ( 'NONE', *, *, #154682, .T. ) ;
#150492=CARTESIAN_POINT ( 'NONE',  ( -20.54999999999999716, 73.50000000001151079, -49.24772940728643533 ) ) ;
#150494=EDGE_CURVE ( 'NONE', #251339, #79018, #11561, .T. ) ;
#150511=AXIS2_PLACEMENT_3D ( 'NONE', #6369, #85882, #89752 ) ;
#150513=ORIENTED_EDGE ( 'NONE', *, *, #81671, .T. ) ;
#150561=CARTESIAN_POINT ( 'NONE',  ( -21.05000000000000071, 74.25000000001156764, -57.85359592662268824 ) ) ;
#150567=DIRECTION ( 'NONE',  ( 0.000000000000000000, -7.487053152578128658E-15, 1.000000000000000000 ) ) ;
#150590=PLANE ( 'NONE',  #144385 ) ;
#150598=DIRECTION ( 'NONE',  ( 0.000000000000000000, -0.9915357197604892647, 0.1298341882519715440 ) ) ;
#150610=EDGE_LOOP ( 'NONE', ( #56451, #101154, #113012, #215126 ) ) ;
#150668=LINE ( 'NONE', #50260, #107324 ) ;
#150690=CARTESIAN_POINT ( 'NONE',  ( 23.14999999999999858, 70.50000000001151079, -48.42837350343745584 ) ) ;
#150727=CARTESIAN_POINT ( 'NONE',  ( 23.14999999999999503, 64.35000000001156195, -57.27310748452440237 ) ) ;
#150744=EDGE_CURVE ( 'NONE', #136580, #197749, #246793, .T. ) ;
#150800=CARTESIAN_POINT ( 'NONE',  ( 18.56308993302896226, 65.61930884468735314, -44.78388484558566063 ) ) ;
#150817=AXIS2_PLACEMENT_3D ( 'NONE', #240246, #139831, #17342 ) ;
#150826=DIRECTION ( 'NONE',  ( 0.000000000000000000, 0.000000000000000000, 1.000000000000000000 ) ) ;
#150838=CARTESIAN_POINT ( 'NONE',  ( -18.59999999999999787, 77.36242903720467723, -28.13422623660311217 ) ) ;
#150862=ORIENTED_EDGE ( 'NONE', *, *, #99767, .T. ) ;
#150884=ORIENTED_EDGE ( 'NONE', *, *, #32806, .F. ) ;
#150893=ORIENTED_EDGE ( 'NONE', *, *, #89728, .F. ) ;
#150897=CIRCLE ( 'NONE', #13544, 0.1999999999999987899 ) ;
#150923=CIRCLE ( 'NONE', #100803, 11.90000000000000036 ) ;
#150942=VERTEX_POINT ( 'NONE', #198476 ) ;
#150989=DIRECTION ( 'NONE',  ( 1.000000000000000000, 0.000000000000000000, 0.000000000000000000 ) ) ;
#151056=CYLINDRICAL_SURFACE ( 'NONE', #144743, 0.09999999999999939493 ) ;
#151102=CARTESIAN_POINT ( 'NONE',  ( 22.47110162079220785, 75.97120258720904928, -81.17304342120864646 ) ) ;
#151129=VERTEX_POINT ( 'NONE', #169674 ) ;
#151149=ADVANCED_FACE ( 'NONE', ( #208765 ), #112238, .T. ) ;
#151187=ORIENTED_EDGE ( 'NONE', *, *, #228724, .T. ) ;
#151191=EDGE_LOOP ( 'NONE', ( #77220, #108878, #156564, #125513 ) ) ;
#151199=EDGE_LOOP ( 'NONE', ( #134832, #249308, #199058, #118544 ) ) ;
#151201=ORIENTED_EDGE ( 'NONE', *, *, #48199, .T. ) ;
#151218=CARTESIAN_POINT ( 'NONE',  ( 22.39999999999999503, 64.25000000001165290, -69.52310748452438816 ) ) ;
#151228=CARTESIAN_POINT ( 'NONE',  ( 20.95512820512820440, 65.37615131629972609, -61.85819391543678591 ) ) ;
#151264=CARTESIAN_POINT ( 'NONE',  ( 23.14999999999999858, 76.00000000001142553, -36.02310748452432421 ) ) ;
#151266=CIRCLE ( 'NONE', #18153, 0.1999999999999987899 ) ;
#151281=ORIENTED_EDGE ( 'NONE', *, *, #168780, .F. ) ;
#151283=CARTESIAN_POINT ( 'NONE',  ( 21.53699400380201467, 69.21228820681596972, -69.52310748452435973 ) ) ;
#151288=AXIS2_PLACEMENT_3D ( 'NONE', #47850, #12622, #145677 ) ;
#151319=ORIENTED_EDGE ( 'NONE', *, *, #144412, .F. ) ;
#151333=AXIS2_PLACEMENT_3D ( 'NONE', #53317, #235789, #113286 ) ;
#151382=VERTEX_POINT ( 'NONE', #204582 ) ;
#151440=EDGE_CURVE ( 'NONE', #171475, #191840, #7820, .T. ) ;
#151442=CARTESIAN_POINT ( 'NONE',  ( 21.05000000000000426, 76.10000000001167564, -76.00015386631419290 ) ) ;
#151458=CARTESIAN_POINT ( 'NONE',  ( 20.94999999999999929, 76.00000000001143974, -37.92310748452432989 ) ) ;
#151509=ORIENTED_EDGE ( 'NONE', *, *, #171306, .T. ) ;
#151597=ORIENTED_EDGE ( 'NONE', *, *, #104944, .F. ) ;
#151688=ADVANCED_FACE ( 'NONE', ( #93631 ), #74105, .T. ) ;
#151701=FACE_OUTER_BOUND ( 'NONE', #16044, .T. ) ;
#151711=DIRECTION ( 'NONE',  ( 0.000000000000000000, 0.000000000000000000, 1.000000000000000000 ) ) ;
#151760=CARTESIAN_POINT ( 'NONE',  ( 21.14999999999999858, 64.35000000001156195, -57.37310748452439668 ) ) ;
#151775=DIRECTION ( 'NONE',  ( -1.000000000000000000, -0.000000000000000000, -0.000000000000000000 ) ) ;
#151798=EDGE_CURVE ( 'NONE', #97691, #90665, #244359, .T. ) ;
#151831=AXIS2_PLACEMENT_3D ( 'NONE', #129565, #112574, #16061 ) ;
#151835=CARTESIAN_POINT ( 'NONE',  ( -20.64999999999999858, 71.65000000001155911, -57.27310748452435263 ) ) ;
#151878=CARTESIAN_POINT ( 'NONE',  ( 21.05000000000000071, 67.12338541492449906, -61.13802700567970305 ) ) ;
#151888=ORIENTED_EDGE ( 'NONE', *, *, #120406, .T. ) ;
#151893=DIRECTION ( 'NONE',  ( 1.000000000000000000, 0.000000000000000000, 0.000000000000000000 ) ) ;
#151896=DIRECTION ( 'NONE',  ( 2.952720810173289112E-16, 1.000000000000000000, -6.088138035986627436E-46 ) ) ;
#151918=DIRECTION ( 'NONE',  ( -0.000000000000000000, 7.109473446599835262E-15, -1.000000000000000000 ) ) ;
#151925=DIRECTION ( 'NONE',  ( -1.000000000000000000, -0.000000000000000000, -0.000000000000000000 ) ) ;
#151932=CARTESIAN_POINT ( 'NONE',  ( -21.05000000000000071, 76.10000000001170406, -76.06376443622556849 ) ) ;
#151935=DIRECTION ( 'NONE',  ( 0.000000000000000000, -0.4999999999999689138, -0.8660254037844565822 ) ) ;
#151946=CARTESIAN_POINT ( 'NONE',  ( -23.25000000000000000, 74.00000000001151079, -49.24772940728643533 ) ) ;
#151956=DIRECTION ( 'NONE',  ( 0.000000000000000000, -6.982962677686266711E-15, 1.000000000000000000 ) ) ;
#151964=AXIS2_PLACEMENT_3D ( 'NONE', #111960, #51941, #114508 ) ;
#151993=ORIENTED_EDGE ( 'NONE', *, *, #131190, .T. ) ;
#151996=DIRECTION ( 'NONE',  ( -0.000000000000000000, 0.9887567792719327286, 0.1495327102803745423 ) ) ;
#152003=LINE ( 'NONE', #150690, #63426 ) ;
#152007=AXIS2_PLACEMENT_3D ( 'NONE', #117099, #139193, #237042 ) ;
#152029=DIRECTION ( 'NONE',  ( 0.000000000000000000, -7.026728003956686545E-15, 1.000000000000000000 ) ) ;
#152044=EDGE_CURVE ( 'NONE', #148706, #120086, #49686, .T. ) ;
#152068=ORIENTED_EDGE ( 'NONE', *, *, #199479, .F. ) ;
#152070=CARTESIAN_POINT ( 'NONE',  ( 18.59999999999999076, 69.55000000001159322, -59.50608031408435039 ) ) ;
#152077=DIRECTION ( 'NONE',  ( 0.000000000000000000, 0.01283462868040226822, 0.9999176327611370985 ) ) ;
#152093=DIRECTION ( 'NONE',  ( -0.000000000000000000, -0.8660254037844420383, 0.4999999999999943379 ) ) ;
#152130=EDGE_CURVE ( 'NONE', #60425, #212130, #70741, .T. ) ;
#152138=CIRCLE ( 'NONE', #18836, 2.000000000000001776 ) ;
#152139=AXIS2_PLACEMENT_3D ( 'NONE', #149286, #230084, #11038 ) ;
#152140=CARTESIAN_POINT ( 'NONE',  ( -23.15000000000000213, 64.35000000001146248, -43.03791325517835276 ) ) ;
#152159=CARTESIAN_POINT ( 'NONE',  ( 21.00000000000000000, 66.25000000001151079, -48.37310748452438958 ) ) ;
#152177=EDGE_LOOP ( 'NONE', ( #63640, #166704, #207039, #31870 ) ) ;
#152184=DIRECTION ( 'NONE',  ( 0.000000000000000000, -6.467318590049456648E-15, 1.000000000000000000 ) ) ;
#152212=EDGE_LOOP ( 'NONE', ( #224472, #35543, #184774, #204430 ) ) ;
#152230=DIRECTION ( 'NONE',  ( 0.000000000000000000, 0.000000000000000000, -1.000000000000000000 ) ) ;
#152255=ORIENTED_EDGE ( 'NONE', *, *, #250499, .F. ) ;
#152291=CARTESIAN_POINT ( 'NONE',  ( 22.50497660315937765, 76.07871793023727491, -81.27290298941976232 ) ) ;
#152292=SPHERICAL_SURFACE ( 'NONE', #187503, 0.1000000000000000056 ) ;
#152305=CYLINDRICAL_SURFACE ( 'NONE', #124573, 0.1000000000000028644 ) ;
#152320=AXIS2_PLACEMENT_3D ( 'NONE', #60701, #200236, #140235 ) ;
#152343=CIRCLE ( 'NONE', #39909, 0.1000000000000028644 ) ;
#152405=CARTESIAN_POINT ( 'NONE',  ( 20.85000000000000142, 77.75000000001134026, -24.40415744590205804 ) ) ;
#152407=CARTESIAN_POINT ( 'NONE',  ( 22.40736611211992368, 76.00000000001173817, -81.17267829206912211 ) ) ;
#152421=VECTOR ( 'NONE', #235116, 1000.000000000000000 ) ;
#152443=VERTEX_POINT ( 'NONE', #237349 ) ;
#152456=EDGE_CURVE ( 'NONE', #25147, #134587, #233238, .T. ) ;
#152499=AXIS2_PLACEMENT_3D ( 'NONE', #211359, #191819, #173560 ) ;
#152503=CIRCLE ( 'NONE', #173369, 11.74999999999999645 ) ;
#152508=FACE_OUTER_BOUND ( 'NONE', #19511, .T. ) ;
#152510=ORIENTED_EDGE ( 'NONE', *, *, #113093, .F. ) ;
#152511=AXIS2_PLACEMENT_3D ( 'NONE', #13178, #190546, #250484 ) ;
#152525=VERTEX_POINT ( 'NONE', #87233 ) ;
#152546=CARTESIAN_POINT ( 'NONE',  ( 23.15000000000000213, 84.66355140188075268, -59.99900636645695329 ) ) ;
#152564=CARTESIAN_POINT ( 'NONE',  ( -21.65000000000000213, 68.29142135624888965, -57.17310748452437963 ) ) ;
#152589=CARTESIAN_POINT ( 'NONE',  ( -21.05000000000000071, 69.45934304831041572, -69.42310748452437963 ) ) ;
#152604=CARTESIAN_POINT ( 'NONE',  ( -21.05000000000000071, 74.26374286841418382, -57.95445515550683524 ) ) ;
#152615=VERTEX_POINT ( 'NONE', #122545 ) ;
#152633=VECTOR ( 'NONE', #200789, 1000.000000000000000 ) ;
#152635=ORIENTED_EDGE ( 'NONE', *, *, #133098, .T. ) ;
#152656=LINE ( 'NONE', #93929, #46459 ) ;
#152662=AXIS2_PLACEMENT_3D ( 'NONE', #223167, #44555, #53531 ) ;
#152670=AXIS2_PLACEMENT_3D ( 'NONE', #163715, #181997, #244518 ) ;
#152680=CYLINDRICAL_SURFACE ( 'NONE', #68359, 0.09999999999999939493 ) ;
#152694=TOROIDAL_SURFACE ( 'NONE', #40259, 12.77499999999999858, 0.1000000000000000056 ) ;
#152740=EDGE_CURVE ( 'NONE', #110576, #172081, #250184, .T. ) ;
#152799=CARTESIAN_POINT ( 'NONE',  ( 19.75857864376268935, 64.25000000001148237, -44.67310748452440095 ) ) ;
#152807=ORIENTED_EDGE ( 'NONE', *, *, #250499, .T. ) ;
#152812=EDGE_LOOP ( 'NONE', ( #13382, #111116, #101776 ) ) ;
#152820=DIRECTION ( 'NONE',  ( 0.000000000000000000, -1.000000000000000000, -6.352154140967427193E-15 ) ) ;
#152834=AXIS2_PLACEMENT_3D ( 'NONE', #201898, #23288, #3686 ) ;
#152841=LINE ( 'NONE', #234919, #100780 ) ;
#152852=EDGE_LOOP ( 'NONE', ( #23642, #150196, #159238, #120302 ) ) ;
#152857=VECTOR ( 'NONE', #142217, 1000.000000000000000 ) ;
#152895=EDGE_LOOP ( 'NONE', ( #106374, #82179, #218817, #80947 ) ) ;
#152904=CARTESIAN_POINT ( 'NONE',  ( -20.00857864376270001, 66.85000000001150511, -48.27310748452438816 ) ) ;
#152939=EDGE_CURVE ( 'NONE', #175419, #13038, #81769, .T. ) ;
#152942=EDGE_CURVE ( 'NONE', #208701, #204082, #58595, .T. ) ;
#152952=CARTESIAN_POINT ( 'NONE',  ( 18.49999999999998934, 64.35000000001147669, -44.77310748452440237 ) ) ;
#152954=ORIENTED_EDGE ( 'NONE', *, *, #87426, .T. ) ;
#152958=EDGE_CURVE ( 'NONE', #69378, #136580, #179250, .T. ) ;
#152993=CARTESIAN_POINT ( 'NONE',  ( -20.54999999999999716, 76.00000000001142553, -36.02310748452432421 ) ) ;
#152995=DIRECTION ( 'NONE',  ( -1.836970198721029934E-16, -1.000000000000000000, -6.982962677686266711E-15 ) ) ;
#153010=EDGE_CURVE ( 'NONE', #231849, #203482, #8690, .T. ) ;
#153013=EDGE_CURVE ( 'NONE', #189305, #72671, #50211, .T. ) ;
#153030=ORIENTED_EDGE ( 'NONE', *, *, #212325, .F. ) ;
#153033=CARTESIAN_POINT ( 'NONE',  ( -2.995603634470891112E-16, 69.35000000001151932, -48.27310748452436684 ) ) ;
#153035=CARTESIAN_POINT ( 'NONE',  ( -22.40000000000000213, 76.00000000001173817, -81.27354037698292188 ) ) ;
#153071=CIRCLE ( 'NONE', #241104, 0.1000000000000052097 ) ;
#153080=CARTESIAN_POINT ( 'NONE',  ( 23.14999999999999858, 76.00000000001143974, -38.02310748452432421 ) ) ;
#153101=CIRCLE ( 'NONE', #157374, 11.80000000000000426 ) ;
#153128=EDGE_CURVE ( 'NONE', #13038, #238989, #213293, .T. ) ;
#153131=CARTESIAN_POINT ( 'NONE',  ( 21.17356465864818915, 75.90108875899782959, -75.94591061076604888 ) ) ;
#153142=CARTESIAN_POINT ( 'NONE',  ( -23.15000000000000213, 76.00000000001142553, -36.02310748452432421 ) ) ;
#153178=AXIS2_PLACEMENT_3D ( 'NONE', #169445, #91147, #131558 ) ;
#153192=CARTESIAN_POINT ( 'NONE',  ( -23.15000000000000213, 71.65000000001151648, -48.17310748452435121 ) ) ;
#153195=EDGE_LOOP ( 'NONE', ( #47658, #160073, #27923, #231300 ) ) ;
#153201=ORIENTED_EDGE ( 'NONE', *, *, #222822, .T. ) ;
#153244=AXIS2_PLACEMENT_3D ( 'NONE', #85985, #70345, #207272 ) ;
#153254=PLANE ( 'NONE',  #7427 ) ;
#153262=CARTESIAN_POINT ( 'NONE',  ( 20.94999999999999929, 69.45000000001157048, -57.27310748452437394 ) ) ;
#153267=CARTESIAN_POINT ( 'NONE',  ( -18.59999999999999787, 77.16270174994961906, -61.42310748452431568 ) ) ;
#153298=DIRECTION ( 'NONE',  ( -1.000000000000000000, 0.000000000000000000, -0.000000000000000000 ) ) ;
#153307=ORIENTED_EDGE ( 'NONE', *, *, #231423, .F. ) ;
#153320=ADVANCED_FACE ( 'NONE', ( #84013 ), #39835, .T. ) ;
#153354=ORIENTED_EDGE ( 'NONE', *, *, #155654, .T. ) ;
#153410=ORIENTED_EDGE ( 'NONE', *, *, #131227, .T. ) ;
#153444=CARTESIAN_POINT ( 'NONE',  ( 21.05000000000000071, 69.74218538953552127, -69.62089777583315708 ) ) ;
#153447=DIRECTION ( 'NONE',  ( 0.000000000000000000, 6.982962677686266711E-15, -1.000000000000000000 ) ) ;
#153450=DIRECTION ( 'NONE',  ( 0.000000000000000000, -0.1350103645451974088, 0.9908441862701587999 ) ) ;
#153452=ORIENTED_EDGE ( 'NONE', *, *, #181470, .T. ) ;
#153458=CIRCLE ( 'NONE', #41010, 0.09999999999999939493 ) ;
#153513=CARTESIAN_POINT ( 'NONE',  ( 0.000000000000000000, 0.000000000000000000, 0.000000000000000000 ) ) ;
#153540=TOROIDAL_SURFACE ( 'NONE', #195212, 0.2000000000000000111, 0.1000000000000000056 ) ;
#153575=LINE ( 'NONE', #93542, #29184 ) ;
#153589=ORIENTED_EDGE ( 'NONE', *, *, #115871, .T. ) ;
#153608=AXIS2_PLACEMENT_3D ( 'NONE', #149855, #211095, #229385 ) ;
#153609=ORIENTED_EDGE ( 'NONE', *, *, #206248, .T. ) ;
#153626=AXIS2_PLACEMENT_3D ( 'NONE', #115798, #96221, #74136 ) ;
#153650=CIRCLE ( 'NONE', #186939, 11.79999999999999716 ) ;
#153668=CARTESIAN_POINT ( 'NONE',  ( -18.59999999999999787, 85.50000000001156764, -57.37310748452425457 ) ) ;
#153714=CARTESIAN_POINT ( 'NONE',  ( 20.94999999999999929, 85.00000000001159606, -59.62913836187181715 ) ) ;
#153733=CARTESIAN_POINT ( 'NONE',  ( -18.50000000000000000, 64.25000000001173817, -81.27310748452440237 ) ) ;
#153753=CARTESIAN_POINT ( 'NONE',  ( -18.59999994787167310, 85.52363768977302527, -29.14065794975181589 ) ) ;
#153767=VERTEX_POINT ( 'NONE', #125151 ) ;
#153793=DIRECTION ( 'NONE',  ( 0.000000000000000000, 6.982962677686266711E-15, -1.000000000000000000 ) ) ;
#153808=CIRCLE ( 'NONE', #41355, 0.09999999999999489853 ) ;
#153834=CARTESIAN_POINT ( 'NONE',  ( -20.54999999999999716, 76.00000000001165290, -69.52310748452431710 ) ) ;
#153881=CARTESIAN_POINT ( 'NONE',  ( 23.24999999999999645, 71.22429906543214884, -57.67433938047838637 ) ) ;
#153893=CARTESIAN_POINT ( 'NONE',  ( -21.04999999999999716, 69.55922910634974698, -69.50551029751636634 ) ) ;
#153927=AXIS2_PLACEMENT_3D ( 'NONE', #115585, #197681, #234241 ) ;
#153930=DIRECTION ( 'NONE',  ( -2.561896900575096011E-15, 0.5907332058517336115, -0.8068669527896984439 ) ) ;
#153937=VERTEX_POINT ( 'NONE', #247653 ) ;
#153985=ORIENTED_EDGE ( 'NONE', *, *, #132931, .T. ) ;
#154007=DIRECTION ( 'NONE',  ( 0.000000000000000000, 6.982962677686266711E-15, -1.000000000000000000 ) ) ;
#154044=DIRECTION ( 'NONE',  ( 0.000000000000000000, 0.1350103645451974088, -0.9908441862701587999 ) ) ;
#154083=EDGE_CURVE ( 'NONE', #232002, #149532, #162680, .T. ) ;
#154087=AXIS2_PLACEMENT_3D ( 'NONE', #111839, #87115, #131385 ) ;
#154091=ORIENTED_EDGE ( 'NONE', *, *, #121225, .T. ) ;
#154106=EDGE_LOOP ( 'NONE', ( #139822, #238227, #204812, #241670 ) ) ;
#154164=CARTESIAN_POINT ( 'NONE',  ( -21.17356465864818560, 69.57719687376993534, -69.62201872553823989 ) ) ;
#154236=LINE ( 'NONE', #94199, #198544 ) ;
#154253=CARTESIAN_POINT ( 'NONE',  ( 18.39999999999999858, 85.50000000001161027, -62.49103808782458458 ) ) ;
#154256=DIRECTION ( 'NONE',  ( 1.000000000000000000, -2.952720810173289112E-16, -2.061873921506763405E-30 ) ) ;
#154289=CARTESIAN_POINT ( 'NONE',  ( -20.94999999999999929, 77.83534155023598089, -57.96795619196132776 ) ) ;
#154294=ORIENTED_EDGE ( 'NONE', *, *, #59065, .T. ) ;
#154332=DIRECTION ( 'NONE',  ( 1.000000000000000000, 0.000000000000000000, 0.000000000000000000 ) ) ;
#154342=AXIS2_PLACEMENT_3D ( 'NONE', #83047, #62246, #221294 ) ;
#154349=CYLINDRICAL_SURFACE ( 'NONE', #101422, 0.1000000000000028644 ) ;
#154356=AXIS2_PLACEMENT_3D ( 'NONE', #179839, #72062, #112472 ) ;
#154360=DIRECTION ( 'NONE',  ( 0.000000000000000000, 0.000000000000000000, 1.000000000000000000 ) ) ;
#154364=CARTESIAN_POINT ( 'NONE',  ( 20.94999999999999574, 77.25000000001159606, -61.52310748452431710 ) ) ;
#154374=DIRECTION ( 'NONE',  ( 0.000000000000000000, -7.272083257015735086E-15, 1.000000000000000000 ) ) ;
#154409=EDGE_CURVE ( 'NONE', #246837, #131784, #150923, .T. ) ;
#154464=( BOUNDED_CURVE ( )  B_SPLINE_CURVE ( 3, ( #187692, #7758, #226788, #6456 ),
 .UNSPECIFIED., .F., .F. ) 
 B_SPLINE_CURVE_WITH_KNOTS ( ( 4, 4 ),
 ( 3.141592653589778461, 4.712388980384686121 ),
 .UNSPECIFIED. ) 
 CURVE ( )  GEOMETRIC_REPRESENTATION_ITEM ( )  RATIONAL_B_SPLINE_CURVE ( ( 1.000000000000000000, 0.8047378541243622729, 0.8047378541243622729, 1.000000000000000000 ) ) 
 REPRESENTATION_ITEM ( '' )  );
#154475=DIRECTION ( 'NONE',  ( 1.000000000000000000, -0.000000000000000000, 0.000000000000000000 ) ) ;
#154483=EDGE_CURVE ( 'NONE', #64792, #246608, #13557, .T. ) ;
#154490=ORIENTED_EDGE ( 'NONE', *, *, #119647, .T. ) ;
#154496=DIRECTION ( 'NONE',  ( 0.000000000000000000, 1.000000000000000000, 6.982962677686266711E-15 ) ) ;
#154515=ORIENTED_EDGE ( 'NONE', *, *, #140643, .T. ) ;
#154542=ORIENTED_EDGE ( 'NONE', *, *, #108323, .T. ) ;
#154548=DIRECTION ( 'NONE',  ( 0.000000000000000000, 0.9908441862701605762, -0.1350103645451835310 ) ) ;
#154564=VERTEX_POINT ( 'NONE', #18189 ) ;
#154567=DIRECTION ( 'NONE',  ( -1.000000000000000000, 0.000000000000000000, -0.000000000000000000 ) ) ;
#154589=CARTESIAN_POINT ( 'NONE',  ( -21.05000000000000071, 64.35000000001146248, -43.03791325517834565 ) ) ;
#154591=CARTESIAN_POINT ( 'NONE',  ( -23.25000000000000000, 87.65000000001163016, -66.42310748452423752 ) ) ;
#154594=CARTESIAN_POINT ( 'NONE',  ( -23.25000000000000000, 69.01799029515495931, -32.32695536626808774 ) ) ;
#154650=LINE ( 'NONE', #58061, #217923 ) ;
#154652=CARTESIAN_POINT ( 'NONE',  ( 18.59999999999999076, 68.87972903831379767, -32.36354444268504693 ) ) ;
#154682=EDGE_CURVE ( 'NONE', #196464, #105159, #209324, .T. ) ;
#154689=CARTESIAN_POINT ( 'NONE',  ( 20.94999999999999929, 87.65000000001144542, -38.92310748452424463 ) ) ;
#154697=CARTESIAN_POINT ( 'NONE',  ( -20.96077737575335576, 64.37609936600659921, -42.88231552741780206 ) ) ;
#154706=LINE ( 'NONE', #175548, #10109 ) ;
#154707=CARTESIAN_POINT ( 'NONE',  ( 21.04999999999999716, 69.55891531154045992, -69.50538805121503572 ) ) ;
#154722=DIRECTION ( 'NONE',  ( -0.7071067811865127117, -0.7071067811865821007, 0.000000000000000000 ) ) ;
#154756=EDGE_CURVE ( 'NONE', #136422, #97734, #38402, .T. ) ;
#154798=ORIENTED_EDGE ( 'NONE', *, *, #113718, .F. ) ;
#154801=EDGE_CURVE ( 'NONE', #2421, #117589, #257381, .T. ) ;
#154824=DIRECTION ( 'NONE',  ( 1.000000000000000000, -0.000000000000000000, 0.000000000000000000 ) ) ;
#154830=DIRECTION ( 'NONE',  ( 0.000000000000000000, -6.688090509790097607E-15, 1.000000000000000000 ) ) ;
#154855=CARTESIAN_POINT ( 'NONE',  ( -22.50000000000000000, 64.35042919246686210, -69.62310748452439668 ) ) ;
#154873=CARTESIAN_POINT ( 'NONE',  ( -21.45000000000000284, 68.29142135624888965, -57.17310748452437963 ) ) ;
#154902=ORIENTED_EDGE ( 'NONE', *, *, #171016, .T. ) ;
#154904=EDGE_CURVE ( 'NONE', #212207, #100678, #127884, .T. ) ;
#154922=LINE ( 'NONE', #118343, #20683 ) ;
#154939=CYLINDRICAL_SURFACE ( 'NONE', #163697, 0.1000000000000028644 ) ;
#154961=ORIENTED_EDGE ( 'NONE', *, *, #188775, .F. ) ;
#154978=LINE ( 'NONE', #79237, #185280 ) ;
#154996=ADVANCED_FACE ( 'NONE', ( #29156 ), #146467, .T. ) ;
#155006=CARTESIAN_POINT ( 'NONE',  ( -20.64999999999999858, 85.00000000001159606, -59.62913836187181715 ) ) ;
#155019=FACE_OUTER_BOUND ( 'NONE', #15277, .T. ) ;
#155041=AXIS2_PLACEMENT_3D ( 'NONE', #141647, #242029, #221172 ) ;
#155077=CARTESIAN_POINT ( 'NONE',  ( -21.05000000000000071, 74.25000000001156764, -57.85359592662268824 ) ) ;
#155103=CARTESIAN_POINT ( 'NONE',  ( -21.44999999999999929, 68.65000000001150227, -48.37310748452437537 ) ) ;
#155139=AXIS2_PLACEMENT_3D ( 'NONE', #126291, #27240, #166751 ) ;
#155171=CARTESIAN_POINT ( 'NONE',  ( -23.15000000000000213, 76.00000000001168132, -73.67310748452432279 ) ) ;
#155182=DIRECTION ( 'NONE',  ( 1.000000000000000000, 0.000000000000000000, 0.000000000000000000 ) ) ;
#155200=CARTESIAN_POINT ( 'NONE',  ( -21.05000000000000071, 77.16270174994961906, -61.62310748452431142 ) ) ;
#155212=TOROIDAL_SURFACE ( 'NONE', #200966, 0.2000000000000000111, 0.1000000000000000056 ) ;
#155237=CARTESIAN_POINT ( 'NONE',  ( 20.92356734117541706, 65.68026841930851845, -30.47257401318895376 ) ) ;
#155251=DIRECTION ( 'NONE',  ( -0.000000000000000000, 0.4791956752371485107, 0.8777080977375185666 ) ) ;
#155253=ORIENTED_EDGE ( 'NONE', *, *, #216858, .F. ) ;
#155257=ADVANCED_FACE ( 'NONE', ( #64076 ), #117408, .T. ) ;
#155263=FACE_OUTER_BOUND ( 'NONE', #240600, .T. ) ;
#155285=DIRECTION ( 'NONE',  ( -1.000000000000000000, -0.000000000000000000, -0.000000000000000000 ) ) ;
#155322=CARTESIAN_POINT ( 'NONE',  ( -18.46856557590793813, 85.47421590779813982, -62.42112124364197001 ) ) ;
#155334=EDGE_CURVE ( 'NONE', #70064, #136730, #188136, .T. ) ;
#155358=CIRCLE ( 'NONE', #234414, 2.100000000000004530 ) ;
#155414=DIRECTION ( 'NONE',  ( 0.000000000000000000, -1.000000000000000000, -6.982962677686265922E-15 ) ) ;
#155445=CARTESIAN_POINT ( 'NONE',  ( -21.40925344232282512, 69.34148114062121238, -69.62205767314401328 ) ) ;
#155454=VECTOR ( 'NONE', #243539, 1000.000000000000000 ) ;
#155465=DIRECTION ( 'NONE',  ( -1.000000000000000000, 0.000000000000000000, -0.000000000000000000 ) ) ;
#155467=CARTESIAN_POINT ( 'NONE',  ( 23.24999999999999289, 71.85000000001166143, -69.52310748452434552 ) ) ;
#155475=EDGE_LOOP ( 'NONE', ( #28223, #97140, #193412, #48755, #181040, #96510, #253878, #246157, #125029, #100921 ) ) ;
#155485=CARTESIAN_POINT ( 'NONE',  ( -20.94999999999999929, 74.16465844978715438, -57.96795619196135618 ) ) ;
#155495=VERTEX_POINT ( 'NONE', #131753 ) ;
#155503=ORIENTED_EDGE ( 'NONE', *, *, #233898, .F. ) ;
#155528=DIRECTION ( 'NONE',  ( 1.000000000000000000, 0.000000000000000000, 0.000000000000000000 ) ) ;
#155544=SPHERICAL_SURFACE ( 'NONE', #9556, 0.1000000000000000056 ) ;
#155564=CYLINDRICAL_SURFACE ( 'NONE', #238667, 0.1000000000000028644 ) ;
#155565=ORIENTED_EDGE ( 'NONE', *, *, #22329, .F. ) ;
#155567=AXIS2_PLACEMENT_3D ( 'NONE', #203546, #204808, #44485 ) ;
#155610=CARTESIAN_POINT ( 'NONE',  ( -18.50000000000000000, 64.25000000001165290, -69.42310748452440805 ) ) ;
#155614=AXIS2_PLACEMENT_3D ( 'NONE', #4606, #84102, #26786 ) ;
#155654=EDGE_CURVE ( 'NONE', #56627, #216065, #9252, .T. ) ;
#155658=CARTESIAN_POINT ( 'NONE',  ( -18.50000000000000355, 85.40000000001157332, -62.22584772486096938 ) ) ;
#155706=CIRCLE ( 'NONE', #30796, 0.8750000000000007772 ) ;
#155730=DIRECTION ( 'NONE',  ( -1.000000000000000000, -0.000000000000000000, -0.000000000000000000 ) ) ;
#155782=AXIS2_PLACEMENT_3D ( 'NONE', #49812, #26419, #71958 ) ;
#155785=CIRCLE ( 'NONE', #251435, 0.1000000000000028644 ) ;
#155797=VECTOR ( 'NONE', #113988, 1000.000000000000000 ) ;
#155803=DIRECTION ( 'NONE',  ( 1.000000000000000000, 0.000000000000000000, 0.000000000000000000 ) ) ;
#155804=CARTESIAN_POINT ( 'NONE',  ( -18.50000000000000000, 64.35000000001174669, -81.27310748452440237 ) ) ;
#155809=DIRECTION ( 'NONE',  ( 0.000000000000000000, -1.387778780781406043E-13, -1.000000000000000000 ) ) ;
#155813=VERTEX_POINT ( 'NONE', #93605 ) ;
#155814=CARTESIAN_POINT ( 'NONE',  ( -23.15000000000000213, 64.35000000001156195, -57.37310748452439668 ) ) ;
#155816=CARTESIAN_POINT ( 'NONE',  ( 22.57320508075688892, 64.25000000001163869, -69.52310748452440237 ) ) ;
#155832=AXIS2_PLACEMENT_3D ( 'NONE', #130413, #204803, #26200 ) ;
#155846=CARTESIAN_POINT ( 'NONE',  ( -23.25000000000000000, 76.00000000001162448, -65.47310748452431994 ) ) ;
#155849=CARTESIAN_POINT ( 'NONE',  ( -22.39999999999999858, 76.10000000001174669, -81.17267829206912211 ) ) ;
#155862=EDGE_CURVE ( 'NONE', #194241, #79556, #213243, .T. ) ;
#155877=AXIS2_PLACEMENT_3D ( 'NONE', #203728, #223272, #99461 ) ;
#155897=CARTESIAN_POINT ( 'NONE',  ( 21.14999999999999858, 76.00000000001156764, -57.37310748452432563 ) ) ;
#155903=CARTESIAN_POINT ( 'NONE',  ( -1.739115166359751801E-14, 64.35000000001149090, -44.67310748452440095 ) ) ;
#155933=FACE_OUTER_BOUND ( 'NONE', #175105, .T. ) ;
#155940=CARTESIAN_POINT ( 'NONE',  ( -20.54999999999999716, 71.65000000001155911, -57.17310748452435121 ) ) ;
#155960=VECTOR ( 'NONE', #214702, 1000.000000000000114 ) ;
#155969=ORIENTED_EDGE ( 'NONE', *, *, #22070, .T. ) ;
#155985=CARTESIAN_POINT ( 'NONE',  ( 21.09096482362065217, 69.63645563460735843, -69.56255576329859025 ) ) ;
#155988=CARTESIAN_POINT ( 'NONE',  ( -18.59999999999999787, 76.00000000001136868, -28.12310748452432208 ) ) ;
#156001=CARTESIAN_POINT ( 'NONE',  ( -21.37071067811865532, 67.92928932189285263, -48.37310748452437537 ) ) ;
#156003=ADVANCED_FACE ( 'NONE', ( #16650 ), #216107, .T. ) ;
#156056=ORIENTED_EDGE ( 'NONE', *, *, #235817, .F. ) ;
#156105=VERTEX_POINT ( 'NONE', #184681 ) ;
#156109=ORIENTED_EDGE ( 'NONE', *, *, #14510, .F. ) ;
#156157=DIRECTION ( 'NONE',  ( 2.952720810173289112E-16, 1.000000000000000000, 6.982962677686266711E-15 ) ) ;
#156168=CARTESIAN_POINT ( 'NONE',  ( 20.97250901189795513, 65.37543196630971920, -61.85856176755740421 ) ) ;
#156191=ORIENTED_EDGE ( 'NONE', *, *, #131571, .F. ) ;
#156194=CARTESIAN_POINT ( 'NONE',  ( -21.09096482362064506, 75.96055172123749344, -75.88665184992862578 ) ) ;
#156218=ORIENTED_EDGE ( 'NONE', *, *, #15148, .F. ) ;
#156220=DIRECTION ( 'NONE',  ( 1.000000000000000000, 0.000000000000000000, 0.000000000000000000 ) ) ;
#156228=EDGE_CURVE ( 'NONE', #15384, #211799, #192594, .T. ) ;
#156250=CARTESIAN_POINT ( 'NONE',  ( -20.95613430942403355, 64.25000000001159606, -62.66594483630497336 ) ) ;
#156251=CYLINDRICAL_SURFACE ( 'NONE', #156784, 0.09999999999999939493 ) ;
#156256=EDGE_CURVE ( 'NONE', #185953, #112792, #218355, .T. ) ;
#156280=DIRECTION ( 'NONE',  ( 0.000000000000000000, 0.000000000000000000, 1.000000000000000000 ) ) ;
#156281=DIRECTION ( 'NONE',  ( -0.000000000000000000, -6.982962677686266711E-15, 1.000000000000000000 ) ) ;
#156293=DIRECTION ( 'NONE',  ( 1.000000000000000000, 0.000000000000000000, 0.000000000000000000 ) ) ;
#156337=VERTEX_POINT ( 'NONE', #142366 ) ;
#156365=EDGE_LOOP ( 'NONE', ( #32867, #189368, #18832, #89654 ) ) ;
#156370=ORIENTED_EDGE ( 'NONE', *, *, #134717, .T. ) ;
#156378=VERTEX_POINT ( 'NONE', #62836 ) ;
#156408=( GEOMETRIC_REPRESENTATION_CONTEXT ( 3 ) GLOBAL_UNCERTAINTY_ASSIGNED_CONTEXT ( ( #68666 ) ) GLOBAL_UNIT_ASSIGNED_CONTEXT ( ( #32308, #49267, #230480 ) ) REPRESENTATION_CONTEXT ( 'NONE', 'WORKASPACE' ) );
#156440=CARTESIAN_POINT ( 'NONE',  ( 22.00356870143104260, 68.74575763753909996, -69.52310748452437394 ) ) ;
#156445=CARTESIAN_POINT ( 'NONE',  ( -21.05000000000000071, 69.69503888732667463, -69.50172191858641213 ) ) ;
#156461=VECTOR ( 'NONE', #125773, 1000.000000000000000 ) ;
#156533=CARTESIAN_POINT ( 'NONE',  ( 21.08376601933332495, 69.65805272873599563, -69.58688349545435869 ) ) ;
#156564=ORIENTED_EDGE ( 'NONE', *, *, #118586, .F. ) ;
#156568=AXIS2_PLACEMENT_3D ( 'NONE', #5567, #245500, #205055 ) ;
#156597=ADVANCED_FACE ( 'NONE', ( #91395 ), #152680, .T. ) ;
#156642=VECTOR ( 'NONE', #33992, 1000.000000000000114 ) ;
#156651=ADVANCED_FACE ( 'NONE', ( #133088 ), #17003, .T. ) ;
#156700=CARTESIAN_POINT ( 'NONE',  ( -18.50000000000000000, 66.65000000001150227, -48.37310748452438958 ) ) ;
#156706=ORIENTED_EDGE ( 'NONE', *, *, #66169, .T. ) ;
#156722=CARTESIAN_POINT ( 'NONE',  ( -21.12642695952773764, 69.62434007797649826, -69.62201076771371788 ) ) ;
#156725=CARTESIAN_POINT ( 'NONE',  ( -20.85000000000000142, 68.97833521811131163, -32.18954208262707795 ) ) ;
#156726=CIRCLE ( 'NONE', #202481, 0.09999999999999938105 ) ;
#156740=( LENGTH_UNIT ( ) NAMED_UNIT ( * ) SI_UNIT ( .MILLI., .METRE. ) );
#156776=FACE_OUTER_BOUND ( 'NONE', #164832, .T. ) ;
#156784=AXIS2_PLACEMENT_3D ( 'NONE', #125741, #255262, #197901 ) ;
#156792=DIRECTION ( 'NONE',  ( 0.000000000000000000, -1.000000000000000000, -6.352154140967427193E-15 ) ) ;
#156803=ORIENTED_EDGE ( 'NONE', *, *, #140788, .T. ) ;
#156809=DIRECTION ( 'NONE',  ( 2.715809747126117987E-16, 1.000000000000000000, 6.517943393102682774E-15 ) ) ;
#156877=DIRECTION ( 'NONE',  ( -1.000000000000000000, 0.000000000000000000, 0.000000000000000000 ) ) ;
#156906=CARTESIAN_POINT ( 'NONE',  ( 21.05000000000000071, 67.22371710471912820, -60.96447848938343839 ) ) ;
#156917=CARTESIAN_POINT ( 'NONE',  ( -20.85000000000000497, 64.25000000001148237, -42.94225473048309993 ) ) ;
#156923=ORIENTED_EDGE ( 'NONE', *, *, #174541, .F. ) ;
#156931=CARTESIAN_POINT ( 'NONE',  ( -18.46093223321764754, 85.48068296828618884, -62.43855697059758114 ) ) ;
#156934=AXIS2_PLACEMENT_3D ( 'NONE', #23615, #50812, #7883 ) ;
#156991=CARTESIAN_POINT ( 'NONE',  ( 21.05000000000000071, 84.73084112150691283, -59.92503276553992464 ) ) ;
#157004=CARTESIAN_POINT ( 'NONE',  ( -21.14999999999999858, 64.25000000001165290, -69.52310748452438816 ) ) ;
#157040=DIRECTION ( 'NONE',  ( 1.000000000000000000, 0.000000000000000000, 0.000000000000000000 ) ) ;
#157050=CARTESIAN_POINT ( 'NONE',  ( 21.14999999999999858, 87.75000000001156764, -57.27310748452423894 ) ) ;
#157064=EDGE_CURVE ( 'NONE', #126775, #223761, #93844, .T. ) ;
#157073=FACE_OUTER_BOUND ( 'NONE', #173228, .T. ) ;
#157094=CARTESIAN_POINT ( 'NONE',  ( 22.49533356619859958, 64.34999999370755575, -69.58823006484711016 ) ) ;
#157138=DIRECTION ( 'NONE',  ( -1.000000000000000000, 0.000000000000000000, -0.000000000000000000 ) ) ;
#157141=AXIS2_PLACEMENT_3D ( 'NONE', #183251, #244496, #121990 ) ;
#157143=EDGE_LOOP ( 'NONE', ( #33812, #19999, #45592, #146132 ) ) ;
#157170=DIRECTION ( 'NONE',  ( 0.000000000000000000, -6.982962677686266711E-15, 1.000000000000000000 ) ) ;
#157181=DIRECTION ( 'NONE',  ( -1.000000000000000000, -0.000000000000000000, -0.000000000000000000 ) ) ;
#157270=CARTESIAN_POINT ( 'NONE',  ( 21.11833042828127915, 69.55435530615625339, -69.53020799358364457 ) ) ;
#157285=DIRECTION ( 'NONE',  ( -0.000000000000000000, 0.1298341882519735979, 0.9915357197604890427 ) ) ;
#157297=ORIENTED_EDGE ( 'NONE', *, *, #67249, .F. ) ;
#157310=EDGE_CURVE ( 'NONE', #201109, #1289, #135334, .T. ) ;
#157311=CIRCLE ( 'NONE', #210884, 0.09999999999999939493 ) ;
#157314=ORIENTED_EDGE ( 'NONE', *, *, #159758, .F. ) ;
#157323=CARTESIAN_POINT ( 'NONE',  ( 18.39999999999999858, 85.50000000001136868, -29.42291809330221497 ) ) ;
#157344=CARTESIAN_POINT ( 'NONE',  ( 20.85000000000000142, 69.01799029515495931, -32.32695536626808064 ) ) ;
#157368=DIRECTION ( 'NONE',  ( 0.000000000000000000, 0.4999999999999689138, 0.8660254037844565822 ) ) ;
#157372=DIRECTION ( 'NONE',  ( -2.915501640297152804E-16, -1.000000000000000000, -6.997203936713167125E-15 ) ) ;
#157374=AXIS2_PLACEMENT_3D ( 'NONE', #150396, #173849, #193379 ) ;
#157375=DIRECTION ( 'NONE',  ( -6.938893903907222856E-15, -1.000000000000000000, -6.982962677686266711E-15 ) ) ;
#157395=CARTESIAN_POINT ( 'NONE',  ( -23.25000000000000000, 76.00000000001142553, -36.02310748452432421 ) ) ;
#157429=ADVANCED_FACE ( 'NONE', ( #75085 ), #172795, .T. ) ;
#157447=EDGE_CURVE ( 'NONE', #230655, #115707, #239390, .T. ) ;
#157493=CARTESIAN_POINT ( 'NONE',  ( 18.57071067811864040, 65.82071067813016896, -48.17310748452439384 ) ) ;
#157516=ORIENTED_EDGE ( 'NONE', *, *, #33333, .T. ) ;
#157517=FACE_OUTER_BOUND ( 'NONE', #42488, .T. ) ;
#157518=DIRECTION ( 'NONE',  ( 0.000000000000000000, -6.982962677686266711E-15, 1.000000000000000000 ) ) ;
#157526=VECTOR ( 'NONE', #124843, 1000.000000000000000 ) ;
#157543=EDGE_CURVE ( 'NONE', #113349, #48405, #106079, .T. ) ;
#157548=DIRECTION ( 'NONE',  ( 1.000000000000000000, -0.000000000000000000, 0.000000000000000000 ) ) ;
#157601=DIRECTION ( 'NONE',  ( 0.000000000000000000, 0.9908441862701605762, 0.1350103645451835310 ) ) ;
#157644=PLANE ( 'NONE',  #144048 ) ;
#157659=ORIENTED_EDGE ( 'NONE', *, *, #166481, .F. ) ;
#157682=DIRECTION ( 'NONE',  ( -1.000000000000000000, 2.952720810173289112E-16, 2.061873921506763405E-30 ) ) ;
#157698=DIRECTION ( 'NONE',  ( 1.000000000000000000, 0.000000000000000000, 0.000000000000000000 ) ) ;
#157719=EDGE_LOOP ( 'NONE', ( #221428, #8728, #26426, #37541 ) ) ;
#157732=DIRECTION ( 'NONE',  ( 1.000000000000000000, 0.000000000000000000, 0.000000000000000000 ) ) ;
#157745=VECTOR ( 'NONE', #114271, 999.9999999999998863 ) ;
#157759=DIRECTION ( 'NONE',  ( 0.000000000000000000, 0.000000000000000000, -1.000000000000000000 ) ) ;
#157761=CARTESIAN_POINT ( 'NONE',  ( -18.59999999999999787, 74.16465844978715438, -57.86795619196135476 ) ) ;
#157802=DIRECTION ( 'NONE',  ( 6.938893903907270030E-14, 0.000000000000000000, -1.000000000000000000 ) ) ;
#157803=ORIENTED_EDGE ( 'NONE', *, *, #134671, .F. ) ;
#157818=CIRCLE ( 'NONE', #78636, 0.1000000000000028644 ) ;
#157823=CARTESIAN_POINT ( 'NONE',  ( 21.14999999999999858, 69.45934304831041572, -69.52310748452435973 ) ) ;
#157826=AXIS2_PLACEMENT_3D ( 'NONE', #234022, #37136, #237879 ) ;
#157871=AXIS2_PLACEMENT_3D ( 'NONE', #194871, #134846, #100835 ) ;
#157900=DIRECTION ( 'NONE',  ( 0.000000000000000000, 6.982962677686267499E-15, -1.000000000000000000 ) ) ;
#157925=ORIENTED_EDGE ( 'NONE', *, *, #42292, .F. ) ;
#157929=CARTESIAN_POINT ( 'NONE',  ( 21.05000000000000071, 85.00000000001149658, -45.41707660717670336 ) ) ;
#157931=CARTESIAN_POINT ( 'NONE',  ( 20.94999999999999574, 76.00000000001165290, -69.52310748452431710 ) ) ;
#157936=AXIS2_PLACEMENT_3D ( 'NONE', #247529, #126283, #110577 ) ;
#157952=CIRCLE ( 'NONE', #253741, 12.77499999999999858 ) ;
#157970=ORIENTED_EDGE ( 'NONE', *, *, #162882, .F. ) ;
#157977=CARTESIAN_POINT ( 'NONE',  ( -20.85000000000000142, 87.65000000001143121, -36.02310748452423894 ) ) ;
#157984=EDGE_LOOP ( 'NONE', ( #174955, #62088, #140918 ) ) ;
#157990=CARTESIAN_POINT ( 'NONE',  ( -23.25000000000000000, 76.00000000001142553, -36.02310748452432421 ) ) ;
#158003=CARTESIAN_POINT ( 'NONE',  ( -23.25000000000000000, 76.00000000001142553, -36.02310748452432421 ) ) ;
#158020=CARTESIAN_POINT ( 'NONE',  ( -23.24999999999999645, 85.60000000001137721, -29.42291809330221142 ) ) ;
#158059=PLANE ( 'NONE',  #199974 ) ;
#158066=CIRCLE ( 'NONE', #228756, 0.5000000000000004441 ) ;
#158144=AXIS2_PLACEMENT_3D ( 'NONE', #174166, #133704, #253634 ) ;
#158186=CIRCLE ( 'NONE', #220501, 7.900000000000003908 ) ;
#158201=AXIS2_PLACEMENT_3D ( 'NONE', #254357, #82135, #78296 ) ;
#158206=ORIENTED_EDGE ( 'NONE', *, *, #97835, .T. ) ;
#158248=ADVANCED_FACE ( 'NONE', ( #255676 ), #10629, .T. ) ;
#158286=ADVANCED_FACE ( 'NONE', ( #20999 ), #1382, .T. ) ;
#158305=CYLINDRICAL_SURFACE ( 'NONE', #85497, 0.09999999999999939493 ) ;
#158322=EDGE_CURVE ( 'NONE', #101771, #72671, #185587, .T. ) ;
#158324=ORIENTED_EDGE ( 'NONE', *, *, #48770, .F. ) ;
#158339=EDGE_CURVE ( 'NONE', #159190, #105103, #198052, .T. ) ;
#158345=CIRCLE ( 'NONE', #191671, 0.09999999999999939493 ) ;
#158388=EDGE_CURVE ( 'NONE', #39343, #232002, #105606, .T. ) ;
#158395=CIRCLE ( 'NONE', #50183, 0.1000000000000043771 ) ;
#158412=VECTOR ( 'NONE', #136304, 1000.000000000000000 ) ;
#158423=ORIENTED_EDGE ( 'NONE', *, *, #18411, .F. ) ;
#158492=ADVANCED_FACE ( 'NONE', ( #92482 ), #243840, .T. ) ;
#158494=ORIENTED_EDGE ( 'NONE', *, *, #152740, .F. ) ;
#158514=CARTESIAN_POINT ( 'NONE',  ( 20.94999999999999929, 74.16465844978715438, -57.96795619196134908 ) ) ;
#158560=CARTESIAN_POINT ( 'NONE',  ( -20.94999999999999929, 76.00000000001145395, -40.12310748452431852 ) ) ;
#158576=ADVANCED_FACE ( 'NONE', ( #35126 ), #157644, .F. ) ;
#158589=CIRCLE ( 'NONE', #91916, 0.2000000000000057288 ) ;
#158598=EDGE_CURVE ( 'NONE', #229077, #146391, #248306, .T. ) ;
#158610=ORIENTED_EDGE ( 'NONE', *, *, #107102, .T. ) ;
#158622=EDGE_CURVE ( 'NONE', #22349, #193539, #181682, .T. ) ;
#158635=DIRECTION ( 'NONE',  ( 0.000000000000000000, -7.056502275159894776E-15, 1.000000000000000000 ) ) ;
#158639=ORIENTED_EDGE ( 'NONE', *, *, #64179, .F. ) ;
#158640=DIRECTION ( 'NONE',  ( 0.000000000000000000, -7.086529944415893080E-15, 1.000000000000000000 ) ) ;
#158697=CARTESIAN_POINT ( 'NONE',  ( 21.05000000000000071, 76.00000000001142553, -36.02310748452432421 ) ) ;
#158735=DIRECTION ( 'NONE',  ( 0.000000000000000000, 0.000000000000000000, -1.000000000000000000 ) ) ;
#158739=CARTESIAN_POINT ( 'NONE',  ( 20.75572585718182950, 67.11768327161557579, -61.02584908581751222 ) ) ;
#158795=CIRCLE ( 'NONE', #42248, 0.1000000000000028644 ) ;
#158803=DIRECTION ( 'NONE',  ( -2.952720810173289605E-16, -1.000000000000000000, -7.086529944415894657E-15 ) ) ;
#158811=ORIENTED_EDGE ( 'NONE', *, *, #206247, .F. ) ;
#158827=DIRECTION ( 'NONE',  ( 0.000000000000000000, 6.982962677686266711E-15, -1.000000000000000000 ) ) ;
#158840=CARTESIAN_POINT ( 'NONE',  ( -18.59999999999999787, 66.65000000001150227, -48.37310748452438958 ) ) ;
#158850=AXIS2_PLACEMENT_3D ( 'NONE', #159336, #110228, #32012 ) ;
#158858=CARTESIAN_POINT ( 'NONE',  ( -22.48660254037843131, 64.35000000001164722, -69.57310748452438531 ) ) ;
#158883=DIRECTION ( 'NONE',  ( 0.000000000000000000, 0.9654727137038715545, -0.2605042016806676242 ) ) ;
#158887=AXIS2_PLACEMENT_3D ( 'NONE', #240872, #123485, #59624 ) ;
#158894=VERTEX_POINT ( 'NONE', #191318 ) ;
#158923=AXIS2_PLACEMENT_3D ( 'NONE', #94081, #13283, #92796 ) ;
#158939=ORIENTED_EDGE ( 'NONE', *, *, #118830, .T. ) ;
#158971=DIRECTION ( 'NONE',  ( 1.000000000000000000, 0.000000000000000000, 0.000000000000000000 ) ) ;
#158995=DIRECTION ( 'NONE',  ( 0.000000000000000000, -0.9999631594459057471, 0.008583690987121077309 ) ) ;
#158998=EDGE_CURVE ( 'NONE', #89961, #33900, #177618, .T. ) ;
#159003=ORIENTED_EDGE ( 'NONE', *, *, #238321, .T. ) ;
#159018=ADVANCED_FACE ( 'NONE', ( #239401 ), #60736, .F. ) ;
#159054=CARTESIAN_POINT ( 'NONE',  ( -20.00857864376270001, 66.75000000001158185, -57.17310748452438673 ) ) ;
#159080=PLANE ( 'NONE',  #255870 ) ;
#159081=CARTESIAN_POINT ( 'NONE',  ( 18.50211644919734866, 65.69792220476270472, -30.53355541284614816 ) ) ;
#159083=ORIENTED_EDGE ( 'NONE', *, *, #14604, .T. ) ;
#159100=CARTESIAN_POINT ( 'NONE',  ( 18.36493879433316323, 85.50000080620192477, -29.10095882417419944 ) ) ;
#159145=ORIENTED_EDGE ( 'NONE', *, *, #224276, .F. ) ;
#159148=DIRECTION ( 'NONE',  ( 0.000000000000000000, 0.000000000000000000, 1.000000000000000000 ) ) ;
#159154=DIRECTION ( 'NONE',  ( 1.000000000000000000, -0.000000000000000000, 0.000000000000000000 ) ) ;
#159186=ORIENTED_EDGE ( 'NONE', *, *, #52203, .T. ) ;
#159190=VERTEX_POINT ( 'NONE', #250929 ) ;
#159208=ADVANCED_FACE ( 'NONE', ( #233951 ), #117847, .F. ) ;
#159227=VERTEX_POINT ( 'NONE', #213101 ) ;
#159238=ORIENTED_EDGE ( 'NONE', *, *, #177492, .F. ) ;
#159248=EDGE_LOOP ( 'NONE', ( #5183, #237718, #77350, #26438 ) ) ;
#159258=ADVANCED_FACE ( 'NONE', ( #174026 ), #134669, .T. ) ;
#159301=CARTESIAN_POINT ( 'NONE',  ( 18.59999999999999076, 65.50857864377418593, -44.77310748452440237 ) ) ;
#159302=VERTEX_POINT ( 'NONE', #219511 ) ;
#159308=CARTESIAN_POINT ( 'NONE',  ( 21.05000000000000071, 76.00000000001145395, -38.92310748452432279 ) ) ;
#159336=CARTESIAN_POINT ( 'NONE',  ( -21.05000000000000071, 76.00000000001165290, -69.52310748452431710 ) ) ;
#159355=EDGE_LOOP ( 'NONE', ( #207074, #50017, #247359 ) ) ;
#159407=EDGE_CURVE ( 'NONE', #66243, #208701, #131964, .T. ) ;
#159436=VECTOR ( 'NONE', #196640, 999.9999999999998863 ) ;
#159442=ORIENTED_EDGE ( 'NONE', *, *, #220678, .T. ) ;
#159447=DIRECTION ( 'NONE',  ( 0.000000000000000000, -1.000000000000000000, -6.352154140967427193E-15 ) ) ;
#159463=DIRECTION ( 'NONE',  ( 0.9880948137434723000, -0.1538461538461484146, -1.074301950413233906E-15 ) ) ;
#159482=ORIENTED_EDGE ( 'NONE', *, *, #26803, .T. ) ;
#159486=CARTESIAN_POINT ( 'NONE',  ( -18.45037301276633812, 85.49020044755350511, -62.51043334810935193 ) ) ;
#159526=DIRECTION ( 'NONE',  ( 1.000000000000000000, 0.000000000000000000, 0.000000000000000000 ) ) ;
#159570=EDGE_CURVE ( 'NONE', #74560, #18090, #236020, .T. ) ;
#159574=CARTESIAN_POINT ( 'NONE',  ( -21.44999999999999929, 68.65000000001157332, -57.17310748452437252 ) ) ;
#159616=DIRECTION ( 'NONE',  ( 0.000000000000000000, -6.608470384673536824E-15, 1.000000000000000000 ) ) ;
#159624=ORIENTED_EDGE ( 'NONE', *, *, #75939, .F. ) ;
#159633=LINE ( 'NONE', #254817, #116701 ) ;
#159652=CARTESIAN_POINT ( 'NONE',  ( 22.49544290803783753, 64.25012976215460014, -69.58841944378183086 ) ) ;
#159658=DIRECTION ( 'NONE',  ( 1.000000000000000000, -1.836970198721029934E-16, -1.282749433769087582E-30 ) ) ;
#159659=DIRECTION ( 'NONE',  ( 0.7071067811865127117, 0.7071067811865821007, 0.000000000000000000 ) ) ;
#159682=CARTESIAN_POINT ( 'NONE',  ( 21.05095171578076574, 67.22382012124053574, -57.35723420788649918 ) ) ;
#159695=CARTESIAN_POINT ( 'NONE',  ( -23.25000000000000000, 85.00000000001159606, -59.62913836187181715 ) ) ;
#159700=DIRECTION ( 'NONE',  ( 1.000000000000000000, 0.000000000000000000, 0.000000000000000000 ) ) ;
#159726=DIRECTION ( 'NONE',  ( -1.000000000000000000, -7.304098846218135653E-16, -5.100424963727256530E-30 ) ) ;
#159727=CARTESIAN_POINT ( 'NONE',  ( -22.50000000000000000, 75.90000000001165859, -69.52310748452431710 ) ) ;
#159737=DIRECTION ( 'NONE',  ( -0.000000000000000000, -6.982962677686266711E-15, 1.000000000000000000 ) ) ;
#159745=TOROIDAL_SURFACE ( 'NONE', #47289, 0.2000000000000000111, 0.1000000000000000056 ) ;
#159758=EDGE_CURVE ( 'NONE', #201700, #88139, #111318, .T. ) ;
#159759=CARTESIAN_POINT ( 'NONE',  ( 19.75857864376268935, 64.35000000001147669, -44.77310748452440237 ) ) ;
#159762=CARTESIAN_POINT ( 'NONE',  ( -23.15000000000000213, 80.83132476063447314, -52.55341054232553688 ) ) ;
#159765=TOROIDAL_SURFACE ( 'NONE', #97369, 11.65000000000000036, 0.1000000000000000056 ) ;
#159768=DIRECTION ( 'NONE',  ( 0.000000000000000000, -6.982962677686266711E-15, 1.000000000000000000 ) ) ;
#159776=EDGE_CURVE ( 'NONE', #121217, #136766, #11553, .T. ) ;
#159833=AXIS2_PLACEMENT_3D ( 'NONE', #111930, #17934, #192746 ) ;
#159851=VERTEX_POINT ( 'NONE', #13987 ) ;
#159870=VECTOR ( 'NONE', #62190, 1000.000000000000000 ) ;
#159884=CIRCLE ( 'NONE', #14145, 0.1000000000000028644 ) ;
#159920=DIRECTION ( 'NONE',  ( 1.296989514748957922E-15, 0.9887567792719351711, -0.1495327102803594987 ) ) ;
#159977=TOROIDAL_SURFACE ( 'NONE', #5798, 0.4000000000000009104, 0.1000000000000000056 ) ;
#159984=ORIENTED_EDGE ( 'NONE', *, *, #65959, .F. ) ;
#160049=CARTESIAN_POINT ( 'NONE',  ( -20.94999999999999929, 64.35000000001141984, -36.02310748452440237 ) ) ;
#160056=CARTESIAN_POINT ( 'NONE',  ( -21.05000000000000426, 69.58624026620138636, -69.43749442372039482 ) ) ;
#160073=ORIENTED_EDGE ( 'NONE', *, *, #168617, .F. ) ;
#160086=CARTESIAN_POINT ( 'NONE',  ( -23.25000000000000000, 76.00000000001165290, -69.52310748452431710 ) ) ;
#160132=EDGE_CURVE ( 'NONE', #198388, #66243, #249065, .T. ) ;
#160136=VERTEX_POINT ( 'NONE', #51474 ) ;
#160137=DIRECTION ( 'NONE',  ( 0.000000000000000000, 0.000000000000000000, 1.000000000000000000 ) ) ;
#160163=DIRECTION ( 'NONE',  ( -1.000000000000000000, -0.000000000000000000, -0.000000000000000000 ) ) ;
#160176=DIRECTION ( 'NONE',  ( 1.000000000000000000, 0.000000000000000000, 0.000000000000000000 ) ) ;
#160178=ORIENTED_EDGE ( 'NONE', *, *, #93735, .F. ) ;
#160193=CARTESIAN_POINT ( 'NONE',  ( -20.91682497891422798, 65.67736539654895012, -30.46251168765720152 ) ) ;
#160247=AXIS2_PLACEMENT_3D ( 'NONE', #52251, #186668, #9295 ) ;
#160263=CARTESIAN_POINT ( 'NONE',  ( -20.07928932188135107, 66.77928932189284694, -48.27310748452438816 ) ) ;
#160278=EDGE_CURVE ( 'NONE', #32613, #49225, #208033, .T. ) ;
#160284=FACE_OUTER_BOUND ( 'NONE', #244572, .T. ) ;
#160285=ORIENTED_EDGE ( 'NONE', *, *, #15598, .T. ) ;
#160325=CARTESIAN_POINT ( 'NONE',  ( 21.05000000000000071, 84.66355140188063899, -45.54720860259157433 ) ) ;
#160341=CARTESIAN_POINT ( 'NONE',  ( -21.05000000000000071, 70.10000000001149090, -46.24220724918072989 ) ) ;
#160358=EDGE_CURVE ( 'NONE', #215216, #28556, #53230, .T. ) ;
#160368=CARTESIAN_POINT ( 'NONE',  ( -23.25000000000000000, 76.00000000001136868, -28.12310748452432208 ) ) ;
#160369=CARTESIAN_POINT ( 'NONE',  ( 18.51024323315077069, 65.68895814178189596, -30.50265578621380769 ) ) ;
#160370=DIRECTION ( 'NONE',  ( -1.000000000000000000, 7.304098846218164250E-16, -4.217023435051628197E-16 ) ) ;
#160399=EDGE_CURVE ( 'NONE', #156378, #40297, #63048, .T. ) ;
#160441=DIRECTION ( 'NONE',  ( -7.304098846217948299E-16, -1.000000000000000000, 0.000000000000000000 ) ) ;
#160483=VERTEX_POINT ( 'NONE', #208993 ) ;
#160520=CONICAL_SURFACE ( 'NONE', #139616, 4.299999999999956302, 0.7853981633974466137 ) ;
#160554=DIRECTION ( 'NONE',  ( 1.000000000000000000, 0.000000000000000000, 0.000000000000000000 ) ) ;
#160578=VERTEX_POINT ( 'NONE', #66910 ) ;
#160606=FACE_OUTER_BOUND ( 'NONE', #211495, .T. ) ;
#160609=CARTESIAN_POINT ( 'NONE',  ( -20.94999999999999929, 61.95000000001146390, -41.53680255528533394 ) ) ;
#160621=ORIENTED_EDGE ( 'NONE', *, *, #256288, .F. ) ;
#160625=ORIENTED_EDGE ( 'NONE', *, *, #50614, .T. ) ;
#160643=CARTESIAN_POINT ( 'NONE',  ( -18.50000000000000000, 66.75000000001158185, -57.17310748452438673 ) ) ;
#160699=EDGE_CURVE ( 'NONE', #231649, #108629, #120081, .T. ) ;
#160725=VERTEX_POINT ( 'NONE', #57609 ) ;
#160736=AXIS2_PLACEMENT_3D ( 'NONE', #187899, #168373, #229589 ) ;
#160763=CARTESIAN_POINT ( 'NONE',  ( -20.85000000000000142, 76.00000000001136868, -28.12310748452432208 ) ) ;
#160766=DIRECTION ( 'NONE',  ( 1.000000000000000000, -0.000000000000000000, 0.000000000000000000 ) ) ;
#160781=VERTEX_POINT ( 'NONE', #181446 ) ;
#160788=CARTESIAN_POINT ( 'NONE',  ( -18.43599941264908182, 85.51932742860678616, -62.55013069500345324 ) ) ;
#160789=EDGE_CURVE ( 'NONE', #212207, #243532, #53197, .T. ) ;
#160794=TOROIDAL_SURFACE ( 'NONE', #235765, 3.899999999999999467, 0.1000000000000000056 ) ;
#160809=EDGE_LOOP ( 'NONE', ( #42613, #44881, #46692, #191639 ) ) ;
#160816=TOROIDAL_SURFACE ( 'NONE', #148317, 1.900000000000002576, 0.1000000000000000056 ) ;
#160828=DIRECTION ( 'NONE',  ( 1.000000000000000000, 0.000000000000000000, 0.000000000000000000 ) ) ;
#160837=ORIENTED_EDGE ( 'NONE', *, *, #208335, .F. ) ;
#160842=ADVANCED_FACE ( 'NONE', ( #62767 ), #221808, .T. ) ;
#160907=CARTESIAN_POINT ( 'NONE',  ( 20.94999999999999574, 62.00000000001161737, -64.09601495414187866 ) ) ;
#160912=AXIS2_PLACEMENT_3D ( 'NONE', #212086, #88241, #248627 ) ;
#160932=CARTESIAN_POINT ( 'NONE',  ( 18.60000000000000497, 85.52394631232910172, -29.14107948918604407 ) ) ;
#160940=ORIENTED_EDGE ( 'NONE', *, *, #3527, .T. ) ;
#160957=CARTESIAN_POINT ( 'NONE',  ( -20.64999999999999858, 85.00000000001149658, -45.91707660717669626 ) ) ;
#160980=CARTESIAN_POINT ( 'NONE',  ( 18.59999999999999432, 77.83585931145498193, -24.51866831572578320 ) ) ;
#161046=AXIS2_PLACEMENT_3D ( 'NONE', #244435, #246998, #204023 ) ;
#161050=CARTESIAN_POINT ( 'NONE',  ( -20.85000000000000142, 64.25000000001148237, -42.86470817442146597 ) ) ;
#161057=ORIENTED_EDGE ( 'NONE', *, *, #128741, .F. ) ;
#161070=EDGE_CURVE ( 'NONE', #43988, #257957, #93878, .T. ) ;
#161130=VERTEX_POINT ( 'NONE', #157761 ) ;
#161184=VECTOR ( 'NONE', #98034, 1000.000000000000000 ) ;
#161209=FACE_OUTER_BOUND ( 'NONE', #34135, .T. ) ;
#161295=CARTESIAN_POINT ( 'NONE',  ( 20.50589344625198507, 65.51681206853606909, -61.95011250585200457 ) ) ;
#161299=CARTESIAN_POINT ( 'NONE',  ( -20.94999999999999929, 76.00000000001142553, -36.02310748452432421 ) ) ;
#161317=DIRECTION ( 'NONE',  ( 0.000000000000000000, 0.000000000000000000, 1.000000000000000000 ) ) ;
#161325=CARTESIAN_POINT ( 'NONE',  ( 23.24999999999999289, 64.35000000001146248, -43.03791325517834565 ) ) ;
#161356=FACE_OUTER_BOUND ( 'NONE', #152177, .T. ) ;
#161358=FACE_OUTER_BOUND ( 'NONE', #120801, .T. ) ;
#161377=FACE_OUTER_BOUND ( 'NONE', #70394, .T. ) ;
#161386=TOROIDAL_SURFACE ( 'NONE', #228017, 0.2000000000000000111, 0.1000000000000000056 ) ;
#161409=ORIENTED_EDGE ( 'NONE', *, *, #65173, .F. ) ;
#161421=EDGE_LOOP ( 'NONE', ( #79303, #179412, #158206, #121932, #85351, #97932, #236373 ) ) ;
#161423=AXIS2_PLACEMENT_3D ( 'NONE', #79940, #160828, #116546 ) ;
#161431=FACE_OUTER_BOUND ( 'NONE', #72034, .T. ) ;
#161444=ORIENTED_EDGE ( 'NONE', *, *, #127357, .T. ) ;
#161467=EDGE_CURVE ( 'NONE', #121900, #26458, #158066, .T. ) ;
#161469=CIRCLE ( 'NONE', #144870, 11.74999999999999645 ) ;
#161485=EDGE_CURVE ( 'NONE', #188354, #58504, #120449, .T. ) ;
#161494=CIRCLE ( 'NONE', #232422, 2.000000000000001776 ) ;
#161504=CARTESIAN_POINT ( 'NONE',  ( -23.15000000000000213, 76.00000000001141132, -33.92310748452431568 ) ) ;
#161516=VERTEX_POINT ( 'NONE', #81351 ) ;
#161522=ORIENTED_EDGE ( 'NONE', *, *, #142996, .T. ) ;
#161558=FACE_OUTER_BOUND ( 'NONE', #17320, .T. ) ;
#161568=ADVANCED_FACE ( 'NONE', ( #65667 ), #4406, .T. ) ;
#161575=DIRECTION ( 'NONE',  ( 0.000000000000000000, 0.000000000000000000, 1.000000000000000000 ) ) ;
#161578=DIRECTION ( 'NONE',  ( 0.000000000000000000, 0.000000000000000000, -1.000000000000000000 ) ) ;
#161604=DIRECTION ( 'NONE',  ( -1.000000000000000000, 0.000000000000000000, -0.000000000000000000 ) ) ;
#161621=ADVANCED_FACE ( 'NONE', ( #62516 ), #90790, .T. ) ;
#161632=DIRECTION ( 'NONE',  ( 1.000000000000000000, -0.000000000000000000, 0.000000000000000000 ) ) ;
#161642=CIRCLE ( 'NONE', #36754, 0.5000000000000004441 ) ;
#161660=ORIENTED_EDGE ( 'NONE', *, *, #4860, .F. ) ;
#161667=ORIENTED_EDGE ( 'NONE', *, *, #219186, .F. ) ;
#161668=ADVANCED_FACE ( 'NONE', ( #221553 ), #61760, .F. ) ;
#161675=CARTESIAN_POINT ( 'NONE',  ( -22.47007471830798409, 68.27928934808515749, -69.52310748452437394 ) ) ;
#161711=ORIENTED_EDGE ( 'NONE', *, *, #192029, .F. ) ;
#161714=FACE_OUTER_BOUND ( 'NONE', #223635, .T. ) ;
#161736=EDGE_LOOP ( 'NONE', ( #248935, #166888, #172718, #175151 ) ) ;
#161762=AXIS2_PLACEMENT_3D ( 'NONE', #92974, #152995, #12188 ) ;
#161786=AXIS2_PLACEMENT_3D ( 'NONE', #86246, #121590, #203657 ) ;
#161797=ORIENTED_EDGE ( 'NONE', *, *, #221640, .T. ) ;
#161812=ORIENTED_EDGE ( 'NONE', *, *, #204222, .F. ) ;
#161837=VERTEX_POINT ( 'NONE', #230581 ) ;
#161849=CIRCLE ( 'NONE', #232585, 0.1000000000000052097 ) ;
#161850=AXIS2_PLACEMENT_3D ( 'NONE', #207761, #190778, #108637 ) ;
#161866=ORIENTED_EDGE ( 'NONE', *, *, #31208, .F. ) ;
#161875=LINE ( 'NONE', #43195, #255431 ) ;
#161907=CARTESIAN_POINT ( 'NONE',  ( -18.50000324121759121, 65.70692517833182933, -30.56446533783035946 ) ) ;
#161944=CIRCLE ( 'NONE', #241046, 0.9750000000000036415 ) ;
#161954=CARTESIAN_POINT ( 'NONE',  ( 23.14999999999999503, 64.35000000001150511, -48.17310748452440095 ) ) ;
#161959=EDGE_CURVE ( 'NONE', #60391, #180491, #34979, .T. ) ;
#161967=ORIENTED_EDGE ( 'NONE', *, *, #224347, .T. ) ;
#161976=SPHERICAL_SURFACE ( 'NONE', #51350, 0.1000000000000000056 ) ;
#161996=AXIS2_PLACEMENT_3D ( 'NONE', #55244, #250897, #210506 ) ;
#162003=CARTESIAN_POINT ( 'NONE',  ( -23.25000000000000000, 74.00000000001151079, -49.24772940728643533 ) ) ;
#162025=DIRECTION ( 'NONE',  ( 1.000000000000000000, -3.265361837132813093E-16, -2.280189983783949500E-30 ) ) ;
#162036=VERTEX_POINT ( 'NONE', #236993 ) ;
#162037=CARTESIAN_POINT ( 'NONE',  ( -21.05000000000000071, 74.75000000001159606, -61.52310748452433131 ) ) ;
#162057=EDGE_CURVE ( 'NONE', #94760, #20464, #199330, .T. ) ;
#162063=AXIS2_PLACEMENT_3D ( 'NONE', #131030, #19780, #120187 ) ;
#162075=EDGE_LOOP ( 'NONE', ( #151201, #86326, #34210, #85164 ) ) ;
#162078=VERTEX_POINT ( 'NONE', #81721 ) ;
#162083=ORIENTED_EDGE ( 'NONE', *, *, #226601, .F. ) ;
#162089=ORIENTED_EDGE ( 'NONE', *, *, #64093, .T. ) ;
#162107=CARTESIAN_POINT ( 'NONE',  ( -21.05000000000000071, 76.00000000001145395, -40.02310748452431710 ) ) ;
#162122=ADVANCED_FACE ( 'NONE', ( #72486 ), #52896, .F. ) ;
#162198=CARTESIAN_POINT ( 'NONE',  ( 21.00000000000000000, 66.25000000001158185, -57.17310748452438673 ) ) ;
#162204=CARTESIAN_POINT ( 'NONE',  ( -23.25000000000000000, 76.00000000001142553, -36.02310748452432421 ) ) ;
#162213=AXIS2_PLACEMENT_3D ( 'NONE', #227549, #188420, #248404 ) ;
#162228=CARTESIAN_POINT ( 'NONE',  ( -22.47007471830798409, 76.00000000001170974, -77.24381813645081252 ) ) ;
#162234=DIRECTION ( 'NONE',  ( 0.000000000000000000, 1.000000000000000000, 6.982962677686266711E-15 ) ) ;
#162257=CARTESIAN_POINT ( 'NONE',  ( -21.08035267497491816, 75.91731137523568407, -75.85481432430736959 ) ) ;
#162261=CARTESIAN_POINT ( 'NONE',  ( 21.05995757104869526, 67.22461075529028562, -57.32820236153317950 ) ) ;
#162271=CIRCLE ( 'NONE', #87409, 0.1000000000000028644 ) ;
#162296=CARTESIAN_POINT ( 'NONE',  ( -20.64999999999999858, 68.85000000001151932, -48.27310748452437394 ) ) ;
#162297=DIRECTION ( 'NONE',  ( 1.000000000000000000, 0.000000000000000000, 0.000000000000000000 ) ) ;
#162303=ORIENTED_EDGE ( 'NONE', *, *, #69070, .F. ) ;
#162308=CARTESIAN_POINT ( 'NONE',  ( -20.64999999999999858, 76.00000000001165290, -69.52310748452431710 ) ) ;
#162309=FACE_OUTER_BOUND ( 'NONE', #181566, .T. ) ;
#162329=CIRCLE ( 'NONE', #183174, 11.74999999999999645 ) ;
#162347=ORIENTED_EDGE ( 'NONE', *, *, #67249, .T. ) ;
#162357=CARTESIAN_POINT ( 'NONE',  ( -18.50000000000000000, 77.83585931145498193, -24.51866831572578320 ) ) ;
#162359=ORIENTED_EDGE ( 'NONE', *, *, #73351, .F. ) ;
#162371=EDGE_CURVE ( 'NONE', #256858, #191840, #178699, .T. ) ;
#162381=ORIENTED_EDGE ( 'NONE', *, *, #184894, .T. ) ;
#162448=DIRECTION ( 'NONE',  ( 0.000000000000000000, 0.8700118002898357128, -0.4930308989875170633 ) ) ;
#162453=ORIENTED_EDGE ( 'NONE', *, *, #199231, .F. ) ;
#162492=DIRECTION ( 'NONE',  ( 0.000000000000000000, 0.000000000000000000, 1.000000000000000000 ) ) ;
#162502=AXIS2_PLACEMENT_3D ( 'NONE', #72108, #51211, #108650 ) ;
#162503=DIRECTION ( 'NONE',  ( 0.000000000000000000, -0.9908441862701605762, 0.1350103645451835310 ) ) ;
#162505=CYLINDRICAL_SURFACE ( 'NONE', #148486, 0.1000000000000028644 ) ;
#162515=EDGE_CURVE ( 'NONE', #100678, #115794, #250472, .T. ) ;
#162516=AXIS2_PLACEMENT_3D ( 'NONE', #54749, #155182, #203251 ) ;
#162535=CARTESIAN_POINT ( 'NONE',  ( -21.09610168723073542, 69.62104428478687623, -69.55669699141586193 ) ) ;
#162583=DIRECTION ( 'NONE',  ( 1.000000000000000000, 0.000000000000000000, 0.000000000000000000 ) ) ;
#162589=LINE ( 'NONE', #66031, #117621 ) ;
#162609=CARTESIAN_POINT ( 'NONE',  ( -21.05000000000000071, 69.45934304831041572, -69.42310748452437963 ) ) ;
#162648=ORIENTED_EDGE ( 'NONE', *, *, #93735, .T. ) ;
#162657=DIRECTION ( 'NONE',  ( 0.000000000000000000, -6.938893903907234689E-15, 1.000000000000000000 ) ) ;
#162667=VECTOR ( 'NONE', #28289, 1000.000000000000000 ) ;
#162671=CARTESIAN_POINT ( 'NONE',  ( 18.53691006697101784, 65.69784844286101588, -44.82090876722582351 ) ) ;
#162676=VECTOR ( 'NONE', #77939, 1000.000000000000000 ) ;
#162680=LINE ( 'NONE', #244758, #125779 ) ;
#162700=FACE_OUTER_BOUND ( 'NONE', #177737, .T. ) ;
#162794=DIRECTION ( 'NONE',  ( 1.000000000000000000, 0.000000000000000000, 0.000000000000000000 ) ) ;
#162831=( BOUNDED_SURFACE ( )  B_SPLINE_SURFACE ( 3, 2, ( 
 ( #230060, #227476, #147956 ),
 ( #247035, #192234, #48846 ),
 ( #51383, #128394, #210502 ),
 ( #89250, #108815, #130960 ),
 ( #31889, #73587, #111402 ),
 ( #91833, #168848, #12321 ) ),
 .UNSPECIFIED., .F., .F., .F. ) 
 B_SPLINE_SURFACE_WITH_KNOTS ( ( 4, 2, 4 ),
 ( 3, 3 ),
 ( 0.0001342700090130013102, 0.0002909192928057331620, 0.0004475685765984649595 ),
 ( 0.000000000000000000, 1.000000000000000000 ),
 .UNSPECIFIED. ) 
 GEOMETRIC_REPRESENTATION_ITEM ( )  RATIONAL_B_SPLINE_SURFACE ( (
 ( 1.000000000000000000, 0.7250110520819876836, 1.000000000000000000),
 ( 1.000000000000000000, 0.7257599279134849812, 1.000000000000000000),
 ( 1.000000000000000000, 0.7137594617283078424, 1.000000000000000000),
 ( 1.000000000000000000, 0.6959270178811023388, 1.000000000000000000),
 ( 1.000000000000000000, 0.6919879549338179281, 1.000000000000000000),
 ( 1.000000000000000000, 0.7071067811865494601, 1.000000000000000000) ) ) 
 REPRESENTATION_ITEM ( '' )  SURFACE ( )  );
#162882=EDGE_CURVE ( 'NONE', #142859, #127785, #88500, .T. ) ;
#162885=FACE_OUTER_BOUND ( 'NONE', #106337, .T. ) ;
#162898=CIRCLE ( 'NONE', #53955, 0.09999999999999939493 ) ;
#162902=VERTEX_POINT ( 'NONE', #24741 ) ;
#162919=AXIS2_PLACEMENT_3D ( 'NONE', #140564, #41498, #57162 ) ;
#162950=CARTESIAN_POINT ( 'NONE',  ( 18.37172112093850274, 85.57096165225516415, -29.20637303104079407 ) ) ;
#162958=CARTESIAN_POINT ( 'NONE',  ( 21.14999999999999858, 76.00000000001156764, -57.37310748452432563 ) ) ;
#162991=ORIENTED_EDGE ( 'NONE', *, *, #253635, .T. ) ;
#163004=CARTESIAN_POINT ( 'NONE',  ( 18.43473516226059417, 85.49494228276991237, -62.47720880117490339 ) ) ;
#163060=DIRECTION ( 'NONE',  ( 0.000000000000000000, 0.000000000000000000, -1.000000000000000000 ) ) ;
#163087=DIRECTION ( 'NONE',  ( -0.000000000000000000, 0.4791956752371485107, 0.8777080977375185666 ) ) ;
#163090=ORIENTED_EDGE ( 'NONE', *, *, #61961, .T. ) ;
#163103=ORIENTED_EDGE ( 'NONE', *, *, #250849, .T. ) ;
#163129=ADVANCED_FACE ( 'NONE', ( #175788 ), #217435, .T. ) ;
#163133=CIRCLE ( 'NONE', #88059, 0.1999999999999987899 ) ;
#163157=DIRECTION ( 'NONE',  ( -1.000000000000000000, 1.836970198721029934E-16, 1.282749433769087757E-30 ) ) ;
#163182=ORIENTED_EDGE ( 'NONE', *, *, #9299, .F. ) ;
#163188=DIRECTION ( 'NONE',  ( 1.000000000000000000, 0.000000000000000000, -0.000000000000000000 ) ) ;
#163193=AXIS2_PLACEMENT_3D ( 'NONE', #61385, #178808, #197027 ) ;
#163213=AXIS2_PLACEMENT_3D ( 'NONE', #4393, #124366, #46088 ) ;
#163283=DIRECTION ( 'NONE',  ( 0.000000000000000000, -6.454785026890510900E-15, 1.000000000000000000 ) ) ;
#163297=DIRECTION ( 'NONE',  ( -2.827886303505249259E-16, -0.8660254037844378194, -0.5000000000000016653 ) ) ;
#163313=CARTESIAN_POINT ( 'NONE',  ( 21.04999999999999716, 67.12872031401592210, -57.37310748452439668 ) ) ;
#163321=ORIENTED_EDGE ( 'NONE', *, *, #96920, .T. ) ;
#163336=CYLINDRICAL_SURFACE ( 'NONE', #120129, 0.1000000000000028644 ) ;
#163351=CIRCLE ( 'NONE', #117551, 0.09999999999999939493 ) ;
#163377=DIRECTION ( 'NONE',  ( 0.000000000000000000, -1.000000000000000000, -6.982962677686266711E-15 ) ) ;
#163400=VECTOR ( 'NONE', #170262, 1000.000000000000000 ) ;
#163422=AXIS2_PLACEMENT_3D ( 'NONE', #44291, #84641, #24747 ) ;
#163423=EDGE_LOOP ( 'NONE', ( #193347, #113401, #117518, #91902, #235881, #145475, #50082, #92866, #152807, #214148, #11401 ) ) ;
#163449=DIRECTION ( 'NONE',  ( 2.557131231893037478E-16, 0.8660254037844420383, -0.4999999999999942824 ) ) ;
#163452=DIRECTION ( 'NONE',  ( 0.000000000000000000, -7.147358527629762208E-15, 1.000000000000000000 ) ) ;
#163485=CARTESIAN_POINT ( 'NONE',  ( 20.94999999999999574, 65.52661458509869874, -61.94445302027585143 ) ) ;
#163488=CARTESIAN_POINT ( 'NONE',  ( -22.39999999999999503, 76.00000000001170974, -77.31388708289772183 ) ) ;
#163497=CYLINDRICAL_SURFACE ( 'NONE', #148113, 0.09999999999999939493 ) ;
#163524=CARTESIAN_POINT ( 'NONE',  ( 21.05543885634738643, 67.22422895316402958, -57.33872301380969816 ) ) ;
#163580=CIRCLE ( 'NONE', #51109, 0.1000000000000028644 ) ;
#163604=FACE_OUTER_BOUND ( 'NONE', #61894, .T. ) ;
#163615=DIRECTION ( 'NONE',  ( 0.000000000000000000, -0.8660254037844420383, 0.4999999999999942824 ) ) ;
#163633=CARTESIAN_POINT ( 'NONE',  ( 23.14999999999999503, 69.35000000001151932, -48.37310748452436826 ) ) ;
#163634=EDGE_CURVE ( 'NONE', #88477, #71888, #158395, .T. ) ;
#163672=AXIS2_PLACEMENT_3D ( 'NONE', #172123, #157698, #237194 ) ;
#163678=CIRCLE ( 'NONE', #105380, 7.900000000000000355 ) ;
#163697=AXIS2_PLACEMENT_3D ( 'NONE', #77925, #192765, #175778 ) ;
#163702=SPHERICAL_SURFACE ( 'NONE', #206094, 0.1000000000000000056 ) ;
#163710=ORIENTED_EDGE ( 'NONE', *, *, #224874, .F. ) ;
#163715=CARTESIAN_POINT ( 'NONE',  ( -21.05000000000000071, 77.83534155023598089, -57.96795619196132776 ) ) ;
#163739=DIRECTION ( 'NONE',  ( 0.000000000000000000, -0.8660254037844377084, -0.5000000000000016653 ) ) ;
#163787=EDGE_LOOP ( 'NONE', ( #121099, #108826, #5273, #25722 ) ) ;
#163788=CIRCLE ( 'NONE', #217925, 0.09999999999999939493 ) ;
#163837=DIRECTION ( 'NONE',  ( 0.000000000000000000, -6.982962677686266711E-15, 1.000000000000000000 ) ) ;
#163849=EDGE_CURVE ( 'NONE', #21530, #101771, #19955, .T. ) ;
#163900=CARTESIAN_POINT ( 'NONE',  ( 20.87155475150661132, 64.25000000001146816, -42.92752095536695833 ) ) ;
#163908=CIRCLE ( 'NONE', #168055, 0.1000000000000028644 ) ;
#163943=EDGE_CURVE ( 'NONE', #173457, #145606, #125418, .T. ) ;
#164040=ORIENTED_EDGE ( 'NONE', *, *, #39894, .F. ) ;
#164050=ORIENTED_EDGE ( 'NONE', *, *, #170791, .F. ) ;
#164059=ORIENTED_EDGE ( 'NONE', *, *, #53258, .F. ) ;
#164100=CARTESIAN_POINT ( 'NONE',  ( 18.49999999999999645, 77.86671491006887891, -57.77043223824230722 ) ) ;
#164124=AXIS2_PLACEMENT_3D ( 'NONE', #73988, #34854, #93507 ) ;
#164147=VECTOR ( 'NONE', #35426, 1000.000000000000114 ) ;
#164173=ORIENTED_EDGE ( 'NONE', *, *, #65339, .F. ) ;
#164184=LINE ( 'NONE', #200733, #203666 ) ;
#164207=CARTESIAN_POINT ( 'NONE',  ( -20.64999999999999858, 84.73084112150691283, -59.92503276553993175 ) ) ;
#164225=CARTESIAN_POINT ( 'NONE',  ( 18.60000000000000142, 85.48068669529034480, -29.08199231576639576 ) ) ;
#164228=ORIENTED_EDGE ( 'NONE', *, *, #77146, .T. ) ;
#164240=FACE_OUTER_BOUND ( 'NONE', #249322, .T. ) ;
#164266=EDGE_CURVE ( 'NONE', #117589, #58504, #8730, .T. ) ;
#164280=CARTESIAN_POINT ( 'NONE',  ( 18.47073956224755165, 85.47172941248341260, -62.41442173170622709 ) ) ;
#164302=ORIENTED_EDGE ( 'NONE', *, *, #80473, .T. ) ;
#164303=AXIS2_PLACEMENT_3D ( 'NONE', #214723, #36109, #33575 ) ;
#164315=DIRECTION ( 'NONE',  ( 0.000000000000000000, 0.000000000000000000, -1.000000000000000000 ) ) ;
#164365=LINE ( 'NONE', #243882, #206986 ) ;
#164377=CARTESIAN_POINT ( 'NONE',  ( 20.94999999999999929, 76.00000000001142553, -36.02310748452432421 ) ) ;
#164384=ORIENTED_EDGE ( 'NONE', *, *, #243724, .T. ) ;
#164394=DIRECTION ( 'NONE',  ( -1.000000000000000000, -0.000000000000000000, -0.000000000000000000 ) ) ;
#164397=CARTESIAN_POINT ( 'NONE',  ( -23.15000000000000213, 85.00000000001159606, -59.62913836187181715 ) ) ;
#164406=AXIS2_PLACEMENT_3D ( 'NONE', #67161, #87977, #244505 ) ;
#164448=DIRECTION ( 'NONE',  ( 1.000000000000000000, 0.000000000000000000, 0.000000000000000000 ) ) ;
#164456=CIRCLE ( 'NONE', #152007, 11.74999999999999645 ) ;
#164483=DIRECTION ( 'NONE',  ( 0.000000000000000000, -6.982962677686266711E-15, 1.000000000000000000 ) ) ;
#164499=CARTESIAN_POINT ( 'NONE',  ( 22.40000000000020819, 76.10085836911140689, -81.27267460801402876 ) ) ;
#164561=ORIENTED_EDGE ( 'NONE', *, *, #219762, .T. ) ;
#164563=CARTESIAN_POINT ( 'NONE',  ( -21.05000000000000071, 76.00000000001165290, -69.52310748452431710 ) ) ;
#164583=FACE_OUTER_BOUND ( 'NONE', #181699, .T. ) ;
#164612=DIRECTION ( 'NONE',  ( 0.000000000000000000, -1.000000000000000000, 0.000000000000000000 ) ) ;
#164633=ADVANCED_FACE ( 'NONE', ( #141503 ), #47522, .F. ) ;
#164636=CIRCLE ( 'NONE', #218586, 0.1000000000000028644 ) ;
#164637=CARTESIAN_POINT ( 'NONE',  ( 18.59999999999999787, 87.75000000001149658, -48.17310748452423752 ) ) ;
#164640=VECTOR ( 'NONE', #197632, 999.9999999999998863 ) ;
#164648=CIRCLE ( 'NONE', #44017, 1.900000000000005906 ) ;
#164667=ORIENTED_EDGE ( 'NONE', *, *, #29050, .T. ) ;
#164674=EDGE_LOOP ( 'NONE', ( #149744, #186196, #109111, #54940 ) ) ;
#164679=ORIENTED_EDGE ( 'NONE', *, *, #33333, .F. ) ;
#164683=DIRECTION ( 'NONE',  ( -1.000000000000000000, 0.000000000000000000, 0.000000000000000000 ) ) ;
#164744=DIRECTION ( 'NONE',  ( 1.000000000000000000, 0.000000000000000000, 0.000000000000000000 ) ) ;
#164747=AXIS2_PLACEMENT_3D ( 'NONE', #108212, #31277, #33852 ) ;
#164752=CARTESIAN_POINT ( 'NONE',  ( 18.49999999999999645, 70.30054753569015702, -82.06538144109418909 ) ) ;
#164780=AXIS2_PLACEMENT_3D ( 'NONE', #3005, #90243, #91553 ) ;
#164783=CARTESIAN_POINT ( 'NONE',  ( 21.53752568622133623, 75.90102553874103819, -76.30991535907283208 ) ) ;
#164788=DIRECTION ( 'NONE',  ( -1.000000000000000000, 0.000000000000000000, -0.000000000000000000 ) ) ;
#164796=ORIENTED_EDGE ( 'NONE', *, *, #5191, .T. ) ;
#164822=ORIENTED_EDGE ( 'NONE', *, *, #113093, .T. ) ;
#164824=AXIS2_PLACEMENT_3D ( 'NONE', #105541, #62612, #3916 ) ;
#164832=EDGE_LOOP ( 'NONE', ( #73813, #124372, #90588, #160837 ) ) ;
#164839=DIRECTION ( 'NONE',  ( 1.000000000000000000, -3.265361837132813093E-16, -2.280189983783949500E-30 ) ) ;
#164888=FACE_OUTER_BOUND ( 'NONE', #142482, .T. ) ;
#164905=TOROIDAL_SURFACE ( 'NONE', #44095, 0.2000000000000000111, 0.1000000000000000056 ) ;
#164921=ADVANCED_FACE ( 'NONE', ( #225711 ), #113356, .T. ) ;
#164948=CARTESIAN_POINT ( 'NONE',  ( 21.05000000000000071, 76.00000000001142553, -36.02310748452432421 ) ) ;
#164959=TOROIDAL_SURFACE ( 'NONE', #110788, 0.2000000000000000111, 0.1000000000000000056 ) ;
#164980=EDGE_CURVE ( 'NONE', #220391, #44347, #46634, .T. ) ;
#165019=VERTEX_POINT ( 'NONE', #211319 ) ;
#165020=EDGE_CURVE ( 'NONE', #76430, #206635, #152656, .T. ) ;
#165032=DIRECTION ( 'NONE',  ( 0.000000000000000000, 0.000000000000000000, 1.000000000000000000 ) ) ;
#165048=EDGE_CURVE ( 'NONE', #102370, #207654, #252998, .T. ) ;
#165050=DIRECTION ( 'NONE',  ( 0.000000000000000000, -1.000000000000000000, 0.000000000000000000 ) ) ;
#165062=ORIENTED_EDGE ( 'NONE', *, *, #128820, .F. ) ;
#165080=CARTESIAN_POINT ( 'NONE',  ( 19.99999999738052381, 64.25000000001148237, -44.83593553489200900 ) ) ;
#165082=ORIENTED_EDGE ( 'NONE', *, *, #22894, .T. ) ;
#165112=CARTESIAN_POINT ( 'NONE',  ( 22.50000000000000000, 68.25000000001165290, -69.62310748452438247 ) ) ;
#165141=CIRCLE ( 'NONE', #73584, 0.1000000000000028644 ) ;
#165150=AXIS2_PLACEMENT_3D ( 'NONE', #245664, #108722, #68318 ) ;
#165163=AXIS2_PLACEMENT_3D ( 'NONE', #234247, #162448, #146685 ) ;
#165167=ORIENTED_EDGE ( 'NONE', *, *, #219033, .T. ) ;
#165169=PLANE ( 'NONE',  #204331 ) ;
#165183=VERTEX_POINT ( 'NONE', #20842 ) ;
#165192=FACE_OUTER_BOUND ( 'NONE', #28370, .T. ) ;
#165201=ORIENTED_EDGE ( 'NONE', *, *, #1666, .F. ) ;
#165264=DIRECTION ( 'NONE',  ( -0.000000000000000000, 1.000000000000000000, 7.272083257015735086E-15 ) ) ;
#165288=AXIS2_PLACEMENT_3D ( 'NONE', #35155, #212482, #52089 ) ;
#165325=ORIENTED_EDGE ( 'NONE', *, *, #103152, .T. ) ;
#165340=DIRECTION ( 'NONE',  ( 0.000000000000000000, 0.000000000000000000, 1.000000000000000000 ) ) ;
#165355=DIRECTION ( 'NONE',  ( -1.000000000000000000, 7.304098846218163263E-16, -4.217023435051627211E-16 ) ) ;
#165392=CARTESIAN_POINT ( 'NONE',  ( 18.59999999999999787, 76.00000000001165290, -69.52310748452431710 ) ) ;
#165402=EDGE_CURVE ( 'NONE', #94150, #161837, #146595, .T. ) ;
#165412=CARTESIAN_POINT ( 'NONE',  ( 18.59999999999999787, 77.83534155023598089, -57.96795619196132776 ) ) ;
#165413=CARTESIAN_POINT ( 'NONE',  ( 23.24999999999999289, 69.55000000001150795, -48.37310748452436826 ) ) ;
#165435=SPHERICAL_SURFACE ( 'NONE', #157936, 0.1000000000000000056 ) ;
#165442=DIRECTION ( 'NONE',  ( 1.000000000000000000, 0.000000000000000000, 0.000000000000000000 ) ) ;
#165484=DIRECTION ( 'NONE',  ( 0.000000000000000000, -6.938893903907234689E-15, 1.000000000000000000 ) ) ;
#165491=CARTESIAN_POINT ( 'NONE',  ( -18.59999999999999787, 77.25000000001159606, -61.52310748452431710 ) ) ;
#165526=ORIENTED_EDGE ( 'NONE', *, *, #77941, .T. ) ;
#165545=ORIENTED_EDGE ( 'NONE', *, *, #228281, .F. ) ;
#165627=AXIS2_PLACEMENT_3D ( 'NONE', #87199, #23426, #166791 ) ;
#165649=ORIENTED_EDGE ( 'NONE', *, *, #99994, .F. ) ;
#165665=CARTESIAN_POINT ( 'NONE',  ( 20.94999999999999929, 76.00000000001165290, -69.52310748452431710 ) ) ;
#165690=VERTEX_POINT ( 'NONE', #98878 ) ;
#165696=DIRECTION ( 'NONE',  ( 0.000000000000000000, -0.1575844902526579161, -0.9875055080513779338 ) ) ;
#165699=DIRECTION ( 'NONE',  ( -1.000000000000000000, 0.000000000000000000, 0.000000000000000000 ) ) ;
#165731=CARTESIAN_POINT ( 'NONE',  ( -23.25000000000000000, 76.00000000001168132, -73.57310748452432847 ) ) ;
#165736=CARTESIAN_POINT ( 'NONE',  ( 20.94999999999999574, 77.36087058720364951, -61.45010955743335046 ) ) ;
#165805=FACE_OUTER_BOUND ( 'NONE', #62593, .T. ) ;
#165812=VERTEX_POINT ( 'NONE', #50156 ) ;
#165826=CARTESIAN_POINT ( 'NONE',  ( 21.14999999999999858, 64.35000000001164722, -69.42310748452440805 ) ) ;
#165845=VERTEX_POINT ( 'NONE', #89286 ) ;
#165873=DIRECTION ( 'NONE',  ( 0.000000000000000000, 0.5000000000000209832, -0.8660254037844264952 ) ) ;
#165876=AXIS2_PLACEMENT_3D ( 'NONE', #83664, #22476, #100667 ) ;
#165888=FACE_OUTER_BOUND ( 'NONE', #40064, .T. ) ;
#165889=FACE_OUTER_BOUND ( 'NONE', #200398, .T. ) ;
#165909=AXIS2_PLACEMENT_3D ( 'NONE', #222920, #183805, #63860 ) ;
#165940=CIRCLE ( 'NONE', #161850, 0.09999999999999520384 ) ;
#165948=VECTOR ( 'NONE', #240351, 1000.000000000000000 ) ;
#165974=EDGE_LOOP ( 'NONE', ( #156923, #2994, #240528, #120427, #239283 ) ) ;
#166030=CARTESIAN_POINT ( 'NONE',  ( 20.95595624212443653, 65.37610879691743548, -61.89347457039733769 ) ) ;
#166033=ORIENTED_EDGE ( 'NONE', *, *, #143188, .T. ) ;
#166035=CYLINDRICAL_SURFACE ( 'NONE', #223424, 0.09999999999999939493 ) ;
#166036=CARTESIAN_POINT ( 'NONE',  ( 18.49999999999999645, 76.00000000001142553, -36.02310748452432421 ) ) ;
#166050=CARTESIAN_POINT ( 'NONE',  ( -20.94999999999999929, 87.65000000001144542, -39.12310748452424747 ) ) ;
#166067=ORIENTED_EDGE ( 'NONE', *, *, #197138, .F. ) ;
#166087=CARTESIAN_POINT ( 'NONE',  ( 20.95566103547454517, 65.38175234906454136, -61.89126729154380513 ) ) ;
#166096=CARTESIAN_POINT ( 'NONE',  ( 21.53699400384725493, 76.00000000001170974, -76.31081927776408236 ) ) ;
#166112=EDGE_CURVE ( 'NONE', #144573, #93396, #180311, .T. ) ;
#166123=CARTESIAN_POINT ( 'NONE',  ( 23.15000000000000213, 87.65000000001144542, -39.12310748452424747 ) ) ;
#166183=CIRCLE ( 'NONE', #170285, 4.049999999999998046 ) ;
#166196=ORIENTED_EDGE ( 'NONE', *, *, #254682, .T. ) ;
#166199=EDGE_CURVE ( 'NONE', #112286, #47002, #122035, .T. ) ;
#166203=CARTESIAN_POINT ( 'NONE',  ( 20.85000000000000142, 77.83585931145498193, -24.51866831572578675 ) ) ;
#166209=ORIENTED_EDGE ( 'NONE', *, *, #22894, .F. ) ;
#166230=FACE_BOUND ( 'NONE', #9328, .T. ) ;
#166231=CARTESIAN_POINT ( 'NONE',  ( -22.39999999999999858, 75.90000000001170122, -77.31388708289772183 ) ) ;
#166240=LINE ( 'NONE', #116511, #177632 ) ;
#166246=DIRECTION ( 'NONE',  ( 0.000000000000000000, 0.000000000000000000, 1.000000000000000000 ) ) ;
#166248=DIRECTION ( 'NONE',  ( 0.000000000000000000, -0.9908441862701605762, 0.1350103645451835310 ) ) ;
#166256=AXIS2_PLACEMENT_3D ( 'NONE', #199397, #157732, #178559 ) ;
#166260=ORIENTED_EDGE ( 'NONE', *, *, #8409, .F. ) ;
#166277=ORIENTED_EDGE ( 'NONE', *, *, #65009, .T. ) ;
#166279=AXIS2_PLACEMENT_3D ( 'NONE', #79481, #234727, #56059 ) ;
#166280=EDGE_LOOP ( 'NONE', ( #159624, #21128, #224561, #28129 ) ) ;
#166328=EDGE_CURVE ( 'NONE', #56261, #161130, #109740, .T. ) ;
#166333=CIRCLE ( 'NONE', #253764, 0.5000000000000004441 ) ;
#166341=CARTESIAN_POINT ( 'NONE',  ( 21.08804582317324972, 67.12183383291966265, -57.17310765511903270 ) ) ;
#166344=ORIENTED_EDGE ( 'NONE', *, *, #185360, .F. ) ;
#166385=DIRECTION ( 'NONE',  ( -1.000000000000000000, -0.000000000000000000, -0.000000000000000000 ) ) ;
#166386=PLANE ( 'NONE',  #155041 ) ;
#166417=DIRECTION ( 'NONE',  ( -1.000000000000000000, 2.952720810173289112E-16, 2.061873921506763405E-30 ) ) ;
#166430=CARTESIAN_POINT ( 'NONE',  ( 21.00000000000000000, 66.25000000001151079, -48.37310748452438958 ) ) ;
#166455=CIRCLE ( 'NONE', #145560, 0.1000000000000009492 ) ;
#166481=EDGE_CURVE ( 'NONE', #36208, #118151, #175849, .T. ) ;
#166511=CARTESIAN_POINT ( 'NONE',  ( -23.15000000000000213, 87.48912529308749697, -39.12310748452424747 ) ) ;
#166525=DIRECTION ( 'NONE',  ( 0.000000000000000000, -1.000000000000000000, 0.000000000000000000 ) ) ;
#166560=ORIENTED_EDGE ( 'NONE', *, *, #201590, .T. ) ;
#166582=ADVANCED_FACE ( 'NONE', ( #105658, #189078 ), #207369, .T. ) ;
#166607=EDGE_CURVE ( 'NONE', #189305, #218866, #188467, .T. ) ;
#166639=DIRECTION ( 'NONE',  ( 1.000000000000000000, -2.952720810173289112E-16, -2.061873921506763405E-30 ) ) ;
#166676=DIRECTION ( 'NONE',  ( 0.000000000000000000, -0.008583690987162452199, 0.9999631594459053030 ) ) ;
#166683=VECTOR ( 'NONE', #30969, 1000.000000000000114 ) ;
#166704=ORIENTED_EDGE ( 'NONE', *, *, #64894, .F. ) ;
#166714=ORIENTED_EDGE ( 'NONE', *, *, #73878, .T. ) ;
#166751=DIRECTION ( 'NONE',  ( 0.000000000000000000, -6.938893903907222067E-15, 1.000000000000000000 ) ) ;
#166755=DIRECTION ( 'NONE',  ( 1.000000000000000000, 0.000000000000000000, 0.000000000000000000 ) ) ;
#166777=ORIENTED_EDGE ( 'NONE', *, *, #35868, .F. ) ;
#166790=CARTESIAN_POINT ( 'NONE',  ( -18.59999999999999787, 64.35000000001150511, -48.17310748452440095 ) ) ;
#166791=DIRECTION ( 'NONE',  ( 0.000000000000000000, 0.000000000000000000, -1.000000000000000000 ) ) ;
#166840=CARTESIAN_POINT ( 'NONE',  ( -20.64999999999999858, 74.00000000001151079, -49.24772940728643533 ) ) ;
#166859=CARTESIAN_POINT ( 'NONE',  ( 20.94999999999999929, 65.61821452928744236, -30.51526212064022303 ) ) ;
#166862=TOROIDAL_SURFACE ( 'NONE', #88246, 0.4000000000000012990, 0.1000000000000000056 ) ;
#166877=DIRECTION ( 'NONE',  ( 0.000000000000000000, -6.982962677686267499E-15, 1.000000000000000000 ) ) ;
#166888=ORIENTED_EDGE ( 'NONE', *, *, #180062, .T. ) ;
#166911=EDGE_CURVE ( 'NONE', #18090, #184441, #142666, .T. ) ;
#166913=AXIS2_PLACEMENT_3D ( 'NONE', #140043, #22718, #81342 ) ;
#166932=CARTESIAN_POINT ( 'NONE',  ( -23.15000000000000213, 76.00000000001142553, -36.02310748452432421 ) ) ;
#166933=DIRECTION ( 'NONE',  ( -1.000000000000000000, 0.000000000000000000, 0.000000000000000000 ) ) ;
#166951=EDGE_CURVE ( 'NONE', #86948, #202965, #251681, .T. ) ;
#166957=DIRECTION ( 'NONE',  ( 0.000000000000000000, 0.000000000000000000, 1.000000000000000000 ) ) ;
#166958=VERTEX_POINT ( 'NONE', #40308 ) ;
#166982=TOROIDAL_SURFACE ( 'NONE', #29599, 11.65000000000000036, 0.1000000000000000056 ) ;
#166990=VERTEX_POINT ( 'NONE', #207051 ) ;
#166999=CARTESIAN_POINT ( 'NONE',  ( -18.50000000000000000, 85.50000000001161027, -61.42310748452425884 ) ) ;
#167012=DIRECTION ( 'NONE',  ( 0.000000000000000000, -6.982962677686266711E-15, 1.000000000000000000 ) ) ;
#167033=ORIENTED_EDGE ( 'NONE', *, *, #160278, .F. ) ;
#167035=CIRCLE ( 'NONE', #54558, 0.8750000000000007772 ) ;
#167057=DIRECTION ( 'NONE',  ( -1.000000000000000000, 0.000000000000000000, -0.000000000000000000 ) ) ;
#167100=DIRECTION ( 'NONE',  ( 1.000000000000000000, 0.000000000000000000, 0.000000000000000000 ) ) ;
#167106=DIRECTION ( 'NONE',  ( 0.000000000000000000, 0.000000000000000000, 1.000000000000000000 ) ) ;
#167133=DIRECTION ( 'NONE',  ( 0.000000000000000000, -6.982962677686266711E-15, 1.000000000000000000 ) ) ;
#167138=DIRECTION ( 'NONE',  ( 0.000000000000000000, 0.000000000000000000, 1.000000000000000000 ) ) ;
#167172=CARTESIAN_POINT ( 'NONE',  ( 21.05000000000000071, 75.90220970870291239, -75.78092209500044873 ) ) ;
#167174=TOROIDAL_SURFACE ( 'NONE', #196169, 0.6000000000000006439, 0.1000000000000000056 ) ;
#167191=ORIENTED_EDGE ( 'NONE', *, *, #19117, .F. ) ;
#167210=CARTESIAN_POINT ( 'NONE',  ( -18.59999999999999787, 77.16270174994961906, -61.42310748452431568 ) ) ;
#167233=ORIENTED_EDGE ( 'NONE', *, *, #183217, .F. ) ;
#167250=DIRECTION ( 'NONE',  ( -1.000000000000000000, -0.000000000000000000, -0.000000000000000000 ) ) ;
#167252=CARTESIAN_POINT ( 'NONE',  ( 18.50000000000000000, 85.40000000001160174, -62.22584772486096227 ) ) ;
#167253=ADVANCED_FACE ( 'NONE', ( #239453 ), #118217, .T. ) ;
#167259=ORIENTED_EDGE ( 'NONE', *, *, #257013, .F. ) ;
#167272=CIRCLE ( 'NONE', #54794, 0.1000000000000021289 ) ;
#167315=DIRECTION ( 'NONE',  ( 1.000000000000000000, 0.000000000000000000, 0.000000000000000000 ) ) ;
#167410=CARTESIAN_POINT ( 'NONE',  ( -23.25000000000000000, 64.35000000001166143, -69.52310748452440237 ) ) ;
#167438=ORIENTED_EDGE ( 'NONE', *, *, #103608, .T. ) ;
#167453=CARTESIAN_POINT ( 'NONE',  ( -20.64999999999999858, 85.00000000001159606, -59.62913836187181715 ) ) ;
#167463=ORIENTED_EDGE ( 'NONE', *, *, #119874, .F. ) ;
#167486=CARTESIAN_POINT ( 'NONE',  ( 21.14999999999999858, 76.00000000001169553, -76.06376443622556849 ) ) ;
#167509=AXIS2_PLACEMENT_3D ( 'NONE', #234160, #39848, #138875 ) ;
#167553=ADVANCED_FACE ( 'NONE', ( #192315 ), #110191, .T. ) ;
#167571=ORIENTED_EDGE ( 'NONE', *, *, #175334, .F. ) ;
#167572=CARTESIAN_POINT ( 'NONE',  ( -21.44999999999999929, 68.85000000001151932, -48.37310748452436826 ) ) ;
#167581=VERTEX_POINT ( 'NONE', #108911 ) ;
#167642=DIRECTION ( 'NONE',  ( 1.000000000000000000, 0.000000000000000000, 0.000000000000000000 ) ) ;
#167644=ADVANCED_FACE ( 'NONE', ( #211890 ), #114039, .F. ) ;
#167667=DIRECTION ( 'NONE',  ( -4.336808689941751890E-15, -0.8660254037844445918, -0.4999999999999897304 ) ) ;
#167687=ADVANCED_FACE ( 'NONE', ( #141018 ), #202266, .T. ) ;
#167739=ORIENTED_EDGE ( 'NONE', *, *, #87299, .F. ) ;
#167740=CARTESIAN_POINT ( 'NONE',  ( -18.58671080940899145, 85.40693285883820352, -62.39895301961955454 ) ) ;
#167742=ORIENTED_EDGE ( 'NONE', *, *, #209811, .T. ) ;
#167748=CARTESIAN_POINT ( 'NONE',  ( -21.05000000000000071, 77.16270174994961906, -61.52310748452431710 ) ) ;
#167778=VERTEX_POINT ( 'NONE', #204810 ) ;
#167828=DIRECTION ( 'NONE',  ( 1.000000000000000000, -3.265361837132813093E-16, -2.280189983783949500E-30 ) ) ;
#167829=EDGE_CURVE ( 'NONE', #96547, #51183, #88178, .T. ) ;
#167841=CARTESIAN_POINT ( 'NONE',  ( 18.49999999999999289, 64.25000000001149658, -44.67310748452440095 ) ) ;
#167883=ORIENTED_EDGE ( 'NONE', *, *, #33030, .F. ) ;
#167896=CARTESIAN_POINT ( 'NONE',  ( 18.59999999999999076, 61.95000000001160601, -64.00941241376344237 ) ) ;
#167939=ORIENTED_EDGE ( 'NONE', *, *, #170791, .T. ) ;
#167946=CARTESIAN_POINT ( 'NONE',  ( 18.59999999999999076, 64.35000000001147669, -44.67310748452440095 ) ) ;
#167953=EDGE_LOOP ( 'NONE', ( #61300, #166033, #149263, #203177 ) ) ;
#167960=DIRECTION ( 'NONE',  ( 1.000000000000000000, -0.000000000000000000, 0.000000000000000000 ) ) ;
#167966=EDGE_CURVE ( 'NONE', #174912, #113945, #73064, .T. ) ;
#167971=SHAPE_REPRESENTATION_RELATIONSHIP ( 'NONE' , 'NONE' ,  #135069, #48300 ) ;
#167980=DIRECTION ( 'NONE',  ( 0.000000000000000000, -0.8660254037844377084, -0.5000000000000016653 ) ) ;
#168009=EDGE_LOOP ( 'NONE', ( #60763, #225306, #145508, #114247 ) ) ;
#168020=AXIS2_PLACEMENT_3D ( 'NONE', #38430, #60546, #18859 ) ;
#168041=FACE_OUTER_BOUND ( 'NONE', #206256, .T. ) ;
#168055=AXIS2_PLACEMENT_3D ( 'NONE', #41891, #101805, #142243 ) ;
#168063=AXIS2_PLACEMENT_3D ( 'NONE', #197335, #21311, #242892 ) ;
#168096=AXIS2_PLACEMENT_3D ( 'NONE', #164637, #65516, #145054 ) ;
#168104=ADVANCED_FACE ( 'NONE', ( #218939 ), #241106, .T. ) ;
#168141=CARTESIAN_POINT ( 'NONE',  ( 20.94999999999999929, 85.00000000001159606, -59.62913836187181715 ) ) ;
#168146=ORIENTED_EDGE ( 'NONE', *, *, #201003, .F. ) ;
#168167=ORIENTED_EDGE ( 'NONE', *, *, #140149, .F. ) ;
#168169=FACE_OUTER_BOUND ( 'NONE', #216947, .T. ) ;
#168188=VECTOR ( 'NONE', #179749, 1000.000000000000114 ) ;
#168201=AXIS2_PLACEMENT_3D ( 'NONE', #10624, #111003, #91447 ) ;
#168235=DIRECTION ( 'NONE',  ( 0.000000000000000000, -7.116814260417668513E-15, 1.000000000000000000 ) ) ;
#168307=LINE ( 'NONE', #89993, #28835 ) ;
#168320=DIRECTION ( 'NONE',  ( 0.000000000000000000, 0.000000000000000000, 1.000000000000000000 ) ) ;
#168360=AXIS2_PLACEMENT_3D ( 'NONE', #236337, #29510, #215488 ) ;
#168368=TOROIDAL_SURFACE ( 'NONE', #105746, 0.2000000000000000111, 0.1000000000000000056 ) ;
#168373=DIRECTION ( 'NONE',  ( 1.000000000000000000, 0.000000000000000000, 0.000000000000000000 ) ) ;
#168381=EDGE_CURVE ( 'NONE', #140287, #112792, #15329, .T. ) ;
#168408=CARTESIAN_POINT ( 'NONE',  ( 21.05000000000000071, 85.00000000001149658, -45.51707660717670478 ) ) ;
#168415=CARTESIAN_POINT ( 'NONE',  ( -21.45000000000000284, 68.29142135624881860, -48.37310748452437537 ) ) ;
#168432=ORIENTED_EDGE ( 'NONE', *, *, #206338, .T. ) ;
#168433=EDGE_CURVE ( 'NONE', #21500, #96681, #50775, .T. ) ;
#168476=DIRECTION ( 'NONE',  ( 1.000000000000000000, 0.000000000000000000, 0.000000000000000000 ) ) ;
#168522=CARTESIAN_POINT ( 'NONE',  ( 20.94999999999999574, 74.83729825007360148, -61.52310748452433131 ) ) ;
#168541=CIRCLE ( 'NONE', #164406, 0.09999999999999520384 ) ;
#168546=CARTESIAN_POINT ( 'NONE',  ( 21.05000000000000071, 69.35000000001156195, -57.37310748452436826 ) ) ;
#168573=ORIENTED_EDGE ( 'NONE', *, *, #102039, .T. ) ;
#168601=VECTOR ( 'NONE', #91779, 1000.000000000000000 ) ;
#168617=EDGE_CURVE ( 'NONE', #205489, #212829, #205484, .T. ) ;
#168628=DIRECTION ( 'NONE',  ( 0.000000000000000000, -1.000000000000000000, 0.000000000000000000 ) ) ;
#168638=VERTEX_POINT ( 'NONE', #127246 ) ;
#168662=ORIENTED_EDGE ( 'NONE', *, *, #36351, .F. ) ;
#168676=EDGE_LOOP ( 'NONE', ( #110840, #133256, #207590, #202764, #157297 ) ) ;
#168690=EDGE_CURVE ( 'NONE', #214618, #100350, #7286, .T. ) ;
#168717=SPHERICAL_SURFACE ( 'NONE', #125728, 0.1000000000000000056 ) ;
#168720=CARTESIAN_POINT ( 'NONE',  ( 20.94999999999999929, 76.00000000001142553, -36.02310748452432421 ) ) ;
#168762=ADVANCED_FACE ( 'NONE', ( #251020 ), #180182, .F. ) ;
#168766=DIRECTION ( 'NONE',  ( -0.7071067811865389130, -5.024295867788141276E-15, 0.7071067811865561215 ) ) ;
#168780=EDGE_CURVE ( 'NONE', #165019, #122696, #50254, .T. ) ;
#168818=DIRECTION ( 'NONE',  ( -1.000000000000000000, 3.265361837132813093E-16, 2.280189983783949500E-30 ) ) ;
#168848=CARTESIAN_POINT ( 'NONE',  ( 21.13461538461538325, 65.38541703798603066, -57.27310748452440947 ) ) ;
#168884=DIRECTION ( 'NONE',  ( 1.000000000000000000, 0.000000000000000000, 0.000000000000000000 ) ) ;
#168887=CARTESIAN_POINT ( 'NONE',  ( 21.05000000000000071, 67.22371710471912820, -60.96447848938343839 ) ) ;
#168897=ADVANCED_FACE ( 'NONE', ( #136191 ), #75294, .T. ) ;
#168959=ORIENTED_EDGE ( 'NONE', *, *, #127164, .F. ) ;
#168975=AXIS2_PLACEMENT_3D ( 'NONE', #172744, #214386, #35776 ) ;
#168998=VECTOR ( 'NONE', #131675, 1000.000000000000000 ) ;
#169007=CARTESIAN_POINT ( 'NONE',  ( -23.15000000000000213, 74.08971962617978591, -56.89173962932539297 ) ) ;
#169031=EDGE_CURVE ( 'NONE', #124309, #238186, #35119, .T. ) ;
#169037=CARTESIAN_POINT ( 'NONE',  ( -18.43569575749026512, 85.51932773110408448, -62.55013110796496534 ) ) ;
#169039=DIRECTION ( 'NONE',  ( 0.000000000000000000, -7.304098846218112382E-15, 1.000000000000000000 ) ) ;
#169057=ORIENTED_EDGE ( 'NONE', *, *, #257701, .T. ) ;
#169058=( BOUNDED_CURVE ( )  B_SPLINE_CURVE ( 3, ( #90425, #249528, #107430, #30486 ),
 .UNSPECIFIED., .F., .F. ) 
 B_SPLINE_CURVE_WITH_KNOTS ( ( 4, 4 ),
 ( 4.712388980384689674, 6.283185307179586232 ),
 .UNSPECIFIED. ) 
 CURVE ( )  GEOMETRIC_REPRESENTATION_ITEM ( )  RATIONAL_B_SPLINE_CURVE ( ( 1.000000000000000000, 0.8047378541243649375, 0.8047378541243649375, 1.000000000000000000 ) ) 
 REPRESENTATION_ITEM ( '' )  );
#169064=VERTEX_POINT ( 'NONE', #175898 ) ;
#169069=CARTESIAN_POINT ( 'NONE',  ( 21.04386569057615475, 64.25000000001148237, -42.88027013274464849 ) ) ;
#169126=DIRECTION ( 'NONE',  ( 0.000000000000000000, 6.982962677686266711E-15, -1.000000000000000000 ) ) ;
#169136=CARTESIAN_POINT ( 'NONE',  ( -21.02374657821578197, 64.39999999919137963, -42.95131071432642500 ) ) ;
#169141=SPHERICAL_SURFACE ( 'NONE', #57334, 0.1000000000000000056 ) ;
#169145=CARTESIAN_POINT ( 'NONE',  ( -21.05000000000000071, 74.16465844978715438, -57.96795619196135618 ) ) ;
#169193=DIRECTION ( 'NONE',  ( -4.408576920032448588E-17, -0.1350103645451807555, -0.9908441862701609093 ) ) ;
#169194=AXIS2_PLACEMENT_3D ( 'NONE', #162308, #157181, #197555 ) ;
#169208=EDGE_CURVE ( 'NONE', #146292, #47640, #143140, .T. ) ;
#169211=ORIENTED_EDGE ( 'NONE', *, *, #21386, .T. ) ;
#169252=ORIENTED_EDGE ( 'NONE', *, *, #108323, .F. ) ;
#169253=CARTESIAN_POINT ( 'NONE',  ( -21.05000000000000071, 74.14897176987071248, -57.86919421510183525 ) ) ;
#169291=VERTEX_POINT ( 'NONE', #225239 ) ;
#169293=CYLINDRICAL_SURFACE ( 'NONE', #49020, 0.09999999999999520384 ) ;
#169306=DIRECTION ( 'NONE',  ( 1.000000000000000000, 0.000000000000000000, 0.000000000000000000 ) ) ;
#169320=VECTOR ( 'NONE', #188651, 1000.000000000000000 ) ;
#169325=ORIENTED_EDGE ( 'NONE', *, *, #244213, .T. ) ;
#169330=PLANE ( 'NONE',  #238009 ) ;
#169335=ORIENTED_EDGE ( 'NONE', *, *, #174492, .F. ) ;
#169337=PLANE ( 'NONE',  #18489 ) ;
#169377=EDGE_CURVE ( 'NONE', #87492, #102074, #128743, .T. ) ;
#169379=DIRECTION ( 'NONE',  ( -0.000000000000000000, 1.000000000000000000, 6.982962677686266711E-15 ) ) ;
#169415=DIRECTION ( 'NONE',  ( -0.000000000000000000, 0.1298341882519953583, 0.9915357197604862671 ) ) ;
#169445=CARTESIAN_POINT ( 'NONE',  ( -21.05000000000000071, 76.00000000001165290, -69.52310748452431710 ) ) ;
#169455=DIRECTION ( 'NONE',  ( 0.000000000000000000, -0.1568667991644355497, 0.9876197685951332295 ) ) ;
#169481=CARTESIAN_POINT ( 'NONE',  ( 18.59999999999999076, 64.35000000001173248, -81.27310748452440237 ) ) ;
#169501=ORIENTED_EDGE ( 'NONE', *, *, #161485, .T. ) ;
#169509=CARTESIAN_POINT ( 'NONE',  ( -20.94999999999999929, 76.00000000001142553, -36.02310748452432421 ) ) ;
#169549=ORIENTED_EDGE ( 'NONE', *, *, #70304, .T. ) ;
#169563=EDGE_CURVE ( 'NONE', #75472, #71835, #193850, .T. ) ;
#169587=AXIS2_PLACEMENT_3D ( 'NONE', #154652, #93355, #13831 ) ;
#169597=B_SPLINE_CURVE_WITH_KNOTS ( 'NONE', 3,
 ( #220232, #81948, #98951, #1143, #178554, #239787 ),
 .UNSPECIFIED., .F., .F.,
 ( 4, 2, 4 ),
 ( 0.000000000000000000, 0.0001568709654583423218, 0.0003137419309166846436 ),
 .UNSPECIFIED. ) ;
#169669=LINE ( 'NONE', #70555, #85880 ) ;
#169672=EDGE_CURVE ( 'NONE', #237026, #188354, #197280, .T. ) ;
#169674=CARTESIAN_POINT ( 'NONE',  ( -20.94999999999999929, 64.25000000001161027, -62.50830171387040934 ) ) ;
#169691=CYLINDRICAL_SURFACE ( 'NONE', #239624, 0.1000000000000028644 ) ;
#169750=CARTESIAN_POINT ( 'NONE',  ( 20.85000000000000142, 64.35000000001141984, -36.02310748452440237 ) ) ;
#169765=EDGE_CURVE ( 'NONE', #116008, #175005, #193205, .T. ) ;
#169796=AXIS2_PLACEMENT_3D ( 'NONE', #77432, #35788, #14934 ) ;
#169798=EDGE_CURVE ( 'NONE', #234821, #169810, #238988, .T. ) ;
#169803=CARTESIAN_POINT ( 'NONE',  ( -20.94999999999999929, 68.97833521811131163, -32.38954208262708079 ) ) ;
#169804=ORIENTED_EDGE ( 'NONE', *, *, #152942, .F. ) ;
#169810=VERTEX_POINT ( 'NONE', #187141 ) ;
#169865=ORIENTED_EDGE ( 'NONE', *, *, #107102, .F. ) ;
#169878=AXIS2_PLACEMENT_3D ( 'NONE', #250074, #187555, #50559 ) ;
#169887=EDGE_CURVE ( 'NONE', #136730, #99760, #218206, .T. ) ;
#169894=DIRECTION ( 'NONE',  ( 0.000000000000000000, 0.000000000000000000, -1.000000000000000000 ) ) ;
#169940=EDGE_CURVE ( 'NONE', #128154, #31772, #43355, .T. ) ;
#169967=CARTESIAN_POINT ( 'NONE',  ( 22.60000000000000142, 64.25043287652226809, -69.62396585362311896 ) ) ;
#169973=CARTESIAN_POINT ( 'NONE',  ( 20.94999999999999929, 71.18691588786205671, -57.58158972800053022 ) ) ;
#170011=ORIENTED_EDGE ( 'NONE', *, *, #95384, .F. ) ;
#170048=VECTOR ( 'NONE', #5629, 1000.000000000000000 ) ;
#170090=CARTESIAN_POINT ( 'NONE',  ( 19.75857864376268935, 64.35000000001147669, -44.67310748452440095 ) ) ;
#170194=ADVANCED_FACE ( 'NONE', ( #48581 ), #207679, .F. ) ;
#170216=ORIENTED_EDGE ( 'NONE', *, *, #226601, .T. ) ;
#170219=CARTESIAN_POINT ( 'NONE',  ( -18.50000000000000711, 64.25000000001161027, -62.50830171387040934 ) ) ;
#170262=DIRECTION ( 'NONE',  ( -0.000000000000000000, -6.982962677686266711E-15, 1.000000000000000000 ) ) ;
#170264=CARTESIAN_POINT ( 'NONE',  ( -23.15000000000000213, 64.35000000001166143, -69.52310748452440237 ) ) ;
#170285=AXIS2_PLACEMENT_3D ( 'NONE', #246778, #68153, #148997 ) ;
#170301=EDGE_CURVE ( 'NONE', #47971, #58501, #193400, .T. ) ;
#170364=CIRCLE ( 'NONE', #203642, 0.09999999999999939493 ) ;
#170421=ORIENTED_EDGE ( 'NONE', *, *, #177492, .T. ) ;
#170425=AXIS2_PLACEMENT_3D ( 'NONE', #27876, #164788, #89090 ) ;
#170459=FACE_OUTER_BOUND ( 'NONE', #680, .T. ) ;
#170493=CARTESIAN_POINT ( 'NONE',  ( 21.05000000000000071, 69.74218538953552127, -69.62089777583315708 ) ) ;
#170517=ORIENTED_EDGE ( 'NONE', *, *, #23443, .F. ) ;
#170520=ORIENTED_EDGE ( 'NONE', *, *, #162515, .F. ) ;
#170547=ORIENTED_EDGE ( 'NONE', *, *, #136160, .T. ) ;
#170618=CARTESIAN_POINT ( 'NONE',  ( -21.05000000000000071, 77.26178616857662007, -61.43660852097883662 ) ) ;
#170625=AXIS2_PLACEMENT_3D ( 'NONE', #140932, #58789, #142201 ) ;
#170658=AXIS2_PLACEMENT_3D ( 'NONE', #75068, #234099, #169039 ) ;
#170668=DIRECTION ( 'NONE',  ( 1.000000000000000000, 0.000000000000000000, 0.000000000000000000 ) ) ;
#170694=CARTESIAN_POINT ( 'NONE',  ( 21.05000000000000071, 67.22371710471918504, -69.52310748452437394 ) ) ;
#170715=CYLINDRICAL_SURFACE ( 'NONE', #203672, 0.5000000000000004441 ) ;
#170717=ADVANCED_FACE ( 'NONE', ( #76494 ), #256360, .T. ) ;
#170739=AXIS2_PLACEMENT_3D ( 'NONE', #107117, #167133, #87540 ) ;
#170791=EDGE_CURVE ( 'NONE', #206496, #61365, #85176, .T. ) ;
#170804=EDGE_CURVE ( 'NONE', #134285, #46294, #135454, .T. ) ;
#170828=VERTEX_POINT ( 'NONE', #22984 ) ;
#170842=ADVANCED_FACE ( 'NONE', ( #182031 ), #223698, .F. ) ;
#170884=CARTESIAN_POINT ( 'NONE',  ( -23.15000000000000213, 87.65000000001174385, -81.27310748452423184 ) ) ;
#170889=CARTESIAN_POINT ( 'NONE',  ( 20.04142135623730070, 64.35000000001173248, -81.27310748452440237 ) ) ;
#170919=DIRECTION ( 'NONE',  ( 2.952720810173289112E-16, 1.000000000000000000, 6.938893903907222067E-15 ) ) ;
#170929=AXIS2_PLACEMENT_3D ( 'NONE', #198128, #221519, #201987 ) ;
#170948=CARTESIAN_POINT ( 'NONE',  ( 22.49436431346199683, 64.35004905235818740, -69.59001101424667013 ) ) ;
#170980=DIRECTION ( 'NONE',  ( -5.603264701231743991E-32, -7.172728831056617961E-15, 1.000000000000000000 ) ) ;
#171007=VERTEX_POINT ( 'NONE', #9802 ) ;
#171016=EDGE_CURVE ( 'NONE', #191153, #251642, #127094, .T. ) ;
#171045=EDGE_CURVE ( 'NONE', #151129, #2421, #108898, .T. ) ;
#171057=CARTESIAN_POINT ( 'NONE',  ( 21.00000000000000000, 66.25000000001151079, -48.37310748452438958 ) ) ;
#171079=ORIENTED_EDGE ( 'NONE', *, *, #81238, .T. ) ;
#171101=ORIENTED_EDGE ( 'NONE', *, *, #136357, .T. ) ;
#171120=CARTESIAN_POINT ( 'NONE',  ( 18.45068634130097607, 85.48650607335434870, -62.45432905335616169 ) ) ;
#171173=ORIENTED_EDGE ( 'NONE', *, *, #191107, .T. ) ;
#171174=DIRECTION ( 'NONE',  ( 0.000000000000000000, -1.000000000000000000, 0.000000000000000000 ) ) ;
#171183=DIRECTION ( 'NONE',  ( 1.000000000000000000, 0.000000000000000000, 0.000000000000000000 ) ) ;
#171216=ORIENTED_EDGE ( 'NONE', *, *, #23237, .T. ) ;
#171268=DIRECTION ( 'NONE',  ( 1.000000000000000000, 0.000000000000000000, 0.000000000000000000 ) ) ;
#171300=( GEOMETRIC_REPRESENTATION_CONTEXT ( 3 ) GLOBAL_UNCERTAINTY_ASSIGNED_CONTEXT ( ( #98825 ) ) GLOBAL_UNIT_ASSIGNED_CONTEXT ( ( #203409, #222950, #185123 ) ) REPRESENTATION_CONTEXT ( 'NONE', 'WORKASPACE' ) );
#171306=EDGE_CURVE ( 'NONE', #188373, #207310, #256389, .T. ) ;
#171307=FACE_OUTER_BOUND ( 'NONE', #34837, .T. ) ;
#171313=DIRECTION ( 'NONE',  ( 0.000000000000000000, -6.982962677686266711E-15, 1.000000000000000000 ) ) ;
#171351=ADVANCED_FACE ( 'NONE', ( #231146 ), #250670, .F. ) ;
#171354=DIRECTION ( 'NONE',  ( -1.000000000000000000, -0.000000000000000000, -0.000000000000000000 ) ) ;
#171362=CARTESIAN_POINT ( 'NONE',  ( 21.14999999999999858, 65.28660755661168480, -57.27310748452439526 ) ) ;
#171393=ORIENTED_EDGE ( 'NONE', *, *, #228726, .F. ) ;
#171395=ORIENTED_EDGE ( 'NONE', *, *, #64383, .F. ) ;
#171442=DIRECTION ( 'NONE',  ( 0.000000000000000000, -0.1350103645451945777, 0.9908441862701590219 ) ) ;
#171446=AXIS2_PLACEMENT_3D ( 'NONE', #148891, #129316, #228434 ) ;
#171448=DIRECTION ( 'NONE',  ( 0.000000000000000000, 0.000000000000000000, 1.000000000000000000 ) ) ;
#171475=VERTEX_POINT ( 'NONE', #18499 ) ;
#171484=DIRECTION ( 'NONE',  ( -2.978066053179069723E-16, -1.000000000000000000, -7.147358527629766941E-15 ) ) ;
#171504=DIRECTION ( 'NONE',  ( -1.000000000000000000, -0.000000000000000000, -0.000000000000000000 ) ) ;
#171515=DIRECTION ( 'NONE',  ( 0.000000000000000000, -1.000000000000000000, -6.982962677686265922E-15 ) ) ;
#171521=CARTESIAN_POINT ( 'NONE',  ( 18.59999999999999787, 77.26327546522863088, -28.12124281777790813 ) ) ;
#171548=ADVANCED_FACE ( 'NONE', ( #237546 ), #194126, .F. ) ;
#171584=FACE_OUTER_BOUND ( 'NONE', #253631, .T. ) ;
#171599=AXIS2_PLACEMENT_3D ( 'NONE', #87161, #247541, #49332 ) ;
#171665=VECTOR ( 'NONE', #2445, 1000.000000000000000 ) ;
#171681=AXIS2_PLACEMENT_3D ( 'NONE', #159695, #239219, #140099 ) ;
#171743=CIRCLE ( 'NONE', #205008, 7.800000000000001599 ) ;
#171747=ORIENTED_EDGE ( 'NONE', *, *, #238534, .T. ) ;
#171758=CARTESIAN_POINT ( 'NONE',  ( 20.94999999999999929, 77.16412189325258453, -28.10825939895270764 ) ) ;
#171772=AXIS2_PLACEMENT_3D ( 'NONE', #242534, #105557, #23532 ) ;
#171793=ORIENTED_EDGE ( 'NONE', *, *, #236832, .F. ) ;
#171818=ORIENTED_EDGE ( 'NONE', *, *, #167966, .T. ) ;
#171864=DIRECTION ( 'NONE',  ( 0.000000000000000000, 0.8660254037844420383, -0.4999999999999943379 ) ) ;
#171866=CARTESIAN_POINT ( 'NONE',  ( -22.48970261584618058, 64.35000000001166143, -69.57847697274181087 ) ) ;
#171871=DIRECTION ( 'NONE',  ( 0.000000000000000000, -6.467318590049456648E-15, 1.000000000000000000 ) ) ;
#171894=VERTEX_POINT ( 'NONE', #198108 ) ;
#171910=EDGE_CURVE ( 'NONE', #160136, #233017, #135554, .T. ) ;
#171915=EDGE_CURVE ( 'NONE', #193539, #254970, #60806, .T. ) ;
#171939=DIRECTION ( 'NONE',  ( -0.000000000000000000, -6.982962677686266711E-15, 1.000000000000000000 ) ) ;
#171943=DIRECTION ( 'NONE',  ( -1.000000000000000000, -0.000000000000000000, -0.000000000000000000 ) ) ;
#171991=VECTOR ( 'NONE', #215144, 1000.000000000000000 ) ;
#172002=CIRCLE ( 'NONE', #51118, 0.1000000000000028644 ) ;
#172017=CARTESIAN_POINT ( 'NONE',  ( -18.49372193242234275, 85.44248452336948674, -29.25832622448972842 ) ) ;
#172029=CARTESIAN_POINT ( 'NONE',  ( -20.94999999999999929, 70.15000000001163016, -59.39061026024639744 ) ) ;
#172034=DIRECTION ( 'NONE',  ( 0.000000000000000000, -6.938893903907222067E-15, 1.000000000000000000 ) ) ;
#172059=EDGE_CURVE ( 'NONE', #172794, #202854, #241112, .T. ) ;
#172076=AXIS2_PLACEMENT_3D ( 'NONE', #222442, #103782, #60817 ) ;
#172077=EDGE_CURVE ( 'NONE', #191947, #229077, #15232, .T. ) ;
#172081=VERTEX_POINT ( 'NONE', #221504 ) ;
#172119=FACE_OUTER_BOUND ( 'NONE', #254346, .T. ) ;
#172123=CARTESIAN_POINT ( 'NONE',  ( 21.05000000000000071, 76.00000000001165290, -69.52310748452431710 ) ) ;
#172125=ORIENTED_EDGE ( 'NONE', *, *, #141473, .T. ) ;
#172144=EDGE_CURVE ( 'NONE', #118994, #153767, #7026, .T. ) ;
#172176=FACE_OUTER_BOUND ( 'NONE', #215327, .T. ) ;
#172217=VERTEX_POINT ( 'NONE', #165413 ) ;
#172285=DIRECTION ( 'NONE',  ( 1.000000000000000000, 0.000000000000000000, 0.000000000000000000 ) ) ;
#172297=LINE ( 'NONE', #34059, #234776 ) ;
#172301=LINE ( 'NONE', #32780, #47256 ) ;
#172388=ORIENTED_EDGE ( 'NONE', *, *, #192555, .F. ) ;
#172402=CARTESIAN_POINT ( 'NONE',  ( 20.12500000000000355, 66.74195072709427734, -61.15976864738194507 ) ) ;
#172430=CARTESIAN_POINT ( 'NONE',  ( -20.94999999999999929, 77.36242903720467723, -28.13422623660311217 ) ) ;
#172432=ORIENTED_EDGE ( 'NONE', *, *, #91685, .T. ) ;
#172464=CARTESIAN_POINT ( 'NONE',  ( 20.97239005616515328, 67.12515615866146845, -57.27295468237120701 ) ) ;
#172488=DIRECTION ( 'NONE',  ( 0.000000000000000000, -1.000000000000000000, -7.105427357601001859E-15 ) ) ;
#172514=VECTOR ( 'NONE', #137610, 1000.000000000000000 ) ;
#172571=DIRECTION ( 'NONE',  ( 0.000000000000000000, 1.000000000000000000, 1.156482317317864980E-14 ) ) ;
#172596=CARTESIAN_POINT ( 'NONE',  ( -18.59999999999999787, 74.16465844978715438, -57.96795619196135618 ) ) ;
#172613=ORIENTED_EDGE ( 'NONE', *, *, #59113, .T. ) ;
#172640=CARTESIAN_POINT ( 'NONE',  ( 20.94999999999999929, 67.07338541492450190, -61.05142446530125966 ) ) ;
#172641=AXIS2_PLACEMENT_3D ( 'NONE', #64886, #80576, #160176 ) ;
#172669=CIRCLE ( 'NONE', #192905, 0.1000000000000028644 ) ;
#172690=EDGE_LOOP ( 'NONE', ( #202809, #188051, #203099, #56960 ) ) ;
#172698=VERTEX_POINT ( 'NONE', #253281 ) ;
#172702=CARTESIAN_POINT ( 'NONE',  ( 21.05000000000000071, 70.50000000001158185, -57.11784146561126363 ) ) ;
#172707=DIRECTION ( 'NONE',  ( 0.000000000000000000, -6.982962677686266711E-15, 1.000000000000000000 ) ) ;
#172718=ORIENTED_EDGE ( 'NONE', *, *, #19353, .T. ) ;
#172727=ADVANCED_FACE ( 'NONE', ( #173817 ), #233746, .F. ) ;
#172736=VECTOR ( 'NONE', #220652, 1000.000000000000000 ) ;
#172744=CARTESIAN_POINT ( 'NONE',  ( 21.05000000000000071, 76.00000000001155342, -56.54810748452432279 ) ) ;
#172766=EDGE_LOOP ( 'NONE', ( #109449, #105198, #73347, #246406 ) ) ;
#172792=ADVANCED_FACE ( 'NONE', ( #173441 ), #127445, .T. ) ;
#172794=VERTEX_POINT ( 'NONE', #252910 ) ;
#172795=TOROIDAL_SURFACE ( 'NONE', #255903, 6.258578643762700899, 0.1000000000000000056 ) ;
#172817=DIRECTION ( 'NONE',  ( 0.000000000000000000, 6.982962677686266711E-15, -1.000000000000000000 ) ) ;
#172830=CYLINDRICAL_SURFACE ( 'NONE', #158850, 11.80000000000000426 ) ;
#172833=DIRECTION ( 'NONE',  ( 1.000000000000000000, 0.000000000000000000, 0.000000000000000000 ) ) ;
#172870=ORIENTED_EDGE ( 'NONE', *, *, #197557, .T. ) ;
#172883=VECTOR ( 'NONE', #121657, 1000.000000000000000 ) ;
#172919=CYLINDRICAL_SURFACE ( 'NONE', #62886, 0.1000000000000028644 ) ;
#172938=ORIENTED_EDGE ( 'NONE', *, *, #74709, .F. ) ;
#172994=VECTOR ( 'NONE', #233335, 1000.000000000000000 ) ;
#173020=AXIS2_PLACEMENT_3D ( 'NONE', #2986, #139924, #81230 ) ;
#173056=ORIENTED_EDGE ( 'NONE', *, *, #224938, .T. ) ;
#173060=AXIS2_PLACEMENT_3D ( 'NONE', #133017, #230844, #114727 ) ;
#173064=CARTESIAN_POINT ( 'NONE',  ( -20.85000000000000142, 87.65000000001144542, -38.92310748452424463 ) ) ;
#173097=DIRECTION ( 'NONE',  ( 1.000000000000000000, 0.000000000000000000, 0.000000000000000000 ) ) ;
#173129=DIRECTION ( 'NONE',  ( 0.000000000000000000, -6.853228547068871147E-15, 1.000000000000000000 ) ) ;
#173162=CARTESIAN_POINT ( 'NONE',  ( -22.48660254037843487, 64.35000000001166143, -69.57310748452438531 ) ) ;
#173174=DIRECTION ( 'NONE',  ( 0.000000000000000000, -1.000000000000000000, 0.000000000000000000 ) ) ;
#173194=ORIENTED_EDGE ( 'NONE', *, *, #174793, .F. ) ;
#173223=FACE_OUTER_BOUND ( 'NONE', #98379, .T. ) ;
#173228=EDGE_LOOP ( 'NONE', ( #865, #215324, #168959, #203473, #103846 ) ) ;
#173242=CYLINDRICAL_SURFACE ( 'NONE', #126461, 7.900000000000000355 ) ;
#173264=VECTOR ( 'NONE', #243036, 1000.000000000000000 ) ;
#173270=CARTESIAN_POINT ( 'NONE',  ( -21.05439746398122836, 64.25000000001161027, -62.53319099703981720 ) ) ;
#173272=CARTESIAN_POINT ( 'NONE',  ( 20.94999999999999574, 74.83729825007360148, -61.42310748452432989 ) ) ;
#173284=EDGE_CURVE ( 'NONE', #177501, #729, #115168, .T. ) ;
#173316=ORIENTED_EDGE ( 'NONE', *, *, #166951, .T. ) ;
#173323=CARTESIAN_POINT ( 'NONE',  ( 20.94999999999999574, 69.45000000001158469, -59.67928539484123718 ) ) ;
#173332=DIRECTION ( 'NONE',  ( 1.000000000000000000, 0.000000000000000000, 0.000000000000000000 ) ) ;
#173334=VECTOR ( 'NONE', #238769, 1000.000000000000114 ) ;
#173344=CARTESIAN_POINT ( 'NONE',  ( 18.49999999999999289, 64.25000000001161027, -61.42310748452440095 ) ) ;
#173352=CARTESIAN_POINT ( 'NONE',  ( 21.05000000000000071, 71.00000000001151079, -48.02837350343745015 ) ) ;
#173369=AXIS2_PLACEMENT_3D ( 'NONE', #90811, #167828, #226459 ) ;
#173382=ADVANCED_FACE ( 'NONE', ( #17828 ), #36144, .T. ) ;
#173441=FACE_OUTER_BOUND ( 'NONE', #163787, .T. ) ;
#173457=VERTEX_POINT ( 'NONE', #51493 ) ;
#173482=LINE ( 'NONE', #250389, #112487 ) ;
#173483=CARTESIAN_POINT ( 'NONE',  ( 21.05000000000000071, 65.27628289530409234, -61.85819391543678591 ) ) ;
#173496=FACE_OUTER_BOUND ( 'NONE', #178994, .T. ) ;
#173497=AXIS2_PLACEMENT_3D ( 'NONE', #128530, #249760, #88082 ) ;
#173527=DIRECTION ( 'NONE',  ( 0.000000000000000000, -1.186135710069611419E-15, 1.000000000000000000 ) ) ;
#173529=DIRECTION ( 'NONE',  ( 0.000000000000000000, 0.000000000000000000, -1.000000000000000000 ) ) ;
#173531=EDGE_CURVE ( 'NONE', #165019, #116521, #15407, .T. ) ;
#173560=DIRECTION ( 'NONE',  ( 0.000000000000000000, 6.982962677686266711E-15, -1.000000000000000000 ) ) ;
#173570=DIRECTION ( 'NONE',  ( 1.000000000000000000, 0.000000000000000000, 0.000000000000000000 ) ) ;
#173581=CARTESIAN_POINT ( 'NONE',  ( -20.64999999999999858, 73.50000000001151079, -49.24772940728643533 ) ) ;
#173601=ORIENTED_EDGE ( 'NONE', *, *, #88905, .T. ) ;
#173610=LINE ( 'NONE', #129298, #74548 ) ;
#173619=DIRECTION ( 'NONE',  ( -1.000000000000000000, -0.000000000000000000, -0.000000000000000000 ) ) ;
#173646=EDGE_CURVE ( 'NONE', #235108, #98003, #82301, .T. ) ;
#173687=ORIENTED_EDGE ( 'NONE', *, *, #241190, .F. ) ;
#173689=CYLINDRICAL_SURFACE ( 'NONE', #245118, 0.1000000000000028644 ) ;
#173709=CARTESIAN_POINT ( 'NONE',  ( 21.14999999999999858, 76.00000000001169553, -76.06376443622556849 ) ) ;
#173710=ORIENTED_EDGE ( 'NONE', *, *, #16442, .T. ) ;
#173731=FACE_OUTER_BOUND ( 'NONE', #60299, .T. ) ;
#173817=FACE_OUTER_BOUND ( 'NONE', #49028, .T. ) ;
#173824=ORIENTED_EDGE ( 'NONE', *, *, #231933, .F. ) ;
#173836=LINE ( 'NONE', #194662, #8560 ) ;
#173849=DIRECTION ( 'NONE',  ( 1.000000000000000000, -0.000000000000000000, 0.000000000000000000 ) ) ;
#173870=CARTESIAN_POINT ( 'NONE',  ( -23.25000000000000000, 71.75000000001156764, -57.37310748452435405 ) ) ;
#173883=DIRECTION ( 'NONE',  ( -1.000000000000000000, 0.000000000000000000, 0.000000000000000000 ) ) ;
#173890=CARTESIAN_POINT ( 'NONE',  ( -22.50000000000094147, 75.89914163091312105, -81.27267460801373034 ) ) ;
#173892=DIRECTION ( 'NONE',  ( 1.000000000000000000, 0.000000000000000000, 0.000000000000000000 ) ) ;
#173948=CARTESIAN_POINT ( 'NONE',  ( 18.59999999999999076, 65.79142135624880439, -48.17310748452439384 ) ) ;
#173972=VECTOR ( 'NONE', #113437, 1000.000000000000000 ) ;
#173996=DIRECTION ( 'NONE',  ( 0.000000000000000000, -7.056502275159894776E-15, 1.000000000000000000 ) ) ;
#174026=FACE_OUTER_BOUND ( 'NONE', #243213, .T. ) ;
#174034=VERTEX_POINT ( 'NONE', #139410 ) ;
#174084=CARTESIAN_POINT ( 'NONE',  ( -23.15000000000000213, 84.66355140188075268, -59.99900636645695329 ) ) ;
#174104=CARTESIAN_POINT ( 'NONE',  ( 18.39999999999999858, 85.60000000001137721, -29.42291809330221142 ) ) ;
#174150=CARTESIAN_POINT ( 'NONE',  ( 23.24999999999999645, 70.40000000001150227, -48.42837350343745584 ) ) ;
#174166=CARTESIAN_POINT ( 'NONE',  ( -23.25000000000000000, 76.00000000001165290, -69.52310748452431710 ) ) ;
#174231=DIRECTION ( 'NONE',  ( -1.000000000000000000, 3.265361837132813093E-16, 2.280189983783949500E-30 ) ) ;
#174235=TOROIDAL_SURFACE ( 'NONE', #28497, 7.800000000000000711, 0.1000000000000000056 ) ;
#174245=AXIS2_PLACEMENT_3D ( 'NONE', #180235, #290, #22455 ) ;
#174260=TOROIDAL_SURFACE ( 'NONE', #149293, 12.97499999999999609, 0.1000000000000000056 ) ;
#174282=FACE_OUTER_BOUND ( 'NONE', #56216, .T. ) ;
#174291=ADVANCED_FACE ( 'NONE', ( #141680 ), #120875, .F. ) ;
#174294=CARTESIAN_POINT ( 'NONE',  ( 21.05000000000000071, 69.69548367074806094, -69.50200417646566109 ) ) ;
#174299=DIRECTION ( 'NONE',  ( 1.000000000000000000, 0.000000000000000000, 0.000000000000000000 ) ) ;
#174309=FACE_OUTER_BOUND ( 'NONE', #91152, .T. ) ;
#174361=ORIENTED_EDGE ( 'NONE', *, *, #206247, .T. ) ;
#174362=EDGE_LOOP ( 'NONE', ( #60292, #129881, #238490, #174527, #187982 ) ) ;
#174414=LINE ( 'NONE', #190078, #178389 ) ;
#174418=ADVANCED_FACE ( 'NONE', ( #221210 ), #20047, .F. ) ;
#174450=DIRECTION ( 'NONE',  ( 0.000000000000000000, 1.000000000000000000, 6.982962677686266711E-15 ) ) ;
#174465=AXIS2_PLACEMENT_3D ( 'NONE', #4358, #83863, #163452 ) ;
#174492=EDGE_CURVE ( 'NONE', #160578, #137086, #142945, .T. ) ;
#174526=AXIS2_PLACEMENT_3D ( 'NONE', #16263, #31971, #90617 ) ;
#174527=ORIENTED_EDGE ( 'NONE', *, *, #39399, .F. ) ;
#174541=EDGE_CURVE ( 'NONE', #201784, #142525, #211581, .T. ) ;
#174557=CARTESIAN_POINT ( 'NONE',  ( -20.97625342178413277, 64.39999999919147911, -62.59490425472234421 ) ) ;
#174570=LINE ( 'NONE', #135368, #23678 ) ;
#174596=CARTESIAN_POINT ( 'NONE',  ( -21.05000000000000071, 76.10000000001170406, -76.06376443622556849 ) ) ;
#174599=VECTOR ( 'NONE', #20261, 999.9999999999998863 ) ;
#174604=CARTESIAN_POINT ( 'NONE',  ( -18.37151313414656784, 85.57101412579008581, -29.20644457528533877 ) ) ;
#174614=CARTESIAN_POINT ( 'NONE',  ( -20.85000000000000142, 68.92903212821255465, -32.27654326265606954 ) ) ;
#174617=SPHERICAL_SURFACE ( 'NONE', #101856, 0.1000000000000000056 ) ;
#174636=AXIS2_PLACEMENT_3D ( 'NONE', #87815, #199124, #124411 ) ;
#174688=CARTESIAN_POINT ( 'NONE',  ( 18.59999999999999432, 77.73625713160897988, -57.95445515550681392 ) ) ;
#174724=EDGE_LOOP ( 'NONE', ( #3060, #164822, #50759 ) ) ;
#174737=CARTESIAN_POINT ( 'NONE',  ( -21.14999999999999503, 69.45934304831041572, -69.52310748452437394 ) ) ;
#174748=DIRECTION ( 'NONE',  ( -1.000000000000000000, 0.000000000000000000, -0.000000000000000000 ) ) ;
#174762=ORIENTED_EDGE ( 'NONE', *, *, #80024, .T. ) ;
#174784=ORIENTED_EDGE ( 'NONE', *, *, #208089, .T. ) ;
#174793=EDGE_CURVE ( 'NONE', #92561, #187599, #80077, .T. ) ;
#174816=CARTESIAN_POINT ( 'NONE',  ( -21.55000000000000426, 68.29142135624888965, -57.17310748452437963 ) ) ;
#174823=DIRECTION ( 'NONE',  ( 1.000000000000000000, 0.000000000000000000, 0.000000000000000000 ) ) ;
#174834=VERTEX_POINT ( 'NONE', #59225 ) ;
#174836=DIRECTION ( 'NONE',  ( -1.000000000000000000, 2.952720810173289112E-16, 2.061873921506763405E-30 ) ) ;
#174852=EDGE_CURVE ( 'NONE', #44347, #97848, #90940, .T. ) ;
#174888=DIRECTION ( 'NONE',  ( -0.000000000000000000, 1.000000000000000000, 6.982962677686266711E-15 ) ) ;
#174897=AXIS2_PLACEMENT_3D ( 'NONE', #60575, #41054, #120587 ) ;
#174904=CIRCLE ( 'NONE', #228838, 0.1000000000000028644 ) ;
#174905=FACE_OUTER_BOUND ( 'NONE', #228236, .T. ) ;
#174912=VERTEX_POINT ( 'NONE', #5688 ) ;
#174913=DIRECTION ( 'NONE',  ( -1.000000000000000000, 0.000000000000000000, -0.000000000000000000 ) ) ;
#174916=EDGE_CURVE ( 'NONE', #223761, #209328, #157818, .T. ) ;
#174941=AXIS2_PLACEMENT_3D ( 'NONE', #129583, #31797, #10926 ) ;
#174955=ORIENTED_EDGE ( 'NONE', *, *, #209231, .F. ) ;
#174975=ORIENTED_EDGE ( 'NONE', *, *, #234141, .F. ) ;
#174979=CARTESIAN_POINT ( 'NONE',  ( -18.59999999999999787, 64.35000000001161879, -62.50830171387040934 ) ) ;
#174984=ORIENTED_EDGE ( 'NONE', *, *, #250436, .F. ) ;
#174995=CIRCLE ( 'NONE', #91749, 0.09999999999999939493 ) ;
#175005=VERTEX_POINT ( 'NONE', #6995 ) ;
#175016=FACE_OUTER_BOUND ( 'NONE', #62954, .T. ) ;
#175018=CARTESIAN_POINT ( 'NONE',  ( -22.01447462590972748, 68.73619979878172614, -69.62214448458389882 ) ) ;
#175021=ADVANCED_FACE ( 'NONE', ( #42285 ), #153540, .F. ) ;
#175049=CARTESIAN_POINT ( 'NONE',  ( 23.14999999999999858, 70.50000000001158185, -57.11784146561126363 ) ) ;
#175084=CARTESIAN_POINT ( 'NONE',  ( 21.14999999999999858, 64.25000000001165290, -69.42310748452440805 ) ) ;
#175105=EDGE_LOOP ( 'NONE', ( #182644, #107446, #139944, #148618 ) ) ;
#175112=DIRECTION ( 'NONE',  ( -1.000000000000000000, 2.952720810173289112E-16, 2.061873921506763405E-30 ) ) ;
#175124=SPHERICAL_SURFACE ( 'NONE', #19026, 0.1000000000000000056 ) ;
#175151=ORIENTED_EDGE ( 'NONE', *, *, #131737, .T. ) ;
#175187=AXIS2_PLACEMENT_3D ( 'NONE', #119641, #54514, #117065 ) ;
#175206=CARTESIAN_POINT ( 'NONE',  ( -23.25000000000000000, 77.85161776048025217, -24.41991776492064758 ) ) ;
#175232=FACE_OUTER_BOUND ( 'NONE', #122139, .T. ) ;
#175233=FACE_OUTER_BOUND ( 'NONE', #146810, .T. ) ;
#175273=VERTEX_POINT ( 'NONE', #235683 ) ;
#175279=DIRECTION ( 'NONE',  ( 0.000000000000000000, 6.982962677686266711E-15, -1.000000000000000000 ) ) ;
#175295=DIRECTION ( 'NONE',  ( 0.000000000000000000, 0.4999999999999689138, -0.8660254037844565822 ) ) ;
#175334=EDGE_CURVE ( 'NONE', #175005, #69752, #99652, .T. ) ;
#175341=CARTESIAN_POINT ( 'NONE',  ( -23.25000000000000000, 76.00000000001165290, -69.52310748452431710 ) ) ;
#175343=VERTEX_POINT ( 'NONE', #108373 ) ;
#175345=FACE_OUTER_BOUND ( 'NONE', #94929, .T. ) ;
#175346=VERTEX_POINT ( 'NONE', #54482 ) ;
#175352=AXIS2_PLACEMENT_3D ( 'NONE', #219300, #100603, #1529 ) ;
#175374=CARTESIAN_POINT ( 'NONE',  ( -21.64999999999999858, 68.75000000001152500, -48.27310748452437394 ) ) ;
#175419=VERTEX_POINT ( 'NONE', #240833 ) ;
#175425=AXIS2_PLACEMENT_3D ( 'NONE', #45443, #207093, #124990 ) ;
#175492=CARTESIAN_POINT ( 'NONE',  ( -20.94999999999999929, 87.65000000001163016, -66.42310748452423752 ) ) ;
#175504=CARTESIAN_POINT ( 'NONE',  ( -23.25000000000000000, 64.25000000001165290, -69.52310748452440237 ) ) ;
#175507=CARTESIAN_POINT ( 'NONE',  ( -23.25000000000000000, 77.14957036958705316, -28.20719500002235236 ) ) ;
#175514=ORIENTED_EDGE ( 'NONE', *, *, #227545, .F. ) ;
#175548=CARTESIAN_POINT ( 'NONE',  ( 20.94999999999999929, 76.00000000001141132, -34.02310748452431710 ) ) ;
#175574=CIRCLE ( 'NONE', #204595, 0.09999999999999520384 ) ;
#175584=DIRECTION ( 'NONE',  ( 0.000000000000000000, 0.4930308989875575865, 0.8700118002898125091 ) ) ;
#175639=ORIENTED_EDGE ( 'NONE', *, *, #89467, .F. ) ;
#175667=DIRECTION ( 'NONE',  ( 0.000000000000000000, 1.000000000000000000, 6.982962677686266711E-15 ) ) ;
#175682=DIRECTION ( 'NONE',  ( 1.000000000000000000, 0.000000000000000000, 0.000000000000000000 ) ) ;
#175712=CARTESIAN_POINT ( 'NONE',  ( -20.64999999999999858, 85.40000000001148805, -45.91707660717669626 ) ) ;
#175718=ADVANCED_FACE ( 'NONE', ( #37204 ), #121870, .F. ) ;
#175756=CARTESIAN_POINT ( 'NONE',  ( 20.94999999999999929, 76.00000000001142553, -36.02310748452432421 ) ) ;
#175774=ADVANCED_FACE ( 'NONE', ( #201386 ), #199855, .F. ) ;
#175778=DIRECTION ( 'NONE',  ( 0.000000000000000000, 0.000000000000000000, 1.000000000000000000 ) ) ;
#175788=FACE_OUTER_BOUND ( 'NONE', #4472, .T. ) ;
#175801=LINE ( 'NONE', #122231, #182748 ) ;
#175817=EDGE_CURVE ( 'NONE', #42405, #21500, #198819, .T. ) ;
#175844=CARTESIAN_POINT ( 'NONE',  ( -18.46154800491001069, 85.48020627425343321, -29.36565664614284898 ) ) ;
#175847=CARTESIAN_POINT ( 'NONE',  ( -21.05000000000000071, 77.26178616857662007, -61.43660852097883662 ) ) ;
#175849=CIRCLE ( 'NONE', #188865, 2.100000000000004530 ) ;
#175851=CARTESIAN_POINT ( 'NONE',  ( -22.59999999999999787, 64.25043287652226809, -69.62396585362311896 ) ) ;
#175857=DIRECTION ( 'NONE',  ( 0.000000000000000000, -1.000000000000000000, -6.982962677686265922E-15 ) ) ;
#175878=DIRECTION ( 'NONE',  ( -3.265361837132813093E-16, -1.000000000000000000, -6.982962677686266711E-15 ) ) ;
#175898=CARTESIAN_POINT ( 'NONE',  ( 21.87500000000000355, 66.25000000001151079, -48.37310748452438958 ) ) ;
#175904=CARTESIAN_POINT ( 'NONE',  ( -20.85882249326303040, 65.66751761918619934, -30.42826094061123854 ) ) ;
#175906=DIRECTION ( 'NONE',  ( 0.000000000000000000, 0.000000000000000000, 1.000000000000000000 ) ) ;
#175919=EDGE_LOOP ( 'NONE', ( #205215, #90763, #243576, #222266 ) ) ;
#175944=CARTESIAN_POINT ( 'NONE',  ( 23.14999999999999858, 76.00000000001165290, -69.52310748452431710 ) ) ;
#175946=DIRECTION ( 'NONE',  ( 0.000000000000000000, -7.086529944415893080E-15, 1.000000000000000000 ) ) ;
#175949=EDGE_LOOP ( 'NONE', ( #32984, #49725, #87898, #33191 ) ) ;
#175997=CIRCLE ( 'NONE', #192533, 11.80000000000000426 ) ;
#176001=EDGE_CURVE ( 'NONE', #136430, #41111, #70903, .T. ) ;
#176005=CIRCLE ( 'NONE', #105186, 0.6000000000000033085 ) ;
#176009=FACE_OUTER_BOUND ( 'NONE', #58205, .T. ) ;
#176010=CARTESIAN_POINT ( 'NONE',  ( -20.64999999999999858, 73.60000000001151932, -49.24772940728643533 ) ) ;
#176014=VECTOR ( 'NONE', #132521, 1000.000000000000000 ) ;
#176023=VERTEX_POINT ( 'NONE', #72174 ) ;
#176032=DIRECTION ( 'NONE',  ( 0.000000000000000000, 0.8068669527897009974, 0.5907332058517299478 ) ) ;
#176079=CARTESIAN_POINT ( 'NONE',  ( 18.50016250449482413, 65.70233904877068198, -30.54874109119651848 ) ) ;
#176087=CARTESIAN_POINT ( 'NONE',  ( 21.11927991906888025, 69.55150688152023974, -69.53219116399826305 ) ) ;
#176110=CARTESIAN_POINT ( 'NONE',  ( -21.05000000000000071, 76.00000000001139711, -32.02310748452432421 ) ) ;
#176159=CARTESIAN_POINT ( 'NONE',  ( -18.44362607810620958, 85.49049615809643399, -62.46515361767715291 ) ) ;
#176190=CIRCLE ( 'NONE', #63739, 0.6000000000000033085 ) ;
#176232=VERTEX_POINT ( 'NONE', #257154 ) ;
#176258=TOROIDAL_SURFACE ( 'NONE', #247134, 0.2000000000000000111, 0.1000000000000000056 ) ;
#176270=ORIENTED_EDGE ( 'NONE', *, *, #216228, .T. ) ;
#176324=ADVANCED_FACE ( 'NONE', ( #17799 ), #87566, .T. ) ;
#176368=AXIS2_PLACEMENT_3D ( 'NONE', #182183, #3521, #29550 ) ;
#176407=AXIS2_PLACEMENT_3D ( 'NONE', #169750, #49758, #71908 ) ;
#176421=ORIENTED_EDGE ( 'NONE', *, *, #108436, .T. ) ;
#176423=ORIENTED_EDGE ( 'NONE', *, *, #207560, .F. ) ;
#176443=ORIENTED_EDGE ( 'NONE', *, *, #87426, .F. ) ;
#176457=CIRCLE ( 'NONE', #64012, 0.1000000000000011990 ) ;
#176487=CARTESIAN_POINT ( 'NONE',  ( -18.42609945526418258, 85.49999971050182523, -62.52374499427813959 ) ) ;
#176506=ORIENTED_EDGE ( 'NONE', *, *, #77597, .F. ) ;
#176512=ORIENTED_EDGE ( 'NONE', *, *, #195180, .F. ) ;
#176519=CARTESIAN_POINT ( 'NONE',  ( 22.24259225415828567, 75.90093411655887223, -77.01504535508973959 ) ) ;
#176547=VERTEX_POINT ( 'NONE', #177592 ) ;
#176556=EDGE_LOOP ( 'NONE', ( #212743, #209323, #195811, #99916 ) ) ;
#176560=ADVANCED_FACE ( 'NONE', ( #194579 ), #121594, .T. ) ;
#176600=DIRECTION ( 'NONE',  ( 0.7071067811865474617, -0.7071067811865474617, -5.142139384388980375E-15 ) ) ;
#176611=CARTESIAN_POINT ( 'NONE',  ( -22.39999999999999858, 64.35000000001166143, -69.42310748452440805 ) ) ;
#176618=( BOUNDED_SURFACE ( )  B_SPLINE_SURFACE ( 3, 2, ( 
 ( #35081, #93726, #175851 ),
 ( #257879, #36344, #194136 ),
 ( #54593, #79274, #115862 ),
 ( #158858, #14218, #18035 ) ),
 .UNSPECIFIED., .F., .F., .F. ) 
 B_SPLINE_SURFACE_WITH_KNOTS ( ( 4, 4 ),
 ( 3, 3 ),
 ( 0.0006461284895273902403, 0.0007503702773986316125 ),
 ( 0.000000000000000000, 1.000000000000000000 ),
 .UNSPECIFIED. ) 
 GEOMETRIC_REPRESENTATION_ITEM ( )  RATIONAL_B_SPLINE_SURFACE ( (
 ( 1.000000000000000000, 0.7071067811865475727, 1.000000000000000000),
 ( 1.000000000000000000, 0.7076476444648814867, 1.000000000000000000),
 ( 1.000000000000000000, 0.7075727925191590550, 1.000000000000000000),
 ( 1.000000000000000000, 0.7071067811865581199, 1.000000000000000000) ) ) 
 REPRESENTATION_ITEM ( '' )  SURFACE ( )  );
#176632=ORIENTED_EDGE ( 'NONE', *, *, #188036, .T. ) ;
#176638=LINE ( 'NONE', #140034, #113020 ) ;
#176650=DIRECTION ( 'NONE',  ( 1.000000000000000000, -0.000000000000000000, 0.000000000000000000 ) ) ;
#176715=FACE_OUTER_BOUND ( 'NONE', #38503, .T. ) ;
#176717=DIRECTION ( 'NONE',  ( -0.000000000000000000, 1.000000000000000000, 6.352154140967427193E-15 ) ) ;
#176770=AXIS2_PLACEMENT_3D ( 'NONE', #157493, #83012, #179606 ) ;
#176779=VERTEX_POINT ( 'NONE', #209970 ) ;
#176813=CARTESIAN_POINT ( 'NONE',  ( 20.94999999999999929, 76.00000000001145395, -40.12310748452431852 ) ) ;
#176838=ORIENTED_EDGE ( 'NONE', *, *, #6940, .T. ) ;
#176857=ORIENTED_EDGE ( 'NONE', *, *, #96078, .F. ) ;
#176883=AXIS2_PLACEMENT_3D ( 'NONE', #75, #44365, #118768 ) ;
#176896=CIRCLE ( 'NONE', #110232, 0.1000000000000028644 ) ;
#176926=CARTESIAN_POINT ( 'NONE',  ( -23.15000000000000213, 64.25000000001158185, -57.37310748452440379 ) ) ;
#176951=VECTOR ( 'NONE', #241558, 1000.000000000000000 ) ;
#176961=CARTESIAN_POINT ( 'NONE',  ( 23.24999999999999645, 76.00000000001165290, -69.52310748452431710 ) ) ;
#176966=CARTESIAN_POINT ( 'NONE',  ( -20.54999999999999716, 85.00000000001159606, -59.62913836187181715 ) ) ;
#176973=EDGE_LOOP ( 'NONE', ( #249896, #75176, #44578, #15737 ) ) ;
#176976=DIRECTION ( 'NONE',  ( -1.000000000000000000, -0.000000000000000000, -0.000000000000000000 ) ) ;
#176994=ADVANCED_FACE ( 'NONE', ( #16904 ), #6732, .F. ) ;
#177015=ADVANCED_FACE ( 'NONE', ( #160284 ), #241096, .F. ) ;
#177039=DIRECTION ( 'NONE',  ( -1.000000000000000000, -0.000000000000000000, -0.000000000000000000 ) ) ;
#177076=EDGE_CURVE ( 'NONE', #239074, #154564, #100246, .T. ) ;
#177093=CARTESIAN_POINT ( 'NONE',  ( -21.05000000000000071, 64.36312671090715298, -62.70134827119954934 ) ) ;
#177101=ADVANCED_FACE ( 'NONE', ( #161558 ), #19466, .F. ) ;
#177102=VECTOR ( 'NONE', #102578, 1000.000000000000000 ) ;
#177164=ORIENTED_EDGE ( 'NONE', *, *, #246360, .F. ) ;
#177184=ORIENTED_EDGE ( 'NONE', *, *, #130371, .T. ) ;
#177198=AXIS2_PLACEMENT_3D ( 'NONE', #82883, #106313, #127193 ) ;
#177216=LINE ( 'NONE', #237166, #172994 ) ;
#177244=CIRCLE ( 'NONE', #210532, 0.09999999999999520384 ) ;
#177255=CARTESIAN_POINT ( 'NONE',  ( -20.64999999999999858, 74.00000000001151079, -48.74772940728643533 ) ) ;
#177288=DIRECTION ( 'NONE',  ( 0.000000000000000000, 1.000000000000000000, 6.982962677686266711E-15 ) ) ;
#177291=VECTOR ( 'NONE', #84424, 1000.000000000000000 ) ;
#177296=DIRECTION ( 'NONE',  ( 0.000000000000000000, -3.469446951953635015E-14, 1.000000000000000000 ) ) ;
#177299=DIRECTION ( 'NONE',  ( -1.000000000000000000, -0.000000000000000000, -0.000000000000000000 ) ) ;
#177301=AXIS2_PLACEMENT_3D ( 'NONE', #88798, #247894, #69278 ) ;
#177334=DIRECTION ( 'NONE',  ( 1.000000000000000000, 0.000000000000000000, 0.000000000000000000 ) ) ;
#177335=ORIENTED_EDGE ( 'NONE', *, *, #160699, .T. ) ;
#177367=CARTESIAN_POINT ( 'NONE',  ( 18.57399277249656322, 65.66887361445283489, -30.43298459182692639 ) ) ;
#177369=ORIENTED_EDGE ( 'NONE', *, *, #15029, .T. ) ;
#177399=DIRECTION ( 'NONE',  ( 1.000000000000000000, 0.000000000000000000, -0.000000000000000000 ) ) ;
#177492=EDGE_CURVE ( 'NONE', #139895, #116521, #65510, .T. ) ;
#177501=VERTEX_POINT ( 'NONE', #245907 ) ;
#177548=FACE_OUTER_BOUND ( 'NONE', #223411, .T. ) ;
#177589=CARTESIAN_POINT ( 'NONE',  ( -21.55000000000000426, 68.29142135624881860, -48.37310748452437537 ) ) ;
#177592=CARTESIAN_POINT ( 'NONE',  ( -23.15000000000000213, 85.00000000001149658, -45.41707660717669626 ) ) ;
#177618=CIRCLE ( 'NONE', #90076, 0.09999999999999976963 ) ;
#177621=EDGE_CURVE ( 'NONE', #121432, #211306, #157311, .T. ) ;
#177629=CIRCLE ( 'NONE', #73575, 0.1000000000000009492 ) ;
#177632=VECTOR ( 'NONE', #55208, 1000.000000000000000 ) ;
#177661=VERTEX_POINT ( 'NONE', #114075 ) ;
#177676=DIRECTION ( 'NONE',  ( 0.000000000000000000, -6.982962677686266711E-15, 1.000000000000000000 ) ) ;
#177678=DIRECTION ( 'NONE',  ( 0.000000000000000000, 0.000000000000000000, 1.000000000000000000 ) ) ;
#177695=ADVANCED_FACE ( 'NONE', ( #69851 ), #153254, .F. ) ;
#177701=AXIS2_PLACEMENT_3D ( 'NONE', #174979, #30296, #109805 ) ;
#177728=EDGE_CURVE ( 'NONE', #185953, #224921, #78787, .T. ) ;
#177732=FACE_OUTER_BOUND ( 'NONE', #221377, .T. ) ;
#177733=VERTEX_POINT ( 'NONE', #102188 ) ;
#177737=EDGE_LOOP ( 'NONE', ( #153452, #223985, #6230 ) ) ;
#177740=AXIS2_PLACEMENT_3D ( 'NONE', #157395, #195231, #255115 ) ;
#177768=EDGE_CURVE ( 'NONE', #60425, #95061, #32428, .T. ) ;
#177800=ORIENTED_EDGE ( 'NONE', *, *, #197010, .T. ) ;
#177806=VERTEX_POINT ( 'NONE', #254823 ) ;
#177846=CARTESIAN_POINT ( 'NONE',  ( -21.07928932188134041, 76.00000000001165290, -69.52310748452431710 ) ) ;
#177848=DIRECTION ( 'NONE',  ( 0.000000000000000000, -6.938893903907222067E-15, 1.000000000000000000 ) ) ;
#177884=DIRECTION ( 'NONE',  ( -1.000000000000000000, 0.000000000000000000, -0.000000000000000000 ) ) ;
#177908=ADVANCED_FACE ( 'NONE', ( #29159 ), #48600, .F. ) ;
#177918=AXIS2_PLACEMENT_3D ( 'NONE', #37262, #196304, #33431 ) ;
#177930=ORIENTED_EDGE ( 'NONE', *, *, #71271, .T. ) ;
#177944=ORIENTED_EDGE ( 'NONE', *, *, #57762, .T. ) ;
#177983=AXIS2_PLACEMENT_3D ( 'NONE', #138352, #178827, #217890 ) ;
#177996=CARTESIAN_POINT ( 'NONE',  ( 20.94999999999999574, 87.41227409416133298, -66.62310748452424036 ) ) ;
#178006=ORIENTED_EDGE ( 'NONE', *, *, #68505, .F. ) ;
#178009=DIRECTION ( 'NONE',  ( 0.000000000000000000, 1.000000000000000000, 6.982962677686266711E-15 ) ) ;
#178026=DIRECTION ( 'NONE',  ( -7.304098846217948299E-16, -1.000000000000000000, 0.000000000000000000 ) ) ;
#178053=AXIS2_PLACEMENT_3D ( 'NONE', #10930, #108731, #69620 ) ;
#178060=CARTESIAN_POINT ( 'NONE',  ( 23.14999999999999503, 61.95000000001146390, -41.53680255528533394 ) ) ;
#178062=ORIENTED_EDGE ( 'NONE', *, *, #251837, .T. ) ;
#178073=LINE ( 'NONE', #209165, #156461 ) ;
#178079=AXIS2_PLACEMENT_3D ( 'NONE', #48014, #108002, #198431 ) ;
#178085=EDGE_CURVE ( 'NONE', #8900, #196464, #117633, .T. ) ;
#178108=ORIENTED_EDGE ( 'NONE', *, *, #85473, .T. ) ;
#178109=DIRECTION ( 'NONE',  ( 1.000000000000000000, 0.000000000000000000, 0.000000000000000000 ) ) ;
#178118=DIRECTION ( 'NONE',  ( 0.000000000000000000, -0.7397360091702823714, 0.6728971962616756564 ) ) ;
#178128=DIRECTION ( 'NONE',  ( 1.000000000000000000, 0.000000000000000000, 0.000000000000000000 ) ) ;
#178132=EDGE_CURVE ( 'NONE', #117921, #51613, #238246, .T. ) ;
#178149=EDGE_LOOP ( 'NONE', ( #134761, #30216, #52438, #45679 ) ) ;
#178184=AXIS2_PLACEMENT_3D ( 'NONE', #242971, #163449, #86439 ) ;
#178193=CARTESIAN_POINT ( 'NONE',  ( 18.59999999999999076, 64.25000000001148237, -44.67310748452440095 ) ) ;
#178198=ORIENTED_EDGE ( 'NONE', *, *, #153013, .F. ) ;
#178205=CARTESIAN_POINT ( 'NONE',  ( 23.14999999999999503, 64.35000000001146248, -43.03791325517834565 ) ) ;
#178236=VERTEX_POINT ( 'NONE', #207132 ) ;
#178242=CARTESIAN_POINT ( 'NONE',  ( 18.39999999999999858, 85.60000000001137721, -29.42291809330221142 ) ) ;
#178315=CIRCLE ( 'NONE', #211618, 4.150000000000001243 ) ;
#178335=CIRCLE ( 'NONE', #99171, 0.1000000000000028644 ) ;
#178350=CIRCLE ( 'NONE', #119921, 0.1999999999999987899 ) ;
#178388=CARTESIAN_POINT ( 'NONE',  ( 20.94999999999999574, 65.52661458509869874, -61.94445302027585143 ) ) ;
#178389=VECTOR ( 'NONE', #154824, 1000.000000000000000 ) ;
#178397=CIRCLE ( 'NONE', #182485, 0.1000000000000028644 ) ;
#178423=VERTEX_POINT ( 'NONE', #96137 ) ;
#178434=VERTEX_POINT ( 'NONE', #2170 ) ;
#178436=CARTESIAN_POINT ( 'NONE',  ( 23.14999999999999858, 76.00000000001142553, -36.02310748452432421 ) ) ;
#178456=CIRCLE ( 'NONE', #36821, 0.1000000000000028644 ) ;
#178465=EDGE_LOOP ( 'NONE', ( #248644, #14959, #114646, #20698 ) ) ;
#178473=CIRCLE ( 'NONE', #224410, 0.09999999999999939493 ) ;
#178496=AXIS2_PLACEMENT_3D ( 'NONE', #122102, #201625, #26874 ) ;
#178512=CARTESIAN_POINT ( 'NONE',  ( -23.25000000000000000, 76.00000000001142553, -36.02310748452432421 ) ) ;
#178527=CARTESIAN_POINT ( 'NONE',  ( 18.59999999999999432, 77.86671491006887891, -57.77043223824230722 ) ) ;
#178536=LINE ( 'NONE', #80664, #252144 ) ;
#178554=CARTESIAN_POINT ( 'NONE',  ( -22.60000000000080789, 75.95218301954636786, -81.27312991567707456 ) ) ;
#178559=DIRECTION ( 'NONE',  ( 0.000000000000000000, -6.938893903907222067E-15, 1.000000000000000000 ) ) ;
#178565=DIRECTION ( 'NONE',  ( -1.000000000000000000, 0.000000000000000000, -0.000000000000000000 ) ) ;
#178570=CARTESIAN_POINT ( 'NONE',  ( 21.05000000000000071, 65.27628289530404970, -57.37310748452439668 ) ) ;
#178579=EDGE_LOOP ( 'NONE', ( #73495, #80727, #10670, #181417, #152255 ) ) ;
#178581=CARTESIAN_POINT ( 'NONE',  ( -21.14999999999999858, 64.35000000001166143, -69.42310748452440805 ) ) ;
#178647=AXIS2_PLACEMENT_3D ( 'NONE', #82242, #79691, #216650 ) ;
#178671=EDGE_LOOP ( 'NONE', ( #139311, #1336, #50640, #234798, #7596 ) ) ;
#178691=CARTESIAN_POINT ( 'NONE',  ( -23.15000000000000213, 76.00000000001165290, -69.52310748452431710 ) ) ;
#178699=CIRCLE ( 'NONE', #241220, 0.5000000000000004441 ) ;
#178768=DIRECTION ( 'NONE',  ( 1.000000000000000000, -0.000000000000000000, 0.000000000000000000 ) ) ;
#178808=DIRECTION ( 'NONE',  ( 0.000000000000000000, -8.717686153663073805E-15, 1.000000000000000000 ) ) ;
#178818=VERTEX_POINT ( 'NONE', #174150 ) ;
#178827=DIRECTION ( 'NONE',  ( 0.000000000000000000, -1.000000000000000000, -6.982962677686265922E-15 ) ) ;
#178839=AXIS2_PLACEMENT_3D ( 'NONE', #104457, #86175, #4099 ) ;
#178854=EDGE_CURVE ( 'NONE', #40625, #96347, #134942, .T. ) ;
#178894=DIRECTION ( 'NONE',  ( 0.000000000000000000, 1.000000000000000000, 6.982962677686266711E-15 ) ) ;
#178915=CYLINDRICAL_SURFACE ( 'NONE', #37959, 0.09999999999999939493 ) ;
#178961=LINE ( 'NONE', #62823, #118570 ) ;
#178994=EDGE_LOOP ( 'NONE', ( #132822, #118524, #254793, #99530 ) ) ;
#178998=EDGE_CURVE ( 'NONE', #2004, #13565, #182418, .T. ) ;
#179002=CARTESIAN_POINT ( 'NONE',  ( 18.49999999999999289, 65.79142135624880439, -48.17310748452439384 ) ) ;
#179016=LINE ( 'NONE', #57727, #100014 ) ;
#179076=LINE ( 'NONE', #79903, #51458 ) ;
#179107=EDGE_CURVE ( 'NONE', #50215, #159227, #195072, .T. ) ;
#179151=LINE ( 'NONE', #257311, #198846 ) ;
#179199=DIRECTION ( 'NONE',  ( 1.000000000000000000, -3.265361837132813093E-16, -2.280189983783949500E-30 ) ) ;
#179203=CYLINDRICAL_SURFACE ( 'NONE', #73674, 0.09999999999999939493 ) ;
#179213=CARTESIAN_POINT ( 'NONE',  ( 18.60000000000000497, 76.00000000001165290, -69.52310748452431710 ) ) ;
#179218=LINE ( 'NONE', #155804, #187277 ) ;
#179223=CARTESIAN_POINT ( 'NONE',  ( -20.64999999999999858, 68.85000000001151932, -48.37310748452436826 ) ) ;
#179248=CARTESIAN_POINT ( 'NONE',  ( -20.54999999999999716, 71.65000000001151648, -48.37310748452435405 ) ) ;
#179250=CIRCLE ( 'NONE', #150203, 0.1000000000000028644 ) ;
#179264=AXIS2_PLACEMENT_3D ( 'NONE', #8283, #68248, #147793 ) ;
#179272=CARTESIAN_POINT ( 'NONE',  ( 21.04999999999998650, 69.35000000001156195, -57.27310748452436684 ) ) ;
#179289=EDGE_CURVE ( 'NONE', #118763, #98142, #115950, .T. ) ;
#179302=CARTESIAN_POINT ( 'NONE',  ( 18.49999999999998934, 69.45000000001149942, -48.27310748452436684 ) ) ;
#179316=CARTESIAN_POINT ( 'NONE',  ( -20.85000000000000142, 76.00000000001142553, -36.02310748452432421 ) ) ;
#179337=DIRECTION ( 'NONE',  ( 2.952720810173289112E-16, 1.000000000000000000, 6.982962677686266711E-15 ) ) ;
#179344=DIRECTION ( 'NONE',  ( 0.000000000000000000, 0.000000000000000000, -1.000000000000000000 ) ) ;
#179363=CIRCLE ( 'NONE', #166913, 0.1000000000000060146 ) ;
#179383=CARTESIAN_POINT ( 'NONE',  ( 22.39999999999999503, 64.35000000001164722, -69.52310748452438816 ) ) ;
#179385=CARTESIAN_POINT ( 'NONE',  ( 20.94999999999999929, 77.34915357198741503, -28.23561014893443044 ) ) ;
#179390=ADVANCED_FACE ( 'NONE', ( #23749 ), #95092, .T. ) ;
#179412=ORIENTED_EDGE ( 'NONE', *, *, #169208, .T. ) ;
#179418=ORIENTED_EDGE ( 'NONE', *, *, #26784, .F. ) ;
#179423=CARTESIAN_POINT ( 'NONE',  ( 20.94999999999999929, 77.36242903720467723, -28.13422623660311217 ) ) ;
#179435=ORIENTED_EDGE ( 'NONE', *, *, #204222, .T. ) ;
#179445=DIRECTION ( 'NONE',  ( 1.000000000000000000, 0.000000000000000000, 0.000000000000000000 ) ) ;
#179459=ORIENTED_EDGE ( 'NONE', *, *, #232758, .T. ) ;
#179493=DIRECTION ( 'NONE',  ( 0.000000000000000000, 0.000000000000000000, 1.000000000000000000 ) ) ;
#179498=AXIS2_PLACEMENT_3D ( 'NONE', #185906, #67243, #8565 ) ;
#179525=DIRECTION ( 'NONE',  ( 1.000000000000000000, 0.000000000000000000, 0.000000000000000000 ) ) ;
#179574=CARTESIAN_POINT ( 'NONE',  ( 20.54374330479327426, 65.49498968578859603, -61.79742384963523705 ) ) ;
#179606=DIRECTION ( 'NONE',  ( 0.7071067811865127117, 0.7071067811865821007, 0.000000000000000000 ) ) ;
#179635=EDGE_LOOP ( 'NONE', ( #93085, #163710, #232061, #195500 ) ) ;
#179672=DIRECTION ( 'NONE',  ( -1.000000000000000000, 0.000000000000000000, -0.000000000000000000 ) ) ;
#179709=FACE_BOUND ( 'NONE', #247621, .T. ) ;
#179727=VERTEX_POINT ( 'NONE', #128793 ) ;
#179731=CARTESIAN_POINT ( 'NONE',  ( -20.94999999999999929, 77.36087058720364951, -61.45010955743335046 ) ) ;
#179749=DIRECTION ( 'NONE',  ( 0.000000000000000000, 0.8660254037844377084, 0.5000000000000015543 ) ) ;
#179756=ORIENTED_EDGE ( 'NONE', *, *, #257013, .T. ) ;
#179808=CARTESIAN_POINT ( 'NONE',  ( 20.04142135623730070, 64.25000000001173817, -81.27310748452440237 ) ) ;
#179818=VECTOR ( 'NONE', #230890, 1000.000000000000000 ) ;
#179839=CARTESIAN_POINT ( 'NONE',  ( -23.15000000000000213, 87.48912529308749697, -39.12310748452424747 ) ) ;
#179912=AXIS2_PLACEMENT_3D ( 'NONE', #76279, #157138, #217064 ) ;
#179926=DIRECTION ( 'NONE',  ( 0.000000000000000000, 0.000000000000000000, 1.000000000000000000 ) ) ;
#179937=CARTESIAN_POINT ( 'NONE',  ( 18.31325810956384359, 85.53638847601837369, -29.15466727821959836 ) ) ;
#179957=ORIENTED_EDGE ( 'NONE', *, *, #75939, .T. ) ;
#179960=ORIENTED_EDGE ( 'NONE', *, *, #43630, .F. ) ;
#179965=ORIENTED_EDGE ( 'NONE', *, *, #78665, .F. ) ;
#180000=DIRECTION ( 'NONE',  ( 1.000000000000000000, 0.000000000000000000, 0.000000000000000000 ) ) ;
#180056=FACE_OUTER_BOUND ( 'NONE', #208890, .T. ) ;
#180062=EDGE_CURVE ( 'NONE', #102074, #161516, #20470, .T. ) ;
#180086=CARTESIAN_POINT ( 'NONE',  ( 23.15000000000000213, 87.48912529308749697, -39.12310748452424747 ) ) ;
#180110=EDGE_CURVE ( 'NONE', #209328, #255664, #249592, .T. ) ;
#180118=DIRECTION ( 'NONE',  ( 1.000000000000000000, 0.000000000000000000, 0.000000000000000000 ) ) ;
#180137=CYLINDRICAL_SURFACE ( 'NONE', #75282, 2.000000000000001776 ) ;
#180149=DIRECTION ( 'NONE',  ( 0.000000000000000000, -7.086529944415894657E-15, 1.000000000000000000 ) ) ;
#180152=VECTOR ( 'NONE', #120838, 1000.000000000000000 ) ;
#180171=ORIENTED_EDGE ( 'NONE', *, *, #18411, .T. ) ;
#180182=TOROIDAL_SURFACE ( 'NONE', #121914, 0.2000000000000000111, 0.1000000000000000056 ) ;
#180211=ADVANCED_FACE ( 'NONE', ( #241681 ), #63030, .F. ) ;
#180235=CARTESIAN_POINT ( 'NONE',  ( -20.94999999999999929, 87.48912529308769592, -66.42310748452423752 ) ) ;
#180247=DIRECTION ( 'NONE',  ( 0.000000000000000000, 0.000000000000000000, 1.000000000000000000 ) ) ;
#180254=DIRECTION ( 'NONE',  ( 0.000000000000000000, -6.467318590049456648E-15, 1.000000000000000000 ) ) ;
#180257=CARTESIAN_POINT ( 'NONE',  ( -20.94999999999999929, 87.75000000001163869, -66.62310748452424036 ) ) ;
#180301=CARTESIAN_POINT ( 'NONE',  ( 20.95512828230159030, 67.12384868768627655, -57.32067721902129875 ) ) ;
#180311=CIRCLE ( 'NONE', #117935, 6.329289321881356400 ) ;
#180371=CARTESIAN_POINT ( 'NONE',  ( 21.05000000000000071, 67.12338541492449906, -61.13802700567970305 ) ) ;
#180397=ORIENTED_EDGE ( 'NONE', *, *, #147890, .F. ) ;
#180429=ORIENTED_EDGE ( 'NONE', *, *, #228070, .F. ) ;
#180435=LINE ( 'NONE', #139997, #201877 ) ;
#180454=EDGE_LOOP ( 'NONE', ( #28406, #158324, #223487, #26062 ) ) ;
#180456=ORIENTED_EDGE ( 'NONE', *, *, #116803, .T. ) ;
#180490=LINE ( 'NONE', #77499, #147989 ) ;
#180491=VERTEX_POINT ( 'NONE', #159301 ) ;
#180519=ADVANCED_FACE ( 'NONE', ( #221789 ), #145518, .F. ) ;
#180531=CARTESIAN_POINT ( 'NONE',  ( -21.55000000000000426, 68.25000000001151079, -48.27310748452437394 ) ) ;
#180571=DIRECTION ( 'NONE',  ( 0.000000000000000000, 1.000000000000000000, 6.938893903907222067E-15 ) ) ;
#180605=DIRECTION ( 'NONE',  ( 0.000000000000000000, -0.4999999999999689138, -0.8660254037844565822 ) ) ;
#180698=CARTESIAN_POINT ( 'NONE',  ( 19.92426406871192412, 64.25000000001148237, -44.67310748452439384 ) ) ;
#180710=ORIENTED_EDGE ( 'NONE', *, *, #181470, .F. ) ;
#180718=FACE_OUTER_BOUND ( 'NONE', #24884, .T. ) ;
#180734=VERTEX_POINT ( 'NONE', #178570 ) ;
#180771=DIRECTION ( 'NONE',  ( 1.000000000000000000, 0.000000000000000000, 0.000000000000000000 ) ) ;
#180788=DIRECTION ( 'NONE',  ( 0.000000000000000000, 1.000000000000000000, 6.688090509790097607E-15 ) ) ;
#180811=ORIENTED_EDGE ( 'NONE', *, *, #231423, .T. ) ;
#180842=DIRECTION ( 'NONE',  ( -1.000000000000000000, 0.000000000000000000, -0.000000000000000000 ) ) ;
#180847=CARTESIAN_POINT ( 'NONE',  ( 20.97217846901851956, 67.12455827530190788, -61.02187980058715766 ) ) ;
#180851=CIRCLE ( 'NONE', #97417, 0.09999999999999939493 ) ;
#180877=CYLINDRICAL_SURFACE ( 'NONE', #176770, 0.1000000000000026007 ) ;
#180883=AXIS2_PLACEMENT_3D ( 'NONE', #230090, #110140, #16206 ) ;
#180962=LINE ( 'NONE', #66141, #65035 ) ;
#180963=CIRCLE ( 'NONE', #22767, 0.1000000000000028644 ) ;
#180972=CARTESIAN_POINT ( 'NONE',  ( -23.15000000000000213, 76.00000000001143974, -38.12310748452432563 ) ) ;
#181026=CARTESIAN_POINT ( 'NONE',  ( -20.87600722750343252, 65.66887361445283489, -30.43298459182692994 ) ) ;
#181033=EDGE_CURVE ( 'NONE', #110576, #101690, #133432, .T. ) ;
#181040=ORIENTED_EDGE ( 'NONE', *, *, #241356, .T. ) ;
#181060=CARTESIAN_POINT ( 'NONE',  ( 21.14999999999999503, 64.25000000001165290, -69.52310748452438816 ) ) ;
#181077=CARTESIAN_POINT ( 'NONE',  ( -20.94999999999999929, 77.83534155023598089, -57.96795619196132776 ) ) ;
#181121=ORIENTED_EDGE ( 'NONE', *, *, #184429, .F. ) ;
#181198=DIRECTION ( 'NONE',  ( 0.000000000000000000, 0.000000000000000000, -1.000000000000000000 ) ) ;
#181203=CARTESIAN_POINT ( 'NONE',  ( 23.14999999999999858, 87.75000000001173817, -81.27310748452423184 ) ) ;
#181228=CARTESIAN_POINT ( 'NONE',  ( 18.52326479938716020, 85.64236444492679823, -29.30835007111852875 ) ) ;
#181273=DIRECTION ( 'NONE',  ( 0.000000000000000000, -7.086529944415894657E-15, 1.000000000000000000 ) ) ;
#181276=EDGE_CURVE ( 'NONE', #14606, #92669, #91896, .T. ) ;
#181320=VERTEX_POINT ( 'NONE', #245585 ) ;
#181342=ORIENTED_EDGE ( 'NONE', *, *, #217354, .F. ) ;
#181371=CIRCLE ( 'NONE', #43790, 0.1000000000000028644 ) ;
#181394=ORIENTED_EDGE ( 'NONE', *, *, #15598, .F. ) ;
#181406=CARTESIAN_POINT ( 'NONE',  ( -18.50000000000000000, 74.65925378207803931, -79.79596998994550461 ) ) ;
#181417=ORIENTED_EDGE ( 'NONE', *, *, #205291, .F. ) ;
#181434=DIRECTION ( 'NONE',  ( 0.000000000000000000, 0.000000000000000000, 1.000000000000000000 ) ) ;
#181441=FACE_OUTER_BOUND ( 'NONE', #5249, .T. ) ;
#181446=CARTESIAN_POINT ( 'NONE',  ( -21.05000000000000071, 70.10000000001149090, -46.24220724918073699 ) ) ;
#181449=EDGE_CURVE ( 'NONE', #64683, #92040, #229869, .T. ) ;
#181452=DIRECTION ( 'NONE',  ( 2.952720810173289112E-16, 1.000000000000000000, 6.982962677686266711E-15 ) ) ;
#181460=DIRECTION ( 'NONE',  ( 1.000000000000000000, 0.000000000000000000, 0.000000000000000000 ) ) ;
#181470=EDGE_CURVE ( 'NONE', #174912, #136430, #96169, .T. ) ;
#181503=CIRCLE ( 'NONE', #27404, 11.70000000000000284 ) ;
#181520=ADVANCED_FACE ( 'NONE', ( #156776 ), #178915, .T. ) ;
#181531=VERTEX_POINT ( 'NONE', #81037 ) ;
#181566=EDGE_LOOP ( 'NONE', ( #245184, #232405, #39520 ) ) ;
#181567=TOROIDAL_SURFACE ( 'NONE', #127374, 0.2000000000000000111, 0.1000000000000000056 ) ;
#181570=VECTOR ( 'NONE', #164483, 1000.000000000000000 ) ;
#181585=CARTESIAN_POINT ( 'NONE',  ( 18.59999999999998366, 68.97833521811131163, -32.18954208262707795 ) ) ;
#181586=VECTOR ( 'NONE', #127722, 1000.000000000000000 ) ;
#181595=ORIENTED_EDGE ( 'NONE', *, *, #40283, .F. ) ;
#181628=ORIENTED_EDGE ( 'NONE', *, *, #66029, .T. ) ;
#181653=CARTESIAN_POINT ( 'NONE',  ( -22.57320508075687115, 64.25000000001165290, -69.52310748452440237 ) ) ;
#181654=EDGE_LOOP ( 'NONE', ( #66828, #80122, #42526, #139911 ) ) ;
#181670=FACE_OUTER_BOUND ( 'NONE', #3081, .T. ) ;
#181675=CYLINDRICAL_SURFACE ( 'NONE', #164780, 0.09999999999999939493 ) ;
#181676=CARTESIAN_POINT ( 'NONE',  ( -18.59999999999999787, 68.97833521811131163, -32.18954208262707795 ) ) ;
#181678=ORIENTED_EDGE ( 'NONE', *, *, #151798, .T. ) ;
#181682=CIRCLE ( 'NONE', #40058, 4.049999999999998046 ) ;
#181697=DIRECTION ( 'NONE',  ( 0.000000000000000000, -1.000000000000000000, -6.982962677686265922E-15 ) ) ;
#181699=EDGE_LOOP ( 'NONE', ( #156706, #31735, #71955, #157803 ) ) ;
#181741=EDGE_LOOP ( 'NONE', ( #75324, #198766, #22863, #205006 ) ) ;
#181751=AXIS2_PLACEMENT_3D ( 'NONE', #146419, #83853, #23950 ) ;
#181755=ORIENTED_EDGE ( 'NONE', *, *, #226797, .T. ) ;
#181769=CARTESIAN_POINT ( 'NONE',  ( 18.39999999999999858, 85.68240343348777799, -29.36626410711146562 ) ) ;
#181806=CYLINDRICAL_SURFACE ( 'NONE', #59052, 0.1000000000000028644 ) ;
#181842=DIRECTION ( 'NONE',  ( -1.000000000000000000, 0.000000000000000000, -0.000000000000000000 ) ) ;
#181877=CIRCLE ( 'NONE', #27789, 0.2000000000000057288 ) ;
#181878=ORIENTED_EDGE ( 'NONE', *, *, #215424, .T. ) ;
#181881=AXIS2_PLACEMENT_3D ( 'NONE', #153714, #130224, #195372 ) ;
#181932=EDGE_LOOP ( 'NONE', ( #219138, #127564, #97020, #85079, #148552 ) ) ;
#181942=ORIENTED_EDGE ( 'NONE', *, *, #111090, .F. ) ;
#181997=DIRECTION ( 'NONE',  ( 1.000000000000000000, 0.000000000000000000, 0.000000000000000000 ) ) ;
#182018=ORIENTED_EDGE ( 'NONE', *, *, #40321, .T. ) ;
#182031=FACE_OUTER_BOUND ( 'NONE', #100456, .T. ) ;
#182033=FACE_OUTER_BOUND ( 'NONE', #147358, .T. ) ;
#182044=DIRECTION ( 'NONE',  ( 1.000000000000000000, 0.000000000000000000, 0.000000000000000000 ) ) ;
#182083=TOROIDAL_SURFACE ( 'NONE', #82082, 0.2000000000000000111, 0.1000000000000000056 ) ;
#182116=DIRECTION ( 'NONE',  ( 1.000000000000000000, 0.000000000000000000, 0.000000000000000000 ) ) ;
#182136=ADVANCED_FACE ( 'NONE', ( #190147 ), #169330, .T. ) ;
#182157=CARTESIAN_POINT ( 'NONE',  ( 22.39999999999999503, 76.00000000001170974, -77.31388708289769340 ) ) ;
#182170=EDGE_CURVE ( 'NONE', #86585, #206520, #204871, .T. ) ;
#182183=CARTESIAN_POINT ( 'NONE',  ( -20.64999999999999858, 71.65000000001155911, -57.17310748452435121 ) ) ;
#182202=CYLINDRICAL_SURFACE ( 'NONE', #51138, 4.049999999999998046 ) ;
#182237=CARTESIAN_POINT ( 'NONE',  ( 18.52928932304157073, 65.72071067696991520, -44.84685405172078987 ) ) ;
#182242=CARTESIAN_POINT ( 'NONE',  ( -23.25000000000000000, 71.65000000001155911, -57.37310748452435405 ) ) ;
#182247=CARTESIAN_POINT ( 'NONE',  ( 21.05000000000000071, 87.75000000001143974, -39.12310748452424747 ) ) ;
#182248=VECTOR ( 'NONE', #96175, 1000.000000000000000 ) ;
#182273=EDGE_LOOP ( 'NONE', ( #202336, #74280, #183869, #250991 ) ) ;
#182312=CARTESIAN_POINT ( 'NONE',  ( 18.52928932188133970, 65.72071067813016043, -48.17310748452439384 ) ) ;
#182316=CARTESIAN_POINT ( 'NONE',  ( -21.05000000000000071, 74.16465844978715438, -57.86795619196135476 ) ) ;
#182332=AXIS2_PLACEMENT_3D ( 'NONE', #240539, #202687, #43626 ) ;
#182346=CARTESIAN_POINT ( 'NONE',  ( 21.00000000000000000, 66.25000000001151079, -48.27310748452438816 ) ) ;
#182366=CARTESIAN_POINT ( 'NONE',  ( -23.15000000000000213, 87.65000000001144542, -39.12310748452424747 ) ) ;
#182381=ORIENTED_EDGE ( 'NONE', *, *, #65959, .T. ) ;
#182398=DIRECTION ( 'NONE',  ( -1.836970198721029934E-16, -1.000000000000000000, -6.982962677686266711E-15 ) ) ;
#182400=ORIENTED_EDGE ( 'NONE', *, *, #188301, .T. ) ;
#182415=SPHERICAL_SURFACE ( 'NONE', #31405, 0.1000000000000000056 ) ;
#182418=CIRCLE ( 'NONE', #132312, 11.65000000000000036 ) ;
#182430=VECTOR ( 'NONE', #240419, 1000.000000000000000 ) ;
#182442=CARTESIAN_POINT ( 'NONE',  ( -22.47071067811865319, 75.90090754530910999, -77.24318222902238062 ) ) ;
#182454=VERTEX_POINT ( 'NONE', #184674 ) ;
#182485=AXIS2_PLACEMENT_3D ( 'NONE', #13142, #110946, #108385 ) ;
#182500=EDGE_CURVE ( 'NONE', #178818, #97821, #54849, .T. ) ;
#182515=CARTESIAN_POINT ( 'NONE',  ( 18.49362639424906263, 85.44260436789944890, -29.25866655101286185 ) ) ;
#182522=CARTESIAN_POINT ( 'NONE',  ( -21.53752568617669994, 69.21319212550778843, -69.62208194579494602 ) ) ;
#182533=ORIENTED_EDGE ( 'NONE', *, *, #62307, .T. ) ;
#182535=EDGE_LOOP ( 'NONE', ( #152068, #211211, #86229, #54173 ) ) ;
#182537=CARTESIAN_POINT ( 'NONE',  ( 18.39999999999999858, 85.51932773110404185, -62.55013110796492271 ) ) ;
#182545=DIRECTION ( 'NONE',  ( -1.000000000000000000, 2.952720810173289112E-16, 2.061873921506763405E-30 ) ) ;
#182554=ORIENTED_EDGE ( 'NONE', *, *, #229381, .F. ) ;
#182574=DIRECTION ( 'NONE',  ( -1.000000000000000000, 0.000000000000000000, 0.000000000000000000 ) ) ;
#182594=AXIS2_PLACEMENT_3D ( 'NONE', #6381, #242416, #125063 ) ;
#182644=ORIENTED_EDGE ( 'NONE', *, *, #238339, .F. ) ;
#182651=ORIENTED_EDGE ( 'NONE', *, *, #131821, .T. ) ;
#182669=AXIS2_PLACEMENT_3D ( 'NONE', #30147, #11873, #109647 ) ;
#182687=DIRECTION ( 'NONE',  ( 0.000000000000000000, 0.000000000000000000, 1.000000000000000000 ) ) ;
#182690=DIRECTION ( 'NONE',  ( 0.000000000000000000, 0.000000000000000000, 1.000000000000000000 ) ) ;
#182696=ORIENTED_EDGE ( 'NONE', *, *, #28142, .F. ) ;
#182718=VERTEX_POINT ( 'NONE', #232824 ) ;
#182741=VERTEX_POINT ( 'NONE', #55406 ) ;
#182747=CARTESIAN_POINT ( 'NONE',  ( -18.51024323315077424, 65.68895814178191017, -30.50265578621381124 ) ) ;
#182748=VECTOR ( 'NONE', #217451, 1000.000000000000000 ) ;
#182773=EDGE_CURVE ( 'NONE', #160725, #235880, #78837, .T. ) ;
#182789=VECTOR ( 'NONE', #196822, 1000.000000000000000 ) ;
#182823=ADVANCED_FACE ( 'NONE', ( #41044 ), #120578, .T. ) ;
#182846=AXIS2_PLACEMENT_3D ( 'NONE', #22115, #161632, #23411 ) ;
#182847=VERTEX_POINT ( 'NONE', #141394 ) ;
#182877=AXIS2_PLACEMENT_3D ( 'NONE', #215614, #232646, #115241 ) ;
#182889=CARTESIAN_POINT ( 'NONE',  ( 21.05000005001279817, 67.12872030824136971, -57.34515989627826826 ) ) ;
#182897=EDGE_LOOP ( 'NONE', ( #86357, #105238, #225743, #13423 ) ) ;
#182920=ORIENTED_EDGE ( 'NONE', *, *, #240506, .F. ) ;
#183008=DIRECTION ( 'NONE',  ( -1.000000000000000000, 2.952720810173289112E-16, 2.061873921506763405E-30 ) ) ;
#183060=CARTESIAN_POINT ( 'NONE',  ( 20.95265033839679347, 65.48774916754445030, -61.95734372849443616 ) ) ;
#183071=B_SPLINE_CURVE_WITH_KNOTS ( 'NONE', 3,
 ( #204491, #25887, #141957, #105364, #104096, #6290, #122410, #84507, #143238, #45434 ),
 .UNSPECIFIED., .F., .F.,
 ( 4, 3, 3, 4 ),
 ( 0.000000000000000000, 0.0002000000000002908468, 0.001000000000045115191, 0.001967863649472108723 ),
 .UNSPECIFIED. ) ;
#183084=CIRCLE ( 'NONE', #170658, 1.900000000000005906 ) ;
#183086=VECTOR ( 'NONE', #114684, 1000.000000000000000 ) ;
#183090=CARTESIAN_POINT ( 'NONE',  ( -23.15000000000000213, 85.00000000001159606, -60.12913836187181715 ) ) ;
#183091=EDGE_CURVE ( 'NONE', #251642, #207654, #6692, .T. ) ;
#183174=AXIS2_PLACEMENT_3D ( 'NONE', #77453, #177884, #13659 ) ;
#183178=CIRCLE ( 'NONE', #20694, 11.90000000000000746 ) ;
#183180=DIRECTION ( 'NONE',  ( 0.000000000000000000, -0.008583690987135041833, 0.9999631594459055250 ) ) ;
#183182=CARTESIAN_POINT ( 'NONE',  ( -20.64999999999999858, 76.00000000001142553, -36.02310748452432421 ) ) ;
#183196=DIRECTION ( 'NONE',  ( -1.000000000000000000, 2.952720810173289112E-16, 2.061873921506763405E-30 ) ) ;
#183209=ORIENTED_EDGE ( 'NONE', *, *, #71037, .T. ) ;
#183217=EDGE_CURVE ( 'NONE', #256296, #47933, #254542, .T. ) ;
#183235=FACE_OUTER_BOUND ( 'NONE', #124563, .T. ) ;
#183251=CARTESIAN_POINT ( 'NONE',  ( -23.15000000000000213, 85.60000000001159037, -59.62913836187181005 ) ) ;
#183255=CARTESIAN_POINT ( 'NONE',  ( -20.94999999999999929, 77.83534155023599510, -57.96795619196132776 ) ) ;
#183260=AXIS2_PLACEMENT_3D ( 'NONE', #132145, #13494, #112591 ) ;
#183296=ORIENTED_EDGE ( 'NONE', *, *, #117001, .F. ) ;
#183316=CARTESIAN_POINT ( 'NONE',  ( -21.14999999999999858, 64.25000000001165290, -69.42310748452440805 ) ) ;
#183342=ADVANCED_FACE ( 'NONE', ( #5915 ), #64621, .F. ) ;
#183363=CARTESIAN_POINT ( 'NONE',  ( -21.05000000000000071, 76.00000000001142553, -36.02310748452432421 ) ) ;
#183365=ORIENTED_EDGE ( 'NONE', *, *, #66843, .F. ) ;
#183412=AXIS2_PLACEMENT_3D ( 'NONE', #235930, #76856, #97683 ) ;
#183418=DIRECTION ( 'NONE',  ( 0.000000000000000000, 7.116814260417668513E-15, -1.000000000000000000 ) ) ;
#183449=AXIS2_PLACEMENT_3D ( 'NONE', #60177, #141023, #219253 ) ;
#183450=DIRECTION ( 'NONE',  ( 1.000000000000000000, 0.000000000000000000, 0.000000000000000000 ) ) ;
#183455=CIRCLE ( 'NONE', #79376, 0.09999999999999766020 ) ;
#183477=PRODUCT_DEFINITION_CONTEXT ( 'detailed design', #247326, 'design' ) ;
#183511=CARTESIAN_POINT ( 'NONE',  ( -22.39999999999999858, 76.00000000001170974, -77.31388708289772183 ) ) ;
#183515=ORIENTED_EDGE ( 'NONE', *, *, #65728, .T. ) ;
#183530=CARTESIAN_POINT ( 'NONE',  ( -23.15000000000000213, 87.65000000001144542, -39.12310748452424747 ) ) ;
#183584=CARTESIAN_POINT ( 'NONE',  ( 21.05000000000000071, 76.00000000001165290, -69.52310748452431710 ) ) ;
#183603=EDGE_CURVE ( 'NONE', #45697, #20936, #42368, .T. ) ;
#183617=ORIENTED_EDGE ( 'NONE', *, *, #230628, .T. ) ;
#183623=DIRECTION ( 'NONE',  ( 1.000000000000000000, 0.000000000000000000, 0.000000000000000000 ) ) ;
#183633=ADVANCED_FACE ( 'NONE', ( #238741 ), #60088, .F. ) ;
#183635=AXIS2_PLACEMENT_3D ( 'NONE', #87838, #67018, #124435 ) ;
#183648=FACE_OUTER_BOUND ( 'NONE', #112442, .T. ) ;
#183656=ADVANCED_FACE ( 'NONE', ( #140935 ), #77092, .T. ) ;
#183674=CARTESIAN_POINT ( 'NONE',  ( 21.05000000000000071, 70.50000000001151079, -48.42837350343745584 ) ) ;
#183735=LINE ( 'NONE', #160341, #230358 ) ;
#183773=CARTESIAN_POINT ( 'NONE',  ( -22.47071067811865319, 76.00000000001165290, -69.52310748452431710 ) ) ;
#183793=VERTEX_POINT ( 'NONE', #243866 ) ;
#183803=DIRECTION ( 'NONE',  ( -1.000000000000000000, -0.000000000000000000, -0.000000000000000000 ) ) ;
#183805=DIRECTION ( 'NONE',  ( 1.000000000000000000, -7.304098846218134667E-16, -5.100424963727255829E-30 ) ) ;
#183814=VERTEX_POINT ( 'NONE', #66530 ) ;
#183833=LINE ( 'NONE', #48166, #181586 ) ;
#183835=DIRECTION ( 'NONE',  ( -1.000000000000000000, 0.000000000000000000, -0.000000000000000000 ) ) ;
#183846=DIRECTION ( 'NONE',  ( 1.000000000000000000, 0.000000000000000000, 0.000000000000000000 ) ) ;
#183869=ORIENTED_EDGE ( 'NONE', *, *, #46107, .T. ) ;
#183881=VERTEX_POINT ( 'NONE', #130333 ) ;
#183914=EDGE_CURVE ( 'NONE', #26458, #208846, #250293, .T. ) ;
#183918=DIRECTION ( 'NONE',  ( 0.000000000000000000, 6.982962677686266711E-15, -1.000000000000000000 ) ) ;
#183947=CARTESIAN_POINT ( 'NONE',  ( 20.85000000000000142, 77.83585931145498193, -24.51866831572578320 ) ) ;
#183949=DIRECTION ( 'NONE',  ( 0.000000000000000000, 0.1350103645451807555, 0.9908441862701609093 ) ) ;
#183951=DIRECTION ( 'NONE',  ( 1.000000000000000000, 0.000000000000000000, 0.000000000000000000 ) ) ;
#183955=DIRECTION ( 'NONE',  ( 0.000000000000000000, -6.938893903907234689E-15, 1.000000000000000000 ) ) ;
#184000=DIRECTION ( 'NONE',  ( 0.000000000000000000, 1.000000000000000000, 6.352154140967427193E-15 ) ) ;
#184011=CARTESIAN_POINT ( 'NONE',  ( 21.03670563405601968, 65.37517631068334367, -57.19756059831524908 ) ) ;
#184028=VECTOR ( 'NONE', #116791, 1000.000000000000000 ) ;
#184036=CARTESIAN_POINT ( 'NONE',  ( -20.64999999999999858, 68.75000000001158185, -57.27310748452437394 ) ) ;
#184039=CARTESIAN_POINT ( 'NONE',  ( 22.50046968638157452, 75.95483015287189232, -81.27315263899684794 ) ) ;
#184055=ORIENTED_EDGE ( 'NONE', *, *, #29132, .F. ) ;
#184088=FACE_OUTER_BOUND ( 'NONE', #83897, .T. ) ;
#184095=DIRECTION ( 'NONE',  ( 0.000000000000000000, 1.000000000000000000, 0.000000000000000000 ) ) ;
#184121=CARTESIAN_POINT ( 'NONE',  ( 18.49999999999999645, 77.63717271298195044, -57.94095411905229298 ) ) ;
#184126=CARTESIAN_POINT ( 'NONE',  ( 21.05000000000000071, 69.65000000001158753, -59.67928539484124428 ) ) ;
#184128=AXIS2_PLACEMENT_3D ( 'NONE', #215524, #36935, #116443 ) ;
#184139=ORIENTED_EDGE ( 'NONE', *, *, #15148, .T. ) ;
#184141=LINE ( 'NONE', #83725, #256050 ) ;
#184171=EDGE_CURVE ( 'NONE', #244003, #88477, #92612, .T. ) ;
#184200=CARTESIAN_POINT ( 'NONE',  ( -22.50000000000000000, 64.35042919246686210, -69.62310748452439668 ) ) ;
#184256=EDGE_CURVE ( 'NONE', #183881, #100350, #63575, .T. ) ;
#184283=CARTESIAN_POINT ( 'NONE',  ( -23.15000000000000213, 76.00000000001165290, -69.52310748452431710 ) ) ;
#184288=PLANE ( 'NONE',  #199220 ) ;
#184289=DIRECTION ( 'NONE',  ( 0.000000000000000000, -0.2605042016806740079, 0.9654727137038698892 ) ) ;
#184296=ORIENTED_EDGE ( 'NONE', *, *, #205097, .F. ) ;
#184354=CARTESIAN_POINT ( 'NONE',  ( -21.08884785362073089, 75.95021690494498046, -75.88030085194994001 ) ) ;
#184390=DIRECTION ( 'NONE',  ( 0.000000000000000000, 1.000000000000000000, 7.272083257015735086E-15 ) ) ;
#184398=CARTESIAN_POINT ( 'NONE',  ( -23.15000000000000213, 76.00000000001142553, -36.02310748452432421 ) ) ;
#184428=DIRECTION ( 'NONE',  ( 0.000000000000000000, 0.000000000000000000, 1.000000000000000000 ) ) ;
#184429=EDGE_CURVE ( 'NONE', #101132, #197749, #234258, .T. ) ;
#184441=VERTEX_POINT ( 'NONE', #40916 ) ;
#184444=DIRECTION ( 'NONE',  ( 0.000000000000000000, -0.1568667991644355497, 0.9876197685951332295 ) ) ;
#184451=CYLINDRICAL_SURFACE ( 'NONE', #136352, 0.09999999999999976963 ) ;
#184457=AXIS2_PLACEMENT_3D ( 'NONE', #79719, #118890, #181434 ) ;
#184513=ORIENTED_EDGE ( 'NONE', *, *, #144629, .T. ) ;
#184521=EDGE_CURVE ( 'NONE', #142859, #62686, #217862, .T. ) ;
#184544=FACE_OUTER_BOUND ( 'NONE', #219102, .T. ) ;
#184551=CIRCLE ( 'NONE', #80468, 0.1000000000000028644 ) ;
#184573=CARTESIAN_POINT ( 'NONE',  ( 20.94999999999997442, 77.26327546522863088, -28.12124281777790813 ) ) ;
#184606=ORIENTED_EDGE ( 'NONE', *, *, #114180, .T. ) ;
#184607=DIRECTION ( 'NONE',  ( 0.000000000000000000, 0.1350103645451807555, 0.9908441862701609093 ) ) ;
#184631=CARTESIAN_POINT ( 'NONE',  ( -20.85000000000000142, 87.75000000001143974, -38.92310748452424463 ) ) ;
#184643=ORIENTED_EDGE ( 'NONE', *, *, #91212, .F. ) ;
#184667=CARTESIAN_POINT ( 'NONE',  ( -23.15000000000000213, 64.25000000001146816, -43.03791325517834565 ) ) ;
#184674=CARTESIAN_POINT ( 'NONE',  ( -21.05000000000000071, 87.65000000001165859, -69.52310748452424605 ) ) ;
#184681=CARTESIAN_POINT ( 'NONE',  ( -20.64999999999999858, 68.75000000001158185, -57.17310748452437252 ) ) ;
#184692=VECTOR ( 'NONE', #235105, 1000.000000000000000 ) ;
#184699=ORIENTED_EDGE ( 'NONE', *, *, #254633, .T. ) ;
#184701=DIRECTION ( 'NONE',  ( 1.000000000000000000, 0.000000000000000000, 0.000000000000000000 ) ) ;
#184750=AXIS2_PLACEMENT_3D ( 'NONE', #19382, #40252, #237144 ) ;
#184753=ORIENTED_EDGE ( 'NONE', *, *, #96704, .T. ) ;
#184773=EDGE_LOOP ( 'NONE', ( #229095, #250839, #104345, #57503, #43433, #165526, #15441, #4662 ) ) ;
#184774=ORIENTED_EDGE ( 'NONE', *, *, #220678, .F. ) ;
#184819=DIRECTION ( 'NONE',  ( -1.000000000000000000, -0.000000000000000000, -0.000000000000000000 ) ) ;
#184829=EDGE_CURVE ( 'NONE', #53002, #177501, #242828, .T. ) ;
#184854=DIRECTION ( 'NONE',  ( 1.000000000000000000, 0.000000000000000000, 0.000000000000000000 ) ) ;
#184865=CIRCLE ( 'NONE', #18281, 0.1000000000000028644 ) ;
#184868=EDGE_LOOP ( 'NONE', ( #63938, #144580, #77804, #43819 ) ) ;
#184870=DIRECTION ( 'NONE',  ( 0.000000000000000000, -6.982962677686266711E-15, 1.000000000000000000 ) ) ;
#184887=EDGE_LOOP ( 'NONE', ( #33643, #150286, #43150, #150477 ) ) ;
#184894=EDGE_CURVE ( 'NONE', #208477, #118994, #163908, .T. ) ;
#184897=EDGE_LOOP ( 'NONE', ( #253087, #22027, #156191, #216707 ) ) ;
#184918=EDGE_LOOP ( 'NONE', ( #65678, #197797, #52800, #184643 ) ) ;
#184923=ORIENTED_EDGE ( 'NONE', *, *, #211467, .F. ) ;
#184957=AXIS2_PLACEMENT_3D ( 'NONE', #196455, #157375, #60788 ) ;
#184990=DIRECTION ( 'NONE',  ( 0.000000000000000000, 0.000000000000000000, -1.000000000000000000 ) ) ;
#185046=EDGE_LOOP ( 'NONE', ( #154294, #231865, #161660, #15286 ) ) ;
#185077=DIRECTION ( 'NONE',  ( 1.000000000000000000, 0.000000000000000000, 0.000000000000000000 ) ) ;
#185079=ADVANCED_FACE ( 'NONE', ( #249076 ), #70459, .F. ) ;
#185098=DIRECTION ( 'NONE',  ( -0.000000000000000000, 1.000000000000000000, 8.717686153663073805E-15 ) ) ;
#185106=FACE_OUTER_BOUND ( 'NONE', #103948, .T. ) ;
#185113=AXIS2_PLACEMENT_3D ( 'NONE', #84697, #228117, #49467 ) ;
#185123=( NAMED_UNIT ( * ) SI_UNIT ( $, .STERADIAN. ) SOLID_ANGLE_UNIT ( ) );
#185152=CYLINDRICAL_SURFACE ( 'NONE', #145951, 0.1000000000000052097 ) ;
#185174=ORIENTED_EDGE ( 'NONE', *, *, #147890, .T. ) ;
#185175=DIRECTION ( 'NONE',  ( 4.026293107431335996E-15, 0.8700118002898393765, -0.4930308989875104575 ) ) ;
#185190=EDGE_LOOP ( 'NONE', ( #72030, #162381, #233600, #165201, #75164 ) ) ;
#185200=ORIENTED_EDGE ( 'NONE', *, *, #189705, .F. ) ;
#185202=VERTEX_POINT ( 'NONE', #177255 ) ;
#185222=VECTOR ( 'NONE', #91450, 1000.000000000000000 ) ;
#185225=EDGE_CURVE ( 'NONE', #166958, #8900, #117254, .T. ) ;
#185226=DIRECTION ( 'NONE',  ( -1.000000000000000000, -0.000000000000000000, -0.000000000000000000 ) ) ;
#185246=AXIS2_PLACEMENT_3D ( 'NONE', #48874, #128419, #207976 ) ;
#185252=EDGE_CURVE ( 'NONE', #111790, #176023, #130766, .T. ) ;
#185271=ORIENTED_EDGE ( 'NONE', *, *, #245235, .F. ) ;
#185280=VECTOR ( 'NONE', #158827, 1000.000000000000000 ) ;
#185290=DIRECTION ( 'NONE',  ( 0.000000000000000000, 0.000000000000000000, 1.000000000000000000 ) ) ;
#185319=CYLINDRICAL_SURFACE ( 'NONE', #175352, 0.1000000000000055705 ) ;
#185348=DIRECTION ( 'NONE',  ( -0.000000000000000000, 1.000000000000000000, 6.982962677686266711E-15 ) ) ;
#185349=FACE_OUTER_BOUND ( 'NONE', #221727, .T. ) ;
#185357=DIRECTION ( 'NONE',  ( 1.000000000000000000, 0.000000000000000000, 0.000000000000000000 ) ) ;
#185360=EDGE_CURVE ( 'NONE', #96681, #138858, #126491, .T. ) ;
#185364=AXIS2_PLACEMENT_3D ( 'NONE', #63342, #204138, #243264 ) ;
#185406=VECTOR ( 'NONE', #118726, 1000.000000000000000 ) ;
#185432=DIRECTION ( 'NONE',  ( -1.000000000000000000, 0.000000000000000000, -0.000000000000000000 ) ) ;
#185477=DIRECTION ( 'NONE',  ( 1.000000000000000000, -2.952720810173289112E-16, -2.061873921506763405E-30 ) ) ;
#185480=B_SPLINE_CURVE_WITH_KNOTS ( 'NONE', 3,
 ( #97052, #210961, #51855, #152291, #18840, #196198 ),
 .UNSPECIFIED., .F., .F.,
 ( 4, 2, 4 ),
 ( 0.000000000000000000, 0.0001569047307838624338, 0.0003138094615677248676 ),
 .UNSPECIFIED. ) ;
#185481=ORIENTED_EDGE ( 'NONE', *, *, #195131, .F. ) ;
#185518=DIRECTION ( 'NONE',  ( -1.000000000000000000, 0.000000000000000000, 0.000000000000000000 ) ) ;
#185529=EDGE_LOOP ( 'NONE', ( #191103, #165649, #60000, #59900 ) ) ;
#185540=CARTESIAN_POINT ( 'NONE',  ( 21.00000000000000000, 66.25000000001158185, -57.17310748452438673 ) ) ;
#185557=LINE ( 'NONE', #6914, #108403 ) ;
#185564=CARTESIAN_POINT ( 'NONE',  ( 20.95512820512820085, 65.37615131629971188, -61.85819391543678591 ) ) ;
#185587=CIRCLE ( 'NONE', #235453, 3.999999999999996447 ) ;
#185619=CARTESIAN_POINT ( 'NONE',  ( -21.07016717457011268, 76.00000000001170974, -75.84404832262522689 ) ) ;
#185652=EDGE_LOOP ( 'NONE', ( #200634, #113786, #140574, #95691 ) ) ;
#185720=EDGE_CURVE ( 'NONE', #90093, #140287, #239459, .T. ) ;
#185727=EDGE_CURVE ( 'NONE', #146391, #28556, #77792, .T. ) ;
#185738=PLANE ( 'NONE',  #221016 ) ;
#185742=CARTESIAN_POINT ( 'NONE',  ( 20.94999999999999929, 71.00000000001151079, -48.42837350343745584 ) ) ;
#185753=AXIS2_PLACEMENT_3D ( 'NONE', #235223, #136088, #185518 ) ;
#185787=EDGE_LOOP ( 'NONE', ( #148724, #112912, #248394, #70234 ) ) ;
#185805=CIRCLE ( 'NONE', #73419, 0.09999999999999939493 ) ;
#185816=EDGE_CURVE ( 'NONE', #236713, #12394, #62107, .T. ) ;
#185829=ORIENTED_EDGE ( 'NONE', *, *, #78483, .F. ) ;
#185832=CARTESIAN_POINT ( 'NONE',  ( -22.46246831459151494, 75.97808783307230840, -81.17297204573428360 ) ) ;
#185840=DIRECTION ( 'NONE',  ( 0.000000000000000000, -0.1350103645451807555, -0.9908441862701610203 ) ) ;
#185895=ADVANCED_FACE ( 'NONE', ( #82908 ), #42525, .F. ) ;
#185906=CARTESIAN_POINT ( 'NONE',  ( 23.14999999999999858, 76.00000000001142553, -36.02310748452432421 ) ) ;
#185913=ADVANCED_FACE ( 'NONE', ( #161209 ), #63363, .F. ) ;
#185925=CARTESIAN_POINT ( 'NONE',  ( 20.00000000000000355, 64.25000000001148237, -44.87310748452439668 ) ) ;
#185953=VERTEX_POINT ( 'NONE', #151932 ) ;
#185957=EDGE_LOOP ( 'NONE', ( #181121, #197320, #204347, #35951, #137 ) ) ;
#185968=DIRECTION ( 'NONE',  ( 0.000000000000000000, -6.982962677686266711E-15, 1.000000000000000000 ) ) ;
#185978=DIRECTION ( 'NONE',  ( 0.000000000000000000, -1.000000000000000000, -7.109473446599835262E-15 ) ) ;
#185990=CIRCLE ( 'NONE', #48613, 0.1000000000000028644 ) ;
#185997=DIRECTION ( 'NONE',  ( 0.000000000000000000, 7.026728003956683390E-15, -1.000000000000000000 ) ) ;
#186024=CARTESIAN_POINT ( 'NONE',  ( 21.05000000000000071, 64.40000000001145963, -42.95131071479990936 ) ) ;
#186064=CARTESIAN_POINT ( 'NONE',  ( -20.85000000000000142, 64.35000000001141984, -36.02310748452440237 ) ) ;
#186066=CARTESIAN_POINT ( 'NONE',  ( -18.59999999999999787, 61.95000000001162022, -64.00941241376342816 ) ) ;
#186074=AXIS2_PLACEMENT_3D ( 'NONE', #78907, #159768, #236708 ) ;
#186091=EDGE_LOOP ( 'NONE', ( #158639, #72587, #200502 ) ) ;
#186114=CARTESIAN_POINT ( 'NONE',  ( -20.94999999999999929, 76.00000000001165290, -69.52310748452431710 ) ) ;
#186119=DIRECTION ( 'NONE',  ( 1.000000000000000000, 0.000000000000000000, 0.000000000000000000 ) ) ;
#186132=VECTOR ( 'NONE', #224338, 1000.000000000000000 ) ;
#186158=ORIENTED_EDGE ( 'NONE', *, *, #4658, .F. ) ;
#186159=ORIENTED_EDGE ( 'NONE', *, *, #231563, .F. ) ;
#186161=VECTOR ( 'NONE', #19799, 1000.000000000000000 ) ;
#186166=AXIS2_PLACEMENT_3D ( 'NONE', #55166, #73517, #96860 ) ;
#186175=DIRECTION ( 'NONE',  ( -1.000000000000000000, -0.000000000000000000, 0.000000000000000000 ) ) ;
#186180=ORIENTED_EDGE ( 'NONE', *, *, #152939, .T. ) ;
#186196=ORIENTED_EDGE ( 'NONE', *, *, #164266, .F. ) ;
#186199=FACE_OUTER_BOUND ( 'NONE', #147607, .T. ) ;
#186221=VECTOR ( 'NONE', #143574, 1000.000000000000000 ) ;
#186245=VERTEX_POINT ( 'NONE', #105701 ) ;
#186253=EDGE_CURVE ( 'NONE', #243532, #101690, #139141, .T. ) ;
#186254=AXIS2_PLACEMENT_3D ( 'NONE', #184398, #85274, #244368 ) ;
#186334=VERTEX_POINT ( 'NONE', #7932 ) ;
#186364=DIRECTION ( 'NONE',  ( 1.000000000000000000, 0.000000000000000000, 0.000000000000000000 ) ) ;
#186372=ADVANCED_FACE ( 'NONE', ( #74351 ), #75622, .F. ) ;
#186376=ORIENTED_EDGE ( 'NONE', *, *, #129794, .F. ) ;
#186381=DIRECTION ( 'NONE',  ( -0.000000000000000000, -6.982962677686266711E-15, 1.000000000000000000 ) ) ;
#186389=FACE_OUTER_BOUND ( 'NONE', #58537, .T. ) ;
#186419=SPHERICAL_SURFACE ( 'NONE', #54088, 0.1000000000000000056 ) ;
#186439=CIRCLE ( 'NONE', #78073, 7.900000000000000355 ) ;
#186446=DIRECTION ( 'NONE',  ( 0.000000000000000000, 0.1350103645451807832, 0.9908441862701610203 ) ) ;
#186451=LINE ( 'NONE', #26098, #252114 ) ;
#186472=ORIENTED_EDGE ( 'NONE', *, *, #16551, .T. ) ;
#186485=ORIENTED_EDGE ( 'NONE', *, *, #14510, .T. ) ;
#186505=DIRECTION ( 'NONE',  ( 0.000000000000000000, 0.000000000000000000, 1.000000000000000000 ) ) ;
#186538=AXIS2_PLACEMENT_3D ( 'NONE', #161504, #241034, #165340 ) ;
#186546=CARTESIAN_POINT ( 'NONE',  ( 23.14999999999999503, 69.55000000001157900, -57.17310748452436542 ) ) ;
#186548=EDGE_CURVE ( 'NONE', #46294, #125917, #220258, .T. ) ;
#186564=ADVANCED_FACE ( 'NONE', ( #59855 ), #139397, .T. ) ;
#186567=CARTESIAN_POINT ( 'NONE',  ( 21.05000000000000071, 76.00000000001141132, -34.12310748452431852 ) ) ;
#186588=ADVANCED_FACE ( 'NONE', ( #1170 ), #182415, .F. ) ;
#186596=CIRCLE ( 'NONE', #119974, 0.1000000000000028644 ) ;
#186656=DIRECTION ( 'NONE',  ( 0.000000000000000000, -6.308085367188388072E-15, 1.000000000000000000 ) ) ;
#186664=CARTESIAN_POINT ( 'NONE',  ( -23.25000000000000000, 76.00000000001168132, -73.57310748452432847 ) ) ;
#186668=DIRECTION ( 'NONE',  ( -1.000000000000000000, 0.000000000000000000, -0.000000000000000000 ) ) ;
#186687=ORIENTED_EDGE ( 'NONE', *, *, #239573, .F. ) ;
#186715=DIRECTION ( 'NONE',  ( 1.000000000000000000, 0.000000000000000000, 0.000000000000000000 ) ) ;
#186719=EDGE_CURVE ( 'NONE', #64921, #184441, #36320, .T. ) ;
#186728=AXIS2_PLACEMENT_3D ( 'NONE', #192000, #190720, #169894 ) ;
#186741=DIRECTION ( 'NONE',  ( -0.000000000000000000, 6.982962677686266711E-15, -1.000000000000000000 ) ) ;
#186772=AXIS2_PLACEMENT_3D ( 'NONE', #159574, #239109, #171174 ) ;
#186818=ORIENTED_EDGE ( 'NONE', *, *, #177728, .T. ) ;
#186862=ORIENTED_EDGE ( 'NONE', *, *, #46408, .T. ) ;
#186870=CARTESIAN_POINT ( 'NONE',  ( 21.05000000000011795, 65.45624872451554666, -61.96671967585964325 ) ) ;
#186871=CARTESIAN_POINT ( 'NONE',  ( -23.15000000000000213, 71.65000000001151648, -48.37310748452435405 ) ) ;
#186885=CARTESIAN_POINT ( 'NONE',  ( -18.50000000000000000, 66.85000000001156195, -57.17310748452438673 ) ) ;
#186887=FACE_OUTER_BOUND ( 'NONE', #80908, .T. ) ;
#186918=VECTOR ( 'NONE', #105771, 1000.000000000000000 ) ;
#186939=AXIS2_PLACEMENT_3D ( 'NONE', #153142, #71017, #173996 ) ;
#187041=DIRECTION ( 'NONE',  ( 0.000000000000000000, 0.000000000000000000, 1.000000000000000000 ) ) ;
#187051=DIRECTION ( 'NONE',  ( 0.000000000000000000, 0.000000000000000000, 1.000000000000000000 ) ) ;
#187080=VECTOR ( 'NONE', #198420, 1000.000000000000000 ) ;
#187133=DIRECTION ( 'NONE',  ( 0.000000000000000000, -1.000000000000000000, -6.982962677686265922E-15 ) ) ;
#187134=ADVANCED_FACE ( 'NONE', ( #59082 ), #138625, .T. ) ;
#187141=CARTESIAN_POINT ( 'NONE',  ( -23.25000000000000000, 87.65000000001165859, -69.52310748452424605 ) ) ;
#187145=DIRECTION ( 'NONE',  ( 0.000000000000000000, -6.982962677686266711E-15, 1.000000000000000000 ) ) ;
#187167=DIRECTION ( 'NONE',  ( 0.000000000000000000, 1.000000000000000000, 6.982962677686266711E-15 ) ) ;
#187198=VERTEX_POINT ( 'NONE', #181653 ) ;
#187216=FACE_OUTER_BOUND ( 'NONE', #61022, .T. ) ;
#187217=DIRECTION ( 'NONE',  ( 0.000000000000000000, -5.551115123125777653E-14, 1.000000000000000000 ) ) ;
#187226=ORIENTED_EDGE ( 'NONE', *, *, #123019, .T. ) ;
#187228=DIRECTION ( 'NONE',  ( -1.000000000000000000, 0.000000000000000000, -0.000000000000000000 ) ) ;
#187263=DIRECTION ( 'NONE',  ( 1.000000000000000000, 0.000000000000000000, 0.000000000000000000 ) ) ;
#187267=CARTESIAN_POINT ( 'NONE',  ( 20.94999999999999574, 87.48912529308769592, -66.42310748452423752 ) ) ;
#187277=VECTOR ( 'NONE', #14999, 1000.000000000000000 ) ;
#187330=ORIENTED_EDGE ( 'NONE', *, *, #76353, .F. ) ;
#187403=CYLINDRICAL_SURFACE ( 'NONE', #247805, 0.1000000000000028644 ) ;
#187442=ORIENTED_EDGE ( 'NONE', *, *, #51399, .T. ) ;
#187485=ADVANCED_FACE ( 'NONE', ( #112543 ), #175124, .T. ) ;
#187503=AXIS2_PLACEMENT_3D ( 'NONE', #190120, #147121, #169306 ) ;
#187524=EDGE_CURVE ( 'NONE', #150942, #214618, #201053, .T. ) ;
#187544=ORIENTED_EDGE ( 'NONE', *, *, #231597, .T. ) ;
#187555=DIRECTION ( 'NONE',  ( 0.000000000000000000, -6.982962677686266711E-15, 1.000000000000000000 ) ) ;
#187557=EDGE_CURVE ( 'NONE', #191947, #146391, #152343, .T. ) ;
#187572=CIRCLE ( 'NONE', #208415, 0.1999999999999987899 ) ;
#187576=CIRCLE ( 'NONE', #20984, 0.09999999999999939493 ) ;
#187599=VERTEX_POINT ( 'NONE', #276 ) ;
#187641=ORIENTED_EDGE ( 'NONE', *, *, #196119, .T. ) ;
#187646=CARTESIAN_POINT ( 'NONE',  ( 18.50000000000000000, 85.48068669529033059, -29.08199231576639932 ) ) ;
#187652=VERTEX_POINT ( 'NONE', #19868 ) ;
#187657=CARTESIAN_POINT ( 'NONE',  ( 20.94999999999999929, 69.35000000001159037, -59.50608031408435039 ) ) ;
#187678=CARTESIAN_POINT ( 'NONE',  ( 20.94999999999999929, 85.00000000001149658, -45.51707660717670478 ) ) ;
#187692=CARTESIAN_POINT ( 'NONE',  ( 18.52928932188133970, 65.72071067813013201, -44.87310748452439668 ) ) ;
#187695=CARTESIAN_POINT ( 'NONE',  ( 20.94999999999999929, 69.45000000001157048, -57.37310748452436115 ) ) ;
#187702=CARTESIAN_POINT ( 'NONE',  ( 18.51997666896852479, 85.39233213153087831, -62.37970129704087441 ) ) ;
#187729=ORIENTED_EDGE ( 'NONE', *, *, #239245, .T. ) ;
#187744=CARTESIAN_POINT ( 'NONE',  ( -23.25000000000000000, 76.10000000001174669, -81.17267829206912211 ) ) ;
#187745=ORIENTED_EDGE ( 'NONE', *, *, #8164, .F. ) ;
#187775=CARTESIAN_POINT ( 'NONE',  ( -20.94999999999999929, 74.16465844978715438, -57.96795619196135618 ) ) ;
#187791=EDGE_LOOP ( 'NONE', ( #95239, #39178, #210843, #147833 ) ) ;
#187800=ORIENTED_EDGE ( 'NONE', *, *, #3966, .T. ) ;
#187808=CIRCLE ( 'NONE', #254392, 0.1000000000000028644 ) ;
#187851=CYLINDRICAL_SURFACE ( 'NONE', #100160, 0.09999999999999939493 ) ;
#187853=EDGE_CURVE ( 'NONE', #1289, #139208, #185805, .T. ) ;
#187868=CIRCLE ( 'NONE', #96243, 0.1000000000000052097 ) ;
#187893=DIRECTION ( 'NONE',  ( 0.000000000000000000, -1.000000000000000000, -6.982962677686266711E-15 ) ) ;
#187899=CARTESIAN_POINT ( 'NONE',  ( -20.64999999999999858, 85.00000000001159606, -59.62913836187181715 ) ) ;
#187907=ORIENTED_EDGE ( 'NONE', *, *, #110912, .T. ) ;
#187916=EDGE_CURVE ( 'NONE', #55596, #120848, #31903, .T. ) ;
#187948=EDGE_LOOP ( 'NONE', ( #32505, #32938, #136037, #131348 ) ) ;
#187966=CYLINDRICAL_SURFACE ( 'NONE', #103195, 0.1000000000000028644 ) ;
#187982=ORIENTED_EDGE ( 'NONE', *, *, #63465, .F. ) ;
#188036=EDGE_CURVE ( 'NONE', #113184, #202471, #56779, .T. ) ;
#188051=ORIENTED_EDGE ( 'NONE', *, *, #28797, .T. ) ;
#188071=DIRECTION ( 'NONE',  ( -1.000000000000000000, 0.000000000000000000, -0.000000000000000000 ) ) ;
#188074=ORIENTED_EDGE ( 'NONE', *, *, #197799, .T. ) ;
#188085=ORIENTED_EDGE ( 'NONE', *, *, #102947, .F. ) ;
#188097=DIRECTION ( 'NONE',  ( -0.8660254037844653530, 0.000000000000000000, -0.4999999999999539257 ) ) ;
#188100=CARTESIAN_POINT ( 'NONE',  ( -23.25000000000000000, 87.75000000001142553, -36.02310748452423894 ) ) ;
#188113=ORIENTED_EDGE ( 'NONE', *, *, #16764, .F. ) ;
#188136=CIRCLE ( 'NONE', #9072, 0.1000000000000028644 ) ;
#188144=EDGE_CURVE ( 'NONE', #206913, #47775, #89083, .T. ) ;
#188148=AXIS2_PLACEMENT_3D ( 'NONE', #14019, #89672, #29753 ) ;
#188172=VECTOR ( 'NONE', #186741, 1000.000000000000000 ) ;
#188187=CARTESIAN_POINT ( 'NONE',  ( -20.15000000000000568, 66.70857864377420299, -48.37310748452438247 ) ) ;
#188202=FACE_OUTER_BOUND ( 'NONE', #135446, .T. ) ;
#188209=DIRECTION ( 'NONE',  ( 1.000000000000000000, 0.000000000000000000, 0.000000000000000000 ) ) ;
#188219=VERTEX_POINT ( 'NONE', #109006 ) ;
#188236=EDGE_CURVE ( 'NONE', #254970, #23444, #36177, .T. ) ;
#188239=AXIS2_PLACEMENT_3D ( 'NONE', #18219, #198132, #217670 ) ;
#188278=CARTESIAN_POINT ( 'NONE',  ( 21.05000000000000071, 87.65000000001144542, -39.02310748452423894 ) ) ;
#188283=CIRCLE ( 'NONE', #75860, 12.97499999999999964 ) ;
#188297=CARTESIAN_POINT ( 'NONE',  ( 21.05000000000000071, 65.27628289530404970, -57.36191719039695158 ) ) ;
#188300=FACE_OUTER_BOUND ( 'NONE', #63966, .T. ) ;
#188301=EDGE_CURVE ( 'NONE', #229077, #248144, #257456, .T. ) ;
#188320=FACE_OUTER_BOUND ( 'NONE', #92224, .T. ) ;
#188346=EDGE_CURVE ( 'NONE', #177661, #256296, #116721, .T. ) ;
#188354=VERTEX_POINT ( 'NONE', #97117 ) ;
#188373=VERTEX_POINT ( 'NONE', #43616 ) ;
#188379=EDGE_LOOP ( 'NONE', ( #44016, #136473, #176512, #233633 ) ) ;
#188386=EDGE_CURVE ( 'NONE', #203476, #218877, #61893, .T. ) ;
#188414=ORIENTED_EDGE ( 'NONE', *, *, #220508, .T. ) ;
#188420=DIRECTION ( 'NONE',  ( 1.000000000000000000, -0.000000000000000000, 0.000000000000000000 ) ) ;
#188445=CIRCLE ( 'NONE', #254842, 0.1000000000000028644 ) ;
#188467=CIRCLE ( 'NONE', #34386, 3.900000000000000799 ) ;
#188533=ADVANCED_FACE ( 'NONE', ( #126999 ), #61089, .F. ) ;
#188546=ADVANCED_FACE ( 'NONE', ( #29230 ), #106127, .F. ) ;
#188574=DIRECTION ( 'NONE',  ( -1.000000000000000000, 2.952720810173289112E-16, 2.061873921506763405E-30 ) ) ;
#188582=CARTESIAN_POINT ( 'NONE',  ( 20.99780126800938262, 64.39461131213495548, -42.93575491281916356 ) ) ;
#188585=ORIENTED_EDGE ( 'NONE', *, *, #167829, .T. ) ;
#188588=ADVANCED_FACE ( 'NONE', ( #96827 ), #112585, .T. ) ;
#188595=UNCERTAINTY_MEASURE_WITH_UNIT (LENGTH_MEASURE( 1.000000000000000082E-05 ), #156740, 'distance_accuracy_value', 'NONE');
#188616=DIRECTION ( 'NONE',  ( -1.000000000000000000, 0.000000000000000000, 0.000000000000000000 ) ) ;
#188651=DIRECTION ( 'NONE',  ( -0.7071067811865389130, 4.937700262164590641E-15, -0.7071067811865561215 ) ) ;
#188652=ORIENTED_EDGE ( 'NONE', *, *, #254633, .F. ) ;
#188722=ORIENTED_EDGE ( 'NONE', *, *, #116803, .F. ) ;
#188733=DIRECTION ( 'NONE',  ( -1.000000000000000000, -0.000000000000000000, -0.000000000000000000 ) ) ;
#188775=EDGE_CURVE ( 'NONE', #119848, #230655, #238953, .T. ) ;
#188777=FILL_AREA_STYLE ('',( #248767 ) ) ;
#188864=ORIENTED_EDGE ( 'NONE', *, *, #197077, .F. ) ;
#188865=AXIS2_PLACEMENT_3D ( 'NONE', #158003, #80965, #61422 ) ;
#188908=CARTESIAN_POINT ( 'NONE',  ( -23.15000000000000213, 76.00000000001145395, -40.02310748452431710 ) ) ;
#188942=CARTESIAN_POINT ( 'NONE',  ( 22.41477678272288188, 75.99917613424879903, -81.17269276903972752 ) ) ;
#188950=ORIENTED_EDGE ( 'NONE', *, *, #70749, .F. ) ;
#188973=DIRECTION ( 'NONE',  ( 1.000000000000000000, 0.000000000000000000, 0.000000000000000000 ) ) ;
#188987=CARTESIAN_POINT ( 'NONE',  ( 23.24999999999999645, 76.00000000001142553, -36.02310748452432421 ) ) ;
#189002=CIRCLE ( 'NONE', #55676, 11.80000000000000426 ) ;
#189058=VERTEX_POINT ( 'NONE', #173581 ) ;
#189078=FACE_OUTER_BOUND ( 'NONE', #244367, .T. ) ;
#189092=EDGE_CURVE ( 'NONE', #188373, #162902, #56751, .T. ) ;
#189101=AXIS2_PLACEMENT_3D ( 'NONE', #214383, #155730, #177848 ) ;
#189126=CARTESIAN_POINT ( 'NONE',  ( 20.95224633520496127, 67.09947783345437244, -61.02983103660312025 ) ) ;
#189158=CARTESIAN_POINT ( 'NONE',  ( -20.94999999999999929, 76.00000000001142553, -36.02310748452432421 ) ) ;
#189166=DIRECTION ( 'NONE',  ( 1.000000000000000000, 0.000000000000000000, 0.000000000000000000 ) ) ;
#189232=ORIENTED_EDGE ( 'NONE', *, *, #249922, .F. ) ;
#189246=VERTEX_POINT ( 'NONE', #217761 ) ;
#189257=FACE_OUTER_BOUND ( 'NONE', #123640, .T. ) ;
#189263=CIRCLE ( 'NONE', #5881, 0.09999999999999939493 ) ;
#189305=VERTEX_POINT ( 'NONE', #5120 ) ;
#189307=VECTOR ( 'NONE', #87890, 1000.000000000000000 ) ;
#189317=ADVANCED_FACE ( 'NONE', ( #28629 ), #128966, .T. ) ;
#189368=ORIENTED_EDGE ( 'NONE', *, *, #39146, .T. ) ;
#189378=LINE ( 'NONE', #30309, #77566 ) ;
#189379=ORIENTED_EDGE ( 'NONE', *, *, #141777, .T. ) ;
#189407=ORIENTED_EDGE ( 'NONE', *, *, #253489, .F. ) ;
#189428=CARTESIAN_POINT ( 'NONE',  ( 21.04999999999999716, 65.37049252075402705, -61.89512808452796122 ) ) ;
#189447=CARTESIAN_POINT ( 'NONE',  ( -20.54999999999999716, 76.00000000001142553, -36.02310748452432421 ) ) ;
#189477=ADVANCED_FACE ( 'NONE', ( #70298 ), #256654, .F. ) ;
#189492=EDGE_CURVE ( 'NONE', #20936, #26749, #198445, .T. ) ;
#189500=CARTESIAN_POINT ( 'NONE',  ( -21.05000000000000071, 75.90220970870291239, -75.78092209500043452 ) ) ;
#189520=EDGE_CURVE ( 'NONE', #138795, #216178, #115239, .T. ) ;
#189565=VERTEX_POINT ( 'NONE', #196620 ) ;
#189585=DIRECTION ( 'NONE',  ( 0.000000000000000000, 0.8660254037844377084, 0.5000000000000016653 ) ) ;
#189592=ADVANCED_FACE ( 'NONE', ( #163604 ), #156251, .F. ) ;
#189604=CARTESIAN_POINT ( 'NONE',  ( 21.06490991615909536, 65.27510865242446414, -57.31939613099126518 ) ) ;
#189640=DIRECTION ( 'NONE',  ( 2.342056488767301376E-15, 0.1350103645451835865, 0.9908441862701605762 ) ) ;
#189654=CYLINDRICAL_SURFACE ( 'NONE', #114598, 0.09999999999999939493 ) ;
#189687=ADVANCED_FACE ( 'NONE', ( #107473, #245703 ), #110038, .F. ) ;
#189697=DIRECTION ( 'NONE',  ( -0.000000000000000000, -6.982962677686266711E-15, 1.000000000000000000 ) ) ;
#189705=EDGE_CURVE ( 'NONE', #108916, #238186, #23877, .T. ) ;
#189718=ORIENTED_EDGE ( 'NONE', *, *, #95512, .T. ) ;
#189740=CARTESIAN_POINT ( 'NONE',  ( -18.50000000000000000, 64.35000000001141984, -36.02310748452440237 ) ) ;
#189777=EDGE_CURVE ( 'NONE', #217695, #232002, #48781, .T. ) ;
#189778=ORIENTED_EDGE ( 'NONE', *, *, #21380, .T. ) ;
#189800=CARTESIAN_POINT ( 'NONE',  ( 20.94999999999999574, 74.16465844978715438, -57.96795619196134908 ) ) ;
#189801=ADVANCED_FACE ( 'NONE', ( #215554 ), #100361, .F. ) ;
#189805=ADVANCED_FACE ( 'NONE', ( #211732 ), #256834, .F. ) ;
#189806=EDGE_CURVE ( 'NONE', #152443, #232528, #38226, .T. ) ;
#189843=AXIS2_PLACEMENT_3D ( 'NONE', #156991, #20043, #100797 ) ;
#189847=CARTESIAN_POINT ( 'NONE',  ( 20.94999999999999929, 77.13501884592155022, -28.30613060109199353 ) ) ;
#189855=CARTESIAN_POINT ( 'NONE',  ( -21.64999999999999858, 68.75000000001158185, -57.27310748452437394 ) ) ;
#189906=ORIENTED_EDGE ( 'NONE', *, *, #4860, .T. ) ;
#189931=CARTESIAN_POINT ( 'NONE',  ( 18.49999999999999289, 65.58283456529508726, -44.67310748510405460 ) ) ;
#189997=EDGE_CURVE ( 'NONE', #195194, #117855, #136244, .T. ) ;
#190005=CYLINDRICAL_SURFACE ( 'NONE', #61876, 0.09999999999999976963 ) ;
#190011=ORIENTED_EDGE ( 'NONE', *, *, #248310, .T. ) ;
#190018=DIRECTION ( 'NONE',  ( 0.000000000000000000, 0.000000000000000000, 1.000000000000000000 ) ) ;
#190024=AXIS2_PLACEMENT_3D ( 'NONE', #157990, #243893, #245192 ) ;
#190075=CIRCLE ( 'NONE', #27790, 0.09999999999999939493 ) ;
#190078=CARTESIAN_POINT ( 'NONE',  ( -20.54999999999999716, 68.75000000001151079, -48.37310748452436826 ) ) ;
#190082=CARTESIAN_POINT ( 'NONE',  ( 23.24999999999999289, 70.05000000001149374, -46.32880978955918039 ) ) ;
#190097=DIRECTION ( 'NONE',  ( -1.000000000000000000, 7.304098846218134667E-16, 5.100424963727256530E-30 ) ) ;
#190101=CARTESIAN_POINT ( 'NONE',  ( -21.14999999999999858, 76.00000000001169553, -75.78168612828702067 ) ) ;
#190120=CARTESIAN_POINT ( 'NONE',  ( 23.14999999999999503, 64.35000000001146248, -43.03791325517834565 ) ) ;
#190147=FACE_OUTER_BOUND ( 'NONE', #247636, .T. ) ;
#190154=FACE_OUTER_BOUND ( 'NONE', #247361, .T. ) ;
#190164=EDGE_LOOP ( 'NONE', ( #100794, #203453, #96170, #218606 ) ) ;
#190280=AXIS2_PLACEMENT_3D ( 'NONE', #68357, #106166, #9659 ) ;
#190281=ADVANCED_FACE ( 'NONE', ( #60019 ), #139554, .F. ) ;
#190285=DIRECTION ( 'NONE',  ( -1.000000000000000000, 3.265361837132813093E-16, 2.280189983783949500E-30 ) ) ;
#190322=AXIS2_PLACEMENT_3D ( 'NONE', #124025, #64039, #203551 ) ;
#190323=ADVANCED_FACE ( 'NONE', ( #198255 ), #148947, .T. ) ;
#190330=CIRCLE ( 'NONE', #77871, 0.1000000000000028644 ) ;
#190360=CYLINDRICAL_SURFACE ( 'NONE', #63585, 0.1000000000000028644 ) ;
#190361=FACE_OUTER_BOUND ( 'NONE', #159248, .T. ) ;
#190374=EDGE_LOOP ( 'NONE', ( #101076, #39379, #150893, #206741, #131866 ) ) ;
#190398=AXIS2_PLACEMENT_3D ( 'NONE', #9339, #168476, #26356 ) ;
#190407=EDGE_CURVE ( 'NONE', #61807, #213807, #128281, .T. ) ;
#190468=EDGE_CURVE ( 'NONE', #214318, #255306, #132356, .T. ) ;
#190500=DIRECTION ( 'NONE',  ( 0.000000000000000000, -6.982962677686266711E-15, 1.000000000000000000 ) ) ;
#190546=DIRECTION ( 'NONE',  ( -0.000000000000000000, 0.4791956752371484551, 0.8777080977375184556 ) ) ;
#190585=ORIENTED_EDGE ( 'NONE', *, *, #240401, .T. ) ;
#190598=ORIENTED_EDGE ( 'NONE', *, *, #182773, .F. ) ;
#190608=DIRECTION ( 'NONE',  ( 0.000000000000000000, -7.116814260417668513E-15, 1.000000000000000000 ) ) ;
#190643=AXIS2_PLACEMENT_3D ( 'NONE', #82522, #124266, #203784 ) ;
#190658=EDGE_CURVE ( 'NONE', #198432, #85964, #253154, .T. ) ;
#190679=ORIENTED_EDGE ( 'NONE', *, *, #134585, .F. ) ;
#190701=AXIS2_PLACEMENT_3D ( 'NONE', #104959, #224933, #122004 ) ;
#190706=DIRECTION ( 'NONE',  ( -0.000000000000000000, -6.982962677686266711E-15, 1.000000000000000000 ) ) ;
#190720=DIRECTION ( 'NONE',  ( 1.000000000000000000, -0.000000000000000000, 0.000000000000000000 ) ) ;
#190733=AXIS2_PLACEMENT_3D ( 'NONE', #166840, #9012, #67701 ) ;
#190738=CARTESIAN_POINT ( 'NONE',  ( -23.15000000000000213, 76.00000000001142553, -36.02310748452432421 ) ) ;
#190744=EDGE_CURVE ( 'NONE', #238726, #195194, #204356, .T. ) ;
#190765=DIRECTION ( 'NONE',  ( -0.000000000000000000, 1.000000000000000000, 6.982962677686266711E-15 ) ) ;
#190774=EDGE_CURVE ( 'NONE', #201923, #87766, #232537, .T. ) ;
#190778=DIRECTION ( 'NONE',  ( 0.000000000000000000, 0.8660254037844378194, 0.5000000000000016653 ) ) ;
#190793=ORIENTED_EDGE ( 'NONE', *, *, #30436, .F. ) ;
#190855=DIRECTION ( 'NONE',  ( -0.000000000000000000, 0.7397360091702708251, 0.6728971962616883129 ) ) ;
#190919=DIRECTION ( 'NONE',  ( 0.000000000000000000, -6.982962677686266711E-15, 1.000000000000000000 ) ) ;
#190962=ADVANCED_FACE ( 'NONE', ( #34743 ), #114253, .T. ) ;
#190970=ORIENTED_EDGE ( 'NONE', *, *, #197077, .T. ) ;
#191006=CIRCLE ( 'NONE', #165876, 12.87499999999999822 ) ;
#191013=AXIS2_PLACEMENT_3D ( 'NONE', #166123, #8312, #46125 ) ;
#191023=PRODUCT_DEFINITION_SHAPE ( 'NONE', 'NONE',  #198277 ) ;
#191027=AXIS2_PLACEMENT_3D ( 'NONE', #132559, #54284, #212104 ) ;
#191028=VECTOR ( 'NONE', #136903, 1000.000000000000000 ) ;
#191041=ADVANCED_FACE ( 'NONE', ( #128251 ), #47401, .T. ) ;
#191071=CARTESIAN_POINT ( 'NONE',  ( 18.59999999999996945, 68.97833521811131163, -32.18954208262707795 ) ) ;
#191103=ORIENTED_EDGE ( 'NONE', *, *, #235202, .F. ) ;
#191107=EDGE_CURVE ( 'NONE', #234494, #221530, #145000, .T. ) ;
#191108=CIRCLE ( 'NONE', #224397, 0.09999999999999939493 ) ;
#191123=DIRECTION ( 'NONE',  ( -1.000000000000000000, 0.000000000000000000, -0.000000000000000000 ) ) ;
#191124=ORIENTED_EDGE ( 'NONE', *, *, #254682, .F. ) ;
#191141=CARTESIAN_POINT ( 'NONE',  ( 20.94999999999999929, 70.50000000001151079, -48.42837350343745584 ) ) ;
#191153=VERTEX_POINT ( 'NONE', #79675 ) ;
#191156=AXIS2_PLACEMENT_3D ( 'NONE', #26502, #183008, #42205 ) ;
#191170=AXIS2_PLACEMENT_3D ( 'NONE', #152993, #134646, #90402 ) ;
#191199=FACE_OUTER_BOUND ( 'NONE', #204282, .T. ) ;
#191242=CARTESIAN_POINT ( 'NONE',  ( 18.58143601961878844, 65.56427058491688342, -44.77310748452440237 ) ) ;
#191257=ORIENTED_EDGE ( 'NONE', *, *, #103152, .F. ) ;
#191266=ADVANCED_FACE ( 'NONE', ( #105651 ), #5264, .F. ) ;
#191289=ORIENTED_EDGE ( 'NONE', *, *, #102713, .F. ) ;
#191318=CARTESIAN_POINT ( 'NONE',  ( -20.94999999999999929, 77.83585931145498193, -24.51866831572578320 ) ) ;
#191324=TOROIDAL_SURFACE ( 'NONE', #45549, 0.2000000000000000111, 0.1000000000000000056 ) ;
#191325=ORIENTED_EDGE ( 'NONE', *, *, #41199, .F. ) ;
#191331=CARTESIAN_POINT ( 'NONE',  ( -21.05000000000000071, 76.00000000001165290, -69.52310748452431710 ) ) ;
#191359=EDGE_LOOP ( 'NONE', ( #15739, #43822, #195721, #254632 ) ) ;
#191368=EDGE_LOOP ( 'NONE', ( #143101, #10532, #165062, #59614 ) ) ;
#191383=SURFACE_STYLE_USAGE ( .BOTH. , #29745 ) ;
#191392=FACE_OUTER_BOUND ( 'NONE', #215982, .T. ) ;
#191415=FACE_OUTER_BOUND ( 'NONE', #142050, .T. ) ;
#191467=CARTESIAN_POINT ( 'NONE',  ( 21.05000000000000071, 64.35000000001164722, -69.52310748452440237 ) ) ;
#191480=LINE ( 'NONE', #213568, #24597 ) ;
#191534=ADVANCED_FACE ( 'NONE', ( #97640 ), #54686, .T. ) ;
#191566=CARTESIAN_POINT ( 'NONE',  ( -18.50000000000000000, 85.42129027953377829, -29.19922530549827755 ) ) ;
#191569=DIRECTION ( 'NONE',  ( 0.000000000000000000, 0.000000000000000000, -1.000000000000000000 ) ) ;
#191574=AXIS2_PLACEMENT_3D ( 'NONE', #254518, #236266, #38089 ) ;
#191627=ADVANCED_FACE ( 'NONE', ( #186199 ), #74693, .T. ) ;
#191639=ORIENTED_EDGE ( 'NONE', *, *, #170804, .F. ) ;
#191645=ORIENTED_EDGE ( 'NONE', *, *, #212137, .T. ) ;
#191671=AXIS2_PLACEMENT_3D ( 'NONE', #219373, #116445, #156877 ) ;
#191676=CIRCLE ( 'NONE', #154087, 0.1000000000000028644 ) ;
#191689=DIRECTION ( 'NONE',  ( -1.000000000000000000, 0.000000000000000000, -0.000000000000000000 ) ) ;
#191705=CARTESIAN_POINT ( 'NONE',  ( 20.94999999999999929, 76.00000000001139711, -31.92310748452432279 ) ) ;
#191720=EDGE_LOOP ( 'NONE', ( #103636, #199057 ) ) ;
#191791=DIRECTION ( 'NONE',  ( -0.7071067811865475727, 0.7071067811865475727, 4.937700262164531476E-15 ) ) ;
#191819=DIRECTION ( 'NONE',  ( -1.000000000000000000, 0.000000000000000000, -0.000000000000000000 ) ) ;
#191823=EDGE_CURVE ( 'NONE', #198469, #247693, #237338, .T. ) ;
#191840=VERTEX_POINT ( 'NONE', #115640 ) ;
#191855=AXIS2_PLACEMENT_3D ( 'NONE', #63732, #217647, #161578 ) ;
#191904=ORIENTED_EDGE ( 'NONE', *, *, #178085, .F. ) ;
#191909=CARTESIAN_POINT ( 'NONE',  ( 18.49999999999996803, 68.92903212821255465, -32.27654326265606954 ) ) ;
#191910=EDGE_CURVE ( 'NONE', #175346, #255664, #245702, .T. ) ;
#191934=EDGE_CURVE ( 'NONE', #66731, #188219, #83163, .T. ) ;
#191947=VERTEX_POINT ( 'NONE', #183316 ) ;
#191948=ADVANCED_FACE ( 'NONE', ( #224978 ), #2090, .T. ) ;
#191951=ORIENTED_EDGE ( 'NONE', *, *, #97972, .F. ) ;
#191986=DIRECTION ( 'NONE',  ( 0.000000000000000000, 0.000000000000000000, 1.000000000000000000 ) ) ;
#191994=CIRCLE ( 'NONE', #196237, 0.1000000000000028644 ) ;
#192000=CARTESIAN_POINT ( 'NONE',  ( -21.05000000000000071, 87.48912529308749697, -39.12310748452424747 ) ) ;
#192006=DIRECTION ( 'NONE',  ( 1.000000000000000000, 0.000000000000000000, 0.000000000000000000 ) ) ;
#192024=CIRCLE ( 'NONE', #191855, 0.1000000000000028644 ) ;
#192029=EDGE_CURVE ( 'NONE', #106650, #223391, #4095, .T. ) ;
#192039=CARTESIAN_POINT ( 'NONE',  ( 20.94999999999999929, 84.73084112150681335, -45.62118220350859588 ) ) ;
#192121=EDGE_CURVE ( 'NONE', #234345, #32328, #162329, .T. ) ;
#192138=CARTESIAN_POINT ( 'NONE',  ( 20.94999999999999929, 70.60000000001157616, -57.11784146561126363 ) ) ;
#192171=CARTESIAN_POINT ( 'NONE',  ( 21.04999999999999716, 67.12791932463382238, -61.00206006569352013 ) ) ;
#192193=LINE ( 'NONE', #150492, #30753 ) ;
#192210=ADVANCED_FACE ( 'NONE', ( #80013 ), #79272, .F. ) ;
#192212=ORIENTED_EDGE ( 'NONE', *, *, #165048, .T. ) ;
#192222=ADVANCED_FACE ( 'NONE', ( #22673 ), #16778, .T. ) ;
#192234=CARTESIAN_POINT ( 'NONE',  ( 21.05000012384952512, 65.37127970113704123, -57.34513015448907680 ) ) ;
#192273=DIRECTION ( 'NONE',  ( 0.000000000000000000, -0.8660254037844468122, -0.4999999999999859557 ) ) ;
#192276=CARTESIAN_POINT ( 'NONE',  ( 21.05000000000000071, 76.02138556594965735, -75.82806859720888326 ) ) ;
#192289=DIRECTION ( 'NONE',  ( 0.000000000000000000, 0.000000000000000000, 1.000000000000000000 ) ) ;
#192315=FACE_OUTER_BOUND ( 'NONE', #74478, .T. ) ;
#192324=DIRECTION ( 'NONE',  ( 0.000000000000000000, 0.000000000000000000, 1.000000000000000000 ) ) ;
#192338=CARTESIAN_POINT ( 'NONE',  ( -23.15000000000000213, 71.85000000001173248, -81.27310748452434552 ) ) ;
#192384=DIRECTION ( 'NONE',  ( 0.000000000000000000, 0.000000000000000000, 1.000000000000000000 ) ) ;
#192396=ADVANCED_FACE ( 'NONE', ( #146421 ), #112618, .T. ) ;
#192458=VERTEX_POINT ( 'NONE', #210287 ) ;
#192470=CARTESIAN_POINT ( 'NONE',  ( -21.93642651522410247, 68.67283376068584744, -69.52310748452435973 ) ) ;
#192497=EDGE_CURVE ( 'NONE', #131784, #196598, #198098, .T. ) ;
#192509=ORIENTED_EDGE ( 'NONE', *, *, #140643, .F. ) ;
#192514=CARTESIAN_POINT ( 'NONE',  ( -20.99780126800933644, 64.39461131213499812, -42.93575491281912804 ) ) ;
#192525=CARTESIAN_POINT ( 'NONE',  ( 21.04999999999999716, 69.65564095796813149, -69.53796311941867714 ) ) ;
#192533=AXIS2_PLACEMENT_3D ( 'NONE', #186114, #184819, #46580 ) ;
#192555=EDGE_CURVE ( 'NONE', #43988, #210362, #62736, .T. ) ;
#192594=CIRCLE ( 'NONE', #34410, 0.1999999999999987899 ) ;
#192603=DIRECTION ( 'NONE',  ( -1.000000000000000000, -0.000000000000000000, -0.000000000000000000 ) ) ;
#192606=ORIENTED_EDGE ( 'NONE', *, *, #153010, .T. ) ;
#192622=FACE_OUTER_BOUND ( 'NONE', #182897, .T. ) ;
#192637=AXIS2_PLACEMENT_3D ( 'NONE', #773, #125879, #80310 ) ;
#192667=CARTESIAN_POINT ( 'NONE',  ( -23.15000000000000213, 87.39257802171711376, -39.09705706435617856 ) ) ;
#192687=EDGE_CURVE ( 'NONE', #246301, #234345, #247496, .T. ) ;
#192692=ORIENTED_EDGE ( 'NONE', *, *, #242913, .T. ) ;
#192693=FACE_OUTER_BOUND ( 'NONE', #17764, .T. ) ;
#192727=EDGE_CURVE ( 'NONE', #43098, #73251, #131392, .T. ) ;
#192744=DIRECTION ( 'NONE',  ( 1.000000000000000000, 0.000000000000000000, 0.000000000000000000 ) ) ;
#192746=DIRECTION ( 'NONE',  ( 0.000000000000000000, -7.026728003956686545E-15, 1.000000000000000000 ) ) ;
#192765=DIRECTION ( 'NONE',  ( 0.000000000000000000, 1.000000000000000000, 6.982962677686266711E-15 ) ) ;
#192770=CARTESIAN_POINT ( 'NONE',  ( 23.14999999999999503, 64.25000000001151079, -48.17310748452440805 ) ) ;
#192820=DIRECTION ( 'NONE',  ( 1.000000000000000000, 0.000000000000000000, 0.000000000000000000 ) ) ;
#192835=DIRECTION ( 'NONE',  ( 0.000000000000000000, -6.982962677686266711E-15, 1.000000000000000000 ) ) ;
#192839=ADVANCED_FACE ( 'NONE', ( #214779 ), #76550, .T. ) ;
#192905=AXIS2_PLACEMENT_3D ( 'NONE', #86564, #245671, #64473 ) ;
#192913=VERTEX_POINT ( 'NONE', #137797 ) ;
#192948=CARTESIAN_POINT ( 'NONE',  ( 21.05000000000000071, 64.25000000001146816, -43.03791325517834565 ) ) ;
#192995=DIRECTION ( 'NONE',  ( -0.000000000000000000, 0.1298341882519953583, 0.9915357197604862671 ) ) ;
#192996=ADVANCED_FACE ( 'NONE', ( #222455 ), #12077, .T. ) ;
#193095=DIRECTION ( 'NONE',  ( 0.000000000000000000, 0.000000000000000000, -1.000000000000000000 ) ) ;
#193104=CARTESIAN_POINT ( 'NONE',  ( 21.05000000000000071, 76.00000000001142553, -36.02310748452432421 ) ) ;
#193176=CIRCLE ( 'NONE', #9991, 0.09999999999999939493 ) ;
#193181=CIRCLE ( 'NONE', #118144, 12.87499999999999822 ) ;
#193194=ORIENTED_EDGE ( 'NONE', *, *, #52348, .F. ) ;
#193195=EDGE_CURVE ( 'NONE', #38899, #69280, #17144, .T. ) ;
#193202=EDGE_CURVE ( 'NONE', #211829, #117589, #162898, .T. ) ;
#193205=CIRCLE ( 'NONE', #134888, 12.97499999999999609 ) ;
#193252=CYLINDRICAL_SURFACE ( 'NONE', #232889, 0.1000000000000028644 ) ;
#193255=DIRECTION ( 'NONE',  ( 0.000000000000000000, 0.000000000000000000, 1.000000000000000000 ) ) ;
#193297=CARTESIAN_POINT ( 'NONE',  ( -20.64999999999999858, 85.40000000001148805, -45.91707660717669626 ) ) ;
#193328=ORIENTED_EDGE ( 'NONE', *, *, #68038, .F. ) ;
#193347=ORIENTED_EDGE ( 'NONE', *, *, #100846, .T. ) ;
#193364=DIRECTION ( 'NONE',  ( 0.000000000000000000, 1.000000000000000000, 0.000000000000000000 ) ) ;
#193379=DIRECTION ( 'NONE',  ( 0.000000000000000000, 7.056502275159890832E-15, -1.000000000000000000 ) ) ;
#193391=DIRECTION ( 'NONE',  ( 1.000000000000000000, 0.000000000000000000, 0.000000000000000000 ) ) ;
#193400=CIRCLE ( 'NONE', #85006, 0.1000000000000052097 ) ;
#193412=ORIENTED_EDGE ( 'NONE', *, *, #79942, .F. ) ;
#193422=CARTESIAN_POINT ( 'NONE',  ( -22.59999970745345976, 76.00935637733928729, -81.27362069219354623 ) ) ;
#193424=PLANE ( 'NONE',  #217946 ) ;
#193451=CIRCLE ( 'NONE', #222630, 0.1000000000000028644 ) ;
#193458=DIRECTION ( 'NONE',  ( 0.000000000000000000, -0.1350103645451807555, -0.9908441862701610203 ) ) ;
#193461=DIRECTION ( 'NONE',  ( 1.000000000000000000, 0.000000000000000000, 0.000000000000000000 ) ) ;
#193493=EDGE_CURVE ( 'NONE', #196143, #97864, #129178, .T. ) ;
#193498=EDGE_LOOP ( 'NONE', ( #235816, #67638, #80153, #48864 ) ) ;
#193528=ORIENTED_EDGE ( 'NONE', *, *, #185720, .F. ) ;
#193535=VERTEX_POINT ( 'NONE', #69545 ) ;
#193539=VERTEX_POINT ( 'NONE', #8281 ) ;
#193555=DIRECTION ( 'NONE',  ( 0.000000000000000000, 0.8700118002898356018, -0.4930308989875170078 ) ) ;
#193611=CARTESIAN_POINT ( 'NONE',  ( 20.94999999999999929, 69.55000000001159322, -59.50608031408435039 ) ) ;
#193622=EDGE_CURVE ( 'NONE', #51613, #60391, #235027, .T. ) ;
#193624=DIRECTION ( 'NONE',  ( 0.000000000000000000, -6.467318590049456648E-15, 1.000000000000000000 ) ) ;
#193630=DIRECTION ( 'NONE',  ( 1.000000000000000000, 0.000000000000000000, 0.000000000000000000 ) ) ;
#193640=DIRECTION ( 'NONE',  ( 1.000000000000000000, 0.000000000000000000, 0.000000000000000000 ) ) ;
#193691=VECTOR ( 'NONE', #177299, 1000.000000000000000 ) ;
#193701=VECTOR ( 'NONE', #53286, 1000.000000000000000 ) ;
#193711=ORIENTED_EDGE ( 'NONE', *, *, #238321, .F. ) ;
#193761=CIRCLE ( 'NONE', #189843, 0.09999999999999739653 ) ;
#193764=DIRECTION ( 'NONE',  ( -1.000000000000000000, 0.000000000000000000, -0.000000000000000000 ) ) ;
#193799=CARTESIAN_POINT ( 'NONE',  ( -20.96428641294161110, 64.25000000001148237, -42.84821430658328012 ) ) ;
#193834=AXIS2_PLACEMENT_3D ( 'NONE', #60075, #219142, #40565 ) ;
#193842=VERTEX_POINT ( 'NONE', #240161 ) ;
#193850=LINE ( 'NONE', #17748, #217926 ) ;
#193906=CARTESIAN_POINT ( 'NONE',  ( -21.14999999999999858, 69.45934304831041572, -69.52310748452435973 ) ) ;
#193913=AXIS2_PLACEMENT_3D ( 'NONE', #119841, #139355, #138078 ) ;
#193949=ORIENTED_EDGE ( 'NONE', *, *, #95372, .F. ) ;
#193968=DIRECTION ( 'NONE',  ( 1.000000000000000000, -7.304098846218134667E-16, -4.639676173203993355E-30 ) ) ;
#193979=CIRCLE ( 'NONE', #98060, 0.1999999999999987899 ) ;
#193989=FACE_OUTER_BOUND ( 'NONE', #24152, .T. ) ;
#194007=CARTESIAN_POINT ( 'NONE',  ( -21.14999999999999503, 64.25000000001161027, -62.60396023856562664 ) ) ;
#194057=AXIS2_PLACEMENT_3D ( 'NONE', #2976, #82496, #202482 ) ;
#194059=EDGE_LOOP ( 'NONE', ( #139055, #215883, #72080, #82478 ) ) ;
#194060=DIRECTION ( 'NONE',  ( 1.000000000000000000, 0.000000000000000000, 0.000000000000000000 ) ) ;
#194075=CARTESIAN_POINT ( 'NONE',  ( 21.05000000000000071, 76.00000000001141132, -34.02310748452431710 ) ) ;
#194087=DIRECTION ( 'NONE',  ( 1.000000000000000000, 0.000000000000000000, 0.000000000000000000 ) ) ;
#194107=AXIS2_PLACEMENT_3D ( 'NONE', #236292, #56355, #156792 ) ;
#194126=TOROIDAL_SURFACE ( 'NONE', #2553, 0.2000000000000000111, 0.1000000000000000056 ) ;
#194128=CARTESIAN_POINT ( 'NONE',  ( -18.43634282235116473, 85.67978719993936920, -29.36245559907037617 ) ) ;
#194136=CARTESIAN_POINT ( 'NONE',  ( -22.59999985501179154, 64.25013020700868083, -69.58870615432405771 ) ) ;
#194142=CYLINDRICAL_SURFACE ( 'NONE', #146773, 0.1000000000000052097 ) ;
#194151=CARTESIAN_POINT ( 'NONE',  ( 22.39999999999999503, 64.25000000001165290, -69.42310748452440805 ) ) ;
#194158=EDGE_CURVE ( 'NONE', #198469, #52116, #238558, .T. ) ;
#194172=DIRECTION ( 'NONE',  ( 1.000000000000000000, 0.000000000000000000, 0.000000000000000000 ) ) ;
#194191=PLANE ( 'NONE',  #8259 ) ;
#194230=EDGE_LOOP ( 'NONE', ( #82907, #242873, #112319 ) ) ;
#194241=VERTEX_POINT ( 'NONE', #29500 ) ;
#194245=ORIENTED_EDGE ( 'NONE', *, *, #39743, .F. ) ;
#194262=ORIENTED_EDGE ( 'NONE', *, *, #98231, .F. ) ;
#194304=CIRCLE ( 'NONE', #123530, 0.09999999999999520384 ) ;
#194306=AXIS2_PLACEMENT_3D ( 'NONE', #175492, #91123, #179344 ) ;
#194338=ORIENTED_EDGE ( 'NONE', *, *, #250436, .T. ) ;
#194357=CARTESIAN_POINT ( 'NONE',  ( -20.15000000000000568, 66.70857864377425983, -57.17310748452438673 ) ) ;
#194358=CARTESIAN_POINT ( 'NONE',  ( 18.55807992284871588, 65.67101464000451472, -30.44043916224795510 ) ) ;
#194367=FACE_OUTER_BOUND ( 'NONE', #109888, .T. ) ;
#194397=ORIENTED_EDGE ( 'NONE', *, *, #187853, .F. ) ;
#194402=CARTESIAN_POINT ( 'NONE',  ( -18.59999999999999787, 74.73821383144657204, -61.43660852097884373 ) ) ;
#194411=ORIENTED_EDGE ( 'NONE', *, *, #166199, .F. ) ;
#194419=ORIENTED_EDGE ( 'NONE', *, *, #251342, .T. ) ;
#194432=DIRECTION ( 'NONE',  ( 1.000000000000000000, 0.000000000000000000, 0.000000000000000000 ) ) ;
#194445=EDGE_CURVE ( 'NONE', #195194, #191153, #213218, .T. ) ;
#194479=ORIENTED_EDGE ( 'NONE', *, *, #10389, .F. ) ;
#194504=ORIENTED_EDGE ( 'NONE', *, *, #180110, .F. ) ;
#194560=CARTESIAN_POINT ( 'NONE',  ( -22.24259225415828567, 68.50806212944624463, -69.62217336797721146 ) ) ;
#194564=EDGE_LOOP ( 'NONE', ( #232178, #132258, #216564, #194245 ) ) ;
#194566=CIRCLE ( 'NONE', #198620, 0.1000000000000028644 ) ;
#194579=FACE_OUTER_BOUND ( 'NONE', #28774, .T. ) ;
#194587=TOROIDAL_SURFACE ( 'NONE', #107062, 2.100000000000002309, 0.1000000000000000056 ) ;
#194595=ORIENTED_EDGE ( 'NONE', *, *, #85791, .F. ) ;
#194618=CIRCLE ( 'NONE', #227908, 0.1000000000000028644 ) ;
#194643=DIRECTION ( 'NONE',  ( -2.557131231893037478E-16, -0.8660254037844420383, 0.4999999999999941713 ) ) ;
#194656=ADVANCED_FACE ( 'NONE', ( #15356 ), #213524, .F. ) ;
#194662=CARTESIAN_POINT ( 'NONE',  ( -23.25000000000000000, 69.06610602788505560, -32.23746165015079868 ) ) ;
#194702=DIRECTION ( 'NONE',  ( 0.000000000000000000, 0.000000000000000000, 1.000000000000000000 ) ) ;
#194706=ORIENTED_EDGE ( 'NONE', *, *, #194445, .F. ) ;
#194723=FACE_OUTER_BOUND ( 'NONE', #56228, .T. ) ;
#194727=CIRCLE ( 'NONE', #24022, 0.1000000000000028644 ) ;
#194742=ORIENTED_EDGE ( 'NONE', *, *, #221763, .T. ) ;
#194743=CARTESIAN_POINT ( 'NONE',  ( 21.05000000000000071, 67.18479819544488407, -61.10256998784131355 ) ) ;
#194768=DIRECTION ( 'NONE',  ( -0.000000000000000000, 1.000000000000000000, 6.982962677686266711E-15 ) ) ;
#194779=DIRECTION ( 'NONE',  ( -4.391705002472927119E-16, -1.000000000000000000, -7.026728003956683390E-15 ) ) ;
#194788=CIRCLE ( 'NONE', #3209, 0.09999999999999939493 ) ;
#194818=CARTESIAN_POINT ( 'NONE',  ( 21.05000000000000071, 64.40000000001145963, -42.95131071479990936 ) ) ;
#194836=LINE ( 'NONE', #215640, #93855 ) ;
#194845=FACE_OUTER_BOUND ( 'NONE', #155475, .T. ) ;
#194851=CARTESIAN_POINT ( 'NONE',  ( 20.94999999999999929, 70.15000000001163016, -59.39061026024639034 ) ) ;
#194853=CARTESIAN_POINT ( 'NONE',  ( 21.05000000000000426, 75.94851711812962947, -75.82328730243888515 ) ) ;
#194869=DIRECTION ( 'NONE',  ( 1.000000000000000000, 0.000000000000000000, 0.000000000000000000 ) ) ;
#194871=CARTESIAN_POINT ( 'NONE',  ( 22.50000000000000000, 76.00000000001165290, -69.52310748452431710 ) ) ;
#194877=( BOUNDED_SURFACE ( )  B_SPLINE_SURFACE ( 3, 2, ( 
 ( #144689, #127718, #26055 ),
 ( #106844, #5158, #228107 ),
 ( #48161, #187702, #104270 ),
 ( #164280, #63884, #27369 ),
 ( #247655, #66451, #9043 ),
 ( #163004, #246375, #147267 ),
 ( #148563, #7772, #207266 ),
 ( #145975, #224230, #225494 ) ),
 .UNSPECIFIED., .F., .F., .F. ) 
 B_SPLINE_SURFACE_WITH_KNOTS ( ( 4, 2, 2, 4 ),
 ( 3, 3 ),
 ( 0.0001704874539069911317, 0.0003809798300636645443, 0.0004862260181420012778, 0.0005914722062203380112 ),
 ( 0.000000000000000000, 1.000000000000000000 ),
 .UNSPECIFIED. ) 
 GEOMETRIC_REPRESENTATION_ITEM ( )  RATIONAL_B_SPLINE_SURFACE ( (
 ( 1.000000000000000000, 0.7071067811864850672, 1.000000000000000000),
 ( 1.000000000000000000, 0.7670648383575194851, 1.000000000000000000),
 ( 1.000000000000000000, 0.8204820770253823392, 1.000000000000000000),
 ( 1.000000000000000000, 0.8877218296113124074, 1.000000000000000000),
 ( 1.000000000000000000, 0.9080815932665092793, 1.000000000000000000),
 ( 1.000000000000000000, 0.9395541505861816356, 1.000000000000000000),
 ( 1.000000000000000000, 0.9506520335379058384, 1.000000000000000000),
 ( 1.000000000000000000, 0.9504532311154573199, 1.000000000000000000) ) ) 
 REPRESENTATION_ITEM ( '' )  SURFACE ( )  );
#194890=CARTESIAN_POINT ( 'NONE',  ( -21.14999999999999858, 69.45934304831041572, -69.42310748452437963 ) ) ;
#194945=LINE ( 'NONE', #197479, #7288 ) ;
#194955=CARTESIAN_POINT ( 'NONE',  ( 23.25000000000000000, 85.60000000001174669, -81.27310748452424605 ) ) ;
#194989=FACE_OUTER_BOUND ( 'NONE', #244724, .T. ) ;
#195038=ORIENTED_EDGE ( 'NONE', *, *, #58547, .T. ) ;
#195059=DIRECTION ( 'NONE',  ( 0.000000000000000000, 0.000000000000000000, 1.000000000000000000 ) ) ;
#195067=CARTESIAN_POINT ( 'NONE',  ( -18.59999999999999787, 77.86671491006887891, -57.77043223824230722 ) ) ;
#195072=CIRCLE ( 'NONE', #161762, 0.09999999999999939493 ) ;
#195131=EDGE_CURVE ( 'NONE', #97821, #202965, #152003, .T. ) ;
#195169=CARTESIAN_POINT ( 'NONE',  ( 18.46905048506370761, 85.47374425739377557, -29.34712119226885108 ) ) ;
#195180=EDGE_CURVE ( 'NONE', #27421, #38202, #213266, .T. ) ;
#195194=VERTEX_POINT ( 'NONE', #137523 ) ;
#195212=AXIS2_PLACEMENT_3D ( 'NONE', #90378, #188209, #211634 ) ;
#195231=DIRECTION ( 'NONE',  ( 1.000000000000000000, 0.000000000000000000, 0.000000000000000000 ) ) ;
#195275=EDGE_LOOP ( 'NONE', ( #206362, #140240, #60918, #257081 ) ) ;
#195318=DIRECTION ( 'NONE',  ( 0.1538461538461484146, -0.9880948137434723000, 0.000000000000000000 ) ) ;
#195332=AXIS2_PLACEMENT_3D ( 'NONE', #146858, #111614, #89462 ) ;
#195360=DIRECTION ( 'NONE',  ( 1.000000000000000000, -3.265361837132813093E-16, -2.280189983783949500E-30 ) ) ;
#195372=DIRECTION ( 'NONE',  ( 0.000000000000000000, 0.000000000000000000, 1.000000000000000000 ) ) ;
#195394=LINE ( 'NONE', #38875, #159436 ) ;
#195395=ORIENTED_EDGE ( 'NONE', *, *, #130619, .F. ) ;
#195414=CARTESIAN_POINT ( 'NONE',  ( -18.31572283045126071, 85.54843783089721398, -29.17248183346574564 ) ) ;
#195456=AXIS2_PLACEMENT_3D ( 'NONE', #100670, #18607, #180254 ) ;
#195458=FACE_OUTER_BOUND ( 'NONE', #217105, .T. ) ;
#195470=CARTESIAN_POINT ( 'NONE',  ( 20.94999999999999929, 70.50000000001151079, -48.42837350343745584 ) ) ;
#195500=ORIENTED_EDGE ( 'NONE', *, *, #228377, .F. ) ;
#195520=CARTESIAN_POINT ( 'NONE',  ( 18.49999999999999645, 77.83534155023598089, -57.96795619196132776 ) ) ;
#195532=CYLINDRICAL_SURFACE ( 'NONE', #198178, 0.09999999999999939493 ) ;
#195556=CARTESIAN_POINT ( 'NONE',  ( -21.11825140030087766, 69.55459243459189622, -69.53031110515726709 ) ) ;
#195570=CARTESIAN_POINT ( 'NONE',  ( 20.94999999999999929, 77.16270174994961906, -61.62310748452431142 ) ) ;
#195601=FACE_OUTER_BOUND ( 'NONE', #164674, .T. ) ;
#195606=LINE ( 'NONE', #119932, #171991 ) ;
#195644=CARTESIAN_POINT ( 'NONE',  ( -21.05000000000000071, 74.14897176987071248, -57.86919421510183525 ) ) ;
#195680=DIRECTION ( 'NONE',  ( 0.000000000000000000, -6.467318590049456648E-15, 1.000000000000000000 ) ) ;
#195702=ORIENTED_EDGE ( 'NONE', *, *, #64373, .F. ) ;
#195705=AXIS2_PLACEMENT_3D ( 'NONE', #40371, #117304, #218956 ) ;
#195721=ORIENTED_EDGE ( 'NONE', *, *, #110116, .T. ) ;
#195760=AXIS2_PLACEMENT_3D ( 'NONE', #239488, #179525, #204188 ) ;
#195763=ORIENTED_EDGE ( 'NONE', *, *, #187524, .F. ) ;
#195794=CARTESIAN_POINT ( 'NONE',  ( 18.42555734704284731, 85.49715836194830842, -62.48327698678934183 ) ) ;
#195811=ORIENTED_EDGE ( 'NONE', *, *, #3357, .F. ) ;
#195840=DIRECTION ( 'NONE',  ( 0.000000000000000000, 0.000000000000000000, 1.000000000000000000 ) ) ;
#195864=CARTESIAN_POINT ( 'NONE',  ( -20.54999999999999716, 85.00000000001149658, -45.91707660717669626 ) ) ;
#195983=ORIENTED_EDGE ( 'NONE', *, *, #132511, .T. ) ;
#195996=VERTEX_POINT ( 'NONE', #233166 ) ;
#196002=DIRECTION ( 'NONE',  ( 1.000000000000000000, 0.000000000000000000, 0.000000000000000000 ) ) ;
#196010=CIRCLE ( 'NONE', #42077, 0.09999999999999971412 ) ;
#196021=CARTESIAN_POINT ( 'NONE',  ( 20.94999999999999929, 85.00000000001149658, -45.91707660717670336 ) ) ;
#196040=EDGE_CURVE ( 'NONE', #101698, #198432, #34796, .T. ) ;
#196041=CARTESIAN_POINT ( 'NONE',  ( -18.41799967126723914, 85.50000000001161027, -62.49103767126882758 ) ) ;
#196119=EDGE_CURVE ( 'NONE', #96547, #69378, #27075, .T. ) ;
#196120=CARTESIAN_POINT ( 'NONE',  ( 21.05000000000000071, 76.01759718701968893, -75.96387837818673461 ) ) ;
#196130=LINE ( 'NONE', #199991, #23533 ) ;
#196143=VERTEX_POINT ( 'NONE', #42635 ) ;
#196165=EDGE_CURVE ( 'NONE', #100350, #216920, #247241, .T. ) ;
#196169=AXIS2_PLACEMENT_3D ( 'NONE', #644, #239293, #56760 ) ;
#196198=CARTESIAN_POINT ( 'NONE',  ( 22.39999999999999503, 76.10085836911045476, -81.27267460801371612 ) ) ;
#196226=ORIENTED_EDGE ( 'NONE', *, *, #71271, .F. ) ;
#196237=AXIS2_PLACEMENT_3D ( 'NONE', #27345, #69016, #229365 ) ;
#196239=CARTESIAN_POINT ( 'NONE',  ( 23.14999999999999503, 69.55000000001173532, -81.27310748452437394 ) ) ;
#196257=CARTESIAN_POINT ( 'NONE',  ( -18.59999999999999787, 64.25000000001151079, -48.27310748452440237 ) ) ;
#196288=EDGE_CURVE ( 'NONE', #195996, #152615, #56250, .T. ) ;
#196290=VERTEX_POINT ( 'NONE', #90733 ) ;
#196304=DIRECTION ( 'NONE',  ( 1.000000000000000000, 0.000000000000000000, 0.000000000000000000 ) ) ;
#196306=DIRECTION ( 'NONE',  ( 0.000000000000000000, -1.000000000000000000, 0.000000000000000000 ) ) ;
#196326=DIRECTION ( 'NONE',  ( 1.000000000000000000, 0.000000000000000000, 0.000000000000000000 ) ) ;
#196376=CARTESIAN_POINT ( 'NONE',  ( -20.64999999999999858, 71.65000000001151648, -48.37310748452435405 ) ) ;
#196413=DIRECTION ( 'NONE',  ( 1.000000000000000000, 0.000000000000000000, 0.000000000000000000 ) ) ;
#196455=CARTESIAN_POINT ( 'NONE',  ( -21.64999999999999858, 68.75000000001152500, -48.37310748452436826 ) ) ;
#196464=VERTEX_POINT ( 'NONE', #77579 ) ;
#196488=CARTESIAN_POINT ( 'NONE',  ( 23.14999999999999503, 64.25000000001156764, -57.37310748452440379 ) ) ;
#196513=VERTEX_POINT ( 'NONE', #202688 ) ;
#196541=CARTESIAN_POINT ( 'NONE',  ( 20.59588692710267921, 65.63127657884294308, -61.88402639001368044 ) ) ;
#196543=ORIENTED_EDGE ( 'NONE', *, *, #89467, .T. ) ;
#196565=DIRECTION ( 'NONE',  ( 0.000000000000000000, -1.616829647512364004E-14, 1.000000000000000000 ) ) ;
#196571=DIRECTION ( 'NONE',  ( 0.000000000000000000, -7.545205021724366615E-15, 1.000000000000000000 ) ) ;
#196583=ORIENTED_EDGE ( 'NONE', *, *, #638, .T. ) ;
#196598=VERTEX_POINT ( 'NONE', #207862 ) ;
#196620=CARTESIAN_POINT ( 'NONE',  ( -23.25000000000000000, 74.08971962617978591, -56.89173962932539297 ) ) ;
#196640=DIRECTION ( 'NONE',  ( 0.000000000000000000, -0.1350103645451807555, -0.9908441862701610203 ) ) ;
#196641=EDGE_LOOP ( 'NONE', ( #179756, #75166, #42301, #35425 ) ) ;
#196658=ORIENTED_EDGE ( 'NONE', *, *, #121852, .T. ) ;
#196661=EDGE_LOOP ( 'NONE', ( #219534, #116910, #164561, #218910 ) ) ;
#196667=DIRECTION ( 'NONE',  ( 0.000000000000000000, -0.8660254037844377084, -0.5000000000000016653 ) ) ;
#196668=DIRECTION ( 'NONE',  ( 1.000000000000000000, 0.000000000000000000, 0.000000000000000000 ) ) ;
#196689=AXIS2_PLACEMENT_3D ( 'NONE', #176961, #243304, #180788 ) ;
#196743=ORIENTED_EDGE ( 'NONE', *, *, #65728, .F. ) ;
#196763=DIRECTION ( 'NONE',  ( 0.000000000000000000, -6.982962677686266711E-15, 1.000000000000000000 ) ) ;
#196769=CARTESIAN_POINT ( 'NONE',  ( 18.59999999999999076, 69.35000000001151932, -48.17310748452437252 ) ) ;
#196771=CYLINDRICAL_SURFACE ( 'NONE', #193913, 0.1000000000000026007 ) ;
#196791=CARTESIAN_POINT ( 'NONE',  ( 22.59999999999999432, 75.90000000001172964, -81.17267829206912211 ) ) ;
#196792=B_SPLINE_CURVE_WITH_KNOTS ( 'NONE', 3,
 ( #30558, #69684, #85341, #104896 ),
 .UNSPECIFIED., .F., .F.,
 ( 4, 4 ),
 ( 0.000000000000000000, 0.0001048066582182452479 ),
 .UNSPECIFIED. ) ;
#196822=DIRECTION ( 'NONE',  ( 1.000000000000000000, -0.000000000000000000, 0.000000000000000000 ) ) ;
#196850=DIRECTION ( 'NONE',  ( 0.000000000000000000, 0.000000000000000000, -1.000000000000000000 ) ) ;
#196858=ADVANCED_FACE ( 'NONE', ( #19923, #113867 ), #193424, .F. ) ;
#196886=CARTESIAN_POINT ( 'NONE',  ( -20.94999999999999929, 87.65000000001144542, -39.02310748452423894 ) ) ;
#196894=CARTESIAN_POINT ( 'NONE',  ( 21.07928932188134397, 69.67148334361836248, -69.62200263017875557 ) ) ;
#196906=CARTESIAN_POINT ( 'NONE',  ( -20.94999999999999929, 64.35000000001160458, -62.50830171387039513 ) ) ;
#196913=CARTESIAN_POINT ( 'NONE',  ( 18.48413544395649666, 85.66430403363912660, -29.34000249148596140 ) ) ;
#196925=DIRECTION ( 'NONE',  ( 0.000000000000000000, 0.000000000000000000, 1.000000000000000000 ) ) ;
#196949=CARTESIAN_POINT ( 'NONE',  ( -20.64999999999999858, 74.00000000001151079, -48.84772940728643675 ) ) ;
#196986=VERTEX_POINT ( 'NONE', #202395 ) ;
#197003=ORIENTED_EDGE ( 'NONE', *, *, #87299, .T. ) ;
#197010=EDGE_CURVE ( 'NONE', #218009, #217695, #118007, .T. ) ;
#197019=DIRECTION ( 'NONE',  ( -3.265361837132813093E-16, -1.000000000000000000, 7.445645354460596589E-46 ) ) ;
#197021=DIRECTION ( 'NONE',  ( 0.000000000000000000, -0.9274965247785504907, -0.3738317757009320674 ) ) ;
#197026=ORIENTED_EDGE ( 'NONE', *, *, #244362, .T. ) ;
#197027=DIRECTION ( 'NONE',  ( 0.000000000000000000, -1.000000000000000000, -8.717686153663073805E-15 ) ) ;
#197042=ORIENTED_EDGE ( 'NONE', *, *, #32828, .F. ) ;
#197044=ORIENTED_EDGE ( 'NONE', *, *, #242558, .T. ) ;
#197046=ORIENTED_EDGE ( 'NONE', *, *, #239573, .T. ) ;
#197077=EDGE_CURVE ( 'NONE', #117921, #86585, #172301, .T. ) ;
#197090=AXIS2_PLACEMENT_3D ( 'NONE', #3596, #222625, #80539 ) ;
#197119=ADVANCED_FACE ( 'NONE', ( #189257 ), #34834, .F. ) ;
#197132=VECTOR ( 'NONE', #134743, 1000.000000000000000 ) ;
#197138=EDGE_CURVE ( 'NONE', #67782, #94150, #22363, .T. ) ;
#197183=CARTESIAN_POINT ( 'NONE',  ( 23.24999999999999645, 76.00000000001142553, -36.02310748452432421 ) ) ;
#197219=ORIENTED_EDGE ( 'NONE', *, *, #112142, .F. ) ;
#197234=EDGE_CURVE ( 'NONE', #221002, #10713, #234914, .T. ) ;
#197252=CARTESIAN_POINT ( 'NONE',  ( 20.94999999999999929, 77.83534155023599510, -57.96795619196132776 ) ) ;
#197271=CARTESIAN_POINT ( 'NONE',  ( -21.45000000000000284, 68.29142135624888965, -57.27310748452437394 ) ) ;
#197280=CIRCLE ( 'NONE', #247343, 0.1000000000000028644 ) ;
#197294=DIRECTION ( 'NONE',  ( 0.000000000000000000, 0.9893560106964510714, -0.1455152366551481502 ) ) ;
#197320=ORIENTED_EDGE ( 'NONE', *, *, #14867, .T. ) ;
#197324=CARTESIAN_POINT ( 'NONE',  ( 21.05000000000000071, 76.00000000001168132, -73.82310748452435689 ) ) ;
#197335=CARTESIAN_POINT ( 'NONE',  ( -18.59999999999999787, 77.63717271298195044, -57.94095411905229298 ) ) ;
#197344=CIRCLE ( 'NONE', #126622, 12.77499999999999503 ) ;
#197382=DIRECTION ( 'NONE',  ( -1.000000000000000000, 0.000000000000000000, 0.000000000000000000 ) ) ;
#197395=AXIS2_PLACEMENT_3D ( 'NONE', #124957, #123673, #166676 ) ;
#197399=DIRECTION ( 'NONE',  ( 1.000000000000000000, -3.265361837132813093E-16, -2.280189983783949500E-30 ) ) ;
#197424=FACE_OUTER_BOUND ( 'NONE', #55619, .T. ) ;
#197433=AXIS2_PLACEMENT_3D ( 'NONE', #207625, #185477, #10695 ) ;
#197468=DIRECTION ( 'NONE',  ( -2.602085213965226419E-14, 6.982962677686266711E-15, -1.000000000000000000 ) ) ;
#197479=CARTESIAN_POINT ( 'NONE',  ( -20.94999999999999929, 87.75000000001143974, -39.12310748452424747 ) ) ;
#197480=CARTESIAN_POINT ( 'NONE',  ( -21.14999999999999858, 64.25000000001161027, -62.73924182154625129 ) ) ;
#197490=CARTESIAN_POINT ( 'NONE',  ( -21.55000000000000071, 68.65000000001157332, -57.17310748452437252 ) ) ;
#197502=CARTESIAN_POINT ( 'NONE',  ( 21.14999999999999858, 67.21339244341145047, -57.27310748452438105 ) ) ;
#197506=ORIENTED_EDGE ( 'NONE', *, *, #80925, .T. ) ;
#197517=ORIENTED_EDGE ( 'NONE', *, *, #76449, .F. ) ;
#197555=DIRECTION ( 'NONE',  ( 0.000000000000000000, 3.341447938192219320E-14, 1.000000000000000000 ) ) ;
#197557=EDGE_CURVE ( 'NONE', #160578, #52356, #51898, .T. ) ;
#197605=ORIENTED_EDGE ( 'NONE', *, *, #199231, .T. ) ;
#197627=CARTESIAN_POINT ( 'NONE',  ( 18.49999999999999645, 77.16412189325258453, -28.10825939895270764 ) ) ;
#197632=DIRECTION ( 'NONE',  ( 0.000000000000000000, -0.1298341882519953583, -0.9915357197604862671 ) ) ;
#197667=EDGE_CURVE ( 'NONE', #50215, #211121, #107481, .T. ) ;
#197681=DIRECTION ( 'NONE',  ( 0.000000000000000000, -6.982962677686266711E-15, 1.000000000000000000 ) ) ;
#197688=CARTESIAN_POINT ( 'NONE',  ( 18.44444291854882323, 85.49010118095463895, -29.39420351963329026 ) ) ;
#197749=VERTEX_POINT ( 'NONE', #153080 ) ;
#197756=ADVANCED_FACE ( 'NONE', ( #48789 ), #250832, .T. ) ;
#197775=ORIENTED_EDGE ( 'NONE', *, *, #127198, .F. ) ;
#197783=CARTESIAN_POINT ( 'NONE',  ( -21.12230431290519661, 69.54243334671865284, -69.52831733621336241 ) ) ;
#197795=DIRECTION ( 'NONE',  ( -0.7070776581708965169, 0.7071359030027827286, 4.937903618720407826E-15 ) ) ;
#197797=ORIENTED_EDGE ( 'NONE', *, *, #82387, .F. ) ;
#197799=EDGE_CURVE ( 'NONE', #252677, #147021, #149203, .T. ) ;
#197829=LINE ( 'NONE', #233148, #118043 ) ;
#197889=AXIS2_PLACEMENT_3D ( 'NONE', #96838, #232561, #216811 ) ;
#197900=CARTESIAN_POINT ( 'NONE',  ( -21.12844524849339223, 64.25000000001161027, -62.61869401368159771 ) ) ;
#197901=DIRECTION ( 'NONE',  ( 1.000000000000000000, 0.000000000000000000, 0.000000000000000000 ) ) ;
#197906=DIRECTION ( 'NONE',  ( 0.000000000000000000, 0.000000000000000000, 1.000000000000000000 ) ) ;
#197940=CARTESIAN_POINT ( 'NONE',  ( -18.40000000000000213, 85.50000000001139711, -29.10095763519389322 ) ) ;
#197943=DIRECTION ( 'NONE',  ( 1.000000000000000000, 0.000000000000000000, 0.000000000000000000 ) ) ;
#197960=VECTOR ( 'NONE', #24662, 1000.000000000000000 ) ;
#197961=ORIENTED_EDGE ( 'NONE', *, *, #96031, .F. ) ;
#197994=CARTESIAN_POINT ( 'NONE',  ( -20.89192007715127986, 65.67101464000451472, -30.44043916224795510 ) ) ;
#198015=EDGE_CURVE ( 'NONE', #117567, #174834, #184141, .T. ) ;
#198023=ORIENTED_EDGE ( 'NONE', *, *, #48316, .F. ) ;
#198040=CARTESIAN_POINT ( 'NONE',  ( 23.14999999999999858, 71.00000000001151079, -48.42837350343745584 ) ) ;
#198052=CIRCLE ( 'NONE', #56390, 0.09999999999999976963 ) ;
#198063=DIRECTION ( 'NONE',  ( -0.000000000000000000, -6.982962677686266711E-15, 1.000000000000000000 ) ) ;
#198094=VERTEX_POINT ( 'NONE', #100291 ) ;
#198098=LINE ( 'NONE', #32968, #254243 ) ;
#198101=ORIENTED_EDGE ( 'NONE', *, *, #77916, .T. ) ;
#198108=CARTESIAN_POINT ( 'NONE',  ( -22.39999999999999858, 76.10085836911045476, -81.27267460801371612 ) ) ;
#198118=CARTESIAN_POINT ( 'NONE',  ( 21.05000000000000426, 65.43724016256057041, -62.06629352660576870 ) ) ;
#198128=CARTESIAN_POINT ( 'NONE',  ( -22.39999999999999858, 75.90000000001170122, -77.31388708289772183 ) ) ;
#198132=DIRECTION ( 'NONE',  ( 0.000000000000000000, -0.1298341882519953860, -0.9915357197604862671 ) ) ;
#198143=ORIENTED_EDGE ( 'NONE', *, *, #158388, .F. ) ;
#198147=AXIS2_PLACEMENT_3D ( 'NONE', #41900, #5281, #165699 ) ;
#198160=AXIS2_PLACEMENT_3D ( 'NONE', #183584, #84425, #152184 ) ;
#198178=AXIS2_PLACEMENT_3D ( 'NONE', #16883, #96379, #124959 ) ;
#198182=CARTESIAN_POINT ( 'NONE',  ( 21.08134388332232234, 69.66531941949371287, -69.59892640203138114 ) ) ;
#198241=LINE ( 'NONE', #256886, #10662 ) ;
#198255=FACE_OUTER_BOUND ( 'NONE', #178579, .T. ) ;
#198277=PRODUCT_DEFINITION ( 'UNKNOWN', '', #123793, #183477 ) ;
#198307=CARTESIAN_POINT ( 'NONE',  ( 23.14999999999999858, 71.18691588786198565, -47.96462524104817504 ) ) ;
#198317=CARTESIAN_POINT ( 'NONE',  ( 21.05000000000000071, 71.14953271029195037, -57.48884007552268116 ) ) ;
#198388=VERTEX_POINT ( 'NONE', #160325 ) ;
#198394=EDGE_CURVE ( 'NONE', #161516, #248655, #31484, .T. ) ;
#198411=DIRECTION ( 'NONE',  ( -1.000000000000000000, 0.000000000000000000, 0.000000000000000000 ) ) ;
#198416=CARTESIAN_POINT ( 'NONE',  ( 23.14999999999999858, 76.00000000001165290, -69.52310748452431710 ) ) ;
#198418=CARTESIAN_POINT ( 'NONE',  ( -23.15000000000000213, 87.65000000001144542, -39.02310748452423894 ) ) ;
#198420=DIRECTION ( 'NONE',  ( -0.000000000000000000, 1.000000000000000000, 6.982962677686266711E-15 ) ) ;
#198431=DIRECTION ( 'NONE',  ( 1.000000000000000000, 0.000000000000000000, 0.000000000000000000 ) ) ;
#198432=VERTEX_POINT ( 'NONE', #201992 ) ;
#198437=VECTOR ( 'NONE', #249477, 1000.000000000000000 ) ;
#198445=CIRCLE ( 'NONE', #181881, 0.3999999999999975797 ) ;
#198452=VECTOR ( 'NONE', #152093, 999.9999999999998863 ) ;
#198467=FACE_OUTER_BOUND ( 'NONE', #51299, .T. ) ;
#198469=VERTEX_POINT ( 'NONE', #28539 ) ;
#198476=CARTESIAN_POINT ( 'NONE',  ( -18.59999999999999787, 74.83729825007360148, -61.52310748452433131 ) ) ;
#198485=ORIENTED_EDGE ( 'NONE', *, *, #147667, .T. ) ;
#198503=VECTOR ( 'NONE', #174299, 1000.000000000000000 ) ;
#198544=VECTOR ( 'NONE', #34274, 1000.000000000000000 ) ;
#198551=DIRECTION ( 'NONE',  ( 0.000000000000000000, -6.938893903907222067E-15, 1.000000000000000000 ) ) ;
#198590=CARTESIAN_POINT ( 'NONE',  ( -18.47079683080344026, 85.47166410525650804, -62.41424694353178637 ) ) ;
#198595=CARTESIAN_POINT ( 'NONE',  ( 18.49999999999999289, 65.75000000001151079, -48.17310748452439384 ) ) ;
#198601=ORIENTED_EDGE ( 'NONE', *, *, #141777, .F. ) ;
#198620=AXIS2_PLACEMENT_3D ( 'NONE', #120205, #21096, #116330 ) ;
#198674=DIRECTION ( 'NONE',  ( -1.000000000000000000, 0.000000000000000000, -6.938893903907270030E-14 ) ) ;
#198698=CARTESIAN_POINT ( 'NONE',  ( -20.94999999999999929, 76.00000000001142553, -36.02310748452432421 ) ) ;
#198722=VECTOR ( 'NONE', #171864, 999.9999999999998863 ) ;
#198754=CARTESIAN_POINT ( 'NONE',  ( -18.59999999999999787, 64.35000000001157616, -57.37310748452439668 ) ) ;
#198766=ORIENTED_EDGE ( 'NONE', *, *, #216858, .T. ) ;
#198804=AXIS2_PLACEMENT_3D ( 'NONE', #219791, #140242, #202803 ) ;
#198817=CARTESIAN_POINT ( 'NONE',  ( -22.59999999999999787, 75.90000000001172964, -81.17267829206912211 ) ) ;
#198819=LINE ( 'NONE', #235374, #237257 ) ;
#198846=VECTOR ( 'NONE', #60439, 1000.000000000000114 ) ;
#198858=AXIS2_PLACEMENT_3D ( 'NONE', #107654, #7263, #88063 ) ;
#198906=ORIENTED_EDGE ( 'NONE', *, *, #9693, .F. ) ;
#198915=AXIS2_PLACEMENT_3D ( 'NONE', #179248, #200074, #102212 ) ;
#198916=ORIENTED_EDGE ( 'NONE', *, *, #203695, .T. ) ;
#198926=DIRECTION ( 'NONE',  ( 0.000000000000000000, -0.4999999999999689138, 0.8660254037844565822 ) ) ;
#198970=EDGE_CURVE ( 'NONE', #25147, #194241, #178961, .T. ) ;
#198985=CARTESIAN_POINT ( 'NONE',  ( 22.39999999999999503, 75.90000000001170122, -77.31388708289770761 ) ) ;
#199016=CARTESIAN_POINT ( 'NONE',  ( -20.94999999999999929, 74.16465844978715438, -57.86795619196135476 ) ) ;
#199020=EDGE_LOOP ( 'NONE', ( #202819, #69151, #37886, #8856 ) ) ;
#199057=ORIENTED_EDGE ( 'NONE', *, *, #247944, .T. ) ;
#199058=ORIENTED_EDGE ( 'NONE', *, *, #139271, .F. ) ;
#199118=FACE_OUTER_BOUND ( 'NONE', #257110, .T. ) ;
#199122=CARTESIAN_POINT ( 'NONE',  ( 20.94999999999999929, 67.22371710471902873, -48.27310748452438105 ) ) ;
#199124=DIRECTION ( 'NONE',  ( -0.000000000000000000, 1.000000000000000000, 6.982962677686267499E-15 ) ) ;
#199211=CIRCLE ( 'NONE', #207787, 0.1000000000000028644 ) ;
#199220=AXIS2_PLACEMENT_3D ( 'NONE', #104718, #245566, #126897 ) ;
#199225=EDGE_CURVE ( 'NONE', #231640, #116304, #81115, .T. ) ;
#199231=EDGE_CURVE ( 'NONE', #37076, #34877, #15724, .T. ) ;
#199280=TOROIDAL_SURFACE ( 'NONE', #240971, 0.2000000000000000111, 0.1000000000000000056 ) ;
#199287=CARTESIAN_POINT ( 'NONE',  ( 21.05000000000000071, 69.74218538953552127, -69.62089777583315708 ) ) ;
#199291=AXIS2_PLACEMENT_3D ( 'NONE', #188187, #228605, #249453 ) ;
#199302=CARTESIAN_POINT ( 'NONE',  ( -20.94999675878240808, 65.70692517833182933, -30.56446533783036656 ) ) ;
#199330=CIRCLE ( 'NONE', #228555, 0.1999999999999987899 ) ;
#199343=ADVANCED_FACE ( 'NONE', ( #220322 ), #159080, .T. ) ;
#199350=DIRECTION ( 'NONE',  ( -1.000000000000000000, 2.952720810173289112E-16, 2.061873921506763405E-30 ) ) ;
#199354=EDGE_CURVE ( 'NONE', #177806, #201109, #41690, .T. ) ;
#199362=EDGE_LOOP ( 'NONE', ( #55952, #163182, #224178, #7369, #75361 ) ) ;
#199363=ORIENTED_EDGE ( 'NONE', *, *, #200247, .F. ) ;
#199371=LINE ( 'NONE', #179808, #220504 ) ;
#199397=CARTESIAN_POINT ( 'NONE',  ( -20.64999999999999858, 76.00000000001142553, -36.02310748452432421 ) ) ;
#199450=CARTESIAN_POINT ( 'NONE',  ( -23.15000000000000213, 71.65000000001155911, -57.17310748452435121 ) ) ;
#199473=LINE ( 'NONE', #140761, #63928 ) ;
#199479=EDGE_CURVE ( 'NONE', #48405, #227579, #84600, .T. ) ;
#199481=CARTESIAN_POINT ( 'NONE',  ( 21.05000000000000071, 77.73625713160897988, -57.95445515550681392 ) ) ;
#199510=ADVANCED_FACE ( 'NONE', ( #1239 ), #80772, .T. ) ;
#199547=DIRECTION ( 'NONE',  ( 2.952720810173289112E-16, 1.000000000000000000, 6.938893903907222067E-15 ) ) ;
#199583=AXIS2_PLACEMENT_3D ( 'NONE', #140772, #117361, #79493 ) ;
#199650=ADVANCED_FACE ( 'NONE', ( #114481 ), #123015, .T. ) ;
#199664=VERTEX_POINT ( 'NONE', #55753 ) ;
#199751=ORIENTED_EDGE ( 'NONE', *, *, #66782, .F. ) ;
#199780=EDGE_LOOP ( 'NONE', ( #213333, #254458, #61745, #255051, #82739 ) ) ;
#199797=DIRECTION ( 'NONE',  ( -1.000000000000000000, 0.000000000000000000, 0.000000000000000000 ) ) ;
#199838=ORIENTED_EDGE ( 'NONE', *, *, #111226, .F. ) ;
#199855=TOROIDAL_SURFACE ( 'NONE', #87385, 0.4000000000000005773, 0.1000000000000000056 ) ;
#199865=FACE_OUTER_BOUND ( 'NONE', #238197, .T. ) ;
#199876=VERTEX_POINT ( 'NONE', #46476 ) ;
#199890=ORIENTED_EDGE ( 'NONE', *, *, #228911, .F. ) ;
#199901=CARTESIAN_POINT ( 'NONE',  ( -18.54159361262948735, 85.46313213550472199, -62.47398526823135967 ) ) ;
#199919=CIRCLE ( 'NONE', #170739, 0.09999999999999939493 ) ;
#199930=CIRCLE ( 'NONE', #170929, 0.1000000000000028783 ) ;
#199936=CARTESIAN_POINT ( 'NONE',  ( 20.95512820512820440, 67.12384868372345181, -57.37310748452438247 ) ) ;
#199974=AXIS2_PLACEMENT_3D ( 'NONE', #160609, #200992, #202277 ) ;
#199991=CARTESIAN_POINT ( 'NONE',  ( -20.94999999999999929, 87.41227409416113403, -38.92310748452424463 ) ) ;
#200030=EDGE_CURVE ( 'NONE', #220609, #82047, #231354, .T. ) ;
#200042=CARTESIAN_POINT ( 'NONE',  ( -23.15000000000000213, 85.00000000001159606, -59.62913836187181715 ) ) ;
#200047=CARTESIAN_POINT ( 'NONE',  ( -22.42357213249529124, 75.90091303601015227, -77.19603987088426322 ) ) ;
#200074=DIRECTION ( 'NONE',  ( 1.000000000000000000, 0.000000000000000000, 0.000000000000000000 ) ) ;
#200101=CIRCLE ( 'NONE', #112794, 0.2000000000000057288 ) ;
#200121=ADVANCED_FACE ( 'NONE', ( #252377 ), #231561, .F. ) ;
#200165=DIRECTION ( 'NONE',  ( 0.000000000000000000, -0.9999631594459053030, -0.008583690987162452199 ) ) ;
#200181=ORIENTED_EDGE ( 'NONE', *, *, #64855, .F. ) ;
#200189=DIRECTION ( 'NONE',  ( 0.000000000000000000, 1.000000000000000000, 0.000000000000000000 ) ) ;
#200203=ORIENTED_EDGE ( 'NONE', *, *, #243897, .T. ) ;
#200215=ORIENTED_EDGE ( 'NONE', *, *, #66475, .T. ) ;
#200228=ORIENTED_EDGE ( 'NONE', *, *, #171306, .F. ) ;
#200236=DIRECTION ( 'NONE',  ( -1.000000000000000000, -0.000000000000000000, -0.000000000000000000 ) ) ;
#200242=CARTESIAN_POINT ( 'NONE',  ( -21.14999999999999858, 76.10000000001174669, -81.17267829206912211 ) ) ;
#200247=EDGE_CURVE ( 'NONE', #191840, #101698, #135830, .T. ) ;
#200265=EDGE_CURVE ( 'NONE', #243492, #178434, #100978, .T. ) ;
#200296=DIRECTION ( 'NONE',  ( 0.000000000000000000, 6.982962677686266711E-15, -1.000000000000000000 ) ) ;
#200344=CARTESIAN_POINT ( 'NONE',  ( -18.59999999999999787, 77.83534155023598089, -57.96795619196132776 ) ) ;
#200398=EDGE_LOOP ( 'NONE', ( #150862, #77347, #4158, #104118 ) ) ;
#200405=CARTESIAN_POINT ( 'NONE',  ( 20.12481660106788439, 66.47365600773666472, -61.29696581543134926 ) ) ;
#200416=ADVANCED_FACE ( 'NONE', ( #67048 ), #160816, .F. ) ;
#200435=FACE_OUTER_BOUND ( 'NONE', #134801, .T. ) ;
#200463=CIRCLE ( 'NONE', #233610, 0.09999999999999520384 ) ;
#200464=TOROIDAL_SURFACE ( 'NONE', #21422, 4.099999999999999645, 0.1000000000000000056 ) ;
#200470=ADVANCED_FACE ( 'NONE', ( #194723 ), #150454, .F. ) ;
#200473=LINE ( 'NONE', #97483, #162676 ) ;
#200474=CARTESIAN_POINT ( 'NONE',  ( -20.94999999999999929, 64.35000000001147669, -42.80697314750250371 ) ) ;
#200502=ORIENTED_EDGE ( 'NONE', *, *, #173284, .T. ) ;
#200504=AXIS2_PLACEMENT_3D ( 'NONE', #81329, #224713, #4385 ) ;
#200571=CARTESIAN_POINT ( 'NONE',  ( -20.86777300164945004, 65.66799936921481162, -30.42993998886010587 ) ) ;
#200578=CARTESIAN_POINT ( 'NONE',  ( 21.05000000000000071, 76.00000000001162448, -65.22310748452429152 ) ) ;
#200580=CARTESIAN_POINT ( 'NONE',  ( -18.50000000000000000, 72.08710075277812734, -58.04128451151338197 ) ) ;
#200586=EDGE_CURVE ( 'NONE', #89321, #128154, #65119, .T. ) ;
#200594=CIRCLE ( 'NONE', #121519, 0.09999999999999939493 ) ;
#200610=AXIS2_PLACEMENT_3D ( 'NONE', #32060, #185968, #148130 ) ;
#200626=DIRECTION ( 'NONE',  ( 0.000000000000000000, 0.000000000000000000, 1.000000000000000000 ) ) ;
#200634=ORIENTED_EDGE ( 'NONE', *, *, #87162, .F. ) ;
#200641=VERTEX_POINT ( 'NONE', #89808 ) ;
#200660=DIRECTION ( 'NONE',  ( 0.000000000000000000, 6.938893903907229955E-15, -1.000000000000000000 ) ) ;
#200687=CARTESIAN_POINT ( 'NONE',  ( -23.25000000000000000, 65.66751761918619934, -30.42826094061123854 ) ) ;
#200713=DIRECTION ( 'NONE',  ( 0.000000000000000000, -0.01562499999996343723, -0.9998779222360104635 ) ) ;
#200733=CARTESIAN_POINT ( 'NONE',  ( -22.50000000000000000, 76.00000000001173817, -81.17267829206912211 ) ) ;
#200762=ORIENTED_EDGE ( 'NONE', *, *, #218439, .F. ) ;
#200771=CARTESIAN_POINT ( 'NONE',  ( 18.46163235739468789, 85.48015080692967160, -29.36549694464667226 ) ) ;
#200789=DIRECTION ( 'NONE',  ( -1.000000000000000000, 0.000000000000000000, -0.000000000000000000 ) ) ;
#200790=ADVANCED_FACE ( 'NONE', ( #137914 ), #143048, .F. ) ;
#200840=FILL_AREA_STYLE_COLOUR ( '', #100472 ) ;
#200870=ORIENTED_EDGE ( 'NONE', *, *, #65345, .F. ) ;
#200966=AXIS2_PLACEMENT_3D ( 'NONE', #15024, #230199, #114093 ) ;
#200976=EDGE_CURVE ( 'NONE', #131784, #43988, #90415, .T. ) ;
#200992=DIRECTION ( 'NONE',  ( 0.000000000000000000, 0.4999999999999943379, 0.8660254037844420383 ) ) ;
#200995=EDGE_CURVE ( 'NONE', #113738, #2960, #7032, .T. ) ;
#201003=EDGE_CURVE ( 'NONE', #118763, #220609, #136169, .T. ) ;
#201021=CARTESIAN_POINT ( 'NONE',  ( 20.97224591636398472, 65.37484658384794045, -57.27318157986082525 ) ) ;
#201036=VECTOR ( 'NONE', #207500, 1000.000000000000114 ) ;
#201053=LINE ( 'NONE', #236328, #69128 ) ;
#201072=AXIS2_PLACEMENT_3D ( 'NONE', #18874, #20179, #119281 ) ;
#201084=CARTESIAN_POINT ( 'NONE',  ( -18.59999999999999787, 64.35000000001161879, -62.50830171387039513 ) ) ;
#201089=ADVANCED_FACE ( 'NONE', ( #155933 ), #215853, .F. ) ;
#201109=VERTEX_POINT ( 'NONE', #101012 ) ;
#201119=CARTESIAN_POINT ( 'NONE',  ( -22.39999999999999503, 68.20922040163824818, -69.62310748452438247 ) ) ;
#201141=CARTESIAN_POINT ( 'NONE',  ( 21.05000000000000071, 67.22371710471909978, -57.37310748452438247 ) ) ;
#201165=LINE ( 'NONE', #42118, #172883 ) ;
#201206=FACE_OUTER_BOUND ( 'NONE', #156365, .T. ) ;
#201221=FACE_OUTER_BOUND ( 'NONE', #126542, .T. ) ;
#201230=DIRECTION ( 'NONE',  ( 0.000000000000000000, -6.938893903907234689E-15, 1.000000000000000000 ) ) ;
#201243=AXIS2_PLACEMENT_3D ( 'NONE', #18958, #116786, #16427 ) ;
#201252=ADVANCED_FACE ( 'NONE', ( #5795 ), #184451, .T. ) ;
#201309=ORIENTED_EDGE ( 'NONE', *, *, #109815, .F. ) ;
#201311=DIRECTION ( 'NONE',  ( 0.000000000000000000, -1.000000000000000000, -6.982962677686266711E-15 ) ) ;
#201319=CARTESIAN_POINT ( 'NONE',  ( -21.76363531954647357, 75.90099812571226323, -76.53604403239606313 ) ) ;
#201321=CARTESIAN_POINT ( 'NONE',  ( 20.95325940946048249, 65.47660992931533031, -61.95864535528431105 ) ) ;
#201337=CARTESIAN_POINT ( 'NONE',  ( -20.54999999999999716, 84.73084112150691283, -59.92503276553992464 ) ) ;
#201349=CYLINDRICAL_SURFACE ( 'NONE', #198915, 0.1000000000000028644 ) ;
#201359=CARTESIAN_POINT ( 'NONE',  ( -21.07933241753356413, 75.90662040959243484, -75.85175343290406147 ) ) ;
#201386=FACE_OUTER_BOUND ( 'NONE', #138542, .T. ) ;
#201456=CIRCLE ( 'NONE', #147304, 3.999999999999996447 ) ;
#201514=VERTEX_POINT ( 'NONE', #11829 ) ;
#201536=DIRECTION ( 'NONE',  ( 0.000000000000000000, 0.000000000000000000, -1.000000000000000000 ) ) ;
#201539=CARTESIAN_POINT ( 'NONE',  ( -22.45372860728439690, 75.98507938046324739, -81.17290461922820555 ) ) ;
#201557=EDGE_LOOP ( 'NONE', ( #80839, #1342, #57249 ) ) ;
#201579=DIRECTION ( 'NONE',  ( -1.000000000000000000, 0.000000000000000000, -0.000000000000000000 ) ) ;
#201582=CARTESIAN_POINT ( 'NONE',  ( -23.15000000000000213, 74.08971962617972906, -48.65447533972326966 ) ) ;
#201590=EDGE_CURVE ( 'NONE', #113945, #162078, #124126, .T. ) ;
#201603=ORIENTED_EDGE ( 'NONE', *, *, #5215, .T. ) ;
#201606=DIRECTION ( 'NONE',  ( -0.000000000000000000, 6.982962677686266711E-15, -1.000000000000000000 ) ) ;
#201625=DIRECTION ( 'NONE',  ( 0.000000000000000000, 6.982962677686266711E-15, -1.000000000000000000 ) ) ;
#201627=FACE_OUTER_BOUND ( 'NONE', #238907, .T. ) ;
#201633=LINE ( 'NONE', #137795, #133873 ) ;
#201644=ORIENTED_EDGE ( 'NONE', *, *, #158322, .F. ) ;
#201666=CARTESIAN_POINT ( 'NONE',  ( -20.54999999999999716, 85.00000000001149658, -45.91707660717669626 ) ) ;
#201676=AXIS2_PLACEMENT_3D ( 'NONE', #126430, #143425, #169455 ) ;
#201700=VERTEX_POINT ( 'NONE', #245193 ) ;
#201719=CARTESIAN_POINT ( 'NONE',  ( -21.04999999999999716, 69.69257478044623610, -69.50628761613869244 ) ) ;
#201748=DIRECTION ( 'NONE',  ( 0.000000000000000000, -6.853228547068871147E-15, 1.000000000000000000 ) ) ;
#201754=CARTESIAN_POINT ( 'NONE',  ( 18.59999999999999787, 74.14897176987071248, -57.86919421510183525 ) ) ;
#201784=VERTEX_POINT ( 'NONE', #95095 ) ;
#201786=DIRECTION ( 'NONE',  ( 1.000000000000000000, 0.000000000000000000, 0.000000000000000000 ) ) ;
#201793=CIRCLE ( 'NONE', #135141, 11.65000000000000036 ) ;
#201821=ORIENTED_EDGE ( 'NONE', *, *, #335, .T. ) ;
#201826=CIRCLE ( 'NONE', #135361, 0.8750000000000007772 ) ;
#201852=VECTOR ( 'NONE', #35029, 1000.000000000000000 ) ;
#201855=CIRCLE ( 'NONE', #31220, 0.1000000000000028644 ) ;
#201867=AXIS2_PLACEMENT_3D ( 'NONE', #147268, #207267, #28664 ) ;
#201868=VERTEX_POINT ( 'NONE', #57225 ) ;
#201877=VECTOR ( 'NONE', #176600, 1000.000000000000114 ) ;
#201884=ADVANCED_FACE ( 'NONE', ( #139332 ), #138054, .T. ) ;
#201898=CARTESIAN_POINT ( 'NONE',  ( -23.25000000000000000, 76.00000000001142553, -36.02310748452432421 ) ) ;
#201909=DIRECTION ( 'NONE',  ( 1.000000000000000000, -2.952720810173289112E-16, -2.061873921506763405E-30 ) ) ;
#201923=VERTEX_POINT ( 'NONE', #19417 ) ;
#201971=DIRECTION ( 'NONE',  ( -1.000000000000000000, 2.952720810173289112E-16, 2.061873921506763405E-30 ) ) ;
#201987=DIRECTION ( 'NONE',  ( 0.000000000000000000, 0.01283462868040226822, 0.9999176327611370985 ) ) ;
#201992=CARTESIAN_POINT ( 'NONE',  ( -20.64999999999999858, 84.66355140188075268, -59.99900636645695329 ) ) ;
#202030=EDGE_CURVE ( 'NONE', #159227, #38202, #84463, .T. ) ;
#202035=DIRECTION ( 'NONE',  ( 0.000000000000000000, 6.982962677686266711E-15, -1.000000000000000000 ) ) ;
#202047=CARTESIAN_POINT ( 'NONE',  ( -20.64999999999999858, 76.00000000001143974, -38.02310748452432421 ) ) ;
#202067=FACE_OUTER_BOUND ( 'NONE', #129146, .T. ) ;
#202085=CARTESIAN_POINT ( 'NONE',  ( 18.60000000000001208, 85.36423601037837727, -62.34285308379966040 ) ) ;
#202097=ORIENTED_EDGE ( 'NONE', *, *, #198970, .F. ) ;
#202116=ORIENTED_EDGE ( 'NONE', *, *, #252883, .F. ) ;
#202122=FILL_AREA_STYLE ('',( #200840 ) ) ;
#202131=CARTESIAN_POINT ( 'NONE',  ( -21.44999999999999929, 68.65000000001150227, -48.27310748452437394 ) ) ;
#202178=ORIENTED_EDGE ( 'NONE', *, *, #94311, .T. ) ;
#202266=CYLINDRICAL_SURFACE ( 'NONE', #184457, 0.1000000000000028644 ) ;
#202277=DIRECTION ( 'NONE',  ( 0.000000000000000000, -0.8660254037844420383, 0.4999999999999943379 ) ) ;
#202294=ADVANCED_FACE ( 'NONE', ( #98584 ), #99316, .F. ) ;
#202296=CARTESIAN_POINT ( 'NONE',  ( -18.50000972452446035, 65.70673848566926267, -30.56382523348289837 ) ) ;
#202304=ORIENTED_EDGE ( 'NONE', *, *, #35265, .F. ) ;
#202329=VECTOR ( 'NONE', #29548, 1000.000000000000000 ) ;
#202332=CIRCLE ( 'NONE', #119137, 0.09999999999999939493 ) ;
#202336=ORIENTED_EDGE ( 'NONE', *, *, #168690, .T. ) ;
#202395=CARTESIAN_POINT ( 'NONE',  ( -23.15000000000000213, 71.65000000001151648, -48.27310748452435263 ) ) ;
#202449=CARTESIAN_POINT ( 'NONE',  ( -18.44448725179914561, 85.49008171549472479, -29.39414719046178348 ) ) ;
#202471=VERTEX_POINT ( 'NONE', #88022 ) ;
#202481=AXIS2_PLACEMENT_3D ( 'NONE', #226981, #10513, #209996 ) ;
#202482=DIRECTION ( 'NONE',  ( 0.000000000000000000, 0.000000000000000000, -1.000000000000000000 ) ) ;
#202523=ORIENTED_EDGE ( 'NONE', *, *, #188236, .T. ) ;
#202556=CARTESIAN_POINT ( 'NONE',  ( 22.39999999999999503, 68.20922040163827660, -69.52310748452437394 ) ) ;
#202587=DIRECTION ( 'NONE',  ( 0.000000000000000000, 6.982962677686266711E-15, -1.000000000000000000 ) ) ;
#202629=CARTESIAN_POINT ( 'NONE',  ( 23.15000000000000213, 87.48912529308749697, -39.12310748452424747 ) ) ;
#202653=DIRECTION ( 'NONE',  ( 1.000000000000000000, 0.000000000000000000, 0.000000000000000000 ) ) ;
#202660=B_SPLINE_CURVE_WITH_KNOTS ( 'NONE', 3,
 ( #157823, #237320, #59934, #34020, #176087, #79503, #217726, #95232, #255537, #58649, #35305, #156533, #37854, #198182, #138187, #57370, #117370, #99056, #196894 ),
 .UNSPECIFIED., .F., .F.,
 ( 4, 3, 3, 3, 3, 3, 4 ),
 ( 0.000000000000000000, 7.110282409889255887E-05, 0.0001508797727291325019, 0.0002027344179858315892, 0.0002343294522348972884, 0.0002454816334821104942, 0.0002619873080085499098 ),
 .UNSPECIFIED. ) ;
#202661=ORIENTED_EDGE ( 'NONE', *, *, #46708, .F. ) ;
#202685=CYLINDRICAL_SURFACE ( 'NONE', #208032, 0.09999999999999867328 ) ;
#202687=DIRECTION ( 'NONE',  ( 1.734723475976817507E-14, 1.000000000000000000, 6.982962677686266711E-15 ) ) ;
#202688=CARTESIAN_POINT ( 'NONE',  ( 19.97071067811864609, 64.27928932189284694, -48.17310748452440805 ) ) ;
#202695=DIRECTION ( 'NONE',  ( 1.000000000000000000, 0.000000000000000000, 0.000000000000000000 ) ) ;
#202737=ADVANCED_FACE ( 'NONE', ( #220831 ), #83850, .F. ) ;
#202764=ORIENTED_EDGE ( 'NONE', *, *, #95512, .F. ) ;
#202769=AXIS2_PLACEMENT_3D ( 'NONE', #118895, #96708, #198411 ) ;
#202780=ADVANCED_FACE ( 'NONE', ( #8227 ), #66398, .T. ) ;
#202783=AXIS2_PLACEMENT_3D ( 'NONE', #214136, #113741, #253244 ) ;
#202803=DIRECTION ( 'NONE',  ( 0.000000000000000000, 0.000000000000000000, -1.000000000000000000 ) ) ;
#202806=ORIENTED_EDGE ( 'NONE', *, *, #245235, .T. ) ;
#202809=ORIENTED_EDGE ( 'NONE', *, *, #199225, .T. ) ;
#202819=ORIENTED_EDGE ( 'NONE', *, *, #4360, .T. ) ;
#202838=AXIS2_PLACEMENT_3D ( 'NONE', #166511, #54223, #230298 ) ;
#202850=ORIENTED_EDGE ( 'NONE', *, *, #76155, .F. ) ;
#202854=VERTEX_POINT ( 'NONE', #150308 ) ;
#202892=ADVANCED_FACE ( 'NONE', ( #207717 ), #191324, .T. ) ;
#202965=VERTEX_POINT ( 'NONE', #175049 ) ;
#202971=EDGE_LOOP ( 'NONE', ( #4132, #200870, #54930, #144835, #142709 ) ) ;
#202980=CARTESIAN_POINT ( 'NONE',  ( -18.50000000000000000, 77.16412189325258453, -28.10825939895270764 ) ) ;
#202986=CARTESIAN_POINT ( 'NONE',  ( 20.94999999999999574, 77.83534155023598089, -57.96795619196132776 ) ) ;
#203027=CARTESIAN_POINT ( 'NONE',  ( 21.05000000000000071, 76.00000000001143974, -37.92310748452432989 ) ) ;
#203033=DIRECTION ( 'NONE',  ( 1.000000000000000000, 0.000000000000000000, 0.000000000000000000 ) ) ;
#203083=CIRCLE ( 'NONE', #157141, 0.09999999999999939493 ) ;
#203086=DIRECTION ( 'NONE',  ( 0.000000000000000000, -1.000000000000000000, -6.860497997771532351E-15 ) ) ;
#203099=ORIENTED_EDGE ( 'NONE', *, *, #108436, .F. ) ;
#203138=DIRECTION ( 'NONE',  ( 0.000000000000000000, -1.000000000000000000, -6.982962677686267499E-15 ) ) ;
#203155=ORIENTED_EDGE ( 'NONE', *, *, #137362, .F. ) ;
#203171=CYLINDRICAL_SURFACE ( 'NONE', #99011, 11.80000000000000426 ) ;
#203177=ORIENTED_EDGE ( 'NONE', *, *, #252883, .T. ) ;
#203235=AXIS2_PLACEMENT_3D ( 'NONE', #84589, #205864, #102894 ) ;
#203237=ORIENTED_EDGE ( 'NONE', *, *, #118864, .F. ) ;
#203246=FACE_OUTER_BOUND ( 'NONE', #142889, .T. ) ;
#203247=CARTESIAN_POINT ( 'NONE',  ( 21.05000000000000071, 74.63912941281955682, -61.45010955743337178 ) ) ;
#203251=DIRECTION ( 'NONE',  ( 0.000000000000000000, -7.086529944415894657E-15, 1.000000000000000000 ) ) ;
#203255=AXIS2_PLACEMENT_3D ( 'NONE', #72375, #146726, #226262 ) ;
#203259=ORIENTED_EDGE ( 'NONE', *, *, #55049, .F. ) ;
#203334=VECTOR ( 'NONE', #64159, 1000.000000000000114 ) ;
#203341=VECTOR ( 'NONE', #226158, 1000.000000000000000 ) ;
#203343=CARTESIAN_POINT ( 'NONE',  ( 20.95512820512820440, 67.12384868372348024, -60.96447848938343839 ) ) ;
#203351=AXIS2_PLACEMENT_3D ( 'NONE', #162958, #226751, #48117 ) ;
#203356=CARTESIAN_POINT ( 'NONE',  ( -20.54999999999999716, 68.75000000001158185, -57.27310748452437394 ) ) ;
#203367=CARTESIAN_POINT ( 'NONE',  ( 21.05000000000000071, 85.40000000001148805, -45.91707660717669626 ) ) ;
#203409=( LENGTH_UNIT ( ) NAMED_UNIT ( * ) SI_UNIT ( .MILLI., .METRE. ) );
#203436=ADVANCED_FACE ( 'NONE', ( #172176 ), #37443, .F. ) ;
#203453=ORIENTED_EDGE ( 'NONE', *, *, #134671, .T. ) ;
#203470=AXIS2_PLACEMENT_3D ( 'NONE', #203919, #9570, #25308 ) ;
#203473=ORIENTED_EDGE ( 'NONE', *, *, #149109, .F. ) ;
#203476=VERTEX_POINT ( 'NONE', #223743 ) ;
#203477=EDGE_LOOP ( 'NONE', ( #93733, #153201, #35461, #29189, #187330 ) ) ;
#203482=VERTEX_POINT ( 'NONE', #240769 ) ;
#203486=CYLINDRICAL_SURFACE ( 'NONE', #61247, 0.09999999999999939493 ) ;
#203506=DIRECTION ( 'NONE',  ( -1.000000000000000000, 0.000000000000000000, 0.000000000000000000 ) ) ;
#203546=CARTESIAN_POINT ( 'NONE',  ( 20.85000000000000142, 76.00000000001142553, -36.02310748452432421 ) ) ;
#203551=DIRECTION ( 'NONE',  ( 0.000000000000000000, 0.000000000000000000, 1.000000000000000000 ) ) ;
#203559=EDGE_CURVE ( 'NONE', #160781, #17664, #37368, .T. ) ;
#203562=DIRECTION ( 'NONE',  ( 1.000000000000000000, -3.265361837132813093E-16, -2.280189983783949500E-30 ) ) ;
#203573=AXIS2_PLACEMENT_3D ( 'NONE', #186546, #83549, #103126 ) ;
#203574=CARTESIAN_POINT ( 'NONE',  ( -18.56579813702276027, 65.66974365629616273, -30.43601455626049912 ) ) ;
#203597=CARTESIAN_POINT ( 'NONE',  ( -21.05000000000000071, 70.15000000001148805, -46.15560470880229360 ) ) ;
#203642=AXIS2_PLACEMENT_3D ( 'NONE', #187657, #12873, #145924 ) ;
#203655=DIRECTION ( 'NONE',  ( 0.000000000000000000, 0.000000000000000000, 1.000000000000000000 ) ) ;
#203657=DIRECTION ( 'NONE',  ( 1.000000000000000000, 0.000000000000000000, 0.000000000000000000 ) ) ;
#203663=ORIENTED_EDGE ( 'NONE', *, *, #102039, .F. ) ;
#203666=VECTOR ( 'NONE', #42946, 1000.000000000000000 ) ;
#203672=AXIS2_PLACEMENT_3D ( 'NONE', #168141, #69015, #229364 ) ;
#203695=EDGE_CURVE ( 'NONE', #197749, #253373, #240980, .T. ) ;
#203728=CARTESIAN_POINT ( 'NONE',  ( 18.59999999999999432, 70.30054753569015702, -82.06538144109418909 ) ) ;
#203739=CIRCLE ( 'NONE', #224570, 0.09999999999999939493 ) ;
#203764=ORIENTED_EDGE ( 'NONE', *, *, #103839, .T. ) ;
#203784=DIRECTION ( 'NONE',  ( 0.000000000000000000, 7.056502275159894776E-15, -1.000000000000000000 ) ) ;
#203899=DIRECTION ( 'NONE',  ( 0.000000000000000000, 6.982962677686266711E-15, -1.000000000000000000 ) ) ;
#203919=CARTESIAN_POINT ( 'NONE',  ( 23.15000000000000213, 88.41227409416113403, -39.12310748452424036 ) ) ;
#203926=DIRECTION ( 'NONE',  ( -0.000000000000000000, 1.000000000000000000, 6.982962677686266711E-15 ) ) ;
#203947=ORIENTED_EDGE ( 'NONE', *, *, #18022, .T. ) ;
#203963=FACE_OUTER_BOUND ( 'NONE', #122199, .T. ) ;
#203973=ORIENTED_EDGE ( 'NONE', *, *, #88852, .F. ) ;
#203986=EDGE_CURVE ( 'NONE', #20467, #181320, #220137, .T. ) ;
#203997=AXIS2_PLACEMENT_3D ( 'NONE', #146551, #74457, #27950 ) ;
#204001=DIRECTION ( 'NONE',  ( 0.000000000000000000, 6.769652589177784668E-15, -1.000000000000000000 ) ) ;
#204010=CARTESIAN_POINT ( 'NONE',  ( 21.08479644141222309, 75.94144555744755110, -75.86814614225623643 ) ) ;
#204023=DIRECTION ( 'NONE',  ( 0.000000000000000000, -0.01562499999996343723, -0.9998779222360104635 ) ) ;
#204052=DIRECTION ( 'NONE',  ( 0.000000000000000000, 0.000000000000000000, -1.000000000000000000 ) ) ;
#204056=ORIENTED_EDGE ( 'NONE', *, *, #189777, .F. ) ;
#204082=VERTEX_POINT ( 'NONE', #99320 ) ;
#204122=VECTOR ( 'NONE', #255923, 1000.000000000000000 ) ;
#204127=LINE ( 'NONE', #184573, #208733 ) ;
#204138=DIRECTION ( 'NONE',  ( 2.659396599871503635E-15, -0.6132151058540604716, 0.7899159663865477077 ) ) ;
#204151=ORIENTED_EDGE ( 'NONE', *, *, #16108, .T. ) ;
#204183=CARTESIAN_POINT ( 'NONE',  ( 21.05000000000000071, 76.00000000001156764, -56.64810748452432421 ) ) ;
#204188=DIRECTION ( 'NONE',  ( 0.000000000000000000, -7.034366652768107165E-15, 1.000000000000000000 ) ) ;
#204203=DIRECTION ( 'NONE',  ( -0.000000000000000000, 6.982962677686266711E-15, -1.000000000000000000 ) ) ;
#204221=EDGE_CURVE ( 'NONE', #159190, #33900, #122788, .T. ) ;
#204222=EDGE_CURVE ( 'NONE', #47209, #185202, #107876, .T. ) ;
#204258=CARTESIAN_POINT ( 'NONE',  ( -21.13422380239054021, 76.00000000001170974, -76.01643399932983414 ) ) ;
#204269=TOROIDAL_SURFACE ( 'NONE', #20977, 0.2000000000000000111, 0.1000000000000000056 ) ;
#204279=FACE_OUTER_BOUND ( 'NONE', #16818, .T. ) ;
#204282=EDGE_LOOP ( 'NONE', ( #59042, #254679, #35114, #207103 ) ) ;
#204298=DIRECTION ( 'NONE',  ( 0.000000000000000000, -6.982962677686266711E-15, 1.000000000000000000 ) ) ;
#204331=AXIS2_PLACEMENT_3D ( 'NONE', #105143, #41395, #6080 ) ;
#204347=ORIENTED_EDGE ( 'NONE', *, *, #238534, .F. ) ;
#204356=LINE ( 'NONE', #167841, #157526 ) ;
#204409=FACE_OUTER_BOUND ( 'NONE', #41781, .T. ) ;
#204430=ORIENTED_EDGE ( 'NONE', *, *, #26412, .F. ) ;
#204433=DIRECTION ( 'NONE',  ( 0.000000000000000000, 0.000000000000000000, 1.000000000000000000 ) ) ;
#204436=EDGE_LOOP ( 'NONE', ( #91149, #132817, #184055, #234213 ) ) ;
#204457=AXIS2_PLACEMENT_3D ( 'NONE', #116025, #174748, #131720 ) ;
#204467=ORIENTED_EDGE ( 'NONE', *, *, #168433, .F. ) ;
#204490=AXIS2_PLACEMENT_3D ( 'NONE', #166790, #42964, #5078 ) ;
#204491=CARTESIAN_POINT ( 'NONE',  ( 22.47071067811865319, 68.27992525551361780, -69.62219993922698791 ) ) ;
#204497=EDGE_CURVE ( 'NONE', #31772, #128154, #45707, .T. ) ;
#204564=DIRECTION ( 'NONE',  ( 0.000000000000000000, 6.938893903907234689E-15, -1.000000000000000000 ) ) ;
#204582=CARTESIAN_POINT ( 'NONE',  ( 21.14999999999999858, 64.35000000001156195, -57.27310748452440237 ) ) ;
#204595=AXIS2_PLACEMENT_3D ( 'NONE', #12432, #13685, #95773 ) ;
#204599=ORIENTED_EDGE ( 'NONE', *, *, #137245, .F. ) ;
#204618=AXIS2_PLACEMENT_3D ( 'NONE', #134760, #8749, #47844 ) ;
#204619=DIRECTION ( 'NONE',  ( 1.000000000000000000, 7.304098846218134667E-16, 5.100424963727256530E-30 ) ) ;
#204644=LINE ( 'NONE', #26036, #114671 ) ;
#204662=EDGE_LOOP ( 'NONE', ( #168432, #131649, #7386, #213945 ) ) ;
#204786=AXIS2_PLACEMENT_3D ( 'NONE', #2484, #161604, #123743 ) ;
#204803=DIRECTION ( 'NONE',  ( 1.713247197920696616E-14, -0.9876197685951263461, 0.1568667991644794590 ) ) ;
#204808=DIRECTION ( 'NONE',  ( -1.000000000000000000, -0.000000000000000000, -0.000000000000000000 ) ) ;
#204810=CARTESIAN_POINT ( 'NONE',  ( -23.25000000000000000, 74.00000000001152500, -48.64772940728643391 ) ) ;
#204812=ORIENTED_EDGE ( 'NONE', *, *, #72054, .F. ) ;
#204851=CYLINDRICAL_SURFACE ( 'NONE', #59287, 12.87499999999999822 ) ;
#204863=CARTESIAN_POINT ( 'NONE',  ( 21.05000000000000071, 77.36087058720364951, -61.45010955743335046 ) ) ;
#204871=CIRCLE ( 'NONE', #171599, 0.09999999999999939493 ) ;
#204888=CARTESIAN_POINT ( 'NONE',  ( -21.05000000000000071, 76.00000000001142553, -36.02310748452432421 ) ) ;
#204903=TOROIDAL_SURFACE ( 'NONE', #92474, 0.4000000000000003553, 0.1000000000000000056 ) ;
#204945=EDGE_CURVE ( 'NONE', #11272, #151129, #59196, .T. ) ;
#204958=FACE_OUTER_BOUND ( 'NONE', #179635, .T. ) ;
#204970=DIRECTION ( 'NONE',  ( 0.000000000000000000, 1.072103779144464410E-14, -1.000000000000000000 ) ) ;
#204980=AXIS2_PLACEMENT_3D ( 'NONE', #205703, #85726, #27112 ) ;
#204992=CIRCLE ( 'NONE', #217465, 11.74999999999999645 ) ;
#205006=ORIENTED_EDGE ( 'NONE', *, *, #197234, .T. ) ;
#205008=AXIS2_PLACEMENT_3D ( 'NONE', #224789, #142679, #46163 ) ;
#205024=EDGE_CURVE ( 'NONE', #87660, #97691, #125022, .T. ) ;
#205030=DIRECTION ( 'NONE',  ( 0.000000000000000000, 0.8660254037844281605, -0.5000000000000185407 ) ) ;
#205055=DIRECTION ( 'NONE',  ( 0.000000000000000000, -6.467318590049456648E-15, 1.000000000000000000 ) ) ;
#205069=CIRCLE ( 'NONE', #192637, 0.4000000000000045186 ) ;
#205090=ORIENTED_EDGE ( 'NONE', *, *, #58218, .T. ) ;
#205095=ADVANCED_FACE ( 'NONE', ( #3476 ), #63450, .F. ) ;
#205097=EDGE_CURVE ( 'NONE', #160136, #124309, #187576, .T. ) ;
#205112=ADVANCED_FACE ( 'NONE', ( #59570 ), #99987, .F. ) ;
#205131=ORIENTED_EDGE ( 'NONE', *, *, #196040, .F. ) ;
#205140=DIRECTION ( 'NONE',  ( 0.000000000000000000, 0.000000000000000000, 1.000000000000000000 ) ) ;
#205147=DIRECTION ( 'NONE',  ( 0.000000000000000000, -2.362176648138631684E-15, -1.000000000000000000 ) ) ;
#205171=CARTESIAN_POINT ( 'NONE',  ( -23.15000000000000213, 87.48912529308749697, -39.12310748452424747 ) ) ;
#205197=DIRECTION ( 'NONE',  ( 1.000000000000000000, 0.000000000000000000, 0.000000000000000000 ) ) ;
#205212=ORIENTED_EDGE ( 'NONE', *, *, #57176, .F. ) ;
#205213=EDGE_CURVE ( 'NONE', #177501, #46909, #124726, .T. ) ;
#205215=ORIENTED_EDGE ( 'NONE', *, *, #13720, .F. ) ;
#205227=AXIS2_PLACEMENT_3D ( 'NONE', #225276, #126191, #47935 ) ;
#205231=DIRECTION ( 'NONE',  ( -0.000000000000000000, 6.982962677686266711E-15, -1.000000000000000000 ) ) ;
#205233=CARTESIAN_POINT ( 'NONE',  ( -20.64999999999999858, 76.00000000001165290, -69.52310748452431710 ) ) ;
#205267=ORIENTED_EDGE ( 'NONE', *, *, #47482, .F. ) ;
#205291=EDGE_CURVE ( 'NONE', #189565, #255281, #183455, .T. ) ;
#205295=FACE_OUTER_BOUND ( 'NONE', #175919, .T. ) ;
#205351=ORIENTED_EDGE ( 'NONE', *, *, #71368, .F. ) ;
#205387=DIRECTION ( 'NONE',  ( 0.000000000000000000, -1.000000000000000000, -6.860497997771532351E-15 ) ) ;
#205406=ORIENTED_EDGE ( 'NONE', *, *, #163849, .F. ) ;
#205413=CARTESIAN_POINT ( 'NONE',  ( 21.13461538461538680, 67.11458296203710461, -57.17310748452437963 ) ) ;
#205416=CARTESIAN_POINT ( 'NONE',  ( 18.59999999999999076, 68.92903212821255465, -32.27654326265606954 ) ) ;
#205426=DIRECTION ( 'NONE',  ( 0.000000000000000000, -0.9908441862701605762, -0.1350103645451835310 ) ) ;
#205484=LINE ( 'NONE', #128531, #134358 ) ;
#205489=VERTEX_POINT ( 'NONE', #65700 ) ;
#205527=PLANE ( 'NONE',  #234691 ) ;
#205535=ORIENTED_EDGE ( 'NONE', *, *, #161959, .F. ) ;
#205563=EDGE_CURVE ( 'NONE', #144573, #112792, #140801, .T. ) ;
#205580=DIRECTION ( 'NONE',  ( 0.000000000000000000, 6.938893903907222067E-15, -1.000000000000000000 ) ) ;
#205583=EDGE_CURVE ( 'NONE', #206022, #30032, #92039, .T. ) ;
#205633=VECTOR ( 'NONE', #116515, 1000.000000000000000 ) ;
#205678=AXIS2_PLACEMENT_3D ( 'NONE', #84722, #83449, #164315 ) ;
#205679=DIRECTION ( 'NONE',  ( 0.000000000000000000, 0.000000000000000000, 1.000000000000000000 ) ) ;
#205703=CARTESIAN_POINT ( 'NONE',  ( 18.59999999999997655, 76.00000000001142553, -36.02310748452432421 ) ) ;
#205724=ORIENTED_EDGE ( 'NONE', *, *, #69772, .T. ) ;
#205729=AXIS2_PLACEMENT_3D ( 'NONE', #46068, #143883, #142587 ) ;
#205765=CARTESIAN_POINT ( 'NONE',  ( -20.94999999999999929, 64.35000000001147669, -42.80697314750250371 ) ) ;
#205769=ORIENTED_EDGE ( 'NONE', *, *, #107044, .T. ) ;
#205792=ORIENTED_EDGE ( 'NONE', *, *, #58888, .T. ) ;
#205805=CARTESIAN_POINT ( 'NONE',  ( 21.05000000000000071, 70.15000000001148805, -46.15560470880229360 ) ) ;
#205810=FACE_OUTER_BOUND ( 'NONE', #229953, .T. ) ;
#205830=EDGE_LOOP ( 'NONE', ( #124, #168662, #242703, #41978 ) ) ;
#205849=CARTESIAN_POINT ( 'NONE',  ( 23.14999999999999858, 76.00000000001139711, -32.02310748452432421 ) ) ;
#205864=DIRECTION ( 'NONE',  ( 1.000000000000000000, 0.000000000000000000, 0.000000000000000000 ) ) ;
#205885=CARTESIAN_POINT ( 'NONE',  ( -21.05000000000000071, 77.83534155023598089, -57.96795619196132776 ) ) ;
#205892=CARTESIAN_POINT ( 'NONE',  ( 21.87500000000000355, 66.25000000001155342, -57.17310748452438673 ) ) ;
#205925=AXIS2_PLACEMENT_3D ( 'NONE', #143108, #126110, #222642 ) ;
#205944=DIRECTION ( 'NONE',  ( 0.000000000000000000, -0.8700118002898356018, 0.4930308989875170078 ) ) ;
#205955=AXIS2_PLACEMENT_3D ( 'NONE', #145988, #28673, #105546 ) ;
#205973=AXIS2_PLACEMENT_3D ( 'NONE', #7243, #184607, #162503 ) ;
#205979=FACE_OUTER_BOUND ( 'NONE', #118218, .T. ) ;
#206022=VERTEX_POINT ( 'NONE', #112250 ) ;
#206047=ORIENTED_EDGE ( 'NONE', *, *, #71889, .T. ) ;
#206072=CARTESIAN_POINT ( 'NONE',  ( -20.94999999999999929, 76.00000000001142553, -36.02310748452432421 ) ) ;
#206076=EDGE_CURVE ( 'NONE', #73365, #47971, #73140, .T. ) ;
#206094=AXIS2_PLACEMENT_3D ( 'NONE', #224930, #187133, #8480 ) ;
#206096=ORIENTED_EDGE ( 'NONE', *, *, #120406, .F. ) ;
#206137=CYLINDRICAL_SURFACE ( 'NONE', #210848, 0.1000000000000028644 ) ;
#206159=ORIENTED_EDGE ( 'NONE', *, *, #154801, .T. ) ;
#206189=CYLINDRICAL_SURFACE ( 'NONE', #118075, 11.74999999999999645 ) ;
#206197=DIRECTION ( 'NONE',  ( 0.000000000000000000, -6.982962677686266711E-15, 1.000000000000000000 ) ) ;
#206231=CARTESIAN_POINT ( 'NONE',  ( -21.05000000000000071, 74.16465844978715438, -57.96795619196135618 ) ) ;
#206244=EDGE_CURVE ( 'NONE', #14406, #72194, #54808, .T. ) ;
#206247=EDGE_CURVE ( 'NONE', #114996, #250305, #202660, .T. ) ;
#206248=EDGE_CURVE ( 'NONE', #14606, #36355, #104625, .T. ) ;
#206251=ORIENTED_EDGE ( 'NONE', *, *, #241049, .T. ) ;
#206256=EDGE_LOOP ( 'NONE', ( #239719, #94585, #149278, #52239, #25662 ) ) ;
#206266=DIRECTION ( 'NONE',  ( 0.000000000000000000, -6.853228547068871147E-15, 1.000000000000000000 ) ) ;
#206305=CARTESIAN_POINT ( 'NONE',  ( -18.47690164073607733, 85.46484453802364101, -29.32172654468814699 ) ) ;
#206313=FACE_OUTER_BOUND ( 'NONE', #226873, .T. ) ;
#206332=AXIS2_PLACEMENT_3D ( 'NONE', #32181, #89544, #230346 ) ;
#206338=EDGE_CURVE ( 'NONE', #225338, #159302, #163133, .T. ) ;
#206341=AXIS2_PLACEMENT_3D ( 'NONE', #187744, #255339, #256620 ) ;
#206357=CARTESIAN_POINT ( 'NONE',  ( 18.50000000000000711, 85.41920976342086647, -62.27533802176532163 ) ) ;
#206362=ORIENTED_EDGE ( 'NONE', *, *, #71583, .T. ) ;
#206363=ORIENTED_EDGE ( 'NONE', *, *, #66782, .T. ) ;
#206371=DIRECTION ( 'NONE',  ( -1.000000000000000000, 0.000000000000000000, -0.000000000000000000 ) ) ;
#206417=CARTESIAN_POINT ( 'NONE',  ( 20.94999999999999929, 64.35000000001141984, -36.02310748452440237 ) ) ;
#206422=DIRECTION ( 'NONE',  ( 1.000000000000000000, 0.000000000000000000, 0.000000000000000000 ) ) ;
#206434=TOROIDAL_SURFACE ( 'NONE', #139773, 0.2000000000000000111, 0.1000000000000000056 ) ;
#206436=AXIS2_PLACEMENT_3D ( 'NONE', #80918, #245154, #103049 ) ;
#206486=DIRECTION ( 'NONE',  ( 1.000000000000000000, 0.000000000000000000, 0.000000000000000000 ) ) ;
#206496=VERTEX_POINT ( 'NONE', #46796 ) ;
#206510=CIRCLE ( 'NONE', #244095, 0.09999999999999939493 ) ;
#206520=VERTEX_POINT ( 'NONE', #15070 ) ;
#206551=ORIENTED_EDGE ( 'NONE', *, *, #10172, .T. ) ;
#206585=CARTESIAN_POINT ( 'NONE',  ( 21.10257677756355932, 75.97504925044370339, -75.92148922705705161 ) ) ;
#206635=VERTEX_POINT ( 'NONE', #162296 ) ;
#206646=DIRECTION ( 'NONE',  ( 1.000000000000000000, 0.000000000000000000, 0.000000000000000000 ) ) ;
#206658=AXIS2_PLACEMENT_3D ( 'NONE', #114048, #171504, #192324 ) ;
#206694=PLANE ( 'NONE',  #27828 ) ;
#206698=CIRCLE ( 'NONE', #177701, 0.1000000000000028644 ) ;
#206741=ORIENTED_EDGE ( 'NONE', *, *, #1666, .T. ) ;
#206755=ORIENTED_EDGE ( 'NONE', *, *, #73778, .F. ) ;
#206806=DIRECTION ( 'NONE',  ( -1.000000000000000000, 0.000000000000000000, -0.000000000000000000 ) ) ;
#206819=AXIS2_PLACEMENT_3D ( 'NONE', #211632, #134626, #253303 ) ;
#206869=CIRCLE ( 'NONE', #98485, 0.09999999999999939493 ) ;
#206876=EDGE_CURVE ( 'NONE', #208477, #121217, #117505, .T. ) ;
#206910=ADVANCED_FACE ( 'NONE', ( #76019 ), #56440, .F. ) ;
#206912=ORIENTED_EDGE ( 'NONE', *, *, #159758, .T. ) ;
#206913=VERTEX_POINT ( 'NONE', #57725 ) ;
#206929=EDGE_LOOP ( 'NONE', ( #197775, #153985, #248631, #245912 ) ) ;
#206963=EDGE_LOOP ( 'NONE', ( #153354, #231469, #150361, #203259, #105443, #204599 ) ) ;
#206986=VECTOR ( 'NONE', #144766, 1000.000000000000000 ) ;
#207034=DIRECTION ( 'NONE',  ( -1.000000000000000000, 0.000000000000000000, 0.000000000000000000 ) ) ;
#207039=ORIENTED_EDGE ( 'NONE', *, *, #26652, .F. ) ;
#207051=CARTESIAN_POINT ( 'NONE',  ( -20.94999999999999929, 87.65000000001163016, -66.52310748452423184 ) ) ;
#207074=ORIENTED_EDGE ( 'NONE', *, *, #131821, .F. ) ;
#207092=ORIENTED_EDGE ( 'NONE', *, *, #23594, .T. ) ;
#207093=DIRECTION ( 'NONE',  ( 0.000000000000000000, -1.000000000000000000, -6.982962677686266711E-15 ) ) ;
#207103=ORIENTED_EDGE ( 'NONE', *, *, #75747, .F. ) ;
#207122=VECTOR ( 'NONE', #193968, 1000.000000000000000 ) ;
#207132=CARTESIAN_POINT ( 'NONE',  ( 20.94999999999999574, 77.83534155023598089, -57.86795619196132634 ) ) ;
#207204=AXIS2_PLACEMENT_3D ( 'NONE', #200242, #84086, #120730 ) ;
#207215=CYLINDRICAL_SURFACE ( 'NONE', #203351, 0.1000000000000028644 ) ;
#207266=CARTESIAN_POINT ( 'NONE',  ( 18.43579564894470835, 85.51932753530414288, -62.55013084066395379 ) ) ;
#207267=DIRECTION ( 'NONE',  ( -0.000000000000000000, 1.000000000000000000, 6.352154140967427193E-15 ) ) ;
#207272=DIRECTION ( 'NONE',  ( 0.000000000000000000, 7.147358527629762208E-15, -1.000000000000000000 ) ) ;
#207296=ORIENTED_EDGE ( 'NONE', *, *, #242727, .T. ) ;
#207298=DIRECTION ( 'NONE',  ( 1.000000000000000000, 0.000000000000000000, 0.000000000000000000 ) ) ;
#207310=VERTEX_POINT ( 'NONE', #225469 ) ;
#207321=CONICAL_SURFACE ( 'NONE', #153178, 4.299999999999956302, 0.7853981633974466137 ) ;
#207351=CARTESIAN_POINT ( 'NONE',  ( 20.12500000000000000, 66.25000000001161027, -61.41133620241011215 ) ) ;
#207369=PLANE ( 'NONE',  #21892 ) ;
#207379=ORIENTED_EDGE ( 'NONE', *, *, #69772, .F. ) ;
#207424=CARTESIAN_POINT ( 'NONE',  ( 22.50000000000000000, 76.00000000001165290, -69.52310748452431710 ) ) ;
#207432=AXIS2_PLACEMENT_3D ( 'NONE', #106648, #124963, #246190 ) ;
#207433=EDGE_CURVE ( 'NONE', #97734, #232002, #1135, .T. ) ;
#207434=CARTESIAN_POINT ( 'NONE',  ( 20.85000000000000142, 64.35000000001141984, -36.02310748452440237 ) ) ;
#207436=AXIS2_PLACEMENT_3D ( 'NONE', #26283, #206197, #223177 ) ;
#207451=EDGE_CURVE ( 'NONE', #146658, #108916, #132826, .T. ) ;
#207455=CARTESIAN_POINT ( 'NONE',  ( -20.85000000000000142, 77.83585931145498193, -24.51866831572578675 ) ) ;
#207465=CARTESIAN_POINT ( 'NONE',  ( 21.14999999999998082, 87.75000000001165290, -69.52310748452424605 ) ) ;
#207500=DIRECTION ( 'NONE',  ( 4.408576920032446739E-17, 0.1350103645451945777, -0.9908441862701590219 ) ) ;
#207507=DIRECTION ( 'NONE',  ( 1.000000000000000000, 0.000000000000000000, 0.000000000000000000 ) ) ;
#207522=EDGE_CURVE ( 'NONE', #118763, #27421, #36298, .T. ) ;
#207537=CARTESIAN_POINT ( 'NONE',  ( -23.15000000000000213, 64.35000000001150511, -48.27310748452440237 ) ) ;
#207539=DIRECTION ( 'NONE',  ( 1.000000000000000000, 0.000000000000000000, 0.000000000000000000 ) ) ;
#207551=AXIS2_PLACEMENT_3D ( 'NONE', #155485, #36817, #116333 ) ;
#207560=EDGE_CURVE ( 'NONE', #203476, #200641, #72093, .T. ) ;
#207580=DIRECTION ( 'NONE',  ( -1.000000000000000000, 2.952720810173289112E-16, 2.061873921506763405E-30 ) ) ;
#207590=ORIENTED_EDGE ( 'NONE', *, *, #230616, .F. ) ;
#207605=FACE_OUTER_BOUND ( 'NONE', #7242, .T. ) ;
#207606=AXIS2_PLACEMENT_3D ( 'NONE', #4386, #104745, #170919 ) ;
#207625=CARTESIAN_POINT ( 'NONE',  ( 23.24999999999999645, 76.00000000001142553, -36.02310748452432421 ) ) ;
#207647=DIRECTION ( 'NONE',  ( 0.000000000000000000, -6.652207440891569552E-15, 1.000000000000000000 ) ) ;
#207654=VERTEX_POINT ( 'NONE', #102633 ) ;
#207679=CYLINDRICAL_SURFACE ( 'NONE', #26804, 0.1000000000000028644 ) ;
#207685=AXIS2_PLACEMENT_3D ( 'NONE', #1705, #121691, #159526 ) ;
#207717=FACE_OUTER_BOUND ( 'NONE', #227707, .T. ) ;
#207741=AXIS2_PLACEMENT_3D ( 'NONE', #22205, #242513, #102988 ) ;
#207761=CARTESIAN_POINT ( 'NONE',  ( -18.59999999999999787, 64.35000000001161879, -62.50830171387039513 ) ) ;
#207783=CIRCLE ( 'NONE', #182846, 7.800000000000001599 ) ;
#207787=AXIS2_PLACEMENT_3D ( 'NONE', #220380, #221622, #3885 ) ;
#207791=CARTESIAN_POINT ( 'NONE',  ( -20.05000000000000426, 66.75000000001151079, -48.27310748452438816 ) ) ;
#207803=DIRECTION ( 'NONE',  ( 1.000000000000000000, 0.000000000000000000, 0.000000000000000000 ) ) ;
#207848=DIRECTION ( 'NONE',  ( 1.000000000000000000, 0.000000000000000000, 0.000000000000000000 ) ) ;
#207862=CARTESIAN_POINT ( 'NONE',  ( -23.25000000000000000, 87.65000000001144542, -39.12310748452424747 ) ) ;
#207866=ORIENTED_EDGE ( 'NONE', *, *, #206076, .F. ) ;
#207897=LINE ( 'NONE', #70963, #20007 ) ;
#207903=DIRECTION ( 'NONE',  ( 0.000000000000000000, 0.000000000000000000, -1.000000000000000000 ) ) ;
#207915=DIRECTION ( 'NONE',  ( -1.000000000000000000, -0.000000000000000000, -0.000000000000000000 ) ) ;
#207931=CARTESIAN_POINT ( 'NONE',  ( 18.59999999999999432, 77.63717271298195044, -57.94095411905229298 ) ) ;
#207972=DIRECTION ( 'NONE',  ( 1.000000000000000000, 0.000000000000000000, 0.000000000000000000 ) ) ;
#207976=DIRECTION ( 'NONE',  ( 0.000000000000000000, 1.000000000000000000, 6.938893903907222067E-15 ) ) ;
#207980=ADVANCED_FACE ( 'NONE', ( #112943 ), #255359, .T. ) ;
#207991=TOROIDAL_SURFACE ( 'NONE', #170625, 0.6000000000000009770, 0.1000000000000000056 ) ;
#208016=CARTESIAN_POINT ( 'NONE',  ( -18.59999999999999787, 77.83585931145498193, -24.41866831572578533 ) ) ;
#208032=AXIS2_PLACEMENT_3D ( 'NONE', #102266, #226074, #224807 ) ;
#208033=LINE ( 'NONE', #107621, #115769 ) ;
#208069=CARTESIAN_POINT ( 'NONE',  ( 21.00000000000000000, 66.25000000001151079, -48.27310748452438816 ) ) ;
#208081=ORIENTED_EDGE ( 'NONE', *, *, #80473, .F. ) ;
#208085=CARTESIAN_POINT ( 'NONE',  ( 22.39999999999999503, 76.10085836911045476, -81.27267460801371612 ) ) ;
#208089=EDGE_CURVE ( 'NONE', #25020, #17722, #238673, .T. ) ;
#208097=DIRECTION ( 'NONE',  ( -1.000000000000000000, -0.000000000000000000, 0.000000000000000000 ) ) ;
#208104=AXIS2_PLACEMENT_3D ( 'NONE', #244058, #107119, #44594 ) ;
#208110=LINE ( 'NONE', #106395, #43406 ) ;
#208112=ADVANCED_FACE ( 'NONE', ( #165888 ), #88990, .T. ) ;
#208119=ORIENTED_EDGE ( 'NONE', *, *, #43109, .T. ) ;
#208129=VECTOR ( 'NONE', #92892, 1000.000000000000114 ) ;
#208133=CARTESIAN_POINT ( 'NONE',  ( 21.05000000000000071, 87.75000000001142553, -38.92310748452424463 ) ) ;
#208149=DIRECTION ( 'NONE',  ( 0.000000000000000000, 6.982962677686266711E-15, -1.000000000000000000 ) ) ;
#208152=CARTESIAN_POINT ( 'NONE',  ( 20.85000000000000142, 76.00000000001136868, -28.12310748452432208 ) ) ;
#208195=ORIENTED_EDGE ( 'NONE', *, *, #161070, .F. ) ;
#208201=ORIENTED_EDGE ( 'NONE', *, *, #73826, .F. ) ;
#208226=ORIENTED_EDGE ( 'NONE', *, *, #255381, .T. ) ;
#208254=DIRECTION ( 'NONE',  ( 1.836970198721029934E-16, 1.000000000000000000, 6.982962677686266711E-15 ) ) ;
#208268=DIRECTION ( 'NONE',  ( 1.000000000000000000, 0.000000000000000000, 0.000000000000000000 ) ) ;
#208272=ORIENTED_EDGE ( 'NONE', *, *, #196165, .F. ) ;
#208277=CIRCLE ( 'NONE', #70931, 0.1000000000000028644 ) ;
#208306=CIRCLE ( 'NONE', #91769, 0.09999999999999939493 ) ;
#208335=EDGE_CURVE ( 'NONE', #121432, #188354, #139559, .T. ) ;
#208376=LINE ( 'NONE', #124975, #73979 ) ;
#208377=PLANE ( 'NONE',  #233933 ) ;
#208395=VECTOR ( 'NONE', #108464, 1000.000000000000000 ) ;
#208412=CARTESIAN_POINT ( 'NONE',  ( -23.15000000000000213, 76.00000000001142553, -36.02310748452432421 ) ) ;
#208415=AXIS2_PLACEMENT_3D ( 'NONE', #152904, #92882, #211567 ) ;
#208424=ADVANCED_FACE ( 'NONE', ( #193989 ), #159745, .F. ) ;
#208433=CARTESIAN_POINT ( 'NONE',  ( 18.59999999999999076, 74.16465844978715438, -57.96795619196135618 ) ) ;
#208456=B_SPLINE_CURVE_WITH_KNOTS ( 'NONE', 3,
 ( #81737, #101281, #43930, #201719, #80448, #160056, #23108, #162609 ),
 .UNSPECIFIED., .F., .F.,
 ( 4, 2, 2, 4 ),
 ( 0.000000000000000000, 9.550056980125310032E-05, 0.0001910011396025062006, 0.0003820022792049910425 ),
 .UNSPECIFIED. ) ;
#208477=VERTEX_POINT ( 'NONE', #2164 ) ;
#208520=CARTESIAN_POINT ( 'NONE',  ( 22.49806830649814060, 75.92253568368623462, -81.17299713936340311 ) ) ;
#208528=CARTESIAN_POINT ( 'NONE',  ( 18.49999999999999289, 65.70729864260954400, -30.56574559737245877 ) ) ;
#208533=DIRECTION ( 'NONE',  ( 1.000000000000000000, 0.000000000000000000, 0.000000000000000000 ) ) ;
#208553=DIRECTION ( 'NONE',  ( 0.000000000000000000, 6.982962677686266711E-15, -1.000000000000000000 ) ) ;
#208569=ADVANCED_FACE ( 'NONE', ( #141685 ), #142951, .T. ) ;
#208607=ORIENTED_EDGE ( 'NONE', *, *, #209470, .F. ) ;
#208662=EDGE_CURVE ( 'NONE', #44347, #10713, #208110, .T. ) ;
#208669=CARTESIAN_POINT ( 'NONE',  ( 18.59999999999999787, 77.83534155023598089, -57.86795619196132634 ) ) ;
#208675=CARTESIAN_POINT ( 'NONE',  ( 20.85000000000000142, 64.25000000001146816, -42.80697314750249660 ) ) ;
#208692=DIRECTION ( 'NONE',  ( 0.000000000000000000, 0.8700118002898393765, -0.4930308989875104575 ) ) ;
#208701=VERTEX_POINT ( 'NONE', #47713 ) ;
#208733=VECTOR ( 'NONE', #127180, 1000.000000000000000 ) ;
#208753=VERTEX_POINT ( 'NONE', #115960 ) ;
#208765=FACE_OUTER_BOUND ( 'NONE', #244588, .T. ) ;
#208783=DIRECTION ( 'NONE',  ( 0.000000000000000000, 6.982962677686267499E-15, -1.000000000000000000 ) ) ;
#208835=ADVANCED_FACE ( 'NONE', ( #172119 ), #31316, .F. ) ;
#208837=CYLINDRICAL_SURFACE ( 'NONE', #176407, 0.09999999999999939493 ) ;
#208846=VERTEX_POINT ( 'NONE', #152546 ) ;
#208876=AXIS2_PLACEMENT_3D ( 'NONE', #91940, #171515, #250993 ) ;
#208890=EDGE_LOOP ( 'NONE', ( #15268, #114704, #217544, #53980 ) ) ;
#208896=AXIS2_PLACEMENT_3D ( 'NONE', #18268, #97767, #256816 ) ;
#208910=CARTESIAN_POINT ( 'NONE',  ( 18.49505832270841310, 85.43802806279451545, -62.32463430963041162 ) ) ;
#208917=EDGE_CURVE ( 'NONE', #14506, #82047, #18068, .T. ) ;
#208921=EDGE_LOOP ( 'NONE', ( #164796, #243206, #115275, #18592 ) ) ;
#208931=ADVANCED_FACE ( 'NONE', ( #122374 ), #243596, .T. ) ;
#208956=B_SPLINE_CURVE_WITH_KNOTS ( 'NONE', 3,
 ( #250652, #8219, #172464, #225932, #47305, #14653 ),
 .UNSPECIFIED., .F., .F.,
 ( 4, 2, 4 ),
 ( 0.000000000000000000, 0.0001496588209255844779, 0.0002993176418511689558 ),
 .UNSPECIFIED. ) ;
#208993=CARTESIAN_POINT ( 'NONE',  ( -20.94999999999999929, 77.85102823015243700, -57.86919421510181394 ) ) ;
#209059=EDGE_CURVE ( 'NONE', #81005, #6871, #201793, .T. ) ;
#209143=CARTESIAN_POINT ( 'NONE',  ( 21.05933563467872460, 65.27547528793024867, -57.32945973556844876 ) ) ;
#209147=VECTOR ( 'NONE', #213827, 1000.000000000000000 ) ;
#209151=VERTEX_POINT ( 'NONE', #193906 ) ;
#209161=CARTESIAN_POINT ( 'NONE',  ( -20.54999999999999716, 84.66355140188075268, -59.99900636645695329 ) ) ;
#209165=CARTESIAN_POINT ( 'NONE',  ( 20.94999999999999929, 70.60000000001149090, -45.91707660717680284 ) ) ;
#209170=VECTOR ( 'NONE', #238007, 1000.000000000000000 ) ;
#209200=CARTESIAN_POINT ( 'NONE',  ( 21.14999999999999503, 87.65000000001163016, -66.62310748452424036 ) ) ;
#209231=EDGE_CURVE ( 'NONE', #89290, #60411, #180963, .T. ) ;
#209232=FACE_OUTER_BOUND ( 'NONE', #186091, .T. ) ;
#209271=ORIENTED_EDGE ( 'NONE', *, *, #26652, .T. ) ;
#209323=ORIENTED_EDGE ( 'NONE', *, *, #78590, .T. ) ;
#209324=LINE ( 'NONE', #90657, #163400 ) ;
#209328=VERTEX_POINT ( 'NONE', #142871 ) ;
#209361=( BOUNDED_CURVE ( )  B_SPLINE_CURVE ( 3, ( #127525, #89659, #147065, #205765 ),
 .UNSPECIFIED., .F., .F. ) 
 B_SPLINE_CURVE_WITH_KNOTS ( ( 4, 4 ),
 ( 3.141592653589793116, 4.712388980384647041 ),
 .UNSPECIFIED. ) 
 CURVE ( )  GEOMETRIC_REPRESENTATION_ITEM ( )  RATIONAL_B_SPLINE_CURVE ( ( 1.000000000000000000, 0.8047378541243750405, 0.8047378541243750405, 1.000000000000000000 ) ) 
 REPRESENTATION_ITEM ( '' )  );
#209371=ADVANCED_FACE ( 'NONE', ( #182033 ), #231134, .T. ) ;
#209389=DIRECTION ( 'NONE',  ( -1.000000000000000000, 0.000000000000000000, 0.000000000000000000 ) ) ;
#209398=CARTESIAN_POINT ( 'NONE',  ( -20.85000000000000142, 77.16412189325258453, -28.30825939895270693 ) ) ;
#209413=DIRECTION ( 'NONE',  ( 1.000000000000000000, 0.000000000000000000, 0.000000000000000000 ) ) ;
#209428=ORIENTED_EDGE ( 'NONE', *, *, #184171, .T. ) ;
#209429=CARTESIAN_POINT ( 'NONE',  ( 20.85000000106584750, 64.25000000001146816, -42.86760282805085609 ) ) ;
#209437=ORIENTED_EDGE ( 'NONE', *, *, #204497, .T. ) ;
#209465=CARTESIAN_POINT ( 'NONE',  ( 21.05000000000000071, 76.00000000001142553, -36.02310748452432421 ) ) ;
#209470=EDGE_CURVE ( 'NONE', #115707, #97104, #84863, .T. ) ;
#209504=EDGE_LOOP ( 'NONE', ( #114916, #220610, #93217, #101779, #247074 ) ) ;
#209508=CARTESIAN_POINT ( 'NONE',  ( 23.14999999999999503, 64.35000000001150511, -48.17310748452440095 ) ) ;
#209519=EDGE_CURVE ( 'NONE', #44233, #67154, #217968, .T. ) ;
#209621=ORIENTED_EDGE ( 'NONE', *, *, #228724, .F. ) ;
#209627=ORIENTED_EDGE ( 'NONE', *, *, #52212, .F. ) ;
#209638=CARTESIAN_POINT ( 'NONE',  ( -23.15000000000000213, 76.00000000001165290, -69.52310748452431710 ) ) ;
#209649=EDGE_LOOP ( 'NONE', ( #115154, #190679, #210382, #232319 ) ) ;
#209731=DIRECTION ( 'NONE',  ( -1.000000000000000000, 0.000000000000000000, -0.000000000000000000 ) ) ;
#209740=DIRECTION ( 'NONE',  ( 0.000000000000000000, 1.000000000000000000, 6.982962677686266711E-15 ) ) ;
#209760=VECTOR ( 'NONE', #143736, 1000.000000000000000 ) ;
#209762=VECTOR ( 'NONE', #229123, 1000.000000000000000 ) ;
#209807=AXIS2_PLACEMENT_3D ( 'NONE', #97991, #192006, #13351 ) ;
#209811=EDGE_CURVE ( 'NONE', #147021, #216194, #85040, .T. ) ;
#209857=DIRECTION ( 'NONE',  ( 0.000000000000000000, -6.982962677686266711E-15, 1.000000000000000000 ) ) ;
#209869=ORIENTED_EDGE ( 'NONE', *, *, #130214, .T. ) ;
#209918=ORIENTED_EDGE ( 'NONE', *, *, #160358, .F. ) ;
#209922=EDGE_CURVE ( 'NONE', #52116, #150942, #247376, .T. ) ;
#209936=AXIS2_PLACEMENT_3D ( 'NONE', #249050, #225586, #70433 ) ;
#209970=CARTESIAN_POINT ( 'NONE',  ( 22.60000000000000142, 75.89914163091303578, -81.27267460801371612 ) ) ;
#209996=DIRECTION ( 'NONE',  ( 0.000000000000000000, 0.1568667991644355497, -0.9876197685951332295 ) ) ;
#210016=LINE ( 'NONE', #75653, #11491 ) ;
#210021=ORIENTED_EDGE ( 'NONE', *, *, #241049, .F. ) ;
#210058=ORIENTED_EDGE ( 'NONE', *, *, #159570, .T. ) ;
#210065=ORIENTED_EDGE ( 'NONE', *, *, #148272, .T. ) ;
#210108=FACE_OUTER_BOUND ( 'NONE', #26325, .T. ) ;
#210141=ORIENTED_EDGE ( 'NONE', *, *, #229381, .T. ) ;
#210154=EDGE_LOOP ( 'NONE', ( #217091, #206251, #93680, #130336 ) ) ;
#210166=ORIENTED_EDGE ( 'NONE', *, *, #168381, .F. ) ;
#210229=ORIENTED_EDGE ( 'NONE', *, *, #100628, .F. ) ;
#210235=VECTOR ( 'NONE', #106497, 1000.000000000000000 ) ;
#210254=CARTESIAN_POINT ( 'NONE',  ( -23.15000000000000213, 73.50000000001156764, -56.29848556176223440 ) ) ;
#210260=AXIS2_PLACEMENT_3D ( 'NONE', #52659, #132211, #194779 ) ;
#210282=DIRECTION ( 'NONE',  ( -3.440080580676165868E-14, 0.1298341882520054891, 0.9915357197604850459 ) ) ;
#210287=CARTESIAN_POINT ( 'NONE',  ( -18.59999999999999787, 77.16412189325258453, -28.20825939895270551 ) ) ;
#210328=CARTESIAN_POINT ( 'NONE',  ( 20.04142135623730070, 64.35000000001150511, -48.27310748452440237 ) ) ;
#210352=CIRCLE ( 'NONE', #14550, 12.77499999999999503 ) ;
#210362=VERTEX_POINT ( 'NONE', #192667 ) ;
#210382=ORIENTED_EDGE ( 'NONE', *, *, #16877, .T. ) ;
#210392=EDGE_CURVE ( 'NONE', #155813, #124582, #143518, .T. ) ;
#210402=EDGE_CURVE ( 'NONE', #90553, #21197, #131046, .T. ) ;
#210416=EDGE_CURVE ( 'NONE', #93396, #209151, #113686, .T. ) ;
#210417=CARTESIAN_POINT ( 'NONE',  ( -22.60000000000094289, 75.89914163091323474, -81.27267460801374455 ) ) ;
#210430=ORIENTED_EDGE ( 'NONE', *, *, #231455, .T. ) ;
#210471=ORIENTED_EDGE ( 'NONE', *, *, #23448, .T. ) ;
#210502=CARTESIAN_POINT ( 'NONE',  ( 21.06089410995830491, 65.27470446788798597, -57.32072675348123880 ) ) ;
#210506=DIRECTION ( 'NONE',  ( 1.000000000000000000, 0.000000000000000000, 0.000000000000000000 ) ) ;
#210532=AXIS2_PLACEMENT_3D ( 'NONE', #63093, #108649, #142618 ) ;
#210546=LINE ( 'NONE', #252221, #82303 ) ;
#210576=VECTOR ( 'NONE', #16972, 1000.000000000000000 ) ;
#210637=AXIS2_PLACEMENT_3D ( 'NONE', #131300, #111747, #231706 ) ;
#210655=DIRECTION ( 'NONE',  ( -1.000000000000000000, -0.000000000000000000, -0.000000000000000000 ) ) ;
#210657=DIRECTION ( 'NONE',  ( 0.000000000000000000, -1.000000000000000000, -6.982962677686266711E-15 ) ) ;
#210658=ORIENTED_EDGE ( 'NONE', *, *, #141336, .T. ) ;
#210704=CARTESIAN_POINT ( 'NONE',  ( -18.50000000000000711, 64.35000000001161879, -62.50830171387040934 ) ) ;
#210714=DIRECTION ( 'NONE',  ( 1.000000000000000000, 0.000000000000000000, 0.000000000000000000 ) ) ;
#210728=CARTESIAN_POINT ( 'NONE',  ( 21.00000000000000000, 66.25000000001158185, -57.17310748452438673 ) ) ;
#210746=CARTESIAN_POINT ( 'NONE',  ( -21.14999999999999858, 69.45934304831041572, -69.52310748452435973 ) ) ;
#210747=DIRECTION ( 'NONE',  ( 0.000000000000000000, 0.000000000000000000, 1.000000000000000000 ) ) ;
#210759=DIRECTION ( 'NONE',  ( 1.000000000000000000, 0.000000000000000000, 0.000000000000000000 ) ) ;
#210765=EDGE_CURVE ( 'NONE', #214123, #202965, #180490, .T. ) ;
#210772=CARTESIAN_POINT ( 'NONE',  ( 18.59999999999997655, 64.25000000001142553, -36.02310748452440237 ) ) ;
#210783=CIRCLE ( 'NONE', #214882, 0.1999999999999987899 ) ;
#210809=ORIENTED_EDGE ( 'NONE', *, *, #24637, .F. ) ;
#210843=ORIENTED_EDGE ( 'NONE', *, *, #169672, .F. ) ;
#210848=AXIS2_PLACEMENT_3D ( 'NONE', #224400, #184000, #185290 ) ;
#210884=AXIS2_PLACEMENT_3D ( 'NONE', #170264, #249751, #211922 ) ;
#210895=EDGE_CURVE ( 'NONE', #71835, #243532, #177244, .T. ) ;
#210914=SURFACE_STYLE_FILL_AREA ( #188777 ) ;
#210952=DIRECTION ( 'NONE',  ( -1.000000000000000000, 3.265361837132813093E-16, 2.280189983783949500E-30 ) ) ;
#210961=CARTESIAN_POINT ( 'NONE',  ( 22.60000000000000142, 75.95218160930696172, -81.27312990357155797 ) ) ;
#210964=CARTESIAN_POINT ( 'NONE',  ( -21.05000000000000071, 87.75000000001143974, -39.02310748452423894 ) ) ;
#211024=AXIS2_PLACEMENT_3D ( 'NONE', #234708, #215140, #56034 ) ;
#211029=EDGE_CURVE ( 'NONE', #183881, #14506, #33019, .T. ) ;
#211046=VECTOR ( 'NONE', #237401, 1000.000000000000000 ) ;
#211078=VERTEX_POINT ( 'NONE', #182442 ) ;
#211095=DIRECTION ( 'NONE',  ( -1.000000000000000000, 2.952720810173289112E-16, 2.061873921506763405E-30 ) ) ;
#211103=CARTESIAN_POINT ( 'NONE',  ( -18.50000000000000000, 85.40000000001138858, -29.14106563635158764 ) ) ;
#211106=CARTESIAN_POINT ( 'NONE',  ( -18.59999999999999787, 68.97833521811131163, -32.18954208262707795 ) ) ;
#211116=CIRCLE ( 'NONE', #127915, 0.1999999999999987899 ) ;
#211121=VERTEX_POINT ( 'NONE', #222819 ) ;
#211137=DIRECTION ( 'NONE',  ( 0.000000000000000000, 0.000000000000000000, 1.000000000000000000 ) ) ;
#211210=CARTESIAN_POINT ( 'NONE',  ( 21.14999999999999858, 69.45000000001157048, -57.17310748452436542 ) ) ;
#211211=ORIENTED_EDGE ( 'NONE', *, *, #65345, .T. ) ;
#211224=ADVANCED_FACE ( 'NONE', ( #8927 ), #128884, .T. ) ;
#211250=ADVANCED_FACE ( 'NONE', ( #168041 ), #206434, .T. ) ;
#211281=AXIS2_PLACEMENT_3D ( 'NONE', #8576, #167667, #46395 ) ;
#211295=AXIS2_PLACEMENT_3D ( 'NONE', #237396, #180000, #222949 ) ;
#211306=VERTEX_POINT ( 'NONE', #97406 ) ;
#211319=CARTESIAN_POINT ( 'NONE',  ( 20.94999999999999929, 69.45000000001158469, -59.50608031408435039 ) ) ;
#211327=CYLINDRICAL_SURFACE ( 'NONE', #23490, 0.09999999999999520384 ) ;
#211333=ORIENTED_EDGE ( 'NONE', *, *, #91830, .F. ) ;
#211340=DIRECTION ( 'NONE',  ( 1.000000000000000000, 0.000000000000000000, 0.000000000000000000 ) ) ;
#211350=AXIS2_PLACEMENT_3D ( 'NONE', #178242, #257685, #79087 ) ;
#211359=CARTESIAN_POINT ( 'NONE',  ( -18.50000000000000000, 85.50000000001175238, -81.27310748452426026 ) ) ;
#211414=ORIENTED_EDGE ( 'NONE', *, *, #221640, .F. ) ;
#211442=CIRCLE ( 'NONE', #98986, 0.1000000000000028644 ) ;
#211467=EDGE_CURVE ( 'NONE', #43683, #196290, #131597, .T. ) ;
#211469=AXIS2_PLACEMENT_3D ( 'NONE', #182346, #222724, #183623 ) ;
#211492=AXIS2_PLACEMENT_3D ( 'NONE', #38742, #197795, #19163 ) ;
#211495=EDGE_LOOP ( 'NONE', ( #9431, #221112, #63449, #39272 ) ) ;
#211564=DIRECTION ( 'NONE',  ( -0.000000000000000000, 1.000000000000000000, 6.982962677686266711E-15 ) ) ;
#211567=DIRECTION ( 'NONE',  ( 1.000000000000000000, 0.000000000000000000, 0.000000000000000000 ) ) ;
#211581=CIRCLE ( 'NONE', #132269, 3.900000000000000799 ) ;
#211618=AXIS2_PLACEMENT_3D ( 'NONE', #253890, #56950, #154830 ) ;
#211632=CARTESIAN_POINT ( 'NONE',  ( -18.59999999999999787, 77.16412189325258453, -28.30825939895270693 ) ) ;
#211634=DIRECTION ( 'NONE',  ( 0.000000000000000000, 0.000000000000000000, 1.000000000000000000 ) ) ;
#211643=DIRECTION ( 'NONE',  ( 1.000000000000000000, 0.000000000000000000, 0.000000000000000000 ) ) ;
#211681=AXIS2_PLACEMENT_3D ( 'NONE', #156700, #40611, #254450 ) ;
#211732=FACE_OUTER_BOUND ( 'NONE', #67277, .T. ) ;
#211799=VERTEX_POINT ( 'NONE', #140093 ) ;
#211829=VERTEX_POINT ( 'NONE', #43589 ) ;
#211867=CARTESIAN_POINT ( 'NONE',  ( 20.85000000000000142, 76.32388570108174974, -36.06551789521033413 ) ) ;
#211890=FACE_OUTER_BOUND ( 'NONE', #27206, .T. ) ;
#211922=DIRECTION ( 'NONE',  ( -1.000000000000000000, 0.000000000000000000, 0.000000000000000000 ) ) ;
#211957=CARTESIAN_POINT ( 'NONE',  ( 20.94999999999999929, 76.00000000001155342, -56.54810748452432279 ) ) ;
#212000=DIRECTION ( 'NONE',  ( 1.000000000000000000, 0.000000000000000000, 0.000000000000000000 ) ) ;
#212013=DIRECTION ( 'NONE',  ( 1.000000000000000000, 0.000000000000000000, 0.000000000000000000 ) ) ;
#212049=DIRECTION ( 'NONE',  ( -1.000000000000000000, 0.000000000000000000, 0.000000000000000000 ) ) ;
#212063=ORIENTED_EDGE ( 'NONE', *, *, #107991, .F. ) ;
#212086=CARTESIAN_POINT ( 'NONE',  ( -23.15000000000000213, 74.00000000001156764, -56.29848556176223440 ) ) ;
#212096=EDGE_CURVE ( 'NONE', #14406, #20329, #115211, .T. ) ;
#212104=DIRECTION ( 'NONE',  ( 0.000000000000000000, -1.000000000000000000, -6.352154140967427193E-15 ) ) ;
#212111=ORIENTED_EDGE ( 'NONE', *, *, #241004, .F. ) ;
#212115=FACE_BOUND ( 'NONE', #120182, .T. ) ;
#212130=VERTEX_POINT ( 'NONE', #9152 ) ;
#212137=EDGE_CURVE ( 'NONE', #70064, #108484, #106947, .T. ) ;
#212142=AXIS2_PLACEMENT_3D ( 'NONE', #249873, #174231, #252421 ) ;
#212146=DIRECTION ( 'NONE',  ( 1.000000000000000000, 0.000000000000000000, 0.000000000000000000 ) ) ;
#212179=CARTESIAN_POINT ( 'NONE',  ( 21.05000000000000071, 71.00000000001151079, -48.42837350343745584 ) ) ;
#212207=VERTEX_POINT ( 'NONE', #178388 ) ;
#212259=CARTESIAN_POINT ( 'NONE',  ( -20.54999999999999716, 85.00000000001159606, -59.62913836187181715 ) ) ;
#212262=EDGE_CURVE ( 'NONE', #92669, #78944, #174570, .T. ) ;
#212267=EDGE_LOOP ( 'NONE', ( #109861, #219224, #183365, #87491 ) ) ;
#212325=EDGE_CURVE ( 'NONE', #50336, #241487, #236197, .T. ) ;
#212370=DIRECTION ( 'NONE',  ( -1.000000000000000000, -0.000000000000000000, -0.000000000000000000 ) ) ;
#212391=CIRCLE ( 'NONE', #24960, 0.1999999999999987899 ) ;
#212432=DIRECTION ( 'NONE',  ( -1.000000000000000000, 0.000000000000000000, -0.000000000000000000 ) ) ;
#212434=DIRECTION ( 'NONE',  ( 1.000000000000000000, -7.304098846218163263E-16, 4.217023435051626718E-16 ) ) ;
#212446=ORIENTED_EDGE ( 'NONE', *, *, #44938, .T. ) ;
#212468=CARTESIAN_POINT ( 'NONE',  ( 20.94999999999999929, 84.66355140188075268, -59.99900636645695329 ) ) ;
#212470=ORIENTED_EDGE ( 'NONE', *, *, #158388, .T. ) ;
#212482=DIRECTION ( 'NONE',  ( -1.000000000000000000, 0.000000000000000000, -0.000000000000000000 ) ) ;
#212489=DIRECTION ( 'NONE',  ( 1.000000000000000000, -2.952720810173289112E-16, -2.061873921506763405E-30 ) ) ;
#212499=CIRCLE ( 'NONE', #41637, 0.1000000000000042799 ) ;
#212518=CARTESIAN_POINT ( 'NONE',  ( -21.05000000000000071, 74.75000000001159606, -61.52310748452433131 ) ) ;
#212531=DIRECTION ( 'NONE',  ( 0.000000000000000000, 0.000000000000000000, -1.000000000000000000 ) ) ;
#212533=ORIENTED_EDGE ( 'NONE', *, *, #183914, .F. ) ;
#212555=AXIS2_PLACEMENT_3D ( 'NONE', #5648, #82609, #205140 ) ;
#212577=AXIS2_PLACEMENT_3D ( 'NONE', #238625, #258106, #221598 ) ;
#212633=DIRECTION ( 'NONE',  ( 0.000000000000000000, 0.000000000000000000, 1.000000000000000000 ) ) ;
#212667=ORIENTED_EDGE ( 'NONE', *, *, #178132, .T. ) ;
#212743=ORIENTED_EDGE ( 'NONE', *, *, #80848, .F. ) ;
#212746=ORIENTED_EDGE ( 'NONE', *, *, #219530, .F. ) ;
#212752=AXIS2_PLACEMENT_3D ( 'NONE', #943, #137909, #256528 ) ;
#212807=EDGE_CURVE ( 'NONE', #124432, #44347, #28315, .T. ) ;
#212819=CARTESIAN_POINT ( 'NONE',  ( -21.59780538579341069, 69.15290947006839417, -69.62208615412235702 ) ) ;
#212829=VERTEX_POINT ( 'NONE', #42392 ) ;
#212833=CARTESIAN_POINT ( 'NONE',  ( -18.50000000000000000, 64.35000000001174669, -81.27310748452440237 ) ) ;
#212844=VERTEX_POINT ( 'NONE', #101026 ) ;
#212866=ORIENTED_EDGE ( 'NONE', *, *, #62432, .F. ) ;
#212871=CARTESIAN_POINT ( 'NONE',  ( 21.05000000000000071, 77.25000000001159606, -61.62310748452431142 ) ) ;
#212927=EDGE_CURVE ( 'NONE', #235108, #162078, #248867, .T. ) ;
#212948=DIRECTION ( 'NONE',  ( 0.000000000000000000, 1.000000000000000000, 7.272083257015735086E-15 ) ) ;
#212950=CARTESIAN_POINT ( 'NONE',  ( 18.59999999999999432, 77.16270174994961906, -61.52310748452431710 ) ) ;
#212979=EDGE_LOOP ( 'NONE', ( #108663, #229462, #34860, #176506, #57153 ) ) ;
#213015=ADVANCED_FACE ( 'NONE', ( #188320 ), #161386, .F. ) ;
#213017=EDGE_CURVE ( 'NONE', #51613, #84837, #194727, .T. ) ;
#213058=EDGE_CURVE ( 'NONE', #22150, #89706, #211442, .T. ) ;
#213063=EDGE_CURVE ( 'NONE', #165183, #209328, #115202, .T. ) ;
#213090=DIRECTION ( 'NONE',  ( 1.000000000000000000, 0.000000000000000000, 0.000000000000000000 ) ) ;
#213095=CARTESIAN_POINT ( 'NONE',  ( 23.14999999999999858, 76.00000000001142553, -36.02310748452432421 ) ) ;
#213101=CARTESIAN_POINT ( 'NONE',  ( 20.94999999999999574, 87.65000000001163016, -66.52310748452423184 ) ) ;
#213120=CARTESIAN_POINT ( 'NONE',  ( -23.15000000000000213, 85.00000000001149658, -45.91707660717669626 ) ) ;
#213171=DIRECTION ( 'NONE',  ( 0.000000000000000000, -7.086529944415893080E-15, 1.000000000000000000 ) ) ;
#213188=DIRECTION ( 'NONE',  ( -0.000000000000000000, 0.1350103645451835865, 0.9908441862701605762 ) ) ;
#213206=EDGE_CURVE ( 'NONE', #8048, #40297, #252953, .T. ) ;
#213213=CIRCLE ( 'NONE', #21703, 0.1000000000000043771 ) ;
#213218=LINE ( 'NONE', #18877, #79803 ) ;
#213243=CIRCLE ( 'NONE', #230009, 0.1000000000000028644 ) ;
#213266=CIRCLE ( 'NONE', #109219, 0.1000000000000028644 ) ;
#213269=EDGE_CURVE ( 'NONE', #8900, #231640, #178335, .T. ) ;
#213274=DIRECTION ( 'NONE',  ( 0.000000000000000000, 0.8660254037844424824, 0.4999999999999934497 ) ) ;
#213293=LINE ( 'NONE', #38528, #158412 ) ;
#213302=DIRECTION ( 'NONE',  ( 1.000000000000000000, 0.000000000000000000, 0.000000000000000000 ) ) ;
#213333=ORIENTED_EDGE ( 'NONE', *, *, #228070, .T. ) ;
#213372=DIRECTION ( 'NONE',  ( 0.000000000000000000, -0.1575844902526579161, -0.9875055080513779338 ) ) ;
#213524=CYLINDRICAL_SURFACE ( 'NONE', #238214, 0.1000000000000028644 ) ;
#213568=CARTESIAN_POINT ( 'NONE',  ( -23.25000000000000000, 73.40000000001157332, -56.29848556176223440 ) ) ;
#213577=CARTESIAN_POINT ( 'NONE',  ( 18.59999999999999787, 87.75000000001146816, -44.67310748452424463 ) ) ;
#213617=CARTESIAN_POINT ( 'NONE',  ( -21.03922262424652345, 64.37609936600685501, -62.66389944163073977 ) ) ;
#213622=ORIENTED_EDGE ( 'NONE', *, *, #335, .F. ) ;
#213651=EDGE_CURVE ( 'NONE', #234718, #120848, #161944, .T. ) ;
#213667=CARTESIAN_POINT ( 'NONE',  ( -18.33682934331482883, 85.51118559110493322, -29.11745271585079919 ) ) ;
#213706=CYLINDRICAL_SURFACE ( 'NONE', #254094, 0.09999999999999939493 ) ;
#213718=DIRECTION ( 'NONE',  ( 0.000000000000000000, 0.000000000000000000, 1.000000000000000000 ) ) ;
#213730=ORIENTED_EDGE ( 'NONE', *, *, #55266, .T. ) ;
#213744=ORIENTED_EDGE ( 'NONE', *, *, #118481, .T. ) ;
#213750=PLANE ( 'NONE',  #26202 ) ;
#213769=DIRECTION ( 'NONE',  ( 0.000000000000000000, -1.000000000000000000, 0.000000000000000000 ) ) ;
#213807=VERTEX_POINT ( 'NONE', #77683 ) ;
#213811=DIRECTION ( 'NONE',  ( 0.000000000000000000, 0.000000000000000000, -1.000000000000000000 ) ) ;
#213816=DIRECTION ( 'NONE',  ( 1.000000000000000000, 0.000000000000000000, 0.000000000000000000 ) ) ;
#213827=DIRECTION ( 'NONE',  ( -1.000000000000000000, 0.000000000000000000, -0.000000000000000000 ) ) ;
#213866=ORIENTED_EDGE ( 'NONE', *, *, #35868, .T. ) ;
#213868=LINE ( 'NONE', #114772, #156642 ) ;
#213929=DIRECTION ( 'NONE',  ( 0.000000000000000000, -1.000000000000000000, -6.982962677686265922E-15 ) ) ;
#213945=ORIENTED_EDGE ( 'NONE', *, *, #65551, .F. ) ;
#213971=EDGE_CURVE ( 'NONE', #50215, #56908, #248848, .T. ) ;
#214049=CARTESIAN_POINT ( 'NONE',  ( 20.12500000000000000, 66.25000000001161027, -61.41133620241011215 ) ) ;
#214064=FACE_OUTER_BOUND ( 'NONE', #84323, .T. ) ;
#214089=CARTESIAN_POINT ( 'NONE',  ( 20.94999999999999929, 85.50000000001149658, -45.91707660717669626 ) ) ;
#214119=DIRECTION ( 'NONE',  ( -0.000000000000000000, 0.1350103645451859180, 0.9908441862701603542 ) ) ;
#214123=VERTEX_POINT ( 'NONE', #172702 ) ;
#214130=FACE_OUTER_BOUND ( 'NONE', #29949, .T. ) ;
#214136=CARTESIAN_POINT ( 'NONE',  ( -20.85000000000000142, 77.83585931145498193, -24.51866831572578675 ) ) ;
#214146=ORIENTED_EDGE ( 'NONE', *, *, #99946, .T. ) ;
#214148=ORIENTED_EDGE ( 'NONE', *, *, #124436, .T. ) ;
#214166=LINE ( 'NONE', #57637, #109204 ) ;
#214181=ORIENTED_EDGE ( 'NONE', *, *, #229620, .F. ) ;
#214182=CARTESIAN_POINT ( 'NONE',  ( -18.59999999999999787, 64.25000000001152500, -48.17310748452440805 ) ) ;
#214188=DIRECTION ( 'NONE',  ( 1.000000000000000000, -0.000000000000000000, 0.000000000000000000 ) ) ;
#214217=EDGE_LOOP ( 'NONE', ( #225151, #247959, #239865, #194706 ) ) ;
#214218=DIRECTION ( 'NONE',  ( 1.836970198721029934E-16, 1.000000000000000000, 6.982962677686266711E-15 ) ) ;
#214245=ORIENTED_EDGE ( 'NONE', *, *, #43549, .F. ) ;
#214281=AXIS2_PLACEMENT_3D ( 'NONE', #76695, #35059, #156280 ) ;
#214293=LINE ( 'NONE', #154364, #45032 ) ;
#214318=VERTEX_POINT ( 'NONE', #62973 ) ;
#214322=ORIENTED_EDGE ( 'NONE', *, *, #235285, .T. ) ;
#214352=AXIS2_PLACEMENT_3D ( 'NONE', #150309, #210282, #233700 ) ;
#214367=ORIENTED_EDGE ( 'NONE', *, *, #78306, .T. ) ;
#214383=CARTESIAN_POINT ( 'NONE',  ( -23.15000000000000213, 76.00000000001142553, -36.02310748452432421 ) ) ;
#214386=DIRECTION ( 'NONE',  ( -0.000000000000000000, 1.000000000000000000, 6.982962677686266711E-15 ) ) ;
#214387=CARTESIAN_POINT ( 'NONE',  ( 21.05000000000000071, 76.08559286337361982, -75.93677021939394933 ) ) ;
#214440=CARTESIAN_POINT ( 'NONE',  ( 18.49999999999998934, 69.45000000001149942, -48.37310748452436826 ) ) ;
#214455=DIRECTION ( 'NONE',  ( -6.938893903907224433E-15, -1.000000000000000000, -6.982962677686266711E-15 ) ) ;
#214459=CIRCLE ( 'NONE', #197889, 0.1000000000000026007 ) ;
#214485=CARTESIAN_POINT ( 'NONE',  ( -18.50000000000000000, 77.16412189325258453, -28.30825939895270693 ) ) ;
#214491=ORIENTED_EDGE ( 'NONE', *, *, #215887, .T. ) ;
#214547=FACE_OUTER_BOUND ( 'NONE', #18490, .T. ) ;
#214556=ORIENTED_EDGE ( 'NONE', *, *, #233109, .F. ) ;
#214584=CARTESIAN_POINT ( 'NONE',  ( 18.49999999999999645, 77.83585931145498193, -24.51866831572578320 ) ) ;
#214598=CARTESIAN_POINT ( 'NONE',  ( 20.94999999999999929, 71.00000000001151079, -47.92837350343745584 ) ) ;
#214601=ADVANCED_FACE ( 'NONE', ( #135772 ), #173689, .T. ) ;
#214618=VERTEX_POINT ( 'NONE', #233617 ) ;
#214636=CARTESIAN_POINT ( 'NONE',  ( 21.05000000000000071, 69.52244781751853964, -69.42310751922482837 ) ) ;
#214683=AXIS2_PLACEMENT_3D ( 'NONE', #240620, #238044, #77673 ) ;
#214702=DIRECTION ( 'NONE',  ( 0.000000000000000000, -0.1350103645451945777, 0.9908441862701590219 ) ) ;
#214723=CARTESIAN_POINT ( 'NONE',  ( 21.05000000000000071, 85.40000000001158753, -59.62913836187181715 ) ) ;
#214779=FACE_OUTER_BOUND ( 'NONE', #74662, .T. ) ;
#214847=CARTESIAN_POINT ( 'NONE',  ( -21.07954763557422595, 75.93412408139332115, -75.85239847456186624 ) ) ;
#214856=CARTESIAN_POINT ( 'NONE',  ( -21.05000000000000071, 74.83729825007360148, -61.42310748452432989 ) ) ;
#214874=ORIENTED_EDGE ( 'NONE', *, *, #251384, .F. ) ;
#214882=AXIS2_PLACEMENT_3D ( 'NONE', #68399, #65820, #166246 ) ;
#214890=CARTESIAN_POINT ( 'NONE',  ( -23.15000000000000213, 85.60000000001173248, -81.27310748452424605 ) ) ;
#214920=ORIENTED_EDGE ( 'NONE', *, *, #197667, .T. ) ;
#214928=DIRECTION ( 'NONE',  ( 1.000000000000000000, 7.304098846218134667E-16, 5.100424963727256530E-30 ) ) ;
#214940=CARTESIAN_POINT ( 'NONE',  ( -18.59999999999999787, 85.48068669529035901, -29.08199231576641353 ) ) ;
#214948=CARTESIAN_POINT ( 'NONE',  ( -18.33981767444299393, 85.56957578981555912, -29.20394564079942867 ) ) ;
#214959=CARTESIAN_POINT ( 'NONE',  ( 20.94999999999999574, 74.15091558138456662, -57.86709696307720918 ) ) ;
#215024=DIRECTION ( 'NONE',  ( -0.000000000000000000, -1.000000000000000000, -6.982962677686266711E-15 ) ) ;
#215053=DIRECTION ( 'NONE',  ( 0.000000000000000000, -1.000000000000000000, 0.000000000000000000 ) ) ;
#215092=CARTESIAN_POINT ( 'NONE',  ( -21.05000000000000071, 69.69982018209479691, -69.57459036640655370 ) ) ;
#215093=CIRCLE ( 'NONE', #106743, 0.1000000000000028644 ) ;
#215109=CARTESIAN_POINT ( 'NONE',  ( -22.39999999999999858, 75.90000000001170122, -77.31388708289772183 ) ) ;
#215126=ORIENTED_EDGE ( 'NONE', *, *, #252395, .F. ) ;
#215140=DIRECTION ( 'NONE',  ( 1.000000000000000000, 7.304098846218133681E-16, 5.311601492717083645E-30 ) ) ;
#215144=DIRECTION ( 'NONE',  ( 0.000000000000000000, -1.000000000000000000, -6.352154140967427193E-15 ) ) ;
#215164=CARTESIAN_POINT ( 'NONE',  ( 18.50000000000000000, 85.50000000001161027, -62.49103808782458458 ) ) ;
#215170=CARTESIAN_POINT ( 'NONE',  ( 20.94999999999999929, 65.70711192142317714, -30.56510546851222188 ) ) ;
#215172=DIRECTION ( 'NONE',  ( 0.000000000000000000, 6.982962677686266711E-15, -1.000000000000000000 ) ) ;
#215173=CARTESIAN_POINT ( 'NONE',  ( 18.50000324121758055, 65.70692517833163038, -30.56446533783042696 ) ) ;
#215199=DIRECTION ( 'NONE',  ( 0.000000000000000000, -0.4999999999999943379, -0.8660254037844420383 ) ) ;
#215205=AXIS2_PLACEMENT_3D ( 'NONE', #25412, #183196, #104889 ) ;
#215207=AXIS2_PLACEMENT_3D ( 'NONE', #11071, #240396, #22650 ) ;
#215216=VERTEX_POINT ( 'NONE', #24542 ) ;
#215270=ORIENTED_EDGE ( 'NONE', *, *, #152044, .T. ) ;
#215272=VERTEX_POINT ( 'NONE', #68786 ) ;
#215320=DIRECTION ( 'NONE',  ( 0.000000000000000000, 0.000000000000000000, -1.000000000000000000 ) ) ;
#215324=ORIENTED_EDGE ( 'NONE', *, *, #58339, .F. ) ;
#215327=EDGE_LOOP ( 'NONE', ( #17260, #215709, #58851, #22537 ) ) ;
#215333=ORIENTED_EDGE ( 'NONE', *, *, #55893, .T. ) ;
#215367=CARTESIAN_POINT ( 'NONE',  ( -22.47071067811865319, 68.27992525551360359, -69.62219993922698791 ) ) ;
#215373=EDGE_LOOP ( 'NONE', ( #189718, #129293, #16535, #186376 ) ) ;
#215415=TOROIDAL_SURFACE ( 'NONE', #32281, 0.2000000000000000111, 0.1000000000000000056 ) ;
#215421=ORIENTED_EDGE ( 'NONE', *, *, #244362, .F. ) ;
#215424=EDGE_CURVE ( 'NONE', #193842, #156378, #91826, .T. ) ;
#215425=DIRECTION ( 'NONE',  ( 0.000000000000000000, -0.8660254037844445918, -0.4999999999999897304 ) ) ;
#215459=CARTESIAN_POINT ( 'NONE',  ( -18.59999999999999787, 74.16465844978715438, -57.96795619196135618 ) ) ;
#215488=DIRECTION ( 'NONE',  ( -1.000000000000000000, 0.000000000000000000, 0.000000000000000000 ) ) ;
#215499=AXIS2_PLACEMENT_3D ( 'NONE', #111939, #209740, #33712 ) ;
#215524=CARTESIAN_POINT ( 'NONE',  ( -1.820710678118658388, 85.92928932189282420, -44.87310748452424747 ) ) ;
#215554=FACE_OUTER_BOUND ( 'NONE', #96916, .T. ) ;
#215558=CARTESIAN_POINT ( 'NONE',  ( -21.55000000000000071, 68.75000000001158185, -57.17310748452437252 ) ) ;
#215565=CIRCLE ( 'NONE', #124008, 0.1000000000000028644 ) ;
#215567=LINE ( 'NONE', #368, #254596 ) ;
#215571=CARTESIAN_POINT ( 'NONE',  ( -20.85000000000000142, 77.13501884592155022, -28.30613060109199353 ) ) ;
#215584=VERTEX_POINT ( 'NONE', #79012 ) ;
#215588=ORIENTED_EDGE ( 'NONE', *, *, #198015, .F. ) ;
#215606=CARTESIAN_POINT ( 'NONE',  ( -21.05000000000000071, 76.00000000001168132, -73.82310748452428584 ) ) ;
#215614=CARTESIAN_POINT ( 'NONE',  ( -20.85000000000000142, 77.16412189325258453, -28.10825939895270764 ) ) ;
#215640=CARTESIAN_POINT ( 'NONE',  ( 18.39999999999999858, 85.50000000001136868, -29.10844914155459051 ) ) ;
#215654=CARTESIAN_POINT ( 'NONE',  ( 21.05000000000000071, 76.01454569058276434, -76.02012527095639882 ) ) ;
#215692=DIRECTION ( 'NONE',  ( -1.000000000000000000, 0.000000000000000000, -0.000000000000000000 ) ) ;
#215709=ORIENTED_EDGE ( 'NONE', *, *, #23556, .T. ) ;
#215718=DIRECTION ( 'NONE',  ( -1.000000000000000000, -0.000000000000000000, -0.000000000000000000 ) ) ;
#215740=VERTEX_POINT ( 'NONE', #251917 ) ;
#215747=CARTESIAN_POINT ( 'NONE',  ( 22.59999999999999432, 64.25043287652226809, -69.62396585362311896 ) ) ;
#215749=CIRCLE ( 'NONE', #103320, 0.1000000000000028644 ) ;
#215780=DIRECTION ( 'NONE',  ( 0.000000000000000000, -6.982962677686266711E-15, 1.000000000000000000 ) ) ;
#215791=DIRECTION ( 'NONE',  ( 0.000000000000000000, 6.982962677686266711E-15, -1.000000000000000000 ) ) ;
#215841=DIRECTION ( 'NONE',  ( 0.000000000000000000, 6.467318590049456648E-15, -1.000000000000000000 ) ) ;
#215853=CYLINDRICAL_SURFACE ( 'NONE', #177918, 0.5000000000000004441 ) ;
#215858=DIRECTION ( 'NONE',  ( 0.000000000000000000, -6.982962677686266711E-15, 1.000000000000000000 ) ) ;
#215866=LINE ( 'NONE', #175504, #209170 ) ;
#215873=DIRECTION ( 'NONE',  ( -0.000000000000000000, -6.982962677686266711E-15, 1.000000000000000000 ) ) ;
#215880=EDGE_CURVE ( 'NONE', #149532, #182718, #96273, .T. ) ;
#215883=ORIENTED_EDGE ( 'NONE', *, *, #185720, .T. ) ;
#215887=EDGE_CURVE ( 'NONE', #111234, #89290, #191994, .T. ) ;
#215946=DIRECTION ( 'NONE',  ( 1.000000000000000000, 0.000000000000000000, 0.000000000000000000 ) ) ;
#215958=ADVANCED_FACE ( 'NONE', ( #179709, #37639 ), #235808, .F. ) ;
#215964=CARTESIAN_POINT ( 'NONE',  ( 18.50000000000000000, 85.40000000001137437, -29.14106563635157698 ) ) ;
#215974=EDGE_LOOP ( 'NONE', ( #164679, #147820, #97119, #5483 ) ) ;
#215982=EDGE_LOOP ( 'NONE', ( #63042, #1503, #46671 ) ) ;
#216034=EDGE_LOOP ( 'NONE', ( #122818, #60076, #130030 ) ) ;
#216062=EDGE_LOOP ( 'NONE', ( #129839, #47813, #14268, #3691 ) ) ;
#216065=VERTEX_POINT ( 'NONE', #61018 ) ;
#216084=ORIENTED_EDGE ( 'NONE', *, *, #203559, .F. ) ;
#216099=CARTESIAN_POINT ( 'NONE',  ( 20.77766267348356166, 65.55095760939242666, -61.93039856864697157 ) ) ;
#216107=SPHERICAL_SURFACE ( 'NONE', #242659, 0.1000000000000000056 ) ;
#216123=EDGE_LOOP ( 'NONE', ( #65830, #138624, #186159, #216608 ) ) ;
#216130=CARTESIAN_POINT ( 'NONE',  ( -20.64999999999999858, 76.00000000001165290, -69.52310748452431710 ) ) ;
#216178=VERTEX_POINT ( 'NONE', #158560 ) ;
#216184=CARTESIAN_POINT ( 'NONE',  ( -20.54999999999999716, 68.85000000001156195, -57.27310748452436684 ) ) ;
#216194=VERTEX_POINT ( 'NONE', #256276 ) ;
#216210=CARTESIAN_POINT ( 'NONE',  ( 20.85000000000000142, 64.25000000001142553, -36.02310748452440237 ) ) ;
#216218=CARTESIAN_POINT ( 'NONE',  ( -18.43459694179561836, 85.49421012500940265, -29.40610228186318409 ) ) ;
#216228=EDGE_CURVE ( 'NONE', #17643, #12394, #1237, .T. ) ;
#216257=DIRECTION ( 'NONE',  ( 0.7070776581708965169, 4.937903618720407826E-15, -0.7071359030027827286 ) ) ;
#216294=EDGE_LOOP ( 'NONE', ( #141024, #193528, #117069, #237063 ) ) ;
#216339=CARTESIAN_POINT ( 'NONE',  ( -20.00857864376270001, 66.75000000001151079, -48.27310748452438816 ) ) ;
#216370=CARTESIAN_POINT ( 'NONE',  ( -21.05000000000000071, 69.52192177891662084, -69.42310754921729199 ) ) ;
#216391=CARTESIAN_POINT ( 'NONE',  ( 21.05000000000000071, 65.57661458509869590, -62.03105556065429482 ) ) ;
#216410=CONICAL_SURFACE ( 'NONE', #158201, 7.750000000000020428, 0.7853981633974531640 ) ;
#216420=CARTESIAN_POINT ( 'NONE',  ( -23.15000000000000213, 74.00000000001151079, -48.64772940728643391 ) ) ;
#216541=EDGE_LOOP ( 'NONE', ( #169211, #166344, #204467 ) ) ;
#216564=ORIENTED_EDGE ( 'NONE', *, *, #54153, .F. ) ;
#216574=AXIS2_PLACEMENT_3D ( 'NONE', #227566, #8529, #143215 ) ;
#216598=DIRECTION ( 'NONE',  ( 1.000000000000000000, -3.265361837132813093E-16, -2.280189983783949500E-30 ) ) ;
#216608=ORIENTED_EDGE ( 'NONE', *, *, #146273, .T. ) ;
#216619=ORIENTED_EDGE ( 'NONE', *, *, #150069, .T. ) ;
#216628=CARTESIAN_POINT ( 'NONE',  ( 22.39999999999999503, 76.00000000001170974, -77.31388708289769340 ) ) ;
#216650=DIRECTION ( 'NONE',  ( 0.000000000000000000, 0.000000000000000000, -1.000000000000000000 ) ) ;
#216661=ORIENTED_EDGE ( 'NONE', *, *, #171045, .F. ) ;
#216676=CARTESIAN_POINT ( 'NONE',  ( -20.85000000000000142, 76.00000000001142553, -36.02310748452432421 ) ) ;
#216707=ORIENTED_EDGE ( 'NONE', *, *, #165402, .T. ) ;
#216712=AXIS2_PLACEMENT_3D ( 'NONE', #12052, #107266, #249369 ) ;
#216731=ORIENTED_EDGE ( 'NONE', *, *, #123019, .F. ) ;
#216748=CIRCLE ( 'NONE', #104308, 7.791421356237317575 ) ;
#216753=CARTESIAN_POINT ( 'NONE',  ( 18.59999999999999076, 65.79142135624880439, -48.27310748452439526 ) ) ;
#216811=DIRECTION ( 'NONE',  ( -0.7071067811865127117, -0.7071067811865821007, 2.081668171172114492E-13 ) ) ;
#216822=DIRECTION ( 'NONE',  ( 0.000000000000000000, 0.1298341882519953583, 0.9915357197604862671 ) ) ;
#216858=EDGE_CURVE ( 'NONE', #228818, #84841, #114031, .T. ) ;
#216869=EDGE_CURVE ( 'NONE', #41808, #198388, #193181, .T. ) ;
#216871=CIRCLE ( 'NONE', #125321, 0.09999999999999939493 ) ;
#216915=DIRECTION ( 'NONE',  ( 0.000000000000000000, 0.000000000000000000, 1.000000000000000000 ) ) ;
#216919=DIRECTION ( 'NONE',  ( 1.000000000000000000, 0.000000000000000000, 0.000000000000000000 ) ) ;
#216920=VERTEX_POINT ( 'NONE', #149925 ) ;
#216938=LINE ( 'NONE', #157004, #32728 ) ;
#216947=EDGE_LOOP ( 'NONE', ( #232665, #114383, #98325, #210166 ) ) ;
#216976=CARTESIAN_POINT ( 'NONE',  ( -20.64999999999999858, 71.65000000001151648, -48.37310748452434694 ) ) ;
#216978=CYLINDRICAL_SURFACE ( 'NONE', #111035, 0.1000000000000028644 ) ;
#216987=LINE ( 'NONE', #157050, #105932 ) ;
#217004=VECTOR ( 'NONE', #210657, 1000.000000000000000 ) ;
#217026=DIRECTION ( 'NONE',  ( -1.000000000000000000, -0.000000000000000000, -0.000000000000000000 ) ) ;
#217027=DIRECTION ( 'NONE',  ( 0.000000000000000000, 0.000000000000000000, 1.000000000000000000 ) ) ;
#217053=ORIENTED_EDGE ( 'NONE', *, *, #198015, .T. ) ;
#217064=DIRECTION ( 'NONE',  ( 0.000000000000000000, 0.000000000000000000, -1.000000000000000000 ) ) ;
#217090=FACE_OUTER_BOUND ( 'NONE', #237186, .T. ) ;
#217091=ORIENTED_EDGE ( 'NONE', *, *, #136570, .T. ) ;
#217105=EDGE_LOOP ( 'NONE', ( #35174, #2927, #96202, #203155 ) ) ;
#217182=ORIENTED_EDGE ( 'NONE', *, *, #24531, .F. ) ;
#217216=CIRCLE ( 'NONE', #133847, 0.1000000000000014488 ) ;
#217287=CARTESIAN_POINT ( 'NONE',  ( 21.14999999999999858, 69.74218538953552127, -69.62089777583315708 ) ) ;
#217304=VECTOR ( 'NONE', #106419, 1000.000000000000000 ) ;
#217305=ORIENTED_EDGE ( 'NONE', *, *, #144412, .T. ) ;
#217309=ORIENTED_EDGE ( 'NONE', *, *, #127464, .F. ) ;
#217327=ORIENTED_EDGE ( 'NONE', *, *, #244213, .F. ) ;
#217354=EDGE_CURVE ( 'NONE', #40138, #148964, #92590, .T. ) ;
#217358=ORIENTED_EDGE ( 'NONE', *, *, #177621, .F. ) ;
#217359=ORIENTED_EDGE ( 'NONE', *, *, #203986, .F. ) ;
#217399=ORIENTED_EDGE ( 'NONE', *, *, #245089, .F. ) ;
#217424=FACE_OUTER_BOUND ( 'NONE', #225228, .T. ) ;
#217433=EDGE_CURVE ( 'NONE', #11272, #152525, #189263, .T. ) ;
#217435=CYLINDRICAL_SURFACE ( 'NONE', #145685, 0.1000000000000028644 ) ;
#217451=DIRECTION ( 'NONE',  ( 0.000000000000000000, -0.1298341882519953860, -0.9915357197604862671 ) ) ;
#217465=AXIS2_PLACEMENT_3D ( 'NONE', #6454, #242501, #181273 ) ;
#217486=AXIS2_PLACEMENT_3D ( 'NONE', #7038, #65733, #246925 ) ;
#217494=CARTESIAN_POINT ( 'NONE',  ( -18.47130263965443220, 85.47115558597528207, -29.33970271904725280 ) ) ;
#217501=FACE_OUTER_BOUND ( 'NONE', #150610, .T. ) ;
#217544=ORIENTED_EDGE ( 'NONE', *, *, #129500, .F. ) ;
#217547=CARTESIAN_POINT ( 'NONE',  ( -20.94788355080264353, 65.69792220476271893, -30.53355541284615526 ) ) ;
#217567=B_SPLINE_CURVE_WITH_KNOTS ( 'NONE', 3,
 ( #233667, #156722, #154164, #36782, #155445, #212819, #35492, #175018, #194560, #215367 ),
 .UNSPECIFIED., .F., .F.,
 ( 4, 3, 3, 4 ),
 ( 0.000000000000000000, 0.0002000000000008537104, 0.001000000000082977483, 0.001967863649483329782 ),
 .UNSPECIFIED. ) ;
#217580=ORIENTED_EDGE ( 'NONE', *, *, #48199, .F. ) ;
#217643=LINE ( 'NONE', #117293, #173972 ) ;
#217646=DIRECTION ( 'NONE',  ( -4.239556034732056743E-17, -0.1298341882519953583, -0.9915357197604862671 ) ) ;
#217647=DIRECTION ( 'NONE',  ( 1.000000000000000000, -0.000000000000000000, -0.000000000000000000 ) ) ;
#217670=DIRECTION ( 'NONE',  ( 0.000000000000000000, 0.9915357197604804940, -0.1298341882520397950 ) ) ;
#217695=VERTEX_POINT ( 'NONE', #30648 ) ;
#217718=CARTESIAN_POINT ( 'NONE',  ( 20.93302460841142931, 65.68434038414308418, -30.48668807260656521 ) ) ;
#217726=CARTESIAN_POINT ( 'NONE',  ( 21.10320863425824811, 69.59972261355248691, -69.54812973575150181 ) ) ;
#217729=( BOUNDED_CURVE ( )  B_SPLINE_CURVE ( 3, ( #73884, #52990, #112981, #30906 ),
 .UNSPECIFIED., .F., .F. ) 
 B_SPLINE_CURVE_WITH_KNOTS ( ( 4, 4 ),
 ( 1.570796326794901665, 3.141592653589768247 ),
 .UNSPECIFIED. ) 
 CURVE ( )  GEOMETRIC_REPRESENTATION_ITEM ( )  RATIONAL_B_SPLINE_CURVE ( ( 1.000000000000000000, 0.8047378541243720429, 0.8047378541243720429, 1.000000000000000000 ) ) 
 REPRESENTATION_ITEM ( '' )  );
#217739=DIRECTION ( 'NONE',  ( 0.000000000000000000, 0.000000000000000000, 1.000000000000000000 ) ) ;
#217753=DIRECTION ( 'NONE',  ( 0.000000000000000000, 0.000000000000000000, -1.000000000000000000 ) ) ;
#217758=CARTESIAN_POINT ( 'NONE',  ( 21.30000000000002558, 76.00000000001162448, -65.47310748452431994 ) ) ;
#217761=CARTESIAN_POINT ( 'NONE',  ( 22.39999999999999503, 68.20922040163827660, -69.52310748452437394 ) ) ;
#217773=CARTESIAN_POINT ( 'NONE',  ( -18.59999999999999787, 85.48068669529035901, -29.08199231576641353 ) ) ;
#217858=DIRECTION ( 'NONE',  ( 0.000000000000000000, 0.3738317757009942399, -0.9274965247785252886 ) ) ;
#217862=CIRCLE ( 'NONE', #238555, 3.999999999999996447 ) ;
#217873=AXIS2_PLACEMENT_3D ( 'NONE', #109825, #5574, #188097 ) ;
#217890=DIRECTION ( 'NONE',  ( 1.000000000000000000, 0.000000000000000000, 0.000000000000000000 ) ) ;
#217891=CARTESIAN_POINT ( 'NONE',  ( -1.820710678118657944, 85.92928932189282420, -44.77310748452425315 ) ) ;
#217906=ORIENTED_EDGE ( 'NONE', *, *, #22545, .F. ) ;
#217923=VECTOR ( 'NONE', #138865, 1000.000000000000000 ) ;
#217925=AXIS2_PLACEMENT_3D ( 'NONE', #183530, #238356, #119714 ) ;
#217926=VECTOR ( 'NONE', #76451, 1000.000000000000000 ) ;
#217946=AXIS2_PLACEMENT_3D ( 'NONE', #14801, #173892, #245382 ) ;
#217952=CARTESIAN_POINT ( 'NONE',  ( 21.14999999999999858, 69.35000000001156195, -57.37310748452436826 ) ) ;
#217968=CIRCLE ( 'NONE', #38936, 0.1000000000000052097 ) ;
#217976=CARTESIAN_POINT ( 'NONE',  ( 23.14999999999999503, 64.35000000001150511, -48.17310748452440095 ) ) ;
#217983=VECTOR ( 'NONE', #212434, 1000.000000000000000 ) ;
#218001=ORIENTED_EDGE ( 'NONE', *, *, #250348, .T. ) ;
#218009=VERTEX_POINT ( 'NONE', #47288 ) ;
#218051=( BOUNDED_SURFACE ( )  B_SPLINE_SURFACE ( 3, 2, ( 
 ( #252474, #73891, #153444 ),
 ( #98500, #254988, #116834 ),
 ( #155985, #192525, #174294 ),
 ( #157270, #154707, #76403 ),
 ( #236765, #235482, #214636 ),
 ( #55533, #58114, #56821 ) ),
 .UNSPECIFIED., .F., .F., .T. ) 
 B_SPLINE_SURFACE_WITH_KNOTS ( ( 4, 2, 4 ),
 ( 3, 3 ),
 ( 0.0001792624049599534481, 0.0003686986002124667365, 0.0005581347954649799707 ),
 ( 0.000000000000000000, 1.000000000000000000 ),
 .UNSPECIFIED. ) 
 GEOMETRIC_REPRESENTATION_ITEM ( )  RATIONAL_B_SPLINE_SURFACE ( (
 ( 1.000000000000000000, 0.9238795325112859613, 1.000000000000000000),
 ( 1.000000000000000000, 0.9229318695239708825, 1.000000000000000000),
 ( 1.000000000000000000, 0.8926288119229073281, 1.000000000000000000),
 ( 1.000000000000000000, 0.8123777807272978269, 1.000000000000000000),
 ( 1.000000000000000000, 0.7629087100930436183, 1.000000000000000000),
 ( 1.000000000000000000, 0.7071067811865475727, 1.000000000000000000) ) ) 
 REPRESENTATION_ITEM ( '' )  SURFACE ( )  );
#218069=B_SPLINE_CURVE_WITH_KNOTS ( 'NONE', 3,
 ( #216391, #113448, #198118, #235952, #35232, #173483 ),
 .UNSPECIFIED., .F., .F.,
 ( 4, 2, 4 ),
 ( 0.000000000000000000, 0.0002113392456165983529, 0.0004226784912331967058 ),
 .UNSPECIFIED. ) ;
#218089=AXIS2_PLACEMENT_3D ( 'NONE', #91218, #93767, #213718 ) ;
#218137=DIRECTION ( 'NONE',  ( 0.000000000000000000, 0.000000000000000000, 1.000000000000000000 ) ) ;
#218147=VERTEX_POINT ( 'NONE', #36785 ) ;
#218149=ADVANCED_FACE ( 'NONE', ( #54993 ), #51453, .T. ) ;
#218159=ORIENTED_EDGE ( 'NONE', *, *, #27309, .T. ) ;
#218187=DIRECTION ( 'NONE',  ( 0.000000000000000000, -0.3738317757008748909, -0.9274965247785733613 ) ) ;
#218189=EDGE_LOOP ( 'NONE', ( #233693, #217327, #182533, #70183 ) ) ;
#218195=DIRECTION ( 'NONE',  ( 0.000000000000000000, -6.982962677686266711E-15, 1.000000000000000000 ) ) ;
#218197=CIRCLE ( 'NONE', #168201, 12.87499999999999822 ) ;
#218206=LINE ( 'NONE', #117841, #155797 ) ;
#218230=VECTOR ( 'NONE', #55421, 1000.000000000000000 ) ;
#218248=DIRECTION ( 'NONE',  ( 0.000000000000000000, -0.8660254037844377084, -0.5000000000000016653 ) ) ;
#218290=CARTESIAN_POINT ( 'NONE',  ( -22.32929514600008503, 75.90092432189779004, -77.10175504990083084 ) ) ;
#218297=EDGE_LOOP ( 'NONE', ( #187544, #196583, #35430, #31910 ) ) ;
#218334=ADVANCED_FACE ( 'NONE', ( #83537 ), #61443, .F. ) ;
#218353=CIRCLE ( 'NONE', #10086, 0.1000000000000028644 ) ;
#218355=CIRCLE ( 'NONE', #168360, 0.09999999999999939493 ) ;
#218362=AXIS2_PLACEMENT_3D ( 'NONE', #47466, #124473, #125733 ) ;
#218431=DIRECTION ( 'NONE',  ( 0.000000000000000000, 6.982962677686266711E-15, -1.000000000000000000 ) ) ;
#218439=EDGE_CURVE ( 'NONE', #252677, #42291, #76613, .T. ) ;
#218466=ORIENTED_EDGE ( 'NONE', *, *, #52238, .F. ) ;
#218484=VERTEX_POINT ( 'NONE', #247449 ) ;
#218521=CARTESIAN_POINT ( 'NONE',  ( 18.49505816908824229, 85.43787255322250473, -29.24545028285334780 ) ) ;
#218524=AXIS2_PLACEMENT_3D ( 'NONE', #65190, #6497, #92449 ) ;
#218532=ADVANCED_FACE ( 'NONE', ( #192622 ), #13989, .F. ) ;
#218543=VERTEX_POINT ( 'NONE', #255098 ) ;
#218586=AXIS2_PLACEMENT_3D ( 'NONE', #226431, #106479, #210747 ) ;
#218593=ORIENTED_EDGE ( 'NONE', *, *, #212096, .T. ) ;
#218606=ORIENTED_EDGE ( 'NONE', *, *, #94963, .T. ) ;
#218645=CIRCLE ( 'NONE', #160247, 0.1999999999999987899 ) ;
#218663=CARTESIAN_POINT ( 'NONE',  ( 20.51284917709620359, 65.68911337716694732, -61.85063429893225617 ) ) ;
#218666=DIRECTION ( 'NONE',  ( 0.000000000000000000, -7.172728831056617961E-15, 1.000000000000000000 ) ) ;
#218735=CARTESIAN_POINT ( 'NONE',  ( -20.94999999999999929, 64.25000000001161027, -62.50830171387039513 ) ) ;
#218748=TOROIDAL_SURFACE ( 'NONE', #193834, 0.2000000000000000111, 0.1000000000000000056 ) ;
#218797=DIRECTION ( 'NONE',  ( 0.000000000000000000, 0.000000000000000000, 1.000000000000000000 ) ) ;
#218807=DIRECTION ( 'NONE',  ( 0.000000000000000000, -2.775557561562888827E-14, 1.000000000000000000 ) ) ;
#218817=ORIENTED_EDGE ( 'NONE', *, *, #57285, .T. ) ;
#218821=DIRECTION ( 'NONE',  ( 0.7071359030027593029, 0.000000000000000000, 0.7070776581709197206 ) ) ;
#218836=CARTESIAN_POINT ( 'NONE',  ( -20.88420186297724257, 65.66974365629616273, -30.43601455626050978 ) ) ;
#218838=CARTESIAN_POINT ( 'NONE',  ( -23.15000000000000213, 76.00000000001165290, -69.52310748452431710 ) ) ;
#218846=ORIENTED_EDGE ( 'NONE', *, *, #104620, .F. ) ;
#218866=VERTEX_POINT ( 'NONE', #38374 ) ;
#218877=VERTEX_POINT ( 'NONE', #237851 ) ;
#218910=ORIENTED_EDGE ( 'NONE', *, *, #21103, .T. ) ;
#218922=ORIENTED_EDGE ( 'NONE', *, *, #108468, .F. ) ;
#218939=FACE_OUTER_BOUND ( 'NONE', #16069, .T. ) ;
#218956=DIRECTION ( 'NONE',  ( 0.000000000000000000, 0.000000000000000000, -1.000000000000000000 ) ) ;
#218981=VECTOR ( 'NONE', #27089, 1000.000000000000000 ) ;
#219002=CIRCLE ( 'NONE', #23413, 0.1000000000000028644 ) ;
#219003=ORIENTED_EDGE ( 'NONE', *, *, #14309, .T. ) ;
#219033=EDGE_CURVE ( 'NONE', #162036, #6351, #220849, .T. ) ;
#219053=ORIENTED_EDGE ( 'NONE', *, *, #7372, .T. ) ;
#219091=AXIS2_PLACEMENT_3D ( 'NONE', #10592, #215199, #131808 ) ;
#219102=EDGE_LOOP ( 'NONE', ( #236309, #49945, #153410, #136490 ) ) ;
#219107=AXIS2_PLACEMENT_3D ( 'NONE', #8708, #69987, #128665 ) ;
#219138=ORIENTED_EDGE ( 'NONE', *, *, #137384, .T. ) ;
#219142=DIRECTION ( 'NONE',  ( 1.000000000000000000, 0.000000000000000000, 0.000000000000000000 ) ) ;
#219162=EDGE_LOOP ( 'NONE', ( #100987, #233570, #220482, #141233 ) ) ;
#219186=EDGE_CURVE ( 'NONE', #183814, #149811, #247861, .T. ) ;
#219187=SPHERICAL_SURFACE ( 'NONE', #177983, 0.1000000000000000056 ) ;
#219224=ORIENTED_EDGE ( 'NONE', *, *, #44938, .F. ) ;
#219253=DIRECTION ( 'NONE',  ( 0.000000000000000000, -7.056502275159890043E-15, 1.000000000000000000 ) ) ;
#219264=CARTESIAN_POINT ( 'NONE',  ( -20.94999999999999929, 76.00000000001149658, -47.72310748452432705 ) ) ;
#219287=AXIS2_PLACEMENT_3D ( 'NONE', #216976, #119190, #157040 ) ;
#219300=CARTESIAN_POINT ( 'NONE',  ( -20.85000000000000142, 76.32388570108174974, -36.06551789521033413 ) ) ;
#219359=AXIS2_PLACEMENT_3D ( 'NONE', #41683, #79489, #181198 ) ;
#219373=CARTESIAN_POINT ( 'NONE',  ( 21.05000000000000071, 87.65000000001144542, -38.92310748452424463 ) ) ;
#219384=VECTOR ( 'NONE', #215718, 1000.000000000000000 ) ;
#219387=LINE ( 'NONE', #117735, #8723 ) ;
#219414=AXIS2_PLACEMENT_3D ( 'NONE', #213120, #151893, #37086 ) ;
#219443=FACE_OUTER_BOUND ( 'NONE', #92238, .T. ) ;
#219490=ORIENTED_EDGE ( 'NONE', *, *, #172077, .T. ) ;
#219511=CARTESIAN_POINT ( 'NONE',  ( -20.94999999999999929, 77.16412189325258453, -28.30825939895270693 ) ) ;
#219517=ADVANCED_FACE ( 'NONE', ( #162885 ), #143288, .F. ) ;
#219530=EDGE_CURVE ( 'NONE', #238989, #193535, #106712, .T. ) ;
#219534=ORIENTED_EDGE ( 'NONE', *, *, #22545, .T. ) ;
#219547=CARTESIAN_POINT ( 'NONE',  ( -18.50000000000000000, 77.73625713160897988, -57.95445515550681392 ) ) ;
#219559=CIRCLE ( 'NONE', #52967, 11.65000000000000036 ) ;
#219711=CARTESIAN_POINT ( 'NONE',  ( 21.05000000000000071, 87.48912529308769592, -66.42310748452423752 ) ) ;
#219726=CYLINDRICAL_SURFACE ( 'NONE', #30829, 0.8750000000000007772 ) ;
#219762=EDGE_CURVE ( 'NONE', #188219, #44233, #72780, .T. ) ;
#219770=DIRECTION ( 'NONE',  ( 0.000000000000000000, 0.9893560106964510714, -0.1455152366551481502 ) ) ;
#219786=ORIENTED_EDGE ( 'NONE', *, *, #112350, .T. ) ;
#219791=CARTESIAN_POINT ( 'NONE',  ( -18.59999999999999787, 66.65000000001157332, -57.17310748452438673 ) ) ;
#219812=CARTESIAN_POINT ( 'NONE',  ( 20.94999999999999574, 69.60000000001157616, -59.59268285446279378 ) ) ;
#219815=EDGE_CURVE ( 'NONE', #149532, #38617, #37482, .T. ) ;
#219891=ORIENTED_EDGE ( 'NONE', *, *, #92262, .T. ) ;
#219901=DIRECTION ( 'NONE',  ( 0.000000000000000000, 0.000000000000000000, -1.000000000000000000 ) ) ;
#219919=CARTESIAN_POINT ( 'NONE',  ( 19.97071067811865674, 64.27928932189281852, -44.87310748452440379 ) ) ;
#219966=CARTESIAN_POINT ( 'NONE',  ( -18.59999999999999787, 64.35000000001161879, -62.50830171387039513 ) ) ;
#219981=CARTESIAN_POINT ( 'NONE',  ( -21.05000000000000071, 75.96824164695655668, -75.78195460760348112 ) ) ;
#220020=AXIS2_PLACEMENT_3D ( 'NONE', #114948, #10720, #131941 ) ;
#220036=FACE_OUTER_BOUND ( 'NONE', #144961, .T. ) ;
#220073=ORIENTED_EDGE ( 'NONE', *, *, #84324, .F. ) ;
#220074=AXIS2_PLACEMENT_3D ( 'NONE', #139974, #5599, #120476 ) ;
#220084=SPHERICAL_SURFACE ( 'NONE', #132281, 0.1000000000000000056 ) ;
#220101=CARTESIAN_POINT ( 'NONE',  ( -18.59999999999999787, 64.35000000001161879, -62.60830171387041077 ) ) ;
#220137=CIRCLE ( 'NONE', #199291, 0.1000000000000026007 ) ;
#220152=DIRECTION ( 'NONE',  ( 0.000000000000000000, 0.8660254037844420383, -0.4999999999999941713 ) ) ;
#220155=AXIS2_PLACEMENT_3D ( 'NONE', #60465, #1775, #81293 ) ;
#220163=CARTESIAN_POINT ( 'NONE',  ( -18.59999999999999787, 64.25000000001173817, -81.27310748452440237 ) ) ;
#220202=ORIENTED_EDGE ( 'NONE', *, *, #210895, .T. ) ;
#220208=DIRECTION ( 'NONE',  ( 0.000000000000000000, 0.000000000000000000, 1.000000000000000000 ) ) ;
#220218=ORIENTED_EDGE ( 'NONE', *, *, #228911, .T. ) ;
#220232=CARTESIAN_POINT ( 'NONE',  ( -22.39999999999999858, 76.10085836911045476, -81.27267460801371612 ) ) ;
#220238=LINE ( 'NONE', #101517, #235369 ) ;
#220240=DIRECTION ( 'NONE',  ( -3.265361837132813093E-16, -1.000000000000000000, -6.938893903907229955E-15 ) ) ;
#220248=EDGE_CURVE ( 'NONE', #253340, #216920, #215093, .T. ) ;
#220258=LINE ( 'NONE', #200687, #193691 ) ;
#220321=CARTESIAN_POINT ( 'NONE',  ( 20.85882249326303040, 65.66751761918619934, -30.42826094061123854 ) ) ;
#220322=FACE_OUTER_BOUND ( 'NONE', #69410, .T. ) ;
#220324=AXIS2_PLACEMENT_3D ( 'NONE', #135291, #113181, #227020 ) ;
#220355=CARTESIAN_POINT ( 'NONE',  ( -22.39999999999999503, 68.20922040163824818, -69.52310748452435973 ) ) ;
#220380=CARTESIAN_POINT ( 'NONE',  ( -21.05000000000000071, 76.00000000001145395, -40.12310748452431852 ) ) ;
#220391=VERTEX_POINT ( 'NONE', #127934 ) ;
#220452=EDGE_CURVE ( 'NONE', #59275, #43988, #169669, .T. ) ;
#220482=ORIENTED_EDGE ( 'NONE', *, *, #252656, .T. ) ;
#220501=AXIS2_PLACEMENT_3D ( 'NONE', #7355, #106429, #185997 ) ;
#220504=VECTOR ( 'NONE', #1125, 1000.000000000000000 ) ;
#220508=EDGE_CURVE ( 'NONE', #182741, #58501, #98334, .T. ) ;
#220556=DIRECTION ( 'NONE',  ( -0.000000000000000000, 6.982962677686266711E-15, -1.000000000000000000 ) ) ;
#220569=EDGE_CURVE ( 'NONE', #102057, #88538, #135615, .T. ) ;
#220576=CARTESIAN_POINT ( 'NONE',  ( -18.57399277249657032, 65.66887361445283489, -30.43298459182691929 ) ) ;
#220609=VERTEX_POINT ( 'NONE', #100326 ) ;
#220610=ORIENTED_EDGE ( 'NONE', *, *, #113454, .T. ) ;
#220652=DIRECTION ( 'NONE',  ( 1.000000000000000000, 7.304098846218163263E-16, -4.217023435051627211E-16 ) ) ;
#220678=EDGE_CURVE ( 'NONE', #243492, #15384, #6980, .T. ) ;
#220706=DIRECTION ( 'NONE',  ( 1.000000000000000000, -1.836970198721029934E-16, -1.282749433769087582E-30 ) ) ;
#220730=CARTESIAN_POINT ( 'NONE',  ( -18.51991288638499356, 85.39243678968496454, -62.37984108056530630 ) ) ;
#220731=ORIENTED_EDGE ( 'NONE', *, *, #133598, .F. ) ;
#220737=CARTESIAN_POINT ( 'NONE',  ( -20.54999999999999716, 85.00000000001159606, -60.12913836187181715 ) ) ;
#220758=VECTOR ( 'NONE', #225982, 1000.000000000000000 ) ;
#220761=AXIS2_PLACEMENT_3D ( 'NONE', #61771, #25233, #123039 ) ;
#220823=DIRECTION ( 'NONE',  ( -1.000000000000000000, -0.000000000000000000, -0.000000000000000000 ) ) ;
#220831=FACE_OUTER_BOUND ( 'NONE', #161736, .T. ) ;
#220837=CARTESIAN_POINT ( 'NONE',  ( 18.59999999999999076, 64.35000000001147669, -44.67310748452440095 ) ) ;
#220849=LINE ( 'NONE', #142583, #243573 ) ;
#220853=AXIS2_PLACEMENT_3D ( 'NONE', #141705, #221231, #218666 ) ;
#220870=CARTESIAN_POINT ( 'NONE',  ( 22.60000000000000142, 76.00000000001165290, -69.52310748452431710 ) ) ;
#220876=CARTESIAN_POINT ( 'NONE',  ( 18.58719872626880232, 85.56664439761000551, -29.20062928812724223 ) ) ;
#220893=ADVANCED_FACE ( 'NONE', ( #144596 ), #7686, .F. ) ;
#220896=DIRECTION ( 'NONE',  ( 0.000000000000000000, 0.000000000000000000, -1.000000000000000000 ) ) ;
#220905=CARTESIAN_POINT ( 'NONE',  ( -18.59999999999999787, 64.35000000001161879, -62.50830171387039513 ) ) ;
#220910=FACE_OUTER_BOUND ( 'NONE', #28709, .T. ) ;
#220946=EDGE_LOOP ( 'NONE', ( #178108, #115444, #49112, #50620 ) ) ;
#220998=DIRECTION ( 'NONE',  ( 0.000000000000000000, 6.982962677686266711E-15, -1.000000000000000000 ) ) ;
#221002=VERTEX_POINT ( 'NONE', #248857 ) ;
#221016=AXIS2_PLACEMENT_3D ( 'NONE', #47484, #226111, #43658 ) ;
#221049=ORIENTED_EDGE ( 'NONE', *, *, #193202, .F. ) ;
#221068=DIRECTION ( 'NONE',  ( -2.602085213965226419E-14, -6.982962677686266711E-15, 1.000000000000000000 ) ) ;
#221071=AXIS2_PLACEMENT_3D ( 'NONE', #217976, #36837, #117620 ) ;
#221079=EDGE_LOOP ( 'NONE', ( #253897, #49338 ) ) ;
#221084=CARTESIAN_POINT ( 'NONE',  ( 20.04142135623730070, 64.25000000001148237, -44.87310748452440379 ) ) ;
#221098=CARTESIAN_POINT ( 'NONE',  ( -22.50000000000000000, 75.90000000001172964, -81.17267829206912211 ) ) ;
#221109=AXIS2_PLACEMENT_3D ( 'NONE', #148108, #106384, #68574 ) ;
#221112=ORIENTED_EDGE ( 'NONE', *, *, #95384, .T. ) ;
#221113=VERTEX_POINT ( 'NONE', #255209 ) ;
#221147=CARTESIAN_POINT ( 'NONE',  ( 20.85000000000000142, 68.97833521811131163, -32.18954208262707795 ) ) ;
#221158=CARTESIAN_POINT ( 'NONE',  ( -20.64999999999999858, 68.75000000001158185, -57.17310748452437252 ) ) ;
#221172=DIRECTION ( 'NONE',  ( 0.000000000000000000, -6.982962677686266711E-15, 1.000000000000000000 ) ) ;
#221177=CARTESIAN_POINT ( 'NONE',  ( -23.15000000000000213, 85.50000000001159606, -59.62913836187181005 ) ) ;
#221210=FACE_OUTER_BOUND ( 'NONE', #157719, .T. ) ;
#221213=DIRECTION ( 'NONE',  ( 3.265361837132813093E-16, 1.000000000000000000, 6.982962677686266711E-15 ) ) ;
#221221=ORIENTED_EDGE ( 'NONE', *, *, #16495, .T. ) ;
#221231=DIRECTION ( 'NONE',  ( -0.000000000000000000, 1.000000000000000000, 7.172728831056617961E-15 ) ) ;
#221239=CARTESIAN_POINT ( 'NONE',  ( 21.14999999999999858, 69.35000000001156195, -57.17310748452436542 ) ) ;
#221282=ORIENTED_EDGE ( 'NONE', *, *, #188386, .F. ) ;
#221283=MECHANICAL_DESIGN_GEOMETRIC_PRESENTATION_REPRESENTATION('',(#33926),#171300);
#221285=VERTEX_POINT ( 'NONE', #150727 ) ;
#221294=DIRECTION ( 'NONE',  ( 0.000000000000000000, 0.000000000000000000, 1.000000000000000000 ) ) ;
#221296=DIRECTION ( 'NONE',  ( 1.000000000000000000, 0.000000000000000000, 0.000000000000000000 ) ) ;
#221303=ORIENTED_EDGE ( 'NONE', *, *, #257436, .T. ) ;
#221319=DIRECTION ( 'NONE',  ( 0.000000000000000000, 0.000000000000000000, 1.000000000000000000 ) ) ;
#221374=VECTOR ( 'NONE', #8069, 1000.000000000000000 ) ;
#221377=EDGE_LOOP ( 'NONE', ( #167883, #201821, #124680, #191645, #251904, #234758, #156370, #20702, #75609, #149402, #44704, #171216 ) ) ;
#221428=ORIENTED_EDGE ( 'NONE', *, *, #139690, .T. ) ;
#221443=DIRECTION ( 'NONE',  ( 1.000000000000000000, 0.000000000000000000, 0.000000000000000000 ) ) ;
#221497=EDGE_LOOP ( 'NONE', ( #240899, #66558, #235849, #182696 ) ) ;
#221503=DIRECTION ( 'NONE',  ( 0.000000000000000000, 1.000000000000000000, 6.352154140967427193E-15 ) ) ;
#221504=CARTESIAN_POINT ( 'NONE',  ( 21.05000000000000071, 67.22371710471909978, -57.37310748452438247 ) ) ;
#221519=DIRECTION ( 'NONE',  ( 0.000000000000000000, 0.9999176327611370985, -0.01283462868041286391 ) ) ;
#221520=CARTESIAN_POINT ( 'NONE',  ( -20.94999999999999929, 76.00000000001162448, -66.62310748452433984 ) ) ;
#221530=VERTEX_POINT ( 'NONE', #114159 ) ;
#221537=EDGE_CURVE ( 'NONE', #12734, #67154, #15759, .T. ) ;
#221553=FACE_OUTER_BOUND ( 'NONE', #98819, .T. ) ;
#221589=CARTESIAN_POINT ( 'NONE',  ( 18.58725287972292506, 85.56662691070296489, -29.20060267875857818 ) ) ;
#221596=DIRECTION ( 'NONE',  ( 1.000000000000000000, 0.000000000000000000, 0.000000000000000000 ) ) ;
#221598=DIRECTION ( 'NONE',  ( 0.000000000000000000, -0.9908441862701605762, -0.1350103645451835310 ) ) ;
#221605=AXIS2_PLACEMENT_3D ( 'NONE', #47260, #246755, #146362 ) ;
#221622=DIRECTION ( 'NONE',  ( 0.000000000000000000, 1.000000000000000000, 6.982962677686266711E-15 ) ) ;
#221628=TOROIDAL_SURFACE ( 'NONE', #17626, 4.099999999999999645, 0.1000000000000000056 ) ;
#221640=EDGE_CURVE ( 'NONE', #200, #66243, #57397, .T. ) ;
#221644=CIRCLE ( 'NONE', #109226, 0.1000000000000028644 ) ;
#221663=ADVANCED_FACE ( 'NONE', ( #107443 ), #248245, .F. ) ;
#221666=ORIENTED_EDGE ( 'NONE', *, *, #221763, .F. ) ;
#221670=DIRECTION ( 'NONE',  ( 1.000000000000000000, 0.000000000000000000, 0.000000000000000000 ) ) ;
#221672=ORIENTED_EDGE ( 'NONE', *, *, #231455, .F. ) ;
#221711=ORIENTED_EDGE ( 'NONE', *, *, #71037, .F. ) ;
#221727=EDGE_LOOP ( 'NONE', ( #30547, #162453, #222580, #3217 ) ) ;
#221763=EDGE_CURVE ( 'NONE', #134587, #47002, #40882, .T. ) ;
#221784=LINE ( 'NONE', #44479, #229392 ) ;
#221789=FACE_OUTER_BOUND ( 'NONE', #140806, .T. ) ;
#221808=CYLINDRICAL_SURFACE ( 'NONE', #99172, 0.1000000000000028644 ) ;
#221834=DIRECTION ( 'NONE',  ( -1.000000000000000000, 0.000000000000000000, -0.000000000000000000 ) ) ;
#221914=DIRECTION ( 'NONE',  ( 1.000000000000000000, -2.952720810173289112E-16, -2.061873921506763405E-30 ) ) ;
#221932=ADVANCED_FACE ( 'NONE', ( #8995 ), #207215, .T. ) ;
#221974=CARTESIAN_POINT ( 'NONE',  ( -18.41418431465368144, 85.50000000001161027, -29.42291809330281183 ) ) ;
#222077=EDGE_LOOP ( 'NONE', ( #250251, #45158, #78844, #27821 ) ) ;
#222089=AXIS2_PLACEMENT_3D ( 'NONE', #80027, #179199, #115336 ) ;
#222111=DIRECTION ( 'NONE',  ( 1.000000000000000000, 0.000000000000000000, 0.000000000000000000 ) ) ;
#222124=ORIENTED_EDGE ( 'NONE', *, *, #239772, .T. ) ;
#222133=CIRCLE ( 'NONE', #30472, 0.09999999999999489853 ) ;
#222183=CARTESIAN_POINT ( 'NONE',  ( 21.04999999999908411, 67.22371710472090456, -57.36519848187187876 ) ) ;
#222199=CIRCLE ( 'NONE', #143098, 0.1000000000000028644 ) ;
#222209=EDGE_CURVE ( 'NONE', #207654, #147896, #257623, .T. ) ;
#222219=ORIENTED_EDGE ( 'NONE', *, *, #147322, .F. ) ;
#222259=DIRECTION ( 'NONE',  ( 1.000000000000000000, 0.000000000000000000, 0.000000000000000000 ) ) ;
#222266=ORIENTED_EDGE ( 'NONE', *, *, #189520, .F. ) ;
#222279=ORIENTED_EDGE ( 'NONE', *, *, #133197, .T. ) ;
#222288=( BOUNDED_CURVE ( )  B_SPLINE_CURVE ( 3, ( #57769, #40822, #156917, #257216 ),
 .UNSPECIFIED., .F., .T. ) 
 B_SPLINE_CURVE_WITH_KNOTS ( ( 4, 4 ),
 ( 3.141592653589791784, 4.712388980384688786 ),
 .UNSPECIFIED. ) 
 CURVE ( )  GEOMETRIC_REPRESENTATION_ITEM ( )  RATIONAL_B_SPLINE_CURVE ( ( 1.000000000000000000, 0.8047378541243649375, 0.8047378541243649375, 1.000000000000000000 ) ) 
 REPRESENTATION_ITEM ( '' )  );
#222328=ORIENTED_EDGE ( 'NONE', *, *, #13192, .T. ) ;
#222335=DIRECTION ( 'NONE',  ( 0.000000000000000000, -4.562560375171877784E-14, 1.000000000000000000 ) ) ;
#222339=DIRECTION ( 'NONE',  ( 1.000000000000000000, -7.304098846218134667E-16, -5.100424963727256530E-30 ) ) ;
#222347=CARTESIAN_POINT ( 'NONE',  ( -20.54999999999999716, 73.60000000001157616, -56.29848556176223440 ) ) ;
#222349=AXIS2_PLACEMENT_3D ( 'NONE', #2701, #101778, #144770 ) ;
#222357=ORIENTED_EDGE ( 'NONE', *, *, #37735, .T. ) ;
#222385=ADVANCED_FACE ( 'NONE', ( #165192 ), #88187, .T. ) ;
#222403=DIRECTION ( 'NONE',  ( -0.000000000000000000, 0.1350103645451974088, -0.9908441862701587999 ) ) ;
#222425=ORIENTED_EDGE ( 'NONE', *, *, #22240, .F. ) ;
#222442=CARTESIAN_POINT ( 'NONE',  ( -23.15000000000000213, 64.25000000001156764, -57.37310748452440379 ) ) ;
#222455=FACE_OUTER_BOUND ( 'NONE', #52370, .T. ) ;
#222465=ORIENTED_EDGE ( 'NONE', *, *, #108987, .T. ) ;
#222467=AXIS2_PLACEMENT_3D ( 'NONE', #178436, #140548, #40209 ) ;
#222482=DIRECTION ( 'NONE',  ( 0.000000000000000000, -6.982962677686266711E-15, 1.000000000000000000 ) ) ;
#222540=DIRECTION ( 'NONE',  ( 0.000000000000000000, -6.982962677686266711E-15, 1.000000000000000000 ) ) ;
#222549=CIRCLE ( 'NONE', #226848, 6.258578643762696458 ) ;
#222560=CARTESIAN_POINT ( 'NONE',  ( -18.39999999999999858, 85.50000000001161027, -62.49103808782458458 ) ) ;
#222570=DIRECTION ( 'NONE',  ( 0.000000000000000000, 1.000000000000000000, 0.000000000000000000 ) ) ;
#222577=DIRECTION ( 'NONE',  ( -1.000000000000000000, -0.000000000000000000, -0.000000000000000000 ) ) ;
#222580=ORIENTED_EDGE ( 'NONE', *, *, #257539, .F. ) ;
#222596=CARTESIAN_POINT ( 'NONE',  ( 20.94999999999999929, 87.48912529308749697, -39.12310748452424747 ) ) ;
#222607=ADVANCED_FACE ( 'NONE', ( #111635 ), #12559, .T. ) ;
#222608=DIRECTION ( 'NONE',  ( 1.000000000000000000, 0.000000000000000000, 0.000000000000000000 ) ) ;
#222625=DIRECTION ( 'NONE',  ( -1.000000000000000000, 0.000000000000000000, -0.000000000000000000 ) ) ;
#222630=AXIS2_PLACEMENT_3D ( 'NONE', #167572, #227506, #11042 ) ;
#222642=DIRECTION ( 'NONE',  ( 1.000000000000000000, 0.000000000000000000, 0.000000000000000000 ) ) ;
#222654=CARTESIAN_POINT ( 'NONE',  ( -20.85000000000000142, 76.00000000001142553, -36.02310748452432421 ) ) ;
#222668=LINE ( 'NONE', #86997, #218981 ) ;
#222687=ADVANCED_FACE ( 'NONE', ( #56758, #140164, #136301 ), #116766, .F. ) ;
#222690=EDGE_CURVE ( 'NONE', #178423, #186245, #32306, .T. ) ;
#222694=AXIS2_PLACEMENT_3D ( 'NONE', #128369, #168818, #64529 ) ;
#222698=ORIENTED_EDGE ( 'NONE', *, *, #131227, .F. ) ;
#222710=DIRECTION ( 'NONE',  ( 2.710505431213777355E-16, 1.000000000000000000, 6.982962677686266711E-15 ) ) ;
#222723=AXIS2_PLACEMENT_3D ( 'NONE', #161954, #185348, #100636 ) ;
#222724=DIRECTION ( 'NONE',  ( -0.000000000000000000, -6.982962677686266711E-15, 1.000000000000000000 ) ) ;
#222726=CARTESIAN_POINT ( 'NONE',  ( 20.94999999999999574, 87.41227409416133298, -66.52310748452423184 ) ) ;
#222764=DIRECTION ( 'NONE',  ( -1.000000000000000000, 0.000000000000000000, 0.000000000000000000 ) ) ;
#222774=ORIENTED_EDGE ( 'NONE', *, *, #206244, .T. ) ;
#222815=CARTESIAN_POINT ( 'NONE',  ( -20.54999999999999716, 71.75000000001156764, -57.17310748452435121 ) ) ;
#222819=CARTESIAN_POINT ( 'NONE',  ( 21.05000000000000071, 87.65000000001164437, -69.52310748452424605 ) ) ;
#222822=EDGE_CURVE ( 'NONE', #247693, #92943, #3213, .T. ) ;
#222831=DIRECTION ( 'NONE',  ( 0.000000000000000000, -0.4999999999999689138, -0.8660254037844565822 ) ) ;
#222905=ORIENTED_EDGE ( 'NONE', *, *, #192687, .F. ) ;
#222912=CARTESIAN_POINT ( 'NONE',  ( 18.58685178364169488, 85.40673308381587958, -62.39868701543652918 ) ) ;
#222916=DIRECTION ( 'NONE',  ( -0.000000000000000000, 0.4791956752371485107, 0.8777080977375185666 ) ) ;
#222920=CARTESIAN_POINT ( 'NONE',  ( 21.14999999999999858, 64.35000000001156195, -57.37310748452439668 ) ) ;
#222934=DIRECTION ( 'NONE',  ( 1.000000000000000000, -7.304098846218134667E-16, -5.100424963727255829E-30 ) ) ;
#222949=DIRECTION ( 'NONE',  ( 0.000000000000000000, 0.000000000000000000, 1.000000000000000000 ) ) ;
#222950=( NAMED_UNIT ( * ) PLANE_ANGLE_UNIT ( ) SI_UNIT ( $, .RADIAN. ) );
#222957=VECTOR ( 'NONE', #99050, 1000.000000000000000 ) ;
#222975=DIRECTION ( 'NONE',  ( 0.000000000000000000, 7.056502275159890832E-15, -1.000000000000000000 ) ) ;
#222976=EDGE_CURVE ( 'NONE', #180734, #120848, #227125, .T. ) ;
#223017=EDGE_CURVE ( 'NONE', #121084, #206913, #207897, .T. ) ;
#223018=ORIENTED_EDGE ( 'NONE', *, *, #140149, .T. ) ;
#223111=CARTESIAN_POINT ( 'NONE',  ( 20.94999999999999574, 67.07338541492450190, -61.05142446530125966 ) ) ;
#223164=CIRCLE ( 'NONE', #114850, 0.09999999999999520384 ) ;
#223167=CARTESIAN_POINT ( 'NONE',  ( -18.50000000000000000, 76.00000000001142553, -36.02310748452432421 ) ) ;
#223177=DIRECTION ( 'NONE',  ( -1.000000000000000000, 0.000000000000000000, 0.000000000000000000 ) ) ;
#223191=ORIENTED_EDGE ( 'NONE', *, *, #3966, .F. ) ;
#223195=LINE ( 'NONE', #141118, #172736 ) ;
#223203=CIRCLE ( 'NONE', #252412, 11.80000000000000426 ) ;
#223248=DIRECTION ( 'NONE',  ( 0.000000000000000000, 1.000000000000000000, 6.982962677686266711E-15 ) ) ;
#223256=DIRECTION ( 'NONE',  ( -0.000000000000000000, -6.982962677686266711E-15, 1.000000000000000000 ) ) ;
#223267=CARTESIAN_POINT ( 'NONE',  ( 20.94999999999999929, 84.66355140188063899, -45.54720860259157433 ) ) ;
#223272=DIRECTION ( 'NONE',  ( 4.239556034732056743E-17, 0.1298341882519953860, 0.9915357197604862671 ) ) ;
#223275=ORIENTED_EDGE ( 'NONE', *, *, #63294, .F. ) ;
#223276=VECTOR ( 'NONE', #143145, 1000.000000000000000 ) ;
#223289=ORIENTED_EDGE ( 'NONE', *, *, #187853, .T. ) ;
#223328=ORIENTED_EDGE ( 'NONE', *, *, #113245, .F. ) ;
#223385=CARTESIAN_POINT ( 'NONE',  ( 22.16821283564876666, 68.44102665923090001, -69.52310748452437394 ) ) ;
#223391=VERTEX_POINT ( 'NONE', #64551 ) ;
#223411=EDGE_LOOP ( 'NONE', ( #128102, #247021, #6036, #237184 ) ) ;
#223418=DIRECTION ( 'NONE',  ( 4.239556034732057360E-17, 0.1298341882519953860, 0.9915357197604862671 ) ) ;
#223423=ORIENTED_EDGE ( 'NONE', *, *, #251837, .F. ) ;
#223424=AXIS2_PLACEMENT_3D ( 'NONE', #43499, #82578, #142571 ) ;
#223440=CARTESIAN_POINT ( 'NONE',  ( 20.95561247346651967, 65.40499263480805325, -61.92932471754276236 ) ) ;
#223451=CARTESIAN_POINT ( 'NONE',  ( -22.59999999999999787, 64.25043287652226809, -69.62396585362311896 ) ) ;
#223462=EDGE_CURVE ( 'NONE', #117567, #130245, #7716, .T. ) ;
#223487=ORIENTED_EDGE ( 'NONE', *, *, #21386, .F. ) ;
#223491=EDGE_CURVE ( 'NONE', #208753, #165812, #243185, .T. ) ;
#223507=DIRECTION ( 'NONE',  ( 0.000000000000000000, 0.000000000000000000, 1.000000000000000000 ) ) ;
#223540=DIRECTION ( 'NONE',  ( 1.000000000000000000, 0.000000000000000000, 0.000000000000000000 ) ) ;
#223551=EDGE_CURVE ( 'NONE', #52627, #195996, #29326, .T. ) ;
#223554=EDGE_LOOP ( 'NONE', ( #116254, #180397, #115978, #80488 ) ) ;
#223607=CARTESIAN_POINT ( 'NONE',  ( -23.25000000000000000, 64.35000000001173248, -81.27310748452440237 ) ) ;
#223613=DIRECTION ( 'NONE',  ( 1.000000000000000000, 0.000000000000000000, 0.000000000000000000 ) ) ;
#223614=DIRECTION ( 'NONE',  ( 0.000000000000000000, -6.608470384673547079E-15, 1.000000000000000000 ) ) ;
#223618=DIRECTION ( 'NONE',  ( 1.000000000000000000, 0.000000000000000000, -0.000000000000000000 ) ) ;
#223635=EDGE_LOOP ( 'NONE', ( #239989, #254622, #99094, #161711 ) ) ;
#223654=EDGE_CURVE ( 'NONE', #216065, #113349, #53674, .T. ) ;
#223671=CARTESIAN_POINT ( 'NONE',  ( -23.15000000000000213, 76.00000000001145395, -39.92310748452432279 ) ) ;
#223698=CYLINDRICAL_SURFACE ( 'NONE', #177198, 0.09999999999999939493 ) ;
#223722=CARTESIAN_POINT ( 'NONE',  ( 20.94999999999999929, 85.00000000001149658, -45.41707660717670336 ) ) ;
#223734=AXIS2_PLACEMENT_3D ( 'NONE', #175944, #157682, #118532 ) ;
#223743=CARTESIAN_POINT ( 'NONE',  ( -20.64999999999999858, 85.50000000001149658, -45.91707660717669626 ) ) ;
#223761=VERTEX_POINT ( 'NONE', #35735 ) ;
#223818=CARTESIAN_POINT ( 'NONE',  ( -21.04999999999999716, 76.01465611852449911, -76.01979407029223523 ) ) ;
#223901=VERTEX_POINT ( 'NONE', #199936 ) ;
#223905=CARTESIAN_POINT ( 'NONE',  ( -20.64999999999999858, 76.00000000001142553, -36.02310748452432421 ) ) ;
#223948=ORIENTED_EDGE ( 'NONE', *, *, #198970, .T. ) ;
#223956=ORIENTED_EDGE ( 'NONE', *, *, #29132, .T. ) ;
#223985=ORIENTED_EDGE ( 'NONE', *, *, #51942, .T. ) ;
#223992=EDGE_LOOP ( 'NONE', ( #145668, #106002, #186687, #81805, #237229, #92746, #243422, #33755, #33196, #246792, #48767, #28140 ) ) ;
#224011=FACE_OUTER_BOUND ( 'NONE', #242617, .T. ) ;
#224025=CARTESIAN_POINT ( 'NONE',  ( 23.24999999999999289, 64.35000000001156195, -57.37310748452439668 ) ) ;
#224042=VECTOR ( 'NONE', #83672, 1000.000000000000114 ) ;
#224073=VERTEX_POINT ( 'NONE', #168546 ) ;
#224080=DIRECTION ( 'NONE',  ( 0.000000000000000000, -6.547589603894034005E-15, 1.000000000000000000 ) ) ;
#224081=DIRECTION ( 'NONE',  ( 0.000000000000000000, -6.308085367188388072E-15, 1.000000000000000000 ) ) ;
#224131=TOROIDAL_SURFACE ( 'NONE', #257395, 0.6000000000000009770, 0.1000000000000000056 ) ;
#224138=CARTESIAN_POINT ( 'NONE',  ( -22.48660254037843487, 64.35000000001166143, -69.57310748452438531 ) ) ;
#224161=DIRECTION ( 'NONE',  ( 0.000000000000000000, -6.982962677686266711E-15, 1.000000000000000000 ) ) ;
#224166=ORIENTED_EDGE ( 'NONE', *, *, #191910, .F. ) ;
#224178=ORIENTED_EDGE ( 'NONE', *, *, #248413, .F. ) ;
#224197=CARTESIAN_POINT ( 'NONE',  ( 18.52130828395272744, 85.48139550263741171, -62.49860076064062753 ) ) ;
#224211=AXIS2_PLACEMENT_3D ( 'NONE', #248380, #69761, #90573 ) ;
#224230=CARTESIAN_POINT ( 'NONE',  ( 18.40000000000000213, 85.50000000001161027, -62.52374538734413534 ) ) ;
#224239=ORIENTED_EDGE ( 'NONE', *, *, #205213, .F. ) ;
#224271=ADVANCED_FACE ( 'NONE', ( #180056 ), #207991, .T. ) ;
#224276=EDGE_CURVE ( 'NONE', #22349, #52627, #100478, .T. ) ;
#224318=DIRECTION ( 'NONE',  ( -2.952720810173289112E-16, -1.000000000000000000, -6.982962677686266711E-15 ) ) ;
#224329=ORIENTED_EDGE ( 'NONE', *, *, #155334, .F. ) ;
#224338=DIRECTION ( 'NONE',  ( -1.000000000000000000, 0.000000000000000000, -0.000000000000000000 ) ) ;
#224347=EDGE_CURVE ( 'NONE', #206635, #181531, #104334, .T. ) ;
#224373=ORIENTED_EDGE ( 'NONE', *, *, #183603, .T. ) ;
#224378=VERTEX_POINT ( 'NONE', #69104 ) ;
#224386=CARTESIAN_POINT ( 'NONE',  ( 20.95159278453404283, 67.09210366206254150, -61.03838729941513463 ) ) ;
#224397=AXIS2_PLACEMENT_3D ( 'NONE', #100341, #143341, #179926 ) ;
#224400=CARTESIAN_POINT ( 'NONE',  ( 22.39999999999999503, 64.25000000001165290, -69.62310748452439668 ) ) ;
#224410=AXIS2_PLACEMENT_3D ( 'NONE', #6606, #167012, #86114 ) ;
#224425=ORIENTED_EDGE ( 'NONE', *, *, #135832, .T. ) ;
#224472=ORIENTED_EDGE ( 'NONE', *, *, #51733, .T. ) ;
#224491=CIRCLE ( 'NONE', #7850, 0.8750000000000007772 ) ;
#224503=CARTESIAN_POINT ( 'NONE',  ( -20.64999999999999858, 85.40000000001158753, -59.62913836187181715 ) ) ;
#224528=ADVANCED_FACE ( 'NONE', ( #152508 ), #194191, .F. ) ;
#224559=CYLINDRICAL_SURFACE ( 'NONE', #155877, 0.1000000000000064587 ) ;
#224561=ORIENTED_EDGE ( 'NONE', *, *, #192727, .F. ) ;
#224570=AXIS2_PLACEMENT_3D ( 'NONE', #123989, #164394, #144802 ) ;
#224673=ORIENTED_EDGE ( 'NONE', *, *, #64855, .T. ) ;
#224708=ORIENTED_EDGE ( 'NONE', *, *, #189705, .T. ) ;
#224713=DIRECTION ( 'NONE',  ( 1.000000000000000000, 0.000000000000000000, 0.000000000000000000 ) ) ;
#224725=DIRECTION ( 'NONE',  ( 0.000000000000000000, 0.000000000000000000, 1.000000000000000000 ) ) ;
#224733=CARTESIAN_POINT ( 'NONE',  ( 22.39999999999999503, 76.00000000001170974, -77.31388708289769340 ) ) ;
#224762=CARTESIAN_POINT ( 'NONE',  ( -21.11927991906891577, 75.99091632053783485, -75.97160060301582973 ) ) ;
#224771=ORIENTED_EDGE ( 'NONE', *, *, #195131, .T. ) ;
#224789=CARTESIAN_POINT ( 'NONE',  ( 20.94999999999999929, 76.00000000001142553, -36.02310748452432421 ) ) ;
#224807=DIRECTION ( 'NONE',  ( 0.000000000000000000, -0.5000000000000209832, -0.8660254037844264952 ) ) ;
#224874=EDGE_CURVE ( 'NONE', #130245, #212130, #33553, .T. ) ;
#224921=VERTEX_POINT ( 'NONE', #54336 ) ;
#224925=DIRECTION ( 'NONE',  ( 0.000000000000000000, -1.000000000000000000, -6.982962677686265922E-15 ) ) ;
#224930=CARTESIAN_POINT ( 'NONE',  ( -18.59999999999999787, 77.83585931145498193, -24.51866831572578320 ) ) ;
#224933=DIRECTION ( 'NONE',  ( -0.000000000000000000, -6.982962677686266711E-15, 1.000000000000000000 ) ) ;
#224938=EDGE_CURVE ( 'NONE', #74560, #67154, #133880, .T. ) ;
#224963=CARTESIAN_POINT ( 'NONE',  ( -21.05000000000000071, 61.95000000001162022, -64.00941241376342816 ) ) ;
#224978=FACE_OUTER_BOUND ( 'NONE', #50160, .T. ) ;
#224993=CARTESIAN_POINT ( 'NONE',  ( 21.05000000000000071, 85.40000000001148805, -45.91707660717669626 ) ) ;
#224995=FACE_OUTER_BOUND ( 'NONE', #106033, .T. ) ;
#225019=DIRECTION ( 'NONE',  ( -0.000000000000000000, -6.982962677686266711E-15, 1.000000000000000000 ) ) ;
#225031=AXIS2_PLACEMENT_3D ( 'NONE', #98228, #175279, #216919 ) ;
#225048=DIRECTION ( 'NONE',  ( 2.952720810173289112E-16, 1.000000000000000000, 7.006261805886911631E-15 ) ) ;
#225054=ORIENTED_EDGE ( 'NONE', *, *, #129954, .T. ) ;
#225056=CIRCLE ( 'NONE', #54391, 0.09999999999999939493 ) ;
#225059=DIRECTION ( 'NONE',  ( 0.000000000000000000, 1.000000000000000000, 0.000000000000000000 ) ) ;
#225068=VECTOR ( 'NONE', #27772, 1000.000000000000000 ) ;
#225091=DIRECTION ( 'NONE',  ( 0.000000000000000000, 0.000000000000000000, -1.000000000000000000 ) ) ;
#225124=ADVANCED_FACE ( 'NONE', ( #26468 ), #70996, .F. ) ;
#225134=CARTESIAN_POINT ( 'NONE',  ( -22.39999999999999858, 68.20922040163824818, -69.52310748452437394 ) ) ;
#225151=ORIENTED_EDGE ( 'NONE', *, *, #189997, .T. ) ;
#225158=LINE ( 'NONE', #47808, #198452 ) ;
#225162=EDGE_CURVE ( 'NONE', #150112, #87393, #91565, .T. ) ;
#225202=DIRECTION ( 'NONE',  ( 0.000000000000000000, -1.000000000000000000, -6.982962677686265922E-15 ) ) ;
#225212=DIRECTION ( 'NONE',  ( 0.000000000000000000, 0.000000000000000000, 1.000000000000000000 ) ) ;
#225228=EDGE_LOOP ( 'NONE', ( #151597, #156803, #73722, #44390 ) ) ;
#225239=CARTESIAN_POINT ( 'NONE',  ( -21.14999999999999858, 76.10085836911045476, -81.27267460801371612 ) ) ;
#225276=CARTESIAN_POINT ( 'NONE',  ( -21.05000000000000071, 87.48912529308769592, -66.42310748452423752 ) ) ;
#225280=DIRECTION ( 'NONE',  ( 1.000000000000000000, 0.000000000000000000, 0.000000000000000000 ) ) ;
#225281=DIRECTION ( 'NONE',  ( 0.000000000000000000, -1.000000000000000000, -8.717686153663073805E-15 ) ) ;
#225291=TOROIDAL_SURFACE ( 'NONE', #158887, 4.149999999999999467, 0.1000000000000000056 ) ;
#225306=ORIENTED_EDGE ( 'NONE', *, *, #219762, .F. ) ;
#225338=VERTEX_POINT ( 'NONE', #172430 ) ;
#225347=AXIS2_PLACEMENT_3D ( 'NONE', #225986, #27859, #47366 ) ;
#225393=CARTESIAN_POINT ( 'NONE',  ( 21.05000000000000071, 70.15000000001148805, -46.15560470880229360 ) ) ;
#225403=ORIENTED_EDGE ( 'NONE', *, *, #78590, .F. ) ;
#225426=LINE ( 'NONE', #165491, #240017 ) ;
#225469=CARTESIAN_POINT ( 'NONE',  ( 18.49999999999999645, 77.13501884592155022, -28.30613060109199353 ) ) ;
#225494=CARTESIAN_POINT ( 'NONE',  ( 18.40000000000000213, 85.51932773110404185, -62.55013110796493692 ) ) ;
#225515=AXIS2_PLACEMENT_3D ( 'NONE', #165736, #109577, #84851 ) ;
#225586=DIRECTION ( 'NONE',  ( 0.000000000000000000, 0.1350103645451946055, -0.9908441862701591329 ) ) ;
#225615=CARTESIAN_POINT ( 'NONE',  ( -2.995603634470891112E-16, 87.75000000001151079, -48.27310748452424605 ) ) ;
#225616=DIRECTION ( 'NONE',  ( 0.000000000000000000, 1.000000000000000000, 6.982962677686266711E-15 ) ) ;
#225662=DIRECTION ( 'NONE',  ( 0.000000000000000000, -6.982962677686266711E-15, 1.000000000000000000 ) ) ;
#225676=CARTESIAN_POINT ( 'NONE',  ( 20.95512820512821150, 65.37615131629968346, -57.32294546509999122 ) ) ;
#225680=DIRECTION ( 'NONE',  ( 0.000000000000000000, 6.467318590049456648E-15, -1.000000000000000000 ) ) ;
#225682=DIRECTION ( 'NONE',  ( 0.000000000000000000, 0.000000000000000000, -1.000000000000000000 ) ) ;
#225697=CARTESIAN_POINT ( 'NONE',  ( -18.50000000000000000, 68.97833521811131163, -32.38954208262708079 ) ) ;
#225703=B_SPLINE_CURVE_WITH_KNOTS ( 'NONE', 3,
 ( #106510, #103941, #68701, #183511 ),
 .UNSPECIFIED., .F., .F.,
 ( 4, 4 ),
 ( 0.000000000000000000, 0.001767853679387133359 ),
 .UNSPECIFIED. ) ;
#225711=FACE_OUTER_BOUND ( 'NONE', #127869, .T. ) ;
#225720=AXIS2_PLACEMENT_3D ( 'NONE', #209465, #51649, #92086 ) ;
#225743=ORIENTED_EDGE ( 'NONE', *, *, #207433, .F. ) ;
#225751=VECTOR ( 'NONE', #8946, 1000.000000000000000 ) ;
#225771=LINE ( 'NONE', #244062, #253264 ) ;
#225809=CARTESIAN_POINT ( 'NONE',  ( 23.14999999999999147, 76.00000000001165290, -69.52310748452431710 ) ) ;
#225811=DIRECTION ( 'NONE',  ( 0.000000000000000000, 6.982962677686266711E-15, -1.000000000000000000 ) ) ;
#225853=CIRCLE ( 'NONE', #121853, 0.1000000000000028644 ) ;
#225872=ORIENTED_EDGE ( 'NONE', *, *, #157064, .F. ) ;
#225932=CARTESIAN_POINT ( 'NONE',  ( 21.03675099975491136, 67.12481996722674182, -57.19756534774633394 ) ) ;
#225982=DIRECTION ( 'NONE',  ( 0.000000000000000000, -6.982962677686266711E-15, 1.000000000000000000 ) ) ;
#225986=CARTESIAN_POINT ( 'NONE',  ( -23.15000000000000213, 64.35000000001173248, -81.27310748452440237 ) ) ;
#226031=DIRECTION ( 'NONE',  ( -6.938893903907222067E-15, -1.000000000000000000, -6.982962677686266711E-15 ) ) ;
#226052=FACE_OUTER_BOUND ( 'NONE', #223554, .T. ) ;
#226067=ORIENTED_EDGE ( 'NONE', *, *, #186253, .F. ) ;
#226074=DIRECTION ( 'NONE',  ( 0.000000000000000000, -0.8660254037844419273, 0.4999999999999942824 ) ) ;
#226083=AXIS2_PLACEMENT_3D ( 'NONE', #66346, #63766, #123755 ) ;
#226111=DIRECTION ( 'NONE',  ( 0.000000000000000000, 0.9915357197604862671, -0.1298341882519953583 ) ) ;
#226126=FACE_OUTER_BOUND ( 'NONE', #194059, .T. ) ;
#226131=DIRECTION ( 'NONE',  ( 1.000000000000000000, 0.000000000000000000, 0.000000000000000000 ) ) ;
#226158=DIRECTION ( 'NONE',  ( 0.7071067811865487940, -4.937700262164522799E-15, 0.7071067811865463515 ) ) ;
#226170=VECTOR ( 'NONE', #20211, 1000.000000000000000 ) ;
#226262=DIRECTION ( 'NONE',  ( 0.000000000000000000, 0.6728971962616412394, -0.7397360091703134577 ) ) ;
#226358=ORIENTED_EDGE ( 'NONE', *, *, #188036, .F. ) ;
#226365=AXIS2_PLACEMENT_3D ( 'NONE', #126163, #102735, #81879 ) ;
#226371=ORIENTED_EDGE ( 'NONE', *, *, #27309, .F. ) ;
#226372=CARTESIAN_POINT ( 'NONE',  ( -23.25000000000000000, 76.00000000001165290, -69.52310748452431710 ) ) ;
#226387=ORIENTED_EDGE ( 'NONE', *, *, #66350, .T. ) ;
#226431=CARTESIAN_POINT ( 'NONE',  ( -20.64999999999999858, 85.00000000001149658, -45.51707660717670478 ) ) ;
#226441=DIRECTION ( 'NONE',  ( 0.000000000000000000, -6.982962677686266711E-15, 1.000000000000000000 ) ) ;
#226442=AXIS2_PLACEMENT_3D ( 'NONE', #143298, #44217, #200713 ) ;
#226459=DIRECTION ( 'NONE',  ( -2.952720810173289605E-16, -1.000000000000000000, -7.086529944415894657E-15 ) ) ;
#226524=DIRECTION ( 'NONE',  ( 0.000000000000000000, 0.000000000000000000, 1.000000000000000000 ) ) ;
#226550=ORIENTED_EDGE ( 'NONE', *, *, #215424, .F. ) ;
#226553=CARTESIAN_POINT ( 'NONE',  ( 23.15000000000000213, 87.65000000001144542, -39.12310748452424747 ) ) ;
#226558=ORIENTED_EDGE ( 'NONE', *, *, #237277, .T. ) ;
#226593=ADVANCED_FACE ( 'NONE', ( #175345 ), #100863, .F. ) ;
#226601=EDGE_CURVE ( 'NONE', #206496, #18090, #76361, .T. ) ;
#226704=EDGE_CURVE ( 'NONE', #250549, #183793, #155706, .T. ) ;
#226709=ADVANCED_FACE ( 'NONE', ( #6945 ), #65634, .F. ) ;
#226742=DIRECTION ( 'NONE',  ( 0.000000000000000000, -1.000000000000000000, -6.982962677686265922E-15 ) ) ;
#226751=DIRECTION ( 'NONE',  ( 0.000000000000000000, 1.000000000000000000, 6.982962677686266711E-15 ) ) ;
#226752=CIRCLE ( 'NONE', #177301, 0.1000000000000028644 ) ;
#226788=CARTESIAN_POINT ( 'NONE',  ( 18.55857864376268296, 65.63284271248610935, -44.77310748452438816 ) ) ;
#226797=EDGE_CURVE ( 'NONE', #27421, #216194, #189002, .T. ) ;
#226799=CIRCLE ( 'NONE', #55898, 7.800000000000001599 ) ;
#226807=ORIENTED_EDGE ( 'NONE', *, *, #139690, .F. ) ;
#226817=VERTEX_POINT ( 'NONE', #239997 ) ;
#226836=CARTESIAN_POINT ( 'NONE',  ( 21.00000000000000000, 66.25000000001158185, -57.27310748452438816 ) ) ;
#226839=AXIS2_PLACEMENT_3D ( 'NONE', #38151, #117667, #177678 ) ;
#226841=FACE_OUTER_BOUND ( 'NONE', #245229, .T. ) ;
#226848=AXIS2_PLACEMENT_3D ( 'NONE', #191331, #131317, #231723 ) ;
#226858=EDGE_LOOP ( 'NONE', ( #174361, #135284, #38519, #164059 ) ) ;
#226873=EDGE_LOOP ( 'NONE', ( #137859, #48539, #83965, #36953 ) ) ;
#226948=DIRECTION ( 'NONE',  ( 0.000000000000000000, -6.982962677686266711E-15, 1.000000000000000000 ) ) ;
#226953=CARTESIAN_POINT ( 'NONE',  ( -18.59999999999999787, 85.40000000001154490, -62.22584772486096938 ) ) ;
#226967=CARTESIAN_POINT ( 'NONE',  ( 20.95346350065193519, 67.11282275083711113, -61.01137553748900189 ) ) ;
#226977=DIRECTION ( 'NONE',  ( 0.000000000000000000, -1.000000000000000000, 0.000000000000000000 ) ) ;
#226981=CARTESIAN_POINT ( 'NONE',  ( 20.94999999999999929, 74.16465844978715438, -57.96795619196134908 ) ) ;
#226992=CARTESIAN_POINT ( 'NONE',  ( -18.59999999999999787, 77.16412189325258453, -28.10825939895270764 ) ) ;
#227020=DIRECTION ( 'NONE',  ( 0.000000000000000000, -6.938893903907270030E-14, 1.000000000000000000 ) ) ;
#227060=CARTESIAN_POINT ( 'NONE',  ( 21.05000000000000071, 76.00000000001145395, -40.12310748452431852 ) ) ;
#227066=CARTESIAN_POINT ( 'NONE',  ( 23.14999999999999858, 69.35000000001156195, -57.17310748452436542 ) ) ;
#227103=AXIS2_PLACEMENT_3D ( 'NONE', #222654, #10041, #84390 ) ;
#227116=EDGE_CURVE ( 'NONE', #51183, #69524, #154706, .T. ) ;
#227125=B_SPLINE_CURVE_WITH_KNOTS ( 'NONE', 3,
 ( #128345, #188297, #50074, #33132, #209143, #189604, #132186, #149202, #111343, #89195, #53931, #231302, #249578, #90477, #91776, #171362 ),
 .UNSPECIFIED., .F., .F.,
 ( 4, 3, 3, 3, 3, 4 ),
 ( 0.000000000000000000, 3.357088238233650135E-05, 6.714213034887348832E-05, 0.0001007408646120970340, 0.0001343627955914237268, 0.0001573956632895990877 ),
 .UNSPECIFIED. ) ;
#227127=FACE_OUTER_BOUND ( 'NONE', #218189, .T. ) ;
#227141=ORIENTED_EDGE ( 'NONE', *, *, #16442, .F. ) ;
#227143=DIRECTION ( 'NONE',  ( 0.000000000000000000, 0.000000000000000000, -1.000000000000000000 ) ) ;
#227190=DIRECTION ( 'NONE',  ( 0.000000000000000000, 0.9908441862701605762, 0.1350103645451835310 ) ) ;
#227198=EDGE_CURVE ( 'NONE', #5270, #12040, #64277, .T. ) ;
#227230=AXIS2_PLACEMENT_3D ( 'NONE', #72061, #211564, #92881 ) ;
#227252=CARTESIAN_POINT ( 'NONE',  ( 21.05000000000000071, 65.57661458509871011, -62.03105556065429482 ) ) ;
#227268=AXIS2_PLACEMENT_3D ( 'NONE', #133740, #109036, #9949 ) ;
#227273=CARTESIAN_POINT ( 'NONE',  ( -21.05000000000000071, 74.73821383144657204, -61.43660852097884373 ) ) ;
#227287=ORIENTED_EDGE ( 'NONE', *, *, #138933, .F. ) ;
#227321=DIRECTION ( 'NONE',  ( 0.7071067811865475727, 0.7071067811865475727, 4.937700262164531476E-15 ) ) ;
#227341=CYLINDRICAL_SURFACE ( 'NONE', #51413, 0.5000000000000004441 ) ;
#227392=ADVANCED_FACE ( 'NONE', ( #161431 ), #60169, .F. ) ;
#227461=EDGE_CURVE ( 'NONE', #44321, #165812, #102028, .T. ) ;
#227468=ORIENTED_EDGE ( 'NONE', *, *, #33803, .T. ) ;
#227476=CARTESIAN_POINT ( 'NONE',  ( 21.04999999999999716, 65.37127968600721317, -57.37310748452440379 ) ) ;
#227478=ADVANCED_FACE ( 'NONE', ( #148260 ), #187403, .F. ) ;
#227506=DIRECTION ( 'NONE',  ( 1.000000000000000000, 0.000000000000000000, 0.000000000000000000 ) ) ;
#227525=CARTESIAN_POINT ( 'NONE',  ( -20.94999999999999929, 87.65000000001144542, -38.92310748452424463 ) ) ;
#227528=AXIS2_PLACEMENT_3D ( 'NONE', #21295, #142481, #4250 ) ;
#227545=EDGE_CURVE ( 'NONE', #146292, #169064, #201826, .T. ) ;
#227546=ORIENTED_EDGE ( 'NONE', *, *, #561, .T. ) ;
#227549=CARTESIAN_POINT ( 'NONE',  ( -18.50000000000000000, 68.97833521811131163, -32.18954208262707795 ) ) ;
#227564=ORIENTED_EDGE ( 'NONE', *, *, #23594, .F. ) ;
#227566=CARTESIAN_POINT ( 'NONE',  ( -23.25000000000000000, 87.65000000001144542, -39.12310748452424747 ) ) ;
#227579=VERTEX_POINT ( 'NONE', #155988 ) ;
#227580=ORIENTED_EDGE ( 'NONE', *, *, #89643, .F. ) ;
#227598=DIRECTION ( 'NONE',  ( 1.000000000000000000, 0.000000000000000000, 0.000000000000000000 ) ) ;
#227670=CARTESIAN_POINT ( 'NONE',  ( 23.24999999999999645, 78.10000000001141984, -36.02310748452431000 ) ) ;
#227686=EDGE_CURVE ( 'NONE', #90665, #126512, #93683, .T. ) ;
#227703=CARTESIAN_POINT ( 'NONE',  ( 21.05000000000000071, 64.25000000001146816, -43.03791325517834565 ) ) ;
#227707=EDGE_LOOP ( 'NONE', ( #65947, #197046, #249909, #196658 ) ) ;
#227742=CIRCLE ( 'NONE', #36238, 12.77499999999999503 ) ;
#227745=DIRECTION ( 'NONE',  ( 0.000000000000000000, -7.272083257015735086E-15, 1.000000000000000000 ) ) ;
#227749=EDGE_LOOP ( 'NONE', ( #86574, #37898, #14062, #29401 ) ) ;
#227796=ORIENTED_EDGE ( 'NONE', *, *, #152958, .T. ) ;
#227805=DIRECTION ( 'NONE',  ( -0.000000000000000000, 1.000000000000000000, 6.982962677686266711E-15 ) ) ;
#227840=ADVANCED_FACE ( 'NONE', ( #47544 ), #162831, .F. ) ;
#227852=EDGE_LOOP ( 'NONE', ( #115597, #104688, #147273, #64991 ) ) ;
#227908=AXIS2_PLACEMENT_3D ( 'NONE', #25166, #163377, #23888 ) ;
#227915=ORIENTED_EDGE ( 'NONE', *, *, #221537, .T. ) ;
#227986=LINE ( 'NONE', #32386, #101845 ) ;
#228017=AXIS2_PLACEMENT_3D ( 'NONE', #113915, #154374, #31846 ) ;
#228018=ORIENTED_EDGE ( 'NONE', *, *, #193493, .T. ) ;
#228046=EDGE_CURVE ( 'NONE', #70064, #193535, #181371, .T. ) ;
#228067=CARTESIAN_POINT ( 'NONE',  ( 18.46921299892755641, 85.50937817783538719, -62.53652877515382613 ) ) ;
#228070=EDGE_CURVE ( 'NONE', #246837, #171007, #77107, .T. ) ;
#228073=CARTESIAN_POINT ( 'NONE',  ( 22.45301702632625762, 75.98478912030155641, -81.17289970878471195 ) ) ;
#228077=CARTESIAN_POINT ( 'NONE',  ( -21.44999999999999929, 68.65000000001150227, -48.37310748452437537 ) ) ;
#228102=CARTESIAN_POINT ( 'NONE',  ( 20.94999999999999929, 76.00000000001136868, -28.22310748452431994 ) ) ;
#228107=CARTESIAN_POINT ( 'NONE',  ( 18.59999994388910238, 85.36356618708258281, -62.34199024772312470 ) ) ;
#228117=DIRECTION ( 'NONE',  ( 2.879366945564059217E-14, 0.9875055080513762684, -0.1575844902526679081 ) ) ;
#228155=DIRECTION ( 'NONE',  ( 1.000000000000000000, 0.000000000000000000, 0.000000000000000000 ) ) ;
#228166=AXIS2_PLACEMENT_3D ( 'NONE', #45696, #60429, #186505 ) ;
#228179=EDGE_CURVE ( 'NONE', #245547, #144086, #23350, .T. ) ;
#228193=CARTESIAN_POINT ( 'NONE',  ( 23.24999999999999289, 69.55000000001157900, -57.17310748452436542 ) ) ;
#228194=CYLINDRICAL_SURFACE ( 'NONE', #209936, 0.1000000000000052097 ) ;
#228205=CARTESIAN_POINT ( 'NONE',  ( -23.25000000000000000, 71.65000000001155911, -57.27310748452435263 ) ) ;
#228213=EDGE_LOOP ( 'NONE', ( #170421, #145006, #42966, #46883 ) ) ;
#228236=EDGE_LOOP ( 'NONE', ( #194338, #238378, #3853, #3550 ) ) ;
#228281=EDGE_CURVE ( 'NONE', #213807, #125917, #119136, .T. ) ;
#228377=EDGE_CURVE ( 'NONE', #95061, #117567, #144419, .T. ) ;
#228380=EDGE_CURVE ( 'NONE', #153937, #144828, #246125, .T. ) ;
#228382=DIRECTION ( 'NONE',  ( 0.000000000000000000, 0.000000000000000000, 1.000000000000000000 ) ) ;
#228385=DIRECTION ( 'NONE',  ( 1.000000000000000000, 0.000000000000000000, 0.000000000000000000 ) ) ;
#228391=ADVANCED_FACE ( 'NONE', ( #204409 ), #85629, .F. ) ;
#228409=EDGE_CURVE ( 'NONE', #85564, #97821, #19025, .T. ) ;
#228423=VECTOR ( 'NONE', #74416, 1000.000000000000000 ) ;
#228426=AXIS2_PLACEMENT_3D ( 'NONE', #143093, #146943, #86960 ) ;
#228427=FACE_OUTER_BOUND ( 'NONE', #92311, .T. ) ;
#228434=DIRECTION ( 'NONE',  ( 0.000000000000000000, 0.000000000000000000, -1.000000000000000000 ) ) ;
#228465=ORIENTED_EDGE ( 'NONE', *, *, #238385, .F. ) ;
#228466=DIRECTION ( 'NONE',  ( -1.836970198721029934E-16, -1.000000000000000000, -6.982962677686266711E-15 ) ) ;
#228504=DIRECTION ( 'NONE',  ( -0.000000000000000000, 7.272083257015735086E-15, -1.000000000000000000 ) ) ;
#228555=AXIS2_PLACEMENT_3D ( 'NONE', #141726, #25643, #161317 ) ;
#228559=CARTESIAN_POINT ( 'NONE',  ( 21.05000000000000071, 65.31570632562490175, -61.99643354588710054 ) ) ;
#228581=ADVANCED_FACE ( 'NONE', ( #30955 ), #164959, .T. ) ;
#228590=ORIENTED_EDGE ( 'NONE', *, *, #128741, .T. ) ;
#228605=DIRECTION ( 'NONE',  ( -0.7071067811865475727, 0.7071067811865475727, 4.937700262164531476E-15 ) ) ;
#228628=ADVANCED_FACE ( 'NONE', ( #98547 ), #81562, .T. ) ;
#228641=CARTESIAN_POINT ( 'NONE',  ( -20.54999999999999716, 85.40000000001158753, -59.62913836187181715 ) ) ;
#228718=CYLINDRICAL_SURFACE ( 'NONE', #125797, 0.09999999999999867328 ) ;
#228724=EDGE_CURVE ( 'NONE', #165690, #165183, #28078, .T. ) ;
#228726=EDGE_CURVE ( 'NONE', #165845, #90093, #63231, .T. ) ;
#228753=DIRECTION ( 'NONE',  ( 0.000000000000000000, -6.982962677686266711E-15, 1.000000000000000000 ) ) ;
#228756=AXIS2_PLACEMENT_3D ( 'NONE', #239177, #217026, #549 ) ;
#228787=DIRECTION ( 'NONE',  ( 0.000000000000000000, 6.982962677686266711E-15, -1.000000000000000000 ) ) ;
#228808=ORIENTED_EDGE ( 'NONE', *, *, #123545, .T. ) ;
#228818=VERTEX_POINT ( 'NONE', #123302 ) ;
#228820=PLANE ( 'NONE',  #180883 ) ;
#228838=AXIS2_PLACEMENT_3D ( 'NONE', #153192, #187167, #88014 ) ;
#228890=ORIENTED_EDGE ( 'NONE', *, *, #155334, .T. ) ;
#228905=CARTESIAN_POINT ( 'NONE',  ( -18.59999999999999787, 66.65000000001150227, -48.37310748452438958 ) ) ;
#228911=EDGE_CURVE ( 'NONE', #110576, #71835, #87685, .T. ) ;
#228948=DIRECTION ( 'NONE',  ( 0.000000000000000000, 6.982962677686266711E-15, -1.000000000000000000 ) ) ;
#228963=AXIS2_PLACEMENT_3D ( 'NONE', #120798, #41266, #144162 ) ;
#228971=DIRECTION ( 'NONE',  ( -0.000000000000000000, -6.982962677686266711E-15, 1.000000000000000000 ) ) ;
#228978=DIRECTION ( 'NONE',  ( 0.000000000000000000, -6.688090509790097607E-15, 1.000000000000000000 ) ) ;
#229077=VERTEX_POINT ( 'NONE', #59127 ) ;
#229091=ORIENTED_EDGE ( 'NONE', *, *, #185252, .F. ) ;
#229095=ORIENTED_EDGE ( 'NONE', *, *, #244403, .F. ) ;
#229123=DIRECTION ( 'NONE',  ( -0.000000000000000000, 6.982962677686266711E-15, -1.000000000000000000 ) ) ;
#229128=CARTESIAN_POINT ( 'NONE',  ( -23.15000000000000213, 71.65000000001155911, -57.37310748452435405 ) ) ;
#229157=CARTESIAN_POINT ( 'NONE',  ( 20.94999999999999574, 77.83534155023598089, -57.96795619196132776 ) ) ;
#229165=CARTESIAN_POINT ( 'NONE',  ( 20.94999999999999929, 69.15387683765879956, -32.28538121767450519 ) ) ;
#229199=CARTESIAN_POINT ( 'NONE',  ( -20.94999999999999929, 87.48912529308769592, -66.42310748452423752 ) ) ;
#229254=AXIS2_PLACEMENT_3D ( 'NONE', #228905, #187228, #108941 ) ;
#229258=DIRECTION ( 'NONE',  ( 1.000000000000000000, -2.952720810173289112E-16, -2.061873921506763405E-30 ) ) ;
#229309=FACE_OUTER_BOUND ( 'NONE', #58397, .T. ) ;
#229364=DIRECTION ( 'NONE',  ( 0.000000000000000000, 0.000000000000000000, 1.000000000000000000 ) ) ;
#229365=DIRECTION ( 'NONE',  ( -3.469446951953515108E-14, -1.000000000000000000, 0.000000000000000000 ) ) ;
#229376=ORIENTED_EDGE ( 'NONE', *, *, #248371, .F. ) ;
#229381=EDGE_CURVE ( 'NONE', #199664, #17643, #113702, .T. ) ;
#229385=DIRECTION ( 'NONE',  ( 2.694716079187273439E-16, 1.000000000000000000, 6.467318590049456648E-15 ) ) ;
#229392=VECTOR ( 'NONE', #241395, 999.9999999999998863 ) ;
#229404=CARTESIAN_POINT ( 'NONE',  ( 23.15000000000000213, 85.50000000001149658, -45.91707660717669626 ) ) ;
#229426=DIRECTION ( 'NONE',  ( -1.000000000000000000, -0.000000000000000000, -0.000000000000000000 ) ) ;
#229462=ORIENTED_EDGE ( 'NONE', *, *, #5748, .F. ) ;
#229476=VECTOR ( 'NONE', #130762, 1000.000000000000000 ) ;
#229484=ORIENTED_EDGE ( 'NONE', *, *, #158598, .T. ) ;
#229508=DIRECTION ( 'NONE',  ( 0.000000000000000000, 1.000000000000000000, 6.982962677686266711E-15 ) ) ;
#229523=CARTESIAN_POINT ( 'NONE',  ( -23.15000000000000213, 74.07476635515175190, -56.79286395139820343 ) ) ;
#229566=AXIS2_PLACEMENT_3D ( 'NONE', #140351, #7259, #128508 ) ;
#229576=DIRECTION ( 'NONE',  ( 0.000000000000000000, 7.147358527629762208E-15, -1.000000000000000000 ) ) ;
#229589=DIRECTION ( 'NONE',  ( 0.000000000000000000, 0.000000000000000000, 1.000000000000000000 ) ) ;
#229614=ORIENTED_EDGE ( 'NONE', *, *, #225162, .F. ) ;
#229620=EDGE_CURVE ( 'NONE', #127854, #91133, #24903, .T. ) ;
#229656=VECTOR ( 'NONE', #214455, 1000.000000000000000 ) ;
#229662=DIRECTION ( 'NONE',  ( -0.7071067811865127117, -0.7071067811865821007, 0.000000000000000000 ) ) ;
#229673=ORIENTED_EDGE ( 'NONE', *, *, #50104, .F. ) ;
#229703=ORIENTED_EDGE ( 'NONE', *, *, #46919, .T. ) ;
#229827=DIRECTION ( 'NONE',  ( 0.000000000000000000, 0.000000000000000000, 1.000000000000000000 ) ) ;
#229846=CIRCLE ( 'NONE', #54857, 0.09999999999999939493 ) ;
#229869=LINE ( 'NONE', #51192, #229476 ) ;
#229905=DIRECTION ( 'NONE',  ( 1.000000000000000000, -2.952720810173289112E-16, -2.061873921506763405E-30 ) ) ;
#229953=EDGE_LOOP ( 'NONE', ( #124056, #213730, #251699, #166777 ) ) ;
#229959=FACE_OUTER_BOUND ( 'NONE', #238956, .T. ) ;
#229969=CIRCLE ( 'NONE', #179912, 0.09999999999999939493 ) ;
#229991=DIRECTION ( 'NONE',  ( 0.000000000000000000, -7.429790795770647916E-15, 1.000000000000000000 ) ) ;
#230004=CARTESIAN_POINT ( 'NONE',  ( 18.59999999999999076, 69.35000000001151932, -48.37310748452436826 ) ) ;
#230009=AXIS2_PLACEMENT_3D ( 'NONE', #55716, #92313, #131444 ) ;
#230026=TOROIDAL_SURFACE ( 'NONE', #72397, 0.2000000000000000111, 0.1000000000000000056 ) ;
#230060=CARTESIAN_POINT ( 'NONE',  ( 20.95512820512820440, 65.37615131629968346, -57.37310748452439668 ) ) ;
#230084=DIRECTION ( 'NONE',  ( 1.000000000000000000, 0.000000000000000000, 0.000000000000000000 ) ) ;
#230086=ORIENTED_EDGE ( 'NONE', *, *, #176001, .F. ) ;
#230090=CARTESIAN_POINT ( 'NONE',  ( 23.24999999999999289, 64.25000000001172396, -81.27310748452440237 ) ) ;
#230093=CARTESIAN_POINT ( 'NONE',  ( -23.15000000000000213, 87.65000000001165859, -69.52310748452424605 ) ) ;
#230115=CIRCLE ( 'NONE', #76008, 0.1000000000000028644 ) ;
#230137=VECTOR ( 'NONE', #8719, 1000.000000000000000 ) ;
#230199=DIRECTION ( 'NONE',  ( -1.000000000000000000, 2.952720810173289112E-16, 2.061873921506763405E-30 ) ) ;
#230280=AXIS2_PLACEMENT_3D ( 'NONE', #248922, #9013, #231931 ) ;
#230298=DIRECTION ( 'NONE',  ( -1.000000000000000000, 0.000000000000000000, 0.000000000000000000 ) ) ;
#230306=ORIENTED_EDGE ( 'NONE', *, *, #132534, .T. ) ;
#230309=DIRECTION ( 'NONE',  ( -0.000000000000000000, 6.982962677686266711E-15, -1.000000000000000000 ) ) ;
#230318=AXIS2_PLACEMENT_3D ( 'NONE', #166430, #50278, #187263 ) ;
#230331=ADVANCED_FACE ( 'NONE', ( #496 ), #236547, .F. ) ;
#230346=DIRECTION ( 'NONE',  ( 0.000000000000000000, 0.000000000000000000, -1.000000000000000000 ) ) ;
#230358=VECTOR ( 'NONE', #121227, 999.9999999999998863 ) ;
#230389=DIRECTION ( 'NONE',  ( 0.000000000000000000, 0.000000000000000000, 1.000000000000000000 ) ) ;
#230405=DIRECTION ( 'NONE',  ( -7.304098846218134667E-16, 1.000000000000000000, 6.982962677686267499E-15 ) ) ;
#230414=VECTOR ( 'NONE', #42378, 1000.000000000000000 ) ;
#230426=ADVANCED_FACE ( 'NONE', ( #104712 ), #152694, .T. ) ;
#230474=LINE ( 'NONE', #169253, #77522 ) ;
#230480=( NAMED_UNIT ( * ) SI_UNIT ( $, .STERADIAN. ) SOLID_ANGLE_UNIT ( ) );
#230481=ADVANCED_FACE ( 'NONE', ( #26519 ), #6933, .T. ) ;
#230531=DIRECTION ( 'NONE',  ( 1.000000000000000000, 0.000000000000000000, 0.000000000000000000 ) ) ;
#230539=ORIENTED_EDGE ( 'NONE', *, *, #498, .F. ) ;
#230543=DIRECTION ( 'NONE',  ( -1.000000000000000000, -0.000000000000000000, -0.000000000000000000 ) ) ;
#230544=CARTESIAN_POINT ( 'NONE',  ( -21.05000000000000071, 74.16465844978715438, -57.96795619196135618 ) ) ;
#230581=CARTESIAN_POINT ( 'NONE',  ( 21.05000000000000071, 71.18691588786205671, -57.58158972800053022 ) ) ;
#230594=DIRECTION ( 'NONE',  ( -1.000000000000000000, 0.000000000000000000, 0.000000000000000000 ) ) ;
#230610=CYLINDRICAL_SURFACE ( 'NONE', #250819, 0.09999999999999939493 ) ;
#230616=EDGE_CURVE ( 'NONE', #57945, #159851, #36343, .T. ) ;
#230628=EDGE_CURVE ( 'NONE', #90111, #72671, #36813, .T. ) ;
#230638=VERTEX_POINT ( 'NONE', #236257 ) ;
#230642=CARTESIAN_POINT ( 'NONE',  ( 22.43288208788031568, 75.99510014512635792, -81.17275932824340146 ) ) ;
#230655=VERTEX_POINT ( 'NONE', #75906 ) ;
#230674=EDGE_CURVE ( 'NONE', #31422, #149811, #194566, .T. ) ;
#230683=CARTESIAN_POINT ( 'NONE',  ( 20.02499999999999858, 66.25000000001151079, -48.37310748452438958 ) ) ;
#230698=CARTESIAN_POINT ( 'NONE',  ( 21.05000000000000071, 76.00000000001142553, -36.02310748452432421 ) ) ;
#230702=ORIENTED_EDGE ( 'NONE', *, *, #242727, .F. ) ;
#230709=CARTESIAN_POINT ( 'NONE',  ( -20.54999999999999716, 74.07476635515175190, -56.79286395139820343 ) ) ;
#230718=( BOUNDED_SURFACE ( )  B_SPLINE_SURFACE ( 3, 2, ( 
 ( #77897, #60901, #140435 ),
 ( #214847, #19220, #219981 ),
 ( #156194, #6059, #244669 ),
 ( #144269, #2202, #64757 ),
 ( #204258, #223818, #245975 ),
 ( #26952, #243393, #45196 ) ),
 .UNSPECIFIED., .F., .F., .T. ) 
 B_SPLINE_SURFACE_WITH_KNOTS ( ( 4, 2, 4 ),
 ( 3, 3 ),
 ( 0.0001792624049599621759, 0.0003686986002124750849, 0.0005581347954649879938 ),
 ( 0.000000000000000000, 1.000000000000000000 ),
 .UNSPECIFIED. ) 
 GEOMETRIC_REPRESENTATION_ITEM ( )  RATIONAL_B_SPLINE_SURFACE ( (
 ( 1.000000000000000000, 0.9238795325112859613, 1.000000000000000000),
 ( 1.000000000000000000, 0.9229318695237587189, 1.000000000000000000),
 ( 1.000000000000000000, 0.8926288119231937657, 1.000000000000000000),
 ( 1.000000000000000000, 0.8123777807270391449, 1.000000000000000000),
 ( 1.000000000000000000, 0.7629087100932221421, 1.000000000000000000),
 ( 1.000000000000000000, 0.7071067811865475727, 1.000000000000000000) ) ) 
 REPRESENTATION_ITEM ( '' )  SURFACE ( )  );
#230755=CIRCLE ( 'NONE', #97430, 0.09999999999999766020 ) ;
#230778=VERTEX_POINT ( 'NONE', #100564 ) ;
#230790=SPHERICAL_SURFACE ( 'NONE', #250945, 0.1000000000000000056 ) ;
#230807=DIRECTION ( 'NONE',  ( -1.000000000000000000, 2.952720810173289112E-16, 2.061873921506763405E-30 ) ) ;
#230820=CARTESIAN_POINT ( 'NONE',  ( -20.85000000000000142, 75.83895117929270668, -36.30729732888454464 ) ) ;
#230826=CARTESIAN_POINT ( 'NONE',  ( 21.46681500593528824, 69.14248884062956790, -69.52310748452435973 ) ) ;
#230838=ORIENTED_EDGE ( 'NONE', *, *, #164980, .T. ) ;
#230844=DIRECTION ( 'NONE',  ( 0.000000000000000000, -0.5000000000000016653, 0.8660254037844377084 ) ) ;
#230890=DIRECTION ( 'NONE',  ( 0.000000000000000000, -6.982962677686266711E-15, 1.000000000000000000 ) ) ;
#230919=EDGE_LOOP ( 'NONE', ( #76370, #126629, #210229, #203663 ) ) ;
#230943=TOROIDAL_SURFACE ( 'NONE', #151831, 0.2000000000000000111, 0.1000000000000000056 ) ;
#230950=CIRCLE ( 'NONE', #22656, 0.09999999999999939493 ) ;
#230962=ADVANCED_FACE ( 'NONE', ( #58811 ), #219187, .T. ) ;
#230978=ORIENTED_EDGE ( 'NONE', *, *, #169798, .F. ) ;
#230984=CARTESIAN_POINT ( 'NONE',  ( -23.25000000000000000, 76.00000000001165290, -69.52310748452431710 ) ) ;
#230997=EDGE_LOOP ( 'NONE', ( #13574, #43631, #71277, #251938 ) ) ;
#231018=AXIS2_PLACEMENT_3D ( 'NONE', #54245, #215873, #196326 ) ;
#231036=ORIENTED_EDGE ( 'NONE', *, *, #166911, .F. ) ;
#231066=VECTOR ( 'NONE', #168766, 1000.000000000000000 ) ;
#231069=FACE_OUTER_BOUND ( 'NONE', #44379, .T. ) ;
#231081=AXIS2_PLACEMENT_3D ( 'NONE', #51586, #15075, #112884 ) ;
#231134=CYLINDRICAL_SURFACE ( 'NONE', #134754, 0.09999999999999939493 ) ;
#231140=DIRECTION ( 'NONE',  ( 1.000000000000000000, 0.000000000000000000, 0.000000000000000000 ) ) ;
#231145=EDGE_CURVE ( 'NONE', #253373, #69524, #232152, .T. ) ;
#231146=FACE_OUTER_BOUND ( 'NONE', #184887, .T. ) ;
#231153=DIRECTION ( 'NONE',  ( 0.000000000000000000, 6.982962677686266711E-15, -1.000000000000000000 ) ) ;
#231256=FACE_OUTER_BOUND ( 'NONE', #203477, .T. ) ;
#231274=ORIENTED_EDGE ( 'NONE', *, *, #182500, .T. ) ;
#231289=TOROIDAL_SURFACE ( 'NONE', #206332, 0.2000000000000000111, 0.1000000000000000056 ) ;
#231300=ORIENTED_EDGE ( 'NONE', *, *, #113383, .F. ) ;
#231302=CARTESIAN_POINT ( 'NONE',  ( 21.11701782572533048, 65.27839088400411072, -57.27807005501318827 ) ) ;
#231315=ADVANCED_FACE ( 'NONE', ( #239745 ), #136416, .T. ) ;
#231317=ADVANCED_FACE ( 'NONE', ( #235875 ), #107415, .F. ) ;
#231336=CARTESIAN_POINT ( 'NONE',  ( 18.49999999999999289, 68.97833521811131163, -32.18954208262707795 ) ) ;
#231354=CIRCLE ( 'NONE', #239721, 11.70000000000000284 ) ;
#231367=ORIENTED_EDGE ( 'NONE', *, *, #137384, .F. ) ;
#231391=ADVANCED_FACE ( 'NONE', ( #147038 ), #203171, .F. ) ;
#231408=ADVANCED_FACE ( 'NONE', ( #224011 ), #104049, .T. ) ;
#231423=EDGE_CURVE ( 'NONE', #139208, #165690, #24051, .T. ) ;
#231427=AXIS2_PLACEMENT_3D ( 'NONE', #6208, #88293, #226524 ) ;
#231439=DIRECTION ( 'NONE',  ( -1.000000000000000000, 3.265361837132813093E-16, 2.280189983783949500E-30 ) ) ;
#231455=EDGE_CURVE ( 'NONE', #128154, #36208, #36715, .T. ) ;
#231469=ORIENTED_EDGE ( 'NONE', *, *, #223654, .T. ) ;
#231517=FACE_OUTER_BOUND ( 'NONE', #86366, .T. ) ;
#231527=EDGE_CURVE ( 'NONE', #83438, #43818, #132348, .T. ) ;
#231548=CARTESIAN_POINT ( 'NONE',  ( -18.59999999999999787, 85.32100840337290037, -62.28716923544637751 ) ) ;
#231556=SPHERICAL_SURFACE ( 'NONE', #128816, 0.1000000000000000056 ) ;
#231560=CYLINDRICAL_SURFACE ( 'NONE', #75594, 0.1000000000000028644 ) ;
#231561=CYLINDRICAL_SURFACE ( 'NONE', #94144, 11.80000000000000426 ) ;
#231563=EDGE_CURVE ( 'NONE', #98003, #155495, #3334, .T. ) ;
#231593=DIRECTION ( 'NONE',  ( 0.000000000000000000, -1.000000000000000000, -6.982962677686265922E-15 ) ) ;
#231597=EDGE_CURVE ( 'NONE', #3677, #245148, #257203, .T. ) ;
#231640=VERTEX_POINT ( 'NONE', #73969 ) ;
#231649=VERTEX_POINT ( 'NONE', #199016 ) ;
#231655=CARTESIAN_POINT ( 'NONE',  ( -20.94999999999999929, 64.35000000001147669, -42.80697314750250371 ) ) ;
#231679=ORIENTED_EDGE ( 'NONE', *, *, #226704, .T. ) ;
#231706=DIRECTION ( 'NONE',  ( 0.000000000000000000, 0.000000000000000000, -1.000000000000000000 ) ) ;
#231718=CARTESIAN_POINT ( 'NONE',  ( 18.49999999999999645, 74.27191306321728348, -82.63867247935655769 ) ) ;
#231722=ORIENTED_EDGE ( 'NONE', *, *, #178998, .T. ) ;
#231723=DIRECTION ( 'NONE',  ( 0.000000000000000000, -6.652207440891584540E-15, 1.000000000000000000 ) ) ;
#231739=DIRECTION ( 'NONE',  ( 0.000000000000000000, -2.775557561562888827E-14, 1.000000000000000000 ) ) ;
#231849=VERTEX_POINT ( 'NONE', #87716 ) ;
#231850=ORIENTED_EDGE ( 'NONE', *, *, #7372, .F. ) ;
#231857=CIRCLE ( 'NONE', #48665, 0.1000000000000028644 ) ;
#231862=CIRCLE ( 'NONE', #123704, 0.6000000000000033085 ) ;
#231865=ORIENTED_EDGE ( 'NONE', *, *, #139271, .T. ) ;
#231890=CIRCLE ( 'NONE', #248608, 0.09999999999999939493 ) ;
#231895=DIRECTION ( 'NONE',  ( 0.000000000000000000, 0.000000000000000000, 1.000000000000000000 ) ) ;
#231926=DIRECTION ( 'NONE',  ( 0.000000000000000000, 0.000000000000000000, 1.000000000000000000 ) ) ;
#231931=DIRECTION ( 'NONE',  ( 0.000000000000000000, 0.000000000000000000, 1.000000000000000000 ) ) ;
#231933=EDGE_CURVE ( 'NONE', #257957, #122621, #24413, .T. ) ;
#231934=CARTESIAN_POINT ( 'NONE',  ( 22.49999999999999645, 75.91119002362479762, -81.17287040255624220 ) ) ;
#231966=FACE_OUTER_BOUND ( 'NONE', #132972, .T. ) ;
#231983=AXIS2_PLACEMENT_3D ( 'NONE', #22226, #100429, #105554 ) ;
#232002=VERTEX_POINT ( 'NONE', #177589 ) ;
#232049=EDGE_LOOP ( 'NONE', ( #154490, #234006, #221049 ) ) ;
#232061=ORIENTED_EDGE ( 'NONE', *, *, #223462, .F. ) ;
#232099=FACE_OUTER_BOUND ( 'NONE', #108497, .T. ) ;
#232109=CARTESIAN_POINT ( 'NONE',  ( -21.05000000000000071, 69.74115727647247809, -69.55512117771243652 ) ) ;
#232117=DIRECTION ( 'NONE',  ( -1.000000000000000000, 0.000000000000000000, -0.000000000000000000 ) ) ;
#232130=TOROIDAL_SURFACE ( 'NONE', #119687, 0.2000000000000000111, 0.1000000000000000056 ) ;
#232152=CIRCLE ( 'NONE', #115599, 2.000000000000001776 ) ;
#232178=ORIENTED_EDGE ( 'NONE', *, *, #150270, .F. ) ;
#232182=DIRECTION ( 'NONE',  ( -1.000000000000000000, -0.000000000000000000, -0.000000000000000000 ) ) ;
#232201=DIRECTION ( 'NONE',  ( -1.000000000000000000, 0.000000000000000000, -0.000000000000000000 ) ) ;
#232209=DIRECTION ( 'NONE',  ( 0.000000000000000000, 0.8777080977375072424, -0.4791956752371691608 ) ) ;
#232319=ORIENTED_EDGE ( 'NONE', *, *, #47369, .F. ) ;
#232373=CIRCLE ( 'NONE', #207432, 0.09999999999999971412 ) ;
#232403=ADVANCED_FACE ( 'NONE', ( #19461 ), #241263, .F. ) ;
#232405=ORIENTED_EDGE ( 'NONE', *, *, #139595, .T. ) ;
#232422=AXIS2_PLACEMENT_3D ( 'NONE', #193104, #155285, #110989 ) ;
#232504=EDGE_CURVE ( 'NONE', #201514, #250305, #183071, .T. ) ;
#232528=VERTEX_POINT ( 'NONE', #127539 ) ;
#232537=CIRCLE ( 'NONE', #228426, 0.1000000000000067224 ) ;
#232538=DIRECTION ( 'NONE',  ( 0.000000000000000000, -1.000000000000000000, -6.982962677686266711E-15 ) ) ;
#232541=DIRECTION ( 'NONE',  ( 0.000000000000000000, -0.6728971962616412394, 0.7397360091703134577 ) ) ;
#232558=CARTESIAN_POINT ( 'NONE',  ( -22.45354308602431459, 75.99999978013417490, -81.27354037498388095 ) ) ;
#232561=DIRECTION ( 'NONE',  ( -0.7071067811865475727, 0.7071067811865475727, 4.937700262164531476E-15 ) ) ;
#232585=AXIS2_PLACEMENT_3D ( 'NONE', #153267, #213188, #154548 ) ;
#232597=ORIENTED_EDGE ( 'NONE', *, *, #192121, .T. ) ;
#232600=DIRECTION ( 'NONE',  ( -0.000000000000000000, 0.1350103645451807555, 0.9908441862701610203 ) ) ;
#232606=EDGE_CURVE ( 'NONE', #169810, #121432, #3920, .T. ) ;
#232646=DIRECTION ( 'NONE',  ( -1.000000000000000000, 0.000000000000000000, -0.000000000000000000 ) ) ;
#232647=CARTESIAN_POINT ( 'NONE',  ( 22.01447462590973458, 75.90096299995218487, -76.78690768575422965 ) ) ;
#232654=CARTESIAN_POINT ( 'NONE',  ( 21.05000000000000071, 77.83534155023599510, -57.96795619196132776 ) ) ;
#232665=ORIENTED_EDGE ( 'NONE', *, *, #149124, .F. ) ;
#232666=ORIENTED_EDGE ( 'NONE', *, *, #257400, .F. ) ;
#232748=AXIS2_PLACEMENT_3D ( 'NONE', #189158, #150050, #229576 ) ;
#232758=EDGE_CURVE ( 'NONE', #30729, #4626, #153808, .T. ) ;
#232806=VECTOR ( 'NONE', #221834, 1000.000000000000000 ) ;
#232824=CARTESIAN_POINT ( 'NONE',  ( -21.44999999999999929, 68.75000000001151079, -48.37310748452436826 ) ) ;
#232860=AXIS2_PLACEMENT_3D ( 'NONE', #83905, #162234, #22724 ) ;
#232866=CARTESIAN_POINT ( 'NONE',  ( -21.14999999999999858, 76.00000000001165290, -69.52310748452431710 ) ) ;
#232868=EDGE_CURVE ( 'NONE', #218877, #95340, #3410, .T. ) ;
#232879=CARTESIAN_POINT ( 'NONE',  ( 20.84999999999998721, 65.66751761918619934, -30.42826094061123854 ) ) ;
#232889=AXIS2_PLACEMENT_3D ( 'NONE', #236215, #92847, #191986 ) ;
#232930=AXIS2_PLACEMENT_3D ( 'NONE', #129465, #250680, #72070 ) ;
#232958=DIRECTION ( 'NONE',  ( 1.000000000000000000, 0.000000000000000000, 0.000000000000000000 ) ) ;
#232961=CARTESIAN_POINT ( 'NONE',  ( 18.59999999999999076, 77.25000000001159606, -61.52310748452431710 ) ) ;
#232972=CARTESIAN_POINT ( 'NONE',  ( -18.59999999999999787, 77.83585931145498193, -24.51866831572578320 ) ) ;
#233006=B_SPLINE_CURVE_WITH_KNOTS ( 'NONE', 3,
 ( #216628, #18433, #58812, #173709 ),
 .UNSPECIFIED., .F., .F.,
 ( 4, 4 ),
 ( 0.000000000000000000, 0.001767853679387106471 ),
 .UNSPECIFIED. ) ;
#233017=VERTEX_POINT ( 'NONE', #171521 ) ;
#233026=ORIENTED_EDGE ( 'NONE', *, *, #224347, .F. ) ;
#233068=B_SPLINE_CURVE_WITH_KNOTS ( 'NONE', 3,
 ( #167486, #27987, #244421, #206585, #124492, #204010, #107482, #243136 ),
 .UNSPECIFIED., .F., .F.,
 ( 4, 2, 2, 4 ),
 ( 0.000000000000000000, 0.0001306511400391059284, 0.0001959767100586839647, 0.0002613022800782620011 ),
 .UNSPECIFIED. ) ;
#233097=EDGE_CURVE ( 'NONE', #145606, #47933, #179218, .T. ) ;
#233109=EDGE_CURVE ( 'NONE', #58501, #124582, #159633, .T. ) ;
#233148=CARTESIAN_POINT ( 'NONE',  ( -22.39999999999999858, 64.25000000001165290, -69.52310748452438816 ) ) ;
#233166=CARTESIAN_POINT ( 'NONE',  ( -21.05000000000000071, 76.00000000001162448, -65.22310748452436258 ) ) ;
#233214=CARTESIAN_POINT ( 'NONE',  ( -20.94684162615585166, 64.25000000001162448, -62.68146348457850081 ) ) ;
#233215=ORIENTED_EDGE ( 'NONE', *, *, #189777, .T. ) ;
#233233=VERTEX_POINT ( 'NONE', #21429 ) ;
#233238=CIRCLE ( 'NONE', #241579, 0.1000000000000028644 ) ;
#233245=LINE ( 'NONE', #76696, #14932 ) ;
#233254=CARTESIAN_POINT ( 'NONE',  ( -21.05000000000000426, 76.10000000001171827, -76.00017450564908472 ) ) ;
#233268=AXIS2_PLACEMENT_3D ( 'NONE', #207434, #225662, #148740 ) ;
#233335=DIRECTION ( 'NONE',  ( 1.000000000000000000, 0.000000000000000000, 0.000000000000000000 ) ) ;
#233349=EDGE_CURVE ( 'NONE', #1289, #43098, #130767, .T. ) ;
#233374=DIRECTION ( 'NONE',  ( -0.000000000000000000, -6.982962677686266711E-15, 1.000000000000000000 ) ) ;
#233376=CARTESIAN_POINT ( 'NONE',  ( 23.14999999999999503, 69.45000000001157048, -57.17310748452436542 ) ) ;
#233397=EDGE_CURVE ( 'NONE', #60411, #174912, #8270, .T. ) ;
#233460=LINE ( 'NONE', #53512, #210576 ) ;
#233501=AXIS2_PLACEMENT_3D ( 'NONE', #229199, #234313, #55644 ) ;
#233512=SPHERICAL_SURFACE ( 'NONE', #104020, 0.1000000000000000056 ) ;
#233545=EDGE_CURVE ( 'NONE', #84743, #211078, #199930, .T. ) ;
#233546=DIRECTION ( 'NONE',  ( 0.000000000000000000, 0.9908441862701605762, 0.1350103645451835310 ) ) ;
#233557=ORIENTED_EDGE ( 'NONE', *, *, #188346, .T. ) ;
#233570=ORIENTED_EDGE ( 'NONE', *, *, #110219, .T. ) ;
#233600=ORIENTED_EDGE ( 'NONE', *, *, #54019, .F. ) ;
#233610=AXIS2_PLACEMENT_3D ( 'NONE', #203597, #45808, #44536 ) ;
#233617=CARTESIAN_POINT ( 'NONE',  ( -20.94999999999999929, 74.83729825007360148, -61.52310748452433131 ) ) ;
#233633=ORIENTED_EDGE ( 'NONE', *, *, #207522, .F. ) ;
#233643=CIRCLE ( 'NONE', #382, 0.1000000000000028644 ) ;
#233650=AXIS2_PLACEMENT_3D ( 'NONE', #151946, #253572, #14994 ) ;
#233667=CARTESIAN_POINT ( 'NONE',  ( -21.07928932188134041, 69.67148334361836248, -69.62200263017875557 ) ) ;
#233673=AXIS2_PLACEMENT_3D ( 'NONE', #101137, #200296, #137733 ) ;
#233693=ORIENTED_EDGE ( 'NONE', *, *, #50614, .F. ) ;
#233700=DIRECTION ( 'NONE',  ( 0.000000000000000000, -0.9915357197604849349, 0.1298341882520056834 ) ) ;
#233746=PLANE ( 'NONE',  #194107 ) ;
#233787=DIRECTION ( 'NONE',  ( 1.000000000000000000, 0.000000000000000000, 0.000000000000000000 ) ) ;
#233849=ADVANCED_FACE ( 'NONE', ( #118293 ), #97399, .T. ) ;
#233877=CIRCLE ( 'NONE', #9025, 0.09999999999999939493 ) ;
#233898=EDGE_CURVE ( 'NONE', #223761, #1074, #236947, .T. ) ;
#233933=AXIS2_PLACEMENT_3D ( 'NONE', #114390, #72727, #167980 ) ;
#233936=VERTEX_POINT ( 'NONE', #243358 ) ;
#233951=FACE_OUTER_BOUND ( 'NONE', #167953, .T. ) ;
#234004=ORIENTED_EDGE ( 'NONE', *, *, #78483, .T. ) ;
#234006=ORIENTED_EDGE ( 'NONE', *, *, #134739, .T. ) ;
#234011=ADVANCED_FACE ( 'NONE', ( #127273 ), #45162, .F. ) ;
#234014=DIRECTION ( 'NONE',  ( 0.000000000000000000, -1.000000000000000000, 0.000000000000000000 ) ) ;
#234022=CARTESIAN_POINT ( 'NONE',  ( 23.14999999999999858, 76.00000000001142553, -36.02310748452432421 ) ) ;
#234044=ADVANCED_FACE ( 'NONE', ( #69887 ), #34610, .T. ) ;
#234061=EDGE_CURVE ( 'NONE', #162902, #69280, #110263, .T. ) ;
#234065=DIRECTION ( 'NONE',  ( 1.000000000000000000, 0.000000000000000000, 0.000000000000000000 ) ) ;
#234086=DIRECTION ( 'NONE',  ( 0.000000000000000000, -0.4930308989875170078, -0.8700118002898356018 ) ) ;
#234099=DIRECTION ( 'NONE',  ( 1.000000000000000000, 0.000000000000000000, 0.000000000000000000 ) ) ;
#234112=DIRECTION ( 'NONE',  ( 0.000000000000000000, -1.000000000000000000, -6.982962677686265922E-15 ) ) ;
#234133=EDGE_CURVE ( 'NONE', #94397, #65824, #131113, .T. ) ;
#234141=EDGE_CURVE ( 'NONE', #28771, #160136, #117076, .T. ) ;
#234149=EDGE_LOOP ( 'NONE', ( #37057, #172125 ) ) ;
#234159=EDGE_CURVE ( 'NONE', #97848, #73365, #50280, .T. ) ;
#234160=CARTESIAN_POINT ( 'NONE',  ( -18.59999999999999787, 66.65000000001157332, -57.17310748452438673 ) ) ;
#234186=FACE_OUTER_BOUND ( 'NONE', #24334, .T. ) ;
#234206=LINE ( 'NONE', #232961, #157745 ) ;
#234213=ORIENTED_EDGE ( 'NONE', *, *, #82305, .T. ) ;
#234225=AXIS2_PLACEMENT_3D ( 'NONE', #196906, #117381, #217739 ) ;
#234241=DIRECTION ( 'NONE',  ( -1.000000000000000000, 0.000000000000000000, 0.000000000000000000 ) ) ;
#234247=CARTESIAN_POINT ( 'NONE',  ( 20.85000000000000142, 75.83895117929270668, -36.30729732888454464 ) ) ;
#234256=ORIENTED_EDGE ( 'NONE', *, *, #186548, .F. ) ;
#234258=CIRCLE ( 'NONE', #9408, 2.000000000000001776 ) ;
#234313=DIRECTION ( 'NONE',  ( 1.000000000000000000, 0.000000000000000000, 0.000000000000000000 ) ) ;
#234344=DIRECTION ( 'NONE',  ( 0.000000000000000000, 0.000000000000000000, 1.000000000000000000 ) ) ;
#234345=VERTEX_POINT ( 'NONE', #61861 ) ;
#234367=DIRECTION ( 'NONE',  ( 0.000000000000000000, -7.272083257015735086E-15, 1.000000000000000000 ) ) ;
#234382=ORIENTED_EDGE ( 'NONE', *, *, #123322, .T. ) ;
#234414=AXIS2_PLACEMENT_3D ( 'NONE', #61100, #4946, #42829 ) ;
#234438=AXIS2_PLACEMENT_3D ( 'NONE', #82817, #157285, #102382 ) ;
#234469=DIRECTION ( 'NONE',  ( 0.000000000000000000, 0.000000000000000000, 1.000000000000000000 ) ) ;
#234494=VERTEX_POINT ( 'NONE', #39154 ) ;
#234496=CARTESIAN_POINT ( 'NONE',  ( -18.54270223418607699, 85.62410550289428102, -29.28217243411683413 ) ) ;
#234502=CARTESIAN_POINT ( 'NONE',  ( -18.44204374631838661, 85.49103638960970386, -29.39690621430322892 ) ) ;
#234553=ADVANCED_FACE ( 'NONE', ( #255554 ), #242761, .T. ) ;
#234570=ORIENTED_EDGE ( 'NONE', *, *, #115307, .F. ) ;
#234592=EDGE_LOOP ( 'NONE', ( #82460, #120635, #133550, #103369 ) ) ;
#234593=ORIENTED_EDGE ( 'NONE', *, *, #127464, .T. ) ;
#234628=FACE_OUTER_BOUND ( 'NONE', #206963, .T. ) ;
#234632=EDGE_CURVE ( 'NONE', #105159, #166958, #127658, .T. ) ;
#234662=AXIS2_PLACEMENT_3D ( 'NONE', #156725, #95432, #94138 ) ;
#234690=ADVANCED_FACE ( 'NONE', ( #7719 ), #147214, .F. ) ;
#234691=AXIS2_PLACEMENT_3D ( 'NONE', #26934, #185978, #84251 ) ;
#234708=CARTESIAN_POINT ( 'NONE',  ( -18.50000000000000000, 64.35000000001157616, -57.37310748452439668 ) ) ;
#234711=CYLINDRICAL_SURFACE ( 'NONE', #76076, 0.09999999999999939493 ) ;
#234712=ORIENTED_EDGE ( 'NONE', *, *, #80848, .T. ) ;
#234718=VERTEX_POINT ( 'NONE', #29865 ) ;
#234727=DIRECTION ( 'NONE',  ( 0.000000000000000000, 6.982962677686266711E-15, -1.000000000000000000 ) ) ;
#234736=CARTESIAN_POINT ( 'NONE',  ( 20.94999675878240808, 65.70692517833182933, -30.56446533783036656 ) ) ;
#234758=ORIENTED_EDGE ( 'NONE', *, *, #15429, .T. ) ;
#234776=VECTOR ( 'NONE', #14486, 1000.000000000000000 ) ;
#234798=ORIENTED_EDGE ( 'NONE', *, *, #227198, .F. ) ;
#234805=EDGE_LOOP ( 'NONE', ( #136200, #138723, #97361, #161797, #249047, #12951, #68839, #1966, #4931, #109269, #224373 ) ) ;
#234807=ORIENTED_EDGE ( 'NONE', *, *, #143009, .T. ) ;
#234821=VERTEX_POINT ( 'NONE', #133738 ) ;
#234823=ORIENTED_EDGE ( 'NONE', *, *, #233397, .F. ) ;
#234825=CARTESIAN_POINT ( 'NONE',  ( -18.49499033040906326, 85.43814877175627487, -62.32495425860083316 ) ) ;
#234830=DIRECTION ( 'NONE',  ( 0.000000000000000000, -6.982962677686266711E-15, 1.000000000000000000 ) ) ;
#234860=CIRCLE ( 'NONE', #226442, 0.1000000000000009492 ) ;
#234912=EDGE_LOOP ( 'NONE', ( #194595, #138000, #90748, #201644 ) ) ;
#234914=CIRCLE ( 'NONE', #84839, 0.1999999999999987899 ) ;
#234919=CARTESIAN_POINT ( 'NONE',  ( 18.50000000000000000, 86.35479209693686187, -42.26656650145049099 ) ) ;
#234987=CARTESIAN_POINT ( 'NONE',  ( 20.94999999999999929, 77.83585931145498193, -24.51866831572578320 ) ) ;
#234996=CARTESIAN_POINT ( 'NONE',  ( 21.05000000000000071, 75.90220970870291239, -75.78092209500044873 ) ) ;
#235027=LINE ( 'NONE', #152952, #249964 ) ;
#235043=EDGE_LOOP ( 'NONE', ( #207092, #148615, #30519 ) ) ;
#235078=ADVANCED_FACE ( 'NONE', ( #147887 ), #228718, .F. ) ;
#235100=ORIENTED_EDGE ( 'NONE', *, *, #12814, .F. ) ;
#235105=DIRECTION ( 'NONE',  ( 1.000000000000000000, 0.000000000000000000, 0.000000000000000000 ) ) ;
#235108=VERTEX_POINT ( 'NONE', #86586 ) ;
#235116=DIRECTION ( 'NONE',  ( 1.000000000000000000, 7.304098846218134667E-16, 4.639676173203993355E-30 ) ) ;
#235133=CARTESIAN_POINT ( 'NONE',  ( 21.04999999999987281, 67.10527618163379771, -61.03602316137499884 ) ) ;
#235139=EDGE_LOOP ( 'NONE', ( #48302, #32015, #45437, #166067 ) ) ;
#235168=EDGE_CURVE ( 'NONE', #221002, #84841, #50385, .T. ) ;
#235200=DIRECTION ( 'NONE',  ( -7.304098846218134667E-16, 1.000000000000000000, 6.982962677686267499E-15 ) ) ;
#235202=EDGE_CURVE ( 'NONE', #208753, #68040, #187808, .T. ) ;
#235212=DIRECTION ( 'NONE',  ( -0.000000000000000000, 1.000000000000000000, 6.982962677686266711E-15 ) ) ;
#235223=CARTESIAN_POINT ( 'NONE',  ( -23.15000000000000213, 73.40000000001172964, -81.27310748452434552 ) ) ;
#235246=CARTESIAN_POINT ( 'NONE',  ( 18.59999999999999076, 77.16412189325258453, -28.10825939895270764 ) ) ;
#235280=EDGE_LOOP ( 'NONE', ( #114158, #162303, #108460, #69594 ) ) ;
#235285=EDGE_CURVE ( 'NONE', #192913, #226817, #158589, .T. ) ;
#235286=ORIENTED_EDGE ( 'NONE', *, *, #79942, .T. ) ;
#235301=DIRECTION ( 'NONE',  ( -4.408576920032447355E-17, -0.1350103645451945777, 0.9908441862701589109 ) ) ;
#235307=EDGE_CURVE ( 'NONE', #68363, #43683, #219387, .T. ) ;
#235318=DIRECTION ( 'NONE',  ( 0.000000000000000000, -1.000000000000000000, 0.000000000000000000 ) ) ;
#235345=DIRECTION ( 'NONE',  ( 1.000000000000000000, 0.000000000000000000, 0.000000000000000000 ) ) ;
#235369=VECTOR ( 'NONE', #241093, 1000.000000000000000 ) ;
#235372=ADVANCED_FACE ( 'NONE', ( #61615 ), #166982, .T. ) ;
#235374=CARTESIAN_POINT ( 'NONE',  ( 21.14999999999999503, 76.00000000001169553, -75.77310748452431710 ) ) ;
#235453=AXIS2_PLACEMENT_3D ( 'NONE', #166932, #146036, #123932 ) ;
#235467=VERTEX_POINT ( 'NONE', #116161 ) ;
#235475=ORIENTED_EDGE ( 'NONE', *, *, #56990, .F. ) ;
#235482=CARTESIAN_POINT ( 'NONE',  ( 21.05000000000000071, 69.50331341424364950, -69.50845136601148511 ) ) ;
#235506=DIRECTION ( 'NONE',  ( 0.000000000000000000, 0.000000000000000000, 1.000000000000000000 ) ) ;
#235548=VECTOR ( 'NONE', #28161, 1000.000000000000000 ) ;
#235640=CARTESIAN_POINT ( 'NONE',  ( 18.49999999999999289, 69.35000000001151932, -48.37310748452436826 ) ) ;
#235643=AXIS2_PLACEMENT_3D ( 'NONE', #56494, #13552, #31850 ) ;
#235662=CARTESIAN_POINT ( 'NONE',  ( 20.21494484322215968, 66.69682926214275653, -61.18284229275413821 ) ) ;
#235667=CARTESIAN_POINT ( 'NONE',  ( -21.14999999999999858, 64.25000000001161027, -62.73924182154625129 ) ) ;
#235681=CARTESIAN_POINT ( 'NONE',  ( -18.50000000000000000, 74.13328508995425636, -57.77043223824233564 ) ) ;
#235683=CARTESIAN_POINT ( 'NONE',  ( -21.52071067811865746, 68.22071067813021727, -57.17310748452437963 ) ) ;
#235712=ADVANCED_FACE ( 'NONE', ( #161714 ), #80250, .T. ) ;
#235717=AXIS2_PLACEMENT_3D ( 'NONE', #128711, #208254, #71319 ) ;
#235718=FACE_OUTER_BOUND ( 'NONE', #55663, .T. ) ;
#235725=ORIENTED_EDGE ( 'NONE', *, *, #241334, .T. ) ;
#235742=ORIENTED_EDGE ( 'NONE', *, *, #255069, .T. ) ;
#235744=LINE ( 'NONE', #79223, #201852 ) ;
#235756=EDGE_CURVE ( 'NONE', #86585, #180491, #154464, .T. ) ;
#235765=AXIS2_PLACEMENT_3D ( 'NONE', #80836, #182545, #199547 ) ;
#235771=EDGE_CURVE ( 'NONE', #178818, #4626, #176005, .T. ) ;
#235789=DIRECTION ( 'NONE',  ( -0.000000000000000000, -6.982962677686266711E-15, 1.000000000000000000 ) ) ;
#235807=FACE_OUTER_BOUND ( 'NONE', #209649, .T. ) ;
#235808=PLANE ( 'NONE',  #37871 ) ;
#235816=ORIENTED_EDGE ( 'NONE', *, *, #16877, .F. ) ;
#235817=EDGE_CURVE ( 'NONE', #142182, #64792, #125144, .T. ) ;
#235849=ORIENTED_EDGE ( 'NONE', *, *, #187557, .F. ) ;
#235870=AXIS2_PLACEMENT_3D ( 'NONE', #36240, #115751, #195318 ) ;
#235875=FACE_OUTER_BOUND ( 'NONE', #175949, .T. ) ;
#235880=VERTEX_POINT ( 'NONE', #65145 ) ;
#235881=ORIENTED_EDGE ( 'NONE', *, *, #9299, .T. ) ;
#235897=ORIENTED_EDGE ( 'NONE', *, *, #252395, .T. ) ;
#235916=DIRECTION ( 'NONE',  ( 0.000000000000000000, -0.4930308989875575865, -0.8700118002898125091 ) ) ;
#235930=CARTESIAN_POINT ( 'NONE',  ( 18.59999999999999787, 76.00000000001165290, -69.52310748452431710 ) ) ;
#235942=DIRECTION ( 'NONE',  ( 0.000000000000000000, -1.000000000000000000, -6.982962677686265922E-15 ) ) ;
#235945=CARTESIAN_POINT ( 'NONE',  ( 20.95512820512820440, 67.12384868372339497, -48.27310748452438105 ) ) ;
#235946=DIRECTION ( 'NONE',  ( 0.000000000000000000, -1.000000000000000000, -6.982962677686266711E-15 ) ) ;
#235952=CARTESIAN_POINT ( 'NONE',  ( 21.04999999999999716, 65.31569084252653568, -61.99641069419754302 ) ) ;
#235959=AXIS2_PLACEMENT_3D ( 'NONE', #98451, #257510, #196306 ) ;
#235988=PRODUCT_CONTEXT ( 'NONE', #114050, 'mechanical' ) ;
#236020=CIRCLE ( 'NONE', #119511, 0.2000000000000057288 ) ;
#236031=CARTESIAN_POINT ( 'NONE',  ( -20.85000000000000142, 69.15387683765879956, -32.28538121767450519 ) ) ;
#236067=AXIS2_PLACEMENT_3D ( 'NONE', #205233, #69611, #87845 ) ;
#236082=DIRECTION ( 'NONE',  ( -1.000000000000000000, 0.000000000000000000, 0.000000000000000000 ) ) ;
#236104=ORIENTED_EDGE ( 'NONE', *, *, #10280, .T. ) ;
#236115=CIRCLE ( 'NONE', #11069, 0.09999999999999939493 ) ;
#236136=ADVANCED_FACE ( 'NONE', ( #6131 ), #247397, .T. ) ;
#236140=TOROIDAL_SURFACE ( 'NONE', #252693, 11.89999999999999858, 0.1000000000000000056 ) ;
#236161=CARTESIAN_POINT ( 'NONE',  ( 18.59999999999999787, 77.83534155023598089, -57.96795619196132776 ) ) ;
#236169=CARTESIAN_POINT ( 'NONE',  ( 20.94999999999999929, 76.00000000001165290, -69.52310748452431710 ) ) ;
#236197=CIRCLE ( 'NONE', #252949, 0.09999999999999939493 ) ;
#236200=VECTOR ( 'NONE', #122357, 1000.000000000000000 ) ;
#236215=CARTESIAN_POINT ( 'NONE',  ( -20.54999999999999716, 68.85000000001151932, -48.37310748452436826 ) ) ;
#236223=CIRCLE ( 'NONE', #207204, 0.1000000000000028644 ) ;
#236257=CARTESIAN_POINT ( 'NONE',  ( -22.47071067811865319, 68.27992525551360359, -69.62219993922698791 ) ) ;
#236266=DIRECTION ( 'NONE',  ( -1.000000000000000000, -0.000000000000000000, -0.000000000000000000 ) ) ;
#236275=VECTOR ( 'NONE', #101405, 1000.000000000000114 ) ;
#236280=CARTESIAN_POINT ( 'NONE',  ( -23.15000000000000213, 64.35000000001173248, -81.27310748452440237 ) ) ;
#236292=CARTESIAN_POINT ( 'NONE',  ( -22.50000000000000000, 64.25000000001165290, -69.52310748452438816 ) ) ;
#236309=ORIENTED_EDGE ( 'NONE', *, *, #24637, .T. ) ;
#236328=CARTESIAN_POINT ( 'NONE',  ( -21.05000000000000071, 74.83729825007360148, -61.52310748452433131 ) ) ;
#236337=CARTESIAN_POINT ( 'NONE',  ( -21.14999999999999858, 76.10000000001170406, -76.06376443622556849 ) ) ;
#236350=LINE ( 'NONE', #137247, #238526 ) ;
#236373=ORIENTED_EDGE ( 'NONE', *, *, #46844, .F. ) ;
#236439=LINE ( 'NONE', #198595, #135404 ) ;
#236450=CIRCLE ( 'NONE', #190701, 0.09999999999999939493 ) ;
#236460=CARTESIAN_POINT ( 'NONE',  ( 18.49999999999999645, 76.00000000001142553, -36.02310748452432421 ) ) ;
#236526=ORIENTED_EDGE ( 'NONE', *, *, #95372, .T. ) ;
#236547=SPHERICAL_SURFACE ( 'NONE', #219287, 0.1000000000000000056 ) ;
#236558=ORIENTED_EDGE ( 'NONE', *, *, #189520, .T. ) ;
#236560=ORIENTED_EDGE ( 'NONE', *, *, #91877, .F. ) ;
#236587=ORIENTED_EDGE ( 'NONE', *, *, #15182, .F. ) ;
#236619=ORIENTED_EDGE ( 'NONE', *, *, #256570, .F. ) ;
#236621=DIRECTION ( 'NONE',  ( 0.000000000000000000, 7.116814260417668513E-15, -1.000000000000000000 ) ) ;
#236672=EDGE_LOOP ( 'NONE', ( #184699, #30407, #135458 ) ) ;
#236675=VECTOR ( 'NONE', #40742, 1000.000000000000000 ) ;
#236683=EDGE_LOOP ( 'NONE', ( #49420, #219891, #124521, #35120 ) ) ;
#236708=DIRECTION ( 'NONE',  ( -1.000000000000000000, 0.000000000000000000, 0.000000000000000000 ) ) ;
#236713=VERTEX_POINT ( 'NONE', #157929 ) ;
#236765=CARTESIAN_POINT ( 'NONE',  ( 21.13422380239051535, 69.50667348520610744, -69.52310748452435973 ) ) ;
#236818=EDGE_CURVE ( 'NONE', #47775, #79119, #18645, .T. ) ;
#236829=ORIENTED_EDGE ( 'NONE', *, *, #142375, .T. ) ;
#236832=EDGE_CURVE ( 'NONE', #75472, #212207, #93657, .T. ) ;
#236854=ADVANCED_FACE ( 'NONE', ( #88589 ), #86008, .T. ) ;
#236856=DIRECTION ( 'NONE',  ( 0.000000000000000000, -6.982962677686266711E-15, 1.000000000000000000 ) ) ;
#236889=DIRECTION ( 'NONE',  ( 0.000000000000000000, -0.9915357197604849349, 0.1298341882520056834 ) ) ;
#236929=CARTESIAN_POINT ( 'NONE',  ( 20.85000000000000142, 77.73670573947892137, -24.50568489690058627 ) ) ;
#236938=CIRCLE ( 'NONE', #32791, 4.049999999999998046 ) ;
#236942=EDGE_CURVE ( 'NONE', #224921, #169291, #143539, .T. ) ;
#236947=LINE ( 'NONE', #38755, #169 ) ;
#236962=CARTESIAN_POINT ( 'NONE',  ( 20.30466543256828160, 66.69576306075612138, -61.26944483313238976 ) ) ;
#236993=CARTESIAN_POINT ( 'NONE',  ( -18.39999999999999858, 85.68240343348777799, -29.36626410711146562 ) ) ;
#237026=VERTEX_POINT ( 'NONE', #110736 ) ;
#237042=DIRECTION ( 'NONE',  ( 0.000000000000000000, -7.086529944415894657E-15, 1.000000000000000000 ) ) ;
#237051=CARTESIAN_POINT ( 'NONE',  ( 20.85000000000000142, 76.00000000001136868, -28.22310748452431994 ) ) ;
#237056=ORIENTED_EDGE ( 'NONE', *, *, #40008, .T. ) ;
#237058=CARTESIAN_POINT ( 'NONE',  ( 21.05000000000000071, 85.50000000001149658, -45.91707660717669626 ) ) ;
#237063=ORIENTED_EDGE ( 'NONE', *, *, #125190, .F. ) ;
#237076=CARTESIAN_POINT ( 'NONE',  ( -18.58735405345342429, 85.56647862034795082, -29.20039283825829202 ) ) ;
#237078=CARTESIAN_POINT ( 'NONE',  ( -21.05000000000000426, 76.02103547655181615, -75.82756330647198695 ) ) ;
#237104=DIRECTION ( 'NONE',  ( 0.000000000000000000, 0.000000000000000000, 1.000000000000000000 ) ) ;
#237137=CARTESIAN_POINT ( 'NONE',  ( -20.94999999999999929, 65.70711192142317714, -30.56510546851222188 ) ) ;
#237144=DIRECTION ( 'NONE',  ( 0.000000000000000000, 6.938893903907234689E-15, -1.000000000000000000 ) ) ;
#237166=CARTESIAN_POINT ( 'NONE',  ( -21.05000000000000071, 77.83534155023598089, -57.86795619196132634 ) ) ;
#237184=ORIENTED_EDGE ( 'NONE', *, *, #629, .T. ) ;
#237186=EDGE_LOOP ( 'NONE', ( #41523, #138040, #198485, #253707, #72971, #17608, #89227 ) ) ;
#237194=DIRECTION ( 'NONE',  ( 0.000000000000000000, -6.454785026890385471E-15, 1.000000000000000000 ) ) ;
#237229=ORIENTED_EDGE ( 'NONE', *, *, #223491, .T. ) ;
#237236=ORIENTED_EDGE ( 'NONE', *, *, #91786, .T. ) ;
#237245=CARTESIAN_POINT ( 'NONE',  ( -20.94999999999999929, 74.14897176987071248, -57.86919421510183525 ) ) ;
#237256=DIRECTION ( 'NONE',  ( 0.000000000000000000, -6.454785026890510900E-15, 1.000000000000000000 ) ) ;
#237257=VECTOR ( 'NONE', #87840, 1000.000000000000000 ) ;
#237269=CIRCLE ( 'NONE', #124835, 0.4000000000000045186 ) ;
#237277=EDGE_CURVE ( 'NONE', #150112, #246301, #81326, .T. ) ;
#237282=DIRECTION ( 'NONE',  ( -0.000000000000000000, 1.000000000000000000, 6.982962677686267499E-15 ) ) ;
#237285=EDGE_CURVE ( 'NONE', #235467, #241008, #127427, .T. ) ;
#237312=DIRECTION ( 'NONE',  ( 1.000000000000000000, 0.000000000000000000, 0.000000000000000000 ) ) ;
#237320=CARTESIAN_POINT ( 'NONE',  ( 21.14250536705908345, 69.48182782313092787, -69.52310748452435973 ) ) ;
#237338=CIRCLE ( 'NONE', #8207, 0.1999999999999987899 ) ;
#237349=CARTESIAN_POINT ( 'NONE',  ( 18.59999999999999076, 77.85161776048025217, -24.41991776492064758 ) ) ;
#237363=EDGE_LOOP ( 'NONE', ( #153589, #80489, #68132 ) ) ;
#237396=CARTESIAN_POINT ( 'NONE',  ( -23.15000000000000213, 74.00000000001156764, -56.29848556176223440 ) ) ;
#237401=DIRECTION ( 'NONE',  ( 0.000000000000000000, -6.982962677686266711E-15, 1.000000000000000000 ) ) ;
#237422=DIRECTION ( 'NONE',  ( 0.000000000000000000, -7.056502275159890832E-15, 1.000000000000000000 ) ) ;
#237437=ORIENTED_EDGE ( 'NONE', *, *, #223551, .F. ) ;
#237507=ORIENTED_EDGE ( 'NONE', *, *, #144720, .T. ) ;
#237522=AXIS2_PLACEMENT_3D ( 'NONE', #70865, #229905, #193364 ) ;
#237546=FACE_OUTER_BOUND ( 'NONE', #236683, .T. ) ;
#237551=VECTOR ( 'NONE', #96597, 1000.000000000000000 ) ;
#237565=ORIENTED_EDGE ( 'NONE', *, *, #103608, .F. ) ;
#237581=AXIS2_PLACEMENT_3D ( 'NONE', #75225, #114323, #12684 ) ;
#237601=ORIENTED_EDGE ( 'NONE', *, *, #183091, .F. ) ;
#237602=LINE ( 'NONE', #38127, #18009 ) ;
#237629=LINE ( 'NONE', #19875, #236675 ) ;
#237634=EDGE_CURVE ( 'NONE', #171475, #142182, #106457, .T. ) ;
#237718=ORIENTED_EDGE ( 'NONE', *, *, #57178, .T. ) ;
#237727=CARTESIAN_POINT ( 'NONE',  ( -18.52186455168989454, 85.48101848145425663, -62.49809100660993977 ) ) ;
#237734=EDGE_LOOP ( 'NONE', ( #24807, #144341, #128926, #103712 ) ) ;
#237747=DIRECTION ( 'NONE',  ( -1.000000000000000000, 3.265361837132813093E-16, 2.280189983783949500E-30 ) ) ;
#237772=EDGE_CURVE ( 'NONE', #160483, #118763, #135703, .T. ) ;
#237773=ORIENTED_EDGE ( 'NONE', *, *, #76310, .T. ) ;
#237780=CARTESIAN_POINT ( 'NONE',  ( 21.05000000000000071, 71.14953271029189352, -48.05737489352603120 ) ) ;
#237790=ORIENTED_EDGE ( 'NONE', *, *, #152958, .F. ) ;
#237809=DIRECTION ( 'NONE',  ( 0.000000000000000000, -8.556632174375002828E-15, 1.000000000000000000 ) ) ;
#237833=VECTOR ( 'NONE', #151956, 1000.000000000000000 ) ;
#237837=CARTESIAN_POINT ( 'NONE',  ( -21.05000000000000071, 70.15000000001163016, -59.39061026024639744 ) ) ;
#237851=CARTESIAN_POINT ( 'NONE',  ( -23.15000000000000213, 85.50000000001149658, -45.91707660717669626 ) ) ;
#237862=EDGE_CURVE ( 'NONE', #172081, #224073, #144938, .T. ) ;
#237867=AXIS2_PLACEMENT_3D ( 'NONE', #201666, #182116, #163837 ) ;
#237873=DIRECTION ( 'NONE',  ( -1.000000000000000000, 0.000000000000000000, 0.000000000000000000 ) ) ;
#237879=DIRECTION ( 'NONE',  ( 0.000000000000000000, 1.000000000000000000, 6.938893903907222067E-15 ) ) ;
#237938=ADVANCED_FACE ( 'NONE', ( #30169 ), #113533, .F. ) ;
#237940=ORIENTED_EDGE ( 'NONE', *, *, #107191, .F. ) ;
#237983=ADVANCED_FACE ( 'NONE', ( #155263 ), #134359, .F. ) ;
#238007=DIRECTION ( 'NONE',  ( 1.000000000000000000, 0.000000000000000000, 0.000000000000000000 ) ) ;
#238009=AXIS2_PLACEMENT_3D ( 'NONE', #88431, #248834, #166755 ) ;
#238044=DIRECTION ( 'NONE',  ( 1.000000000000000000, -2.952720810173289112E-16, -2.061873921506763405E-30 ) ) ;
#238085=ORIENTED_EDGE ( 'NONE', *, *, #242558, .F. ) ;
#238133=CARTESIAN_POINT ( 'NONE',  ( 21.14999999999999503, 87.65000000001172964, -81.27310748452423184 ) ) ;
#238155=EDGE_LOOP ( 'NONE', ( #255746, #191289, #173824, #208195 ) ) ;
#238185=DIRECTION ( 'NONE',  ( 0.000000000000000000, 0.000000000000000000, 1.000000000000000000 ) ) ;
#238186=VERTEX_POINT ( 'NONE', #124393 ) ;
#238193=EDGE_LOOP ( 'NONE', ( #37181, #198101, #212111, #57759 ) ) ;
#238197=EDGE_LOOP ( 'NONE', ( #105154, #226387, #115604, #11654, #102096 ) ) ;
#238213=VERTEX_POINT ( 'NONE', #141367 ) ;
#238214=AXIS2_PLACEMENT_3D ( 'NONE', #230544, #31091, #109284 ) ;
#238227=ORIENTED_EDGE ( 'NONE', *, *, #253562, .F. ) ;
#238235=CARTESIAN_POINT ( 'NONE',  ( 20.52683494730046476, 67.01946918171023526, -61.01785476198719493 ) ) ;
#238240=DIRECTION ( 'NONE',  ( -1.000000000000000000, -9.012599976027990443E-15, -6.882867235861669241E-14 ) ) ;
#238246=( BOUNDED_CURVE ( )  B_SPLINE_CURVE ( 3, ( #57641, #58909, #17264, #35559 ),
 .UNSPECIFIED., .F., .F. ) 
 B_SPLINE_CURVE_WITH_KNOTS ( ( 4, 4 ),
 ( 4.937700262164173333E-15, 1.570796326794912323 ),
 .UNSPECIFIED. ) 
 CURVE ( )  GEOMETRIC_REPRESENTATION_ITEM ( )  RATIONAL_B_SPLINE_CURVE ( ( 1.000000000000000000, 0.8047378541243623840, 0.8047378541243623840, 1.000000000000000000 ) ) 
 REPRESENTATION_ITEM ( '' )  );
#238291=CARTESIAN_POINT ( 'NONE',  ( -20.64999999999999858, 74.00000000001156764, -56.29848556176223440 ) ) ;
#238319=EDGE_CURVE ( 'NONE', #93396, #80057, #177629, .T. ) ;
#238321=EDGE_CURVE ( 'NONE', #234821, #212829, #252023, .T. ) ;
#238339=EDGE_CURVE ( 'NONE', #161837, #57945, #72127, .T. ) ;
#238344=DIRECTION ( 'NONE',  ( 0.000000000000000000, 0.000000000000000000, -1.000000000000000000 ) ) ;
#238353=CARTESIAN_POINT ( 'NONE',  ( -18.48408745364680072, 85.66432225867450256, -29.34002895119592225 ) ) ;
#238356=DIRECTION ( 'NONE',  ( 1.734723475976817507E-14, -6.982962677686266711E-15, 1.000000000000000000 ) ) ;
#238366=FACE_OUTER_BOUND ( 'NONE', #212267, .T. ) ;
#238378=ORIENTED_EDGE ( 'NONE', *, *, #4383, .T. ) ;
#238385=EDGE_CURVE ( 'NONE', #192458, #113184, #98430, .T. ) ;
#238468=DIRECTION ( 'NONE',  ( 0.000000000000000000, -0.9876197685951263461, 0.1568667991644794590 ) ) ;
#238482=LINE ( 'NONE', #160263, #33004 ) ;
#238490=ORIENTED_EDGE ( 'NONE', *, *, #253635, .F. ) ;
#238501=CARTESIAN_POINT ( 'NONE',  ( 21.07016717456946253, 69.67905916191141102, -69.52310748452435973 ) ) ;
#238508=AXIS2_PLACEMENT_3D ( 'NONE', #66165, #145687, #225212 ) ;
#238526=VECTOR ( 'NONE', #74754, 1000.000000000000000 ) ;
#238534=EDGE_CURVE ( 'NONE', #248043, #179727, #61057, .T. ) ;
#238555=AXIS2_PLACEMENT_3D ( 'NONE', #61731, #452, #201230 ) ;
#238558=LINE ( 'NONE', #122481, #21236 ) ;
#238588=CARTESIAN_POINT ( 'NONE',  ( 18.50596464788227280, 65.69367753730605841, -30.51892380663480253 ) ) ;
#238616=CARTESIAN_POINT ( 'NONE',  ( 18.41832399655374175, 85.68240326668549756, -29.36626386449693982 ) ) ;
#238625=CARTESIAN_POINT ( 'NONE',  ( 20.94999999999999929, 74.63912941281955682, -61.45010955743337178 ) ) ;
#238640=CARTESIAN_POINT ( 'NONE',  ( 23.14999999999999503, 64.35000000001150511, -48.27310748452440237 ) ) ;
#238667=AXIS2_PLACEMENT_3D ( 'NONE', #135943, #193391, #151711 ) ;
#238673=CIRCLE ( 'NONE', #92909, 4.099999999999999645 ) ;
#238721=CARTESIAN_POINT ( 'NONE',  ( 20.94999999999999574, 74.16465844978715438, -57.96795619196134908 ) ) ;
#238726=VERTEX_POINT ( 'NONE', #87495 ) ;
#238737=EDGE_CURVE ( 'NONE', #72194, #174834, #119531, .T. ) ;
#238741=FACE_OUTER_BOUND ( 'NONE', #222077, .T. ) ;
#238769=DIRECTION ( 'NONE',  ( 0.7071067811865474617, -0.7071067811865474617, -4.937700262164531476E-15 ) ) ;
#238782=AXIS2_PLACEMENT_3D ( 'NONE', #22421, #122801, #84898 ) ;
#238818=( NAMED_UNIT ( * ) PLANE_ANGLE_UNIT ( ) SI_UNIT ( $, .RADIAN. ) );
#238876=LINE ( 'NONE', #104467, #181570 ) ;
#238879=ORIENTED_EDGE ( 'NONE', *, *, #190744, .T. ) ;
#238885=AXIS2_PLACEMENT_3D ( 'NONE', #160907, #37115, #137455 ) ;
#238907=EDGE_LOOP ( 'NONE', ( #31688, #103391, #85386, #15840 ) ) ;
#238923=CIRCLE ( 'NONE', #68035, 0.3999999999999975797 ) ;
#238953=LINE ( 'NONE', #103256, #35790 ) ;
#238956=EDGE_LOOP ( 'NONE', ( #154091, #171393, #72849, #126957 ) ) ;
#238984=DIRECTION ( 'NONE',  ( 1.000000000000000000, 0.000000000000000000, 0.000000000000000000 ) ) ;
#238988=CIRCLE ( 'NONE', #126559, 0.09999999999999939493 ) ;
#238989=VERTEX_POINT ( 'NONE', #104185 ) ;
#239015=CIRCLE ( 'NONE', #59927, 7.800000000000001599 ) ;
#239021=ORIENTED_EDGE ( 'NONE', *, *, #231527, .T. ) ;
#239067=CARTESIAN_POINT ( 'NONE',  ( 20.94999999999999929, 77.83534155023599510, -57.96795619196132776 ) ) ;
#239074=VERTEX_POINT ( 'NONE', #61226 ) ;
#239090=DIRECTION ( 'NONE',  ( 0.000000000000000000, 1.000000000000000000, 6.938893903907222067E-15 ) ) ;
#239109=DIRECTION ( 'NONE',  ( -0.000000000000000000, 7.272083257015735086E-15, -1.000000000000000000 ) ) ;
#239131=CARTESIAN_POINT ( 'NONE',  ( -20.54999999999999361, 64.35000000001150511, -48.17310748452440095 ) ) ;
#239161=DIRECTION ( 'NONE',  ( -2.940209281316621016E-16, -1.000000000000000000, -5.880418562633242623E-15 ) ) ;
#239177=CARTESIAN_POINT ( 'NONE',  ( 21.05000000000000071, 85.00000000001159606, -59.62913836187181715 ) ) ;
#239180=CARTESIAN_POINT ( 'NONE',  ( 22.49999999999999645, 64.35042919246686210, -69.62310748452439668 ) ) ;
#239192=DIRECTION ( 'NONE',  ( 5.603264701231745086E-32, 7.172728831056619538E-15, -1.000000000000000000 ) ) ;
#239207=CARTESIAN_POINT ( 'NONE',  ( 21.06600267594171783, 67.22483393081165559, -57.31884470214964722 ) ) ;
#239219=DIRECTION ( 'NONE',  ( 1.000000000000000000, 0.000000000000000000, 0.000000000000000000 ) ) ;
#239222=ORIENTED_EDGE ( 'NONE', *, *, #227686, .F. ) ;
#239245=EDGE_CURVE ( 'NONE', #121900, #41312, #256485, .T. ) ;
#239263=DIRECTION ( 'NONE',  ( 0.000000000000000000, -6.982962677686266711E-15, 1.000000000000000000 ) ) ;
#239280=ORIENTED_EDGE ( 'NONE', *, *, #150744, .F. ) ;
#239283=ORIENTED_EDGE ( 'NONE', *, *, #41756, .F. ) ;
#239293=DIRECTION ( 'NONE',  ( -1.000000000000000000, 2.952720810173289112E-16, 2.061873921506763405E-30 ) ) ;
#239308=DIRECTION ( 'NONE',  ( -1.000000000000000000, -0.000000000000000000, -0.000000000000000000 ) ) ;
#239362=ORIENTED_EDGE ( 'NONE', *, *, #101465, .F. ) ;
#239369=VERTEX_POINT ( 'NONE', #182157 ) ;
#239379=ORIENTED_EDGE ( 'NONE', *, *, #47004, .F. ) ;
#239390=CIRCLE ( 'NONE', #51923, 0.6000000000000033085 ) ;
#239401=FACE_OUTER_BOUND ( 'NONE', #86905, .T. ) ;
#239428=AXIS2_PLACEMENT_3D ( 'NONE', #103661, #21601, #223613 ) ;
#239445=DIRECTION ( 'NONE',  ( 0.000000000000000000, 0.1495327102803180597, 0.9887567792719412774 ) ) ;
#239453=FACE_OUTER_BOUND ( 'NONE', #168009, .T. ) ;
#239459=LINE ( 'NONE', #136474, #97602 ) ;
#239475=FACE_OUTER_BOUND ( 'NONE', #181932, .T. ) ;
#239488=CARTESIAN_POINT ( 'NONE',  ( 22.39999999999999858, 76.00000000001165290, -69.52310748452431710 ) ) ;
#239493=CIRCLE ( 'NONE', #214352, 0.1000000000000060146 ) ;
#239524=CARTESIAN_POINT ( 'NONE',  ( 21.05000000000000071, 74.16465844978715438, -57.96795619196134908 ) ) ;
#239540=VECTOR ( 'NONE', #237312, 1000.000000000000000 ) ;
#239573=EDGE_CURVE ( 'NONE', #215272, #137086, #178350, .T. ) ;
#239590=CARTESIAN_POINT ( 'NONE',  ( 22.50000000000000000, 75.90000000001172964, -81.17267829206912211 ) ) ;
#239611=EDGE_LOOP ( 'NONE', ( #164228, #177335, #251263, #75226 ) ) ;
#239624=AXIS2_PLACEMENT_3D ( 'NONE', #249192, #170980, #126664 ) ;
#239692=CARTESIAN_POINT ( 'NONE',  ( 22.39999999999999503, 75.90000000001170122, -77.31388708289770761 ) ) ;
#239695=ORIENTED_EDGE ( 'NONE', *, *, #65173, .T. ) ;
#239719=ORIENTED_EDGE ( 'NONE', *, *, #69682, .T. ) ;
#239721=AXIS2_PLACEMENT_3D ( 'NONE', #103876, #183450, #4771 ) ;
#239740=ORIENTED_EDGE ( 'NONE', *, *, #169765, .F. ) ;
#239743=DIRECTION ( 'NONE',  ( 0.000000000000000000, -1.000000000000000000, 0.000000000000000000 ) ) ;
#239745=FACE_OUTER_BOUND ( 'NONE', #168676, .T. ) ;
#239755=DIRECTION ( 'NONE',  ( -1.000000000000000000, 3.265361837132813093E-16, 2.280189983783949500E-30 ) ) ;
#239772=EDGE_CURVE ( 'NONE', #100316, #255281, #191006, .T. ) ;
#239777=ADVANCED_FACE ( 'NONE', ( #184088 ), #244054, .T. ) ;
#239787=CARTESIAN_POINT ( 'NONE',  ( -22.59999999999999787, 75.89914163091303578, -81.27267460801371612 ) ) ;
#239849=DIRECTION ( 'NONE',  ( 0.000000000000000000, 0.000000000000000000, 1.000000000000000000 ) ) ;
#239865=ORIENTED_EDGE ( 'NONE', *, *, #50584, .F. ) ;
#239883=CARTESIAN_POINT ( 'NONE',  ( 20.94999999999999929, 76.00000000001142553, -36.02310748452432421 ) ) ;
#239973=ORIENTED_EDGE ( 'NONE', *, *, #194158, .T. ) ;
#239979=EDGE_LOOP ( 'NONE', ( #247503, #11268, #235100, #190585 ) ) ;
#239983=CIRCLE ( 'NONE', #244050, 0.1000000000000028644 ) ;
#239989=ORIENTED_EDGE ( 'NONE', *, *, #103798, .F. ) ;
#239994=VECTOR ( 'NONE', #201606, 1000.000000000000000 ) ;
#239997=CARTESIAN_POINT ( 'NONE',  ( -21.59142135623730852, 68.15000000001155911, -57.27310748452437394 ) ) ;
#240008=ORIENTED_EDGE ( 'NONE', *, *, #155862, .T. ) ;
#240017=VECTOR ( 'NONE', #67656, 999.9999999999998863 ) ;
#240064=TOROIDAL_SURFACE ( 'NONE', #44439, 11.65000000000000036, 0.1000000000000000056 ) ;
#240079=EDGE_CURVE ( 'NONE', #56972, #89706, #86714, .T. ) ;
#240106=ADVANCED_FACE ( 'NONE', ( #202067 ), #138134, .F. ) ;
#240158=CYLINDRICAL_SURFACE ( 'NONE', #121121, 0.1000000000000052097 ) ;
#240161=CARTESIAN_POINT ( 'NONE',  ( -18.50000000000000000, 77.86671491006887891, -57.77043223824230722 ) ) ;
#240246=CARTESIAN_POINT ( 'NONE',  ( 23.14999999999998437, 76.00000000001165290, -69.52310748452431710 ) ) ;
#240267=ADVANCED_FACE ( 'NONE', ( #147219 ), #106798, .T. ) ;
#240274=DIRECTION ( 'NONE',  ( 0.000000000000000000, 0.000000000000000000, 1.000000000000000000 ) ) ;
#240281=B_SPLINE_CURVE_WITH_KNOTS ( 'NONE', 3,
 ( #252171, #73581, #153131, #14883, #96924, #94383, #134781, #232647, #176519, #76110 ),
 .UNSPECIFIED., .F., .F.,
 ( 4, 3, 3, 4 ),
 ( 0.000000000000000000, 0.0002000000000008536833, 0.001000000000082972495, 0.001967863649483319807 ),
 .UNSPECIFIED. ) ;
#240285=CARTESIAN_POINT ( 'NONE',  ( 21.12400222705960928, 67.22148809293440763, -57.27310748452438105 ) ) ;
#240295=EDGE_LOOP ( 'NONE', ( #153030, #193328, #164384, #76944 ) ) ;
#240309=LINE ( 'NONE', #220737, #113858 ) ;
#240314=CARTESIAN_POINT ( 'NONE',  ( -18.50000000000000000, 77.13501884592155022, -28.30613060109199353 ) ) ;
#240315=EDGE_LOOP ( 'NONE', ( #86649, #49016, #200181, #87875 ) ) ;
#240327=ORIENTED_EDGE ( 'NONE', *, *, #51696, .T. ) ;
#240347=EDGE_CURVE ( 'NONE', #199876, #165019, #170364, .T. ) ;
#240351=DIRECTION ( 'NONE',  ( -0.000000000000000000, 1.000000000000000000, 8.717686153663073805E-15 ) ) ;
#240396=DIRECTION ( 'NONE',  ( 1.000000000000000000, 0.000000000000000000, 0.000000000000000000 ) ) ;
#240401=EDGE_CURVE ( 'NONE', #214618, #65120, #136392, .T. ) ;
#240415=DIRECTION ( 'NONE',  ( 0.000000000000000000, -7.086529944415894657E-15, 1.000000000000000000 ) ) ;
#240419=DIRECTION ( 'NONE',  ( 0.000000000000000000, -6.982962677686266711E-15, 1.000000000000000000 ) ) ;
#240434=DIRECTION ( 'NONE',  ( -1.000000000000000000, 0.000000000000000000, 0.000000000000000000 ) ) ;
#240440=CIRCLE ( 'NONE', #165627, 0.1000000000000028644 ) ;
#240454=CARTESIAN_POINT ( 'NONE',  ( 18.54286124688534798, 85.62391757880919840, -29.28190515266157234 ) ) ;
#240469=ADVANCED_FACE ( 'NONE', ( #161356 ), #79212, .T. ) ;
#240493=CARTESIAN_POINT ( 'NONE',  ( 21.10710606213542206, 67.22310597611837579, -57.28211095812496723 ) ) ;
#240506=EDGE_CURVE ( 'NONE', #134285, #145606, #74502, .T. ) ;
#240518=AXIS2_PLACEMENT_3D ( 'NONE', #188987, #89869, #149880 ) ;
#240528=ORIENTED_EDGE ( 'NONE', *, *, #257436, .F. ) ;
#240535=CARTESIAN_POINT ( 'NONE',  ( -20.85000000000000142, 77.73670573947892137, -24.50568489690058627 ) ) ;
#240539=CARTESIAN_POINT ( 'NONE',  ( 18.59999999999999432, 77.16270174994961906, -61.42310748452431568 ) ) ;
#240565=AXIS2_PLACEMENT_3D ( 'NONE', #88013, #71068, #151896 ) ;
#240568=DIRECTION ( 'NONE',  ( 0.000000000000000000, 6.982962677686266711E-15, -1.000000000000000000 ) ) ;
#240578=CARTESIAN_POINT ( 'NONE',  ( -23.15000000000000213, 76.00000000001149658, -48.89810748452431710 ) ) ;
#240600=EDGE_LOOP ( 'NONE', ( #1076, #150268, #33907, #87064, #239973, #90114, #85812, #231367, #181878, #31815, #118199, #50094, #226358, #114951, #141518, #250572, #76778, #45845, #9781, #7165, #184753, #33696, #189379, #4852, #100433 ) ) ;
#240620=CARTESIAN_POINT ( 'NONE',  ( 23.15000000000000213, 85.00000000001159606, -59.62913836187181715 ) ) ;
#240634=DIRECTION ( 'NONE',  ( 0.000000000000000000, -1.000000000000000000, -6.982962677686265922E-15 ) ) ;
#240637=TOROIDAL_SURFACE ( 'NONE', #128226, 7.800000000000000711, 0.1000000000000000056 ) ;
#240648=FACE_OUTER_BOUND ( 'NONE', #123606, .T. ) ;
#240678=DIRECTION ( 'NONE',  ( -1.000000000000000000, 0.000000000000000000, 0.000000000000000000 ) ) ;
#240684=TOROIDAL_SURFACE ( 'NONE', #220020, 4.149999999999999467, 0.1000000000000000056 ) ;
#240685=ADVANCED_FACE ( 'NONE', ( #11256 ), #126043, .F. ) ;
#240769=CARTESIAN_POINT ( 'NONE',  ( -20.94999999999999929, 64.40000000001161595, -62.59490425424885274 ) ) ;
#240818=CARTESIAN_POINT ( 'NONE',  ( 20.87631937322884212, 65.52850496324762730, -61.94336160994270557 ) ) ;
#240833=CARTESIAN_POINT ( 'NONE',  ( -20.64999999999999858, 71.75000000001151079, -48.37310748452435405 ) ) ;
#240837=VECTOR ( 'NONE', #40102, 1000.000000000000000 ) ;
#240872=CARTESIAN_POINT ( 'NONE',  ( -23.15000000000000213, 76.00000000001165290, -69.52310748452431710 ) ) ;
#240881=ORIENTED_EDGE ( 'NONE', *, *, #188144, .T. ) ;
#240884=DIRECTION ( 'NONE',  ( -1.000000000000000000, 0.000000000000000000, 0.000000000000000000 ) ) ;
#240891=CARTESIAN_POINT ( 'NONE',  ( -23.15000000000000213, 85.00000000001159606, -59.62913836187181715 ) ) ;
#240899=ORIENTED_EDGE ( 'NONE', *, *, #160358, .T. ) ;
#240905=CYLINDRICAL_SURFACE ( 'NONE', #258090, 3.999999999999996447 ) ;
#240961=CARTESIAN_POINT ( 'NONE',  ( -20.94999999999999929, 76.00000000001139711, -31.92310748452432279 ) ) ;
#240970=ADVANCED_FACE ( 'NONE', ( #102302 ), #174260, .F. ) ;
#240971=AXIS2_PLACEMENT_3D ( 'NONE', #15732, #232201, #73141 ) ;
#240975=ORIENTED_EDGE ( 'NONE', *, *, #68251, .T. ) ;
#240980=CIRCLE ( 'NONE', #157826, 2.000000000000001776 ) ;
#241004=EDGE_CURVE ( 'NONE', #120848, #151382, #21537, .T. ) ;
#241008=VERTEX_POINT ( 'NONE', #144025 ) ;
#241034=DIRECTION ( 'NONE',  ( -0.000000000000000000, 1.000000000000000000, 6.982962677686267499E-15 ) ) ;
#241046=AXIS2_PLACEMENT_3D ( 'NONE', #226836, #5196, #207298 ) ;
#241049=EDGE_CURVE ( 'NONE', #256858, #89873, #30537, .T. ) ;
#241074=AXIS2_PLACEMENT_3D ( 'NONE', #43956, #120956, #222570 ) ;
#241093=DIRECTION ( 'NONE',  ( 0.000000000000000000, 6.982962677686266711E-15, -1.000000000000000000 ) ) ;
#241096=PLANE ( 'NONE',  #71690 ) ;
#241104=AXIS2_PLACEMENT_3D ( 'NONE', #32193, #153450, #135099 ) ;
#241106=CYLINDRICAL_SURFACE ( 'NONE', #21781, 11.75000000000000000 ) ;
#241110=ORIENTED_EDGE ( 'NONE', *, *, #82390, .T. ) ;
#241112=LINE ( 'NONE', #62461, #248450 ) ;
#241127=ORIENTED_EDGE ( 'NONE', *, *, #4360, .F. ) ;
#241131=VERTEX_POINT ( 'NONE', #133469 ) ;
#241190=EDGE_CURVE ( 'NONE', #134468, #188219, #214293, .T. ) ;
#241220=AXIS2_PLACEMENT_3D ( 'NONE', #48421, #28920, #203655 ) ;
#241259=ORIENTED_EDGE ( 'NONE', *, *, #54244, .T. ) ;
#241263=TOROIDAL_SURFACE ( 'NONE', #166256, 1.900000000000002576, 0.1000000000000000056 ) ;
#241277=FACE_OUTER_BOUND ( 'NONE', #174724, .T. ) ;
#241332=DIRECTION ( 'NONE',  ( 0.000000000000000000, 0.8777080977375072424, -0.4791956752371691608 ) ) ;
#241334=EDGE_CURVE ( 'NONE', #116437, #40625, #236938, .T. ) ;
#241337=ORIENTED_EDGE ( 'NONE', *, *, #110132, .T. ) ;
#241356=EDGE_CURVE ( 'NONE', #117855, #84837, #57765, .T. ) ;
#241365=DIRECTION ( 'NONE',  ( 0.000000000000000000, 0.000000000000000000, 1.000000000000000000 ) ) ;
#241375=EDGE_CURVE ( 'NONE', #17722, #25020, #141088, .T. ) ;
#241395=DIRECTION ( 'NONE',  ( -0.000000000000000000, -0.1298341882519953583, -0.9915357197604862671 ) ) ;
#241400=CARTESIAN_POINT ( 'NONE',  ( -21.00857864376268935, 64.40000000001161595, -62.59490425424883853 ) ) ;
#241408=DIRECTION ( 'NONE',  ( 0.000000000000000000, -2.139158043593750707E-15, 1.000000000000000000 ) ) ;
#241415=CARTESIAN_POINT ( 'NONE',  ( 20.12500000000000000, 66.25000000001155342, -48.37310748452438958 ) ) ;
#241435=CIRCLE ( 'NONE', #191574, 0.5000000000000004441 ) ;
#241440=ORIENTED_EDGE ( 'NONE', *, *, #110285, .F. ) ;
#241487=VERTEX_POINT ( 'NONE', #228102 ) ;
#241523=TOROIDAL_SURFACE ( 'NONE', #183260, 0.4000000000000017431, 0.1000000000000000056 ) ;
#241538=FACE_OUTER_BOUND ( 'NONE', #157143, .T. ) ;
#241541=EDGE_CURVE ( 'NONE', #159851, #208846, #103632, .T. ) ;
#241548=EDGE_LOOP ( 'NONE', ( #137669, #257509, #176632, #4238 ) ) ;
#241558=DIRECTION ( 'NONE',  ( 1.000000000000000000, 0.000000000000000000, 0.000000000000000000 ) ) ;
#241579=AXIS2_PLACEMENT_3D ( 'NONE', #139511, #75714, #217753 ) ;
#241615=ORIENTED_EDGE ( 'NONE', *, *, #64894, .T. ) ;
#241670=ORIENTED_EDGE ( 'NONE', *, *, #133617, .F. ) ;
#241681=FACE_OUTER_BOUND ( 'NONE', #95480, .T. ) ;
#241736=CARTESIAN_POINT ( 'NONE',  ( -21.07094088545368749, 75.90110629745947790, -75.84327470644144853 ) ) ;
#241750=ORIENTED_EDGE ( 'NONE', *, *, #246397, .F. ) ;
#241756=FACE_OUTER_BOUND ( 'NONE', #172766, .T. ) ;
#241763=CARTESIAN_POINT ( 'NONE',  ( -21.08621493067320429, 75.94380516053566055, -75.87240177569626098 ) ) ;
#241781=EDGE_CURVE ( 'NONE', #251301, #100316, #70564, .T. ) ;
#241796=ORIENTED_EDGE ( 'NONE', *, *, #154483, .T. ) ;
#241924=ADVANCED_FACE ( 'NONE', ( #10886 ), #132112, .T. ) ;
#241927=EDGE_LOOP ( 'NONE', ( #255147, #255576, #34184, #212866 ) ) ;
#241948=AXIS2_PLACEMENT_3D ( 'NONE', #13533, #193461, #14838 ) ;
#241952=CARTESIAN_POINT ( 'NONE',  ( -22.47886152344871036, 75.96249906115004080, -81.17309612757226489 ) ) ;
#241967=ORIENTED_EDGE ( 'NONE', *, *, #171910, .T. ) ;
#242016=DIRECTION ( 'NONE',  ( 0.000000000000000000, 0.000000000000000000, 1.000000000000000000 ) ) ;
#242029=DIRECTION ( 'NONE',  ( 1.000000000000000000, 0.000000000000000000, 0.000000000000000000 ) ) ;
#242031=CYLINDRICAL_SURFACE ( 'NONE', #172076, 0.1000000000000028644 ) ;
#242090=DIRECTION ( 'NONE',  ( 0.000000000000000000, -6.517943393102681197E-15, 1.000000000000000000 ) ) ;
#242124=CARTESIAN_POINT ( 'NONE',  ( -21.14999999999999858, 64.25000000001161027, -62.79697684846522066 ) ) ;
#242129=FACE_OUTER_BOUND ( 'NONE', #18700, .T. ) ;
#242189=CARTESIAN_POINT ( 'NONE',  ( 18.50000000000009948, 65.71984138295431421, -44.79853541332369105 ) ) ;
#242256=LINE ( 'NONE', #63627, #223276 ) ;
#242299=ORIENTED_EDGE ( 'NONE', *, *, #135283, .T. ) ;
#242307=CIRCLE ( 'NONE', #88345, 0.1000000000000028644 ) ;
#242334=ORIENTED_EDGE ( 'NONE', *, *, #247944, .F. ) ;
#242416=DIRECTION ( 'NONE',  ( -1.000000000000000000, 0.000000000000000000, -0.000000000000000000 ) ) ;
#242447=CARTESIAN_POINT ( 'NONE',  ( 18.50000000000000355, 85.42107434499949647, -29.19863542509363441 ) ) ;
#242457=CARTESIAN_POINT ( 'NONE',  ( -22.47071067811865319, 68.27992525551358938, -69.62219993922697370 ) ) ;
#242501=DIRECTION ( 'NONE',  ( 1.000000000000000000, 0.000000000000000000, 0.000000000000000000 ) ) ;
#242507=DIRECTION ( 'NONE',  ( -1.000000000000000000, 0.000000000000000000, 0.000000000000000000 ) ) ;
#242513=DIRECTION ( 'NONE',  ( -1.000000000000000000, -0.000000000000000000, -0.000000000000000000 ) ) ;
#242534=CARTESIAN_POINT ( 'NONE',  ( 20.94999999999999929, 88.41227409416113403, -39.02310748452423894 ) ) ;
#242553=ADVANCED_FACE ( 'NONE', ( #105471 ), #63822, .F. ) ;
#242558=EDGE_CURVE ( 'NONE', #165690, #201109, #174995, .T. ) ;
#242594=ORIENTED_EDGE ( 'NONE', *, *, #102799, .F. ) ;
#242617=EDGE_LOOP ( 'NONE', ( #247670, #104827, #2136 ) ) ;
#242639=ORIENTED_EDGE ( 'NONE', *, *, #245461, .T. ) ;
#242659=AXIS2_PLACEMENT_3D ( 'NONE', #219966, #20507, #17905 ) ;
#242663=ORIENTED_EDGE ( 'NONE', *, *, #81671, .F. ) ;
#242691=CARTESIAN_POINT ( 'NONE',  ( -18.50596464788227635, 65.69367753730607262, -30.51892380663480964 ) ) ;
#242703=ORIENTED_EDGE ( 'NONE', *, *, #163634, .F. ) ;
#242727=EDGE_CURVE ( 'NONE', #234718, #250549, #208277, .T. ) ;
#242761=( BOUNDED_SURFACE ( )  B_SPLINE_SURFACE ( 3, 2, ( 
 ( #19578, #79517, #57390 ),
 ( #119986, #159100, #238616 ),
 ( #76963, #100358, #136942 ),
 ( #37870, #179937, #117384 ),
 ( #1266, #18280, #196913 ),
 ( #200771, #22158, #181228 ),
 ( #63834, #162950, #102930 ),
 ( #182515, #24735, #221589 ),
 ( #242447, #143358, #145917 ),
 ( #105485, #187646, #164225 ) ),
 .UNSPECIFIED., .F., .F., .F. ) 
 B_SPLINE_SURFACE_WITH_KNOTS ( ( 4, 2, 2, 2, 4 ),
 ( 3, 3 ),
 ( 0.0001701955120502367854, 0.0002247052511886119680, 0.0002792149903269871506, 0.0003882344686037374616, 0.0006062734251572381378 ),
 ( 0.000000000000000000, 1.000000000000000000 ),
 .UNSPECIFIED. ) 
 GEOMETRIC_REPRESENTATION_ITEM ( )  RATIONAL_B_SPLINE_SURFACE ( (
 ( 1.000000000000000000, 0.2966190024560742544, 1.000000000000000000),
 ( 1.000000000000000000, 0.2964522492714360968, 1.000000000000000000),
 ( 1.000000000000000000, 0.3059923531879654712, 1.000000000000000000),
 ( 1.000000000000000000, 0.3355751146950147756, 1.000000000000000000),
 ( 1.000000000000000000, 0.3550672384961490180, 1.000000000000000000),
 ( 1.000000000000000000, 0.4157034672184696245, 1.000000000000000000),
 ( 1.000000000000000000, 0.4588031877653353519, 1.000000000000000000),
 ( 1.000000000000000000, 0.5771441759663189508, 1.000000000000000000),
 ( 1.000000000000000000, 0.6469377121770625294, 1.000000000000000000),
 ( 1.000000000000000000, 0.7071067811865402453, 1.000000000000000000) ) ) 
 REPRESENTATION_ITEM ( '' )  SURFACE ( )  );
#242769=CIRCLE ( 'NONE', #163672, 4.300000000000039790 ) ;
#242770=VECTOR ( 'NONE', #165264, 1000.000000000000000 ) ;
#242815=AXIS2_PLACEMENT_3D ( 'NONE', #73467, #232538, #180247 ) ;
#242828=CIRCLE ( 'NONE', #138915, 0.09999999999999939493 ) ;
#242830=EDGE_LOOP ( 'NONE', ( #53888, #185200, #160940 ) ) ;
#242840=CARTESIAN_POINT ( 'NONE',  ( 21.14999999999999858, 67.21339244341145047, -57.17310748452437963 ) ) ;
#242864=( BOUNDED_SURFACE ( )  B_SPLINE_SURFACE ( 3, 2, ( 
 ( #79150, #180847, #257747 ),
 ( #140412, #158739, #99982 ),
 ( #58300, #41354, #238235 ),
 ( #236962, #117016, #235662 ),
 ( #60878, #120896, #200405 ),
 ( #884, #136557, #101246 ),
 ( #57007, #59567, #139102 ),
 ( #218663, #2180, #81693 ),
 ( #196541, #161295, #179574 ),
 ( #216099, #36217, #137840 ),
 ( #240818, #62182, #141701 ),
 ( #115733, #256451, #156168 ) ),
 .UNSPECIFIED., .F., .F., .F. ) 
 B_SPLINE_SURFACE_WITH_KNOTS ( ( 4, 2, 2, 2, 2, 4 ),
 ( 3, 3 ),
 ( 3.174653483277205090, 3.943930578431714018, 4.713207673586222946, 5.482484768740731873, 5.867123316317986337, 6.251761863895240801 ),
 ( 0.000000000000000000, 1.000000000000000000 ),
 .UNSPECIFIED. ) 
 GEOMETRIC_REPRESENTATION_ITEM ( )  RATIONAL_B_SPLINE_SURFACE ( (
 ( 1.000000000000000000, 0.8659465255642289083, 1.000000000000000000),
 ( 1.000000000000000000, 0.8648614068487556761, 1.000000000000000000),
 ( 1.000000000000000000, 0.8489031841324650163, 1.000000000000000000),
 ( 1.000000000000000000, 0.7927507630160894880, 1.000000000000000000),
 ( 1.000000000000000000, 0.7523013859007079418, 1.000000000000000000),
 ( 1.000000000000000000, 0.6616226951198711514, 1.000000000000000000),
 ( 1.000000000000000000, 0.6112214368721650137, 1.000000000000000000),
 ( 1.000000000000000000, 0.5507684314500187472, 1.000000000000000000),
 ( 1.000000000000000000, 0.5333267243151817993, 1.000000000000000000),
 ( 1.000000000000000000, 0.5084565446480915352, 1.000000000000000000),
 ( 1.000000000000000000, 0.5010722703450180004, 1.000000000000000000),
 ( 1.000000000000000000, 0.5001234037138587718, 1.000000000000000000) ) ) 
 REPRESENTATION_ITEM ( '' )  SURFACE ( )  );
#242873=ORIENTED_EDGE ( 'NONE', *, *, #248641, .F. ) ;
#242877=ORIENTED_EDGE ( 'NONE', *, *, #51968, .T. ) ;
#242880=ORIENTED_EDGE ( 'NONE', *, *, #126665, .T. ) ;
#242892=DIRECTION ( 'NONE',  ( 0.000000000000000000, -0.9908441862701605762, 0.1350103645451835310 ) ) ;
#242913=EDGE_CURVE ( 'NONE', #176547, #218877, #338, .T. ) ;
#242921=EDGE_CURVE ( 'NONE', #238186, #13565, #125249, .T. ) ;
#242971=CARTESIAN_POINT ( 'NONE',  ( 23.14999999999999503, 61.90000000001145963, -41.62340509566378444 ) ) ;
#242982=ADVANCED_FACE ( 'NONE', ( #242129 ), #165169, .T. ) ;
#242998=EDGE_LOOP ( 'NONE', ( #228018, #235742, #123855, #229703 ) ) ;
#243008=CARTESIAN_POINT ( 'NONE',  ( 20.95520789717937404, 65.42306940062664466, -61.94287451064954553 ) ) ;
#243022=CARTESIAN_POINT ( 'NONE',  ( -21.45000000000000284, 68.29142135624881860, -48.27310748452437394 ) ) ;
#243036=DIRECTION ( 'NONE',  ( 0.000000000000000000, 6.982962677686266711E-15, -1.000000000000000000 ) ) ;
#243062=DIRECTION ( 'NONE',  ( 0.000000000000000000, -1.000000000000000000, -6.982962677686265922E-15 ) ) ;
#243081=ADVANCED_FACE ( 'NONE', ( #204279 ), #112901, .F. ) ;
#243101=CARTESIAN_POINT ( 'NONE',  ( -23.25000000000000000, 76.00000000001162448, -65.37310748452432563 ) ) ;
#243123=VECTOR ( 'NONE', #234830, 1000.000000000000000 ) ;
#243130=CARTESIAN_POINT ( 'NONE',  ( 18.59999999999999432, 77.13501884592155022, -28.30613060109199353 ) ) ;
#243134=CARTESIAN_POINT ( 'NONE',  ( 21.14999999999999858, 87.75000000001156764, -57.27310748452423894 ) ) ;
#243136=CARTESIAN_POINT ( 'NONE',  ( 21.07928932188134397, 75.90110485435729970, -75.85162414091763594 ) ) ;
#243164=CARTESIAN_POINT ( 'NONE',  ( 20.94999999999999929, 87.29603075034673054, -39.07100664418810965 ) ) ;
#243185=LINE ( 'NONE', #223607, #111748 ) ;
#243188=VECTOR ( 'NONE', #68610, 1000.000000000000000 ) ;
#243206=ORIENTED_EDGE ( 'NONE', *, *, #210402, .F. ) ;
#243213=EDGE_LOOP ( 'NONE', ( #146152, #137622, #104641, #240327 ) ) ;
#243242=ORIENTED_EDGE ( 'NONE', *, *, #139149, .F. ) ;
#243264=DIRECTION ( 'NONE',  ( 1.734723475976823250E-13, 0.7899159663865635839, 0.6132151058540398214 ) ) ;
#243304=DIRECTION ( 'NONE',  ( -1.000000000000000000, 2.952720810173289112E-16, 2.061873921506763405E-30 ) ) ;
#243326=ADVANCED_FACE ( 'NONE', ( #13798 ), #172919, .T. ) ;
#243358=CARTESIAN_POINT ( 'NONE',  ( 22.50000000000000000, 68.20922040163827660, -69.62310748452438247 ) ) ;
#243393=CARTESIAN_POINT ( 'NONE',  ( -21.05000000000000071, 76.00000000001170974, -76.06376443622555428 ) ) ;
#243410=VECTOR ( 'NONE', #132615, 1000.000000000000000 ) ;
#243422=ORIENTED_EDGE ( 'NONE', *, *, #154409, .T. ) ;
#243477=FACE_OUTER_BOUND ( 'NONE', #234912, .T. ) ;
#243486=EDGE_LOOP ( 'NONE', ( #74944, #227796, #45369, #81881 ) ) ;
#243488=AXIS2_PLACEMENT_3D ( 'NONE', #6251, #7550, #124942 ) ;
#243492=VERTEX_POINT ( 'NONE', #188278 ) ;
#243510=CARTESIAN_POINT ( 'NONE',  ( 20.94999999999999929, 84.73084112150691283, -59.92503276553992464 ) ) ;
#243532=VERTEX_POINT ( 'NONE', #146563 ) ;
#243539=DIRECTION ( 'NONE',  ( 0.000000000000000000, 6.982962677686266711E-15, -1.000000000000000000 ) ) ;
#243573=VECTOR ( 'NONE', #222111, 1000.000000000000000 ) ;
#243576=ORIENTED_EDGE ( 'NONE', *, *, #30, .T. ) ;
#243578=ORIENTED_EDGE ( 'NONE', *, *, #99185, .F. ) ;
#243596=SPHERICAL_SURFACE ( 'NONE', #243488, 0.1000000000000000056 ) ;
#243634=DIRECTION ( 'NONE',  ( 1.000000000000000000, -3.265361837132813093E-16, -2.280189983783949500E-30 ) ) ;
#243699=AXIS2_PLACEMENT_3D ( 'NONE', #238291, #103900, #123493 ) ;
#243724=EDGE_CURVE ( 'NONE', #69280, #20464, #133790, .T. ) ;
#243732=DIRECTION ( 'NONE',  ( 0.000000000000000000, 0.000000000000000000, -1.000000000000000000 ) ) ;
#243738=ORIENTED_EDGE ( 'NONE', *, *, #169031, .T. ) ;
#243762=CARTESIAN_POINT ( 'NONE',  ( -18.50000000000000000, 64.25000000001173817, -81.27310748452440237 ) ) ;
#243820=ORIENTED_EDGE ( 'NONE', *, *, #59576, .T. ) ;
#243840=CONICAL_SURFACE ( 'NONE', #164747, 6.250000000000005329, 0.7853981633974431720 ) ;
#243866=CARTESIAN_POINT ( 'NONE',  ( 21.13461538461538325, 67.11458296203710461, -57.17310748452437963 ) ) ;
#243882=CARTESIAN_POINT ( 'NONE',  ( -23.15000000000000213, 73.50000000001151079, -49.24772940728643533 ) ) ;
#243893=DIRECTION ( 'NONE',  ( 1.000000000000000000, 0.000000000000000000, 0.000000000000000000 ) ) ;
#243895=ORIENTED_EDGE ( 'NONE', *, *, #209519, .T. ) ;
#243897=EDGE_CURVE ( 'NONE', #201700, #102074, #4117, .T. ) ;
#244003=VERTEX_POINT ( 'NONE', #117107 ) ;
#244030=ORIENTED_EDGE ( 'NONE', *, *, #219530, .T. ) ;
#244050=AXIS2_PLACEMENT_3D ( 'NONE', #12897, #92392, #234469 ) ;
#244054=CYLINDRICAL_SURFACE ( 'NONE', #161786, 0.09999999999999939493 ) ;
#244058=CARTESIAN_POINT ( 'NONE',  ( 18.59999999999999076, 69.55000000001159322, -59.50608031408435039 ) ) ;
#244062=CARTESIAN_POINT ( 'NONE',  ( -21.05000000000000071, 87.65000000001163016, -66.52310748452423184 ) ) ;
#244070=CIRCLE ( 'NONE', #206658, 0.3999999999999975797 ) ;
#244095=AXIS2_PLACEMENT_3D ( 'NONE', #251498, #9047, #250226 ) ;
#244114=AXIS2_PLACEMENT_3D ( 'NONE', #142873, #222403, #205426 ) ;
#244121=AXIS2_PLACEMENT_3D ( 'NONE', #110930, #254272, #173529 ) ;
#244128=ORIENTED_EDGE ( 'NONE', *, *, #213971, .T. ) ;
#244130=CARTESIAN_POINT ( 'NONE',  ( 18.49999999999998934, 69.35000000001156195, -57.17310748452436542 ) ) ;
#244139=EDGE_LOOP ( 'NONE', ( #116488, #223423, #94486, #209627 ) ) ;
#244145=CARTESIAN_POINT ( 'NONE',  ( -18.59999999999999787, 66.65000000001157332, -57.27310748452438816 ) ) ;
#244154=CIRCLE ( 'NONE', #131740, 4.299999999999956302 ) ;
#244181=EDGE_CURVE ( 'NONE', #13038, #137086, #229846, .T. ) ;
#244185=VECTOR ( 'NONE', #17537, 1000.000000000000000 ) ;
#244198=EDGE_LOOP ( 'NONE', ( #6147, #241440, #150884, #15499, #64334 ) ) ;
#244213=EDGE_CURVE ( 'NONE', #62686, #142859, #117424, .T. ) ;
#244260=DIRECTION ( 'NONE',  ( -0.000000000000000000, -6.982962677686266711E-15, 1.000000000000000000 ) ) ;
#244263=EDGE_CURVE ( 'NONE', #159227, #235467, #242307, .T. ) ;
#244264=FACE_OUTER_BOUND ( 'NONE', #136827, .T. ) ;
#244329=CARTESIAN_POINT ( 'NONE',  ( -21.14999999999999858, 76.00000000001169553, -76.06376443622556849 ) ) ;
#244359=LINE ( 'NONE', #246930, #53781 ) ;
#244362=EDGE_CURVE ( 'NONE', #196464, #92669, #59294, .T. ) ;
#244367=EDGE_LOOP ( 'NONE', ( #6585, #134050, #226371, #246447, #230306, #202178, #197605, #166196, #128219, #250192, #8042, #181678, #59334, #54302, #122359, #71455 ) ) ;
#244368=DIRECTION ( 'NONE',  ( 0.000000000000000000, -6.938893903907233900E-15, 1.000000000000000000 ) ) ;
#244393=EDGE_CURVE ( 'NONE', #79119, #193842, #134152, .T. ) ;
#244403=EDGE_CURVE ( 'NONE', #47002, #1289, #215866, .T. ) ;
#244411=DIRECTION ( 'NONE',  ( 1.000000000000000000, 0.000000000000000000, 0.000000000000000000 ) ) ;
#244417=DIRECTION ( 'NONE',  ( -1.000000000000000000, 0.000000000000000000, -0.000000000000000000 ) ) ;
#244421=CARTESIAN_POINT ( 'NONE',  ( 21.12230431290518951, 75.99479014832267865, -75.98067413781733137 ) ) ;
#244435=CARTESIAN_POINT ( 'NONE',  ( -21.14999999999999858, 75.90220970870291239, -75.78092209500043452 ) ) ;
#244496=DIRECTION ( 'NONE',  ( 0.000000000000000000, -6.982962677686266711E-15, 1.000000000000000000 ) ) ;
#244505=DIRECTION ( 'NONE',  ( 0.000000000000000000, 0.4999999999999689138, -0.8660254037844565822 ) ) ;
#244518=DIRECTION ( 'NONE',  ( 0.000000000000000000, 0.000000000000000000, 1.000000000000000000 ) ) ;
#244525=DIRECTION ( 'NONE',  ( 0.000000000000000000, 0.000000000000000000, -1.000000000000000000 ) ) ;
#244542=ADVANCED_FACE ( 'NONE', ( #205295 ), #221628, .F. ) ;
#244572=EDGE_LOOP ( 'NONE', ( #205351, #80575, #170011, #135797, #59318, #29594, #193711, #210065, #90182, #196226, #184606, #90156, #159186, #134214, #245036, #74586 ) ) ;
#244580=DIRECTION ( 'NONE',  ( 0.000000000000000000, -6.530723674265620862E-15, 1.000000000000000000 ) ) ;
#244588=EDGE_LOOP ( 'NONE', ( #223289, #214874, #255559, #30299 ) ) ;
#244604=VECTOR ( 'NONE', #74210, 1000.000000000000000 ) ;
#244629=DIRECTION ( 'NONE',  ( 0.000000000000000000, -7.429790795770647916E-15, 1.000000000000000000 ) ) ;
#244633=CIRCLE ( 'NONE', #107263, 0.09999999999999938105 ) ;
#244669=CARTESIAN_POINT ( 'NONE',  ( -21.05000000000000071, 76.02110330807039418, -75.82762381378833538 ) ) ;
#244670=DIRECTION ( 'NONE',  ( 0.000000000000000000, 6.982962677686266711E-15, -1.000000000000000000 ) ) ;
#244700=ADVANCED_FACE ( 'NONE', ( #226126 ), #87906, .F. ) ;
#244702=( BOUNDED_CURVE ( )  B_SPLINE_CURVE ( 3, ( #221084, #42455, #180698, #82834 ),
 .UNSPECIFIED., .F., .T. ) 
 B_SPLINE_CURVE_WITH_KNOTS ( ( 4, 4 ),
 ( 0.000000000000000000, 1.570796326794908992 ),
 .UNSPECIFIED. ) 
 CURVE ( )  GEOMETRIC_REPRESENTATION_ITEM ( )  RATIONAL_B_SPLINE_CURVE ( ( 1.000000000000000000, 0.8047378541243619399, 0.8047378541243619399, 1.000000000000000000 ) ) 
 REPRESENTATION_ITEM ( '' )  );
#244719=CARTESIAN_POINT ( 'NONE',  ( -21.05000000000000071, 87.65000000001144542, -38.92310748452424463 ) ) ;
#244724=EDGE_LOOP ( 'NONE', ( #239362, #235725, #18060, #209869, #148784 ) ) ;
#244730=DIRECTION ( 'NONE',  ( -1.000000000000000000, 0.000000000000000000, 0.000000000000000000 ) ) ;
#244758=CARTESIAN_POINT ( 'NONE',  ( -21.55000000000000426, 68.25000000001151079, -48.37310748452437537 ) ) ;
#244759=DIRECTION ( 'NONE',  ( -1.000000000000000000, -0.000000000000000000, -0.000000000000000000 ) ) ;
#244797=ORIENTED_EDGE ( 'NONE', *, *, #135548, .T. ) ;
#244846=CARTESIAN_POINT ( 'NONE',  ( 21.05000000000000071, 87.48912529308749697, -39.12310748452424747 ) ) ;
#244861=DIRECTION ( 'NONE',  ( 0.000000000000000000, 6.982962677686267499E-15, -1.000000000000000000 ) ) ;
#244900=ADVANCED_FACE ( 'NONE', ( #5498 ), #224559, .T. ) ;
#244970=ORIENTED_EDGE ( 'NONE', *, *, #68451, .T. ) ;
#244976=FACE_OUTER_BOUND ( 'NONE', #99408, .T. ) ;
#245036=ORIENTED_EDGE ( 'NONE', *, *, #83493, .T. ) ;
#245046=DIRECTION ( 'NONE',  ( -7.304098846218134667E-16, 1.000000000000000000, 6.982962677686266711E-15 ) ) ;
#245056=CARTESIAN_POINT ( 'NONE',  ( 18.54116936837189300, 85.46356419838404861, -62.47456499363600102 ) ) ;
#245063=ADVANCED_FACE ( 'NONE', ( #227127 ), #135162, .F. ) ;
#245074=CARTESIAN_POINT ( 'NONE',  ( 23.24999999999999645, 71.00000000001151079, -48.42837350343745584 ) ) ;
#245079=DIRECTION ( 'NONE',  ( 1.000000000000000000, 0.000000000000000000, 0.000000000000000000 ) ) ;
#245082=DIRECTION ( 'NONE',  ( 1.000000000000000000, -7.304098846218134667E-16, -5.100424963727256530E-30 ) ) ;
#245089=EDGE_CURVE ( 'NONE', #181320, #217695, #148900, .T. ) ;
#245099=AXIS2_PLACEMENT_3D ( 'NONE', #115630, #79037, #158635 ) ;
#245109=CARTESIAN_POINT ( 'NONE',  ( 20.94999999999999929, 74.16465844978715438, -57.96795619196134908 ) ) ;
#245118=AXIS2_PLACEMENT_3D ( 'NONE', #91529, #152820, #215320 ) ;
#245122=DIRECTION ( 'NONE',  ( -2.952720810173289112E-16, -1.000000000000000000, -6.982962677686266711E-15 ) ) ;
#245148=VERTEX_POINT ( 'NONE', #71931 ) ;
#245154=DIRECTION ( 'NONE',  ( 0.000000000000000000, -1.000000000000000000, -6.982962677686265922E-15 ) ) ;
#245174=CARTESIAN_POINT ( 'NONE',  ( -18.59999999999999787, 69.15387683765879956, -32.28538121767450519 ) ) ;
#245184=ORIENTED_EDGE ( 'NONE', *, *, #258100, .T. ) ;
#245186=DIRECTION ( 'NONE',  ( 0.000000000000000000, 0.000000000000000000, 1.000000000000000000 ) ) ;
#245192=DIRECTION ( 'NONE',  ( 0.000000000000000000, -7.026728003956686545E-15, 1.000000000000000000 ) ) ;
#245193=CARTESIAN_POINT ( 'NONE',  ( 22.39999999999999503, 76.00000000001173817, -81.17267829206912211 ) ) ;
#245203=CIRCLE ( 'NONE', #182669, 0.1999999999999987899 ) ;
#245217=ORIENTED_EDGE ( 'NONE', *, *, #132511, .F. ) ;
#245229=EDGE_LOOP ( 'NONE', ( #71234, #85775, #1723, #214181 ) ) ;
#245235=EDGE_CURVE ( 'NONE', #59781, #251339, #227986, .T. ) ;
#245241=AXIS2_PLACEMENT_3D ( 'NONE', #152070, #231593, #15113 ) ;
#245257=CARTESIAN_POINT ( 'NONE',  ( 20.94999999999999574, 67.07338541492450190, -61.05142446530125966 ) ) ;
#245291=DIRECTION ( 'NONE',  ( -1.000000000000000000, 0.000000000000000000, -0.000000000000000000 ) ) ;
#245296=ORIENTED_EDGE ( 'NONE', *, *, #40321, .F. ) ;
#245305=B_SPLINE_CURVE_WITH_KNOTS ( 'NONE', 3,
 ( #49657, #112223, #129206, #170948, #73114, #131762, #127922 ),
 .UNSPECIFIED., .F., .F.,
 ( 4, 3, 4 ),
 ( 0.000000000000000000, 3.357501770813427151E-05, 5.199112466348487506E-05 ),
 .UNSPECIFIED. ) ;
#245344=ADVANCED_FACE ( 'NONE', ( #190154 ), #169337, .F. ) ;
#245347=DIRECTION ( 'NONE',  ( 1.000000000000000000, 0.000000000000000000, 0.000000000000000000 ) ) ;
#245382=DIRECTION ( 'NONE',  ( 0.000000000000000000, -6.982962677686266711E-15, 1.000000000000000000 ) ) ;
#245409=DIRECTION ( 'NONE',  ( -0.000000000000000000, -6.982962677686266711E-15, 1.000000000000000000 ) ) ;
#245438=CARTESIAN_POINT ( 'NONE',  ( -18.50000000000000000, 85.40000000001138858, -29.14106563635158764 ) ) ;
#245444=AXIS2_PLACEMENT_3D ( 'NONE', #202986, #144270, #63468 ) ;
#245460=ORIENTED_EDGE ( 'NONE', *, *, #146778, .T. ) ;
#245461=EDGE_CURVE ( 'NONE', #28556, #82836, #197829, .T. ) ;
#245486=CARTESIAN_POINT ( 'NONE',  ( 18.44364597020195973, 85.49048731717387284, -62.46512959484039840 ) ) ;
#245497=AXIS2_PLACEMENT_3D ( 'NONE', #125295, #24927, #43190 ) ;
#245500=DIRECTION ( 'NONE',  ( 1.000000000000000000, 0.000000000000000000, 0.000000000000000000 ) ) ;
#245527=DIRECTION ( 'NONE',  ( -3.265361837132813093E-16, -1.000000000000000000, -7.086529944415894657E-15 ) ) ;
#245547=VERTEX_POINT ( 'NONE', #234996 ) ;
#245551=DIRECTION ( 'NONE',  ( 0.000000000000000000, 0.000000000000000000, 1.000000000000000000 ) ) ;
#245566=DIRECTION ( 'NONE',  ( 7.304098846218134667E-16, 1.000000000000000000, 6.982962677686266711E-15 ) ) ;
#245569=DIRECTION ( 'NONE',  ( -1.000000000000000000, -0.000000000000000000, -0.000000000000000000 ) ) ;
#245576=DIRECTION ( 'NONE',  ( -0.000000000000000000, 6.982962677686266711E-15, -1.000000000000000000 ) ) ;
#245584=ORIENTED_EDGE ( 'NONE', *, *, #244403, .T. ) ;
#245585=CARTESIAN_POINT ( 'NONE',  ( -20.07928932188135107, 66.77928932189284694, -48.37310748452438247 ) ) ;
#245603=FACE_OUTER_BOUND ( 'NONE', #100123, .T. ) ;
#245614=ORIENTED_EDGE ( 'NONE', *, *, #166911, .T. ) ;
#245630=CARTESIAN_POINT ( 'NONE',  ( -21.08198257630413508, 75.92735667622712015, -75.85970421853939172 ) ) ;
#245663=ORIENTED_EDGE ( 'NONE', *, *, #21103, .F. ) ;
#245664=CARTESIAN_POINT ( 'NONE',  ( -20.94999999999999929, 76.00000000001159606, -61.62310748452431852 ) ) ;
#245671=DIRECTION ( 'NONE',  ( 0.000000000000000000, 1.000000000000000000, 6.982962677686266711E-15 ) ) ;
#245680=DIRECTION ( 'NONE',  ( 0.000000000000000000, 0.000000000000000000, 1.000000000000000000 ) ) ;
#245695=FACE_OUTER_BOUND ( 'NONE', #116039, .T. ) ;
#245699=AXIS2_PLACEMENT_3D ( 'NONE', #167453, #54835, #245680 ) ;
#245702=CIRCLE ( 'NONE', #129015, 0.09999999999999520384 ) ;
#245703=FACE_BOUND ( 'NONE', #20044, .T. ) ;
#245712=CARTESIAN_POINT ( 'NONE',  ( -20.54999999999999716, 74.00000000001156764, -56.79848556176223440 ) ) ;
#245721=DIRECTION ( 'NONE',  ( 0.000000000000000000, -0.8700118002898357128, 0.4930308989875171188 ) ) ;
#245737=CARTESIAN_POINT ( 'NONE',  ( -23.25000000000000000, 64.25000000001173817, -81.27310748452440237 ) ) ;
#245739=DIRECTION ( 'NONE',  ( 0.000000000000000000, -6.982962677686266711E-15, 1.000000000000000000 ) ) ;
#245765=CIRCLE ( 'NONE', #25034, 7.791421356237338003 ) ;
#245766=ORIENTED_EDGE ( 'NONE', *, *, #237772, .T. ) ;
#245784=DIRECTION ( 'NONE',  ( 0.000000000000000000, 0.000000000000000000, -1.000000000000000000 ) ) ;
#245793=ORIENTED_EDGE ( 'NONE', *, *, #161070, .T. ) ;
#245801=CIRCLE ( 'NONE', #87565, 12.97499999999999964 ) ;
#245844=CARTESIAN_POINT ( 'NONE',  ( 21.11345278033268968, 67.11787792663994878, -57.27708531376936918 ) ) ;
#245890=CIRCLE ( 'NONE', #233268, 0.09999999999999939493 ) ;
#245907=CARTESIAN_POINT ( 'NONE',  ( -18.59999999999999787, 77.73670573947892137, -24.50568489690058627 ) ) ;
#245912=ORIENTED_EDGE ( 'NONE', *, *, #10389, .T. ) ;
#245975=CARTESIAN_POINT ( 'NONE',  ( -21.05000000000000071, 76.09999996531125532, -76.00065966701779985 ) ) ;
#245991=AXIS2_PLACEMENT_3D ( 'NONE', #90353, #248157, #224725 ) ;
#245997=DIRECTION ( 'NONE',  ( 0.000000000000000000, -1.000000000000000000, -6.982962677686265922E-15 ) ) ;
#246005=CARTESIAN_POINT ( 'NONE',  ( 21.05000000000000071, 64.25000000001145395, -42.86470817442145176 ) ) ;
#246028=DIRECTION ( 'NONE',  ( -1.000000000000000000, 1.836970198721029934E-16, 1.282749433769087757E-30 ) ) ;
#246041=DIRECTION ( 'NONE',  ( 1.000000000000000000, 0.000000000000000000, 0.000000000000000000 ) ) ;
#246050=AXIS2_PLACEMENT_3D ( 'NONE', #159762, #163615, #180605 ) ;
#246058=CARTESIAN_POINT ( 'NONE',  ( 18.59999999999998721, 65.50857864377418593, -44.77310748452440237 ) ) ;
#246067=LINE ( 'NONE', #49132, #19061 ) ;
#246079=CARTESIAN_POINT ( 'NONE',  ( -20.64999999999999858, 71.65000000001155911, -57.27310748452435263 ) ) ;
#246086=ORIENTED_EDGE ( 'NONE', *, *, #1373, .F. ) ;
#246098=ORIENTED_EDGE ( 'NONE', *, *, #186253, .T. ) ;
#246101=CARTESIAN_POINT ( 'NONE',  ( -23.25000000000000000, 87.75000000001163869, -66.42310748452423752 ) ) ;
#246114=CARTESIAN_POINT ( 'NONE',  ( -20.85000000000000142, 68.97833521811131163, -32.38954208262708079 ) ) ;
#246118=CIRCLE ( 'NONE', #233650, 0.6000000000000033085 ) ;
#246125=LINE ( 'NONE', #145717, #73241 ) ;
#246156=CARTESIAN_POINT ( 'NONE',  ( 18.59999999999999787, 70.10000000001163301, -59.30400771986794695 ) ) ;
#246157=ORIENTED_EDGE ( 'NONE', *, *, #76768, .T. ) ;
#246174=DIRECTION ( 'NONE',  ( 0.000000000000000000, 1.000000000000000000, 6.853228547068871147E-15 ) ) ;
#246190=DIRECTION ( 'NONE',  ( 0.000000000000000000, -0.9654727137038715545, 0.2605042016806676242 ) ) ;
#246226=DIRECTION ( 'NONE',  ( 0.000000000000000000, 0.8660254037844419273, -0.4999999999999942824 ) ) ;
#246254=ORIENTED_EDGE ( 'NONE', *, *, #7219, .F. ) ;
#246301=VERTEX_POINT ( 'NONE', #84543 ) ;
#246351=DIRECTION ( 'NONE',  ( 0.000000000000000000, 6.982962677686267499E-15, -1.000000000000000000 ) ) ;
#246360=EDGE_CURVE ( 'NONE', #257957, #251754, #251361, .T. ) ;
#246363=ORIENTED_EDGE ( 'NONE', *, *, #79567, .T. ) ;
#246375=CARTESIAN_POINT ( 'NONE',  ( 18.45036689428354393, 85.49018414334042859, -62.51041165703842495 ) ) ;
#246397=EDGE_CURVE ( 'NONE', #49225, #88303, #237269, .T. ) ;
#246406=ORIENTED_EDGE ( 'NONE', *, *, #152939, .F. ) ;
#246428=ORIENTED_EDGE ( 'NONE', *, *, #85473, .F. ) ;
#246447=ORIENTED_EDGE ( 'NONE', *, *, #206338, .F. ) ;
#246460=CARTESIAN_POINT ( 'NONE',  ( 20.94999999999999574, 74.26374286841418382, -57.95445515550683524 ) ) ;
#246468=ORIENTED_EDGE ( 'NONE', *, *, #227116, .T. ) ;
#246511=AXIS2_PLACEMENT_3D ( 'NONE', #198985, #58168, #179445 ) ;
#246546=DIRECTION ( 'NONE',  ( 0.000000000000000000, 0.000000000000000000, -1.000000000000000000 ) ) ;
#246580=AXIS2_PLACEMENT_3D ( 'NONE', #207455, #163188, #48360 ) ;
#246592=EDGE_LOOP ( 'NONE', ( #253859, #141868, #206096, #9333 ) ) ;
#246598=ADVANCED_FACE ( 'NONE', ( #8597 ), #12606, .T. ) ;
#246608=VERTEX_POINT ( 'NONE', #25601 ) ;
#246683=CARTESIAN_POINT ( 'NONE',  ( -18.50000000000000000, 74.83729825007360148, -61.42310748452432989 ) ) ;
#246697=VECTOR ( 'NONE', #85967, 1000.000000000000000 ) ;
#246702=DIRECTION ( 'NONE',  ( 0.000000000000000000, -1.000000000000000000, -6.982962677686265922E-15 ) ) ;
#246728=AXIS2_PLACEMENT_3D ( 'NONE', #178527, #238468, #78099 ) ;
#246755=DIRECTION ( 'NONE',  ( -1.000000000000000000, -0.000000000000000000, -0.000000000000000000 ) ) ;
#246778=CARTESIAN_POINT ( 'NONE',  ( 23.14999999999998437, 76.00000000001165290, -69.52310748452431710 ) ) ;
#246792=ORIENTED_EDGE ( 'NONE', *, *, #232606, .T. ) ;
#246793=LINE ( 'NONE', #129424, #132332 ) ;
#246812=CARTESIAN_POINT ( 'NONE',  ( 21.05000000000000071, 65.52661458509871295, -61.94445302027585853 ) ) ;
#246837=VERTEX_POINT ( 'NONE', #141065 ) ;
#246860=CARTESIAN_POINT ( 'NONE',  ( -21.53752568622142505, 75.90102553874106661, -76.30991535907291734 ) ) ;
#246869=CIRCLE ( 'NONE', #238508, 0.1000000000000028644 ) ;
#246913=AXIS2_PLACEMENT_3D ( 'NONE', #181585, #162025, #62899 ) ;
#246918=CARTESIAN_POINT ( 'NONE',  ( -18.50000000000000000, 68.97833521811131163, -32.18954208262707795 ) ) ;
#246925=DIRECTION ( 'NONE',  ( 0.000000000000000000, 0.000000000000000000, -1.000000000000000000 ) ) ;
#246930=CARTESIAN_POINT ( 'NONE',  ( -20.94999999999999929, 64.30000000001147953, -42.77810563404302258 ) ) ;
#246998=DIRECTION ( 'NONE',  ( 0.000000000000000000, -0.9998779222360097974, 0.01562500000000363945 ) ) ;
#247001=CARTESIAN_POINT ( 'NONE',  ( -18.59999999999999787, 76.00000000001142553, -36.02310748452432421 ) ) ;
#247021=ORIENTED_EDGE ( 'NONE', *, *, #199479, .T. ) ;
#247035=CARTESIAN_POINT ( 'NONE',  ( 20.95512840106816199, 65.37615130623825621, -57.32062826372554554 ) ) ;
#247038=EDGE_LOOP ( 'NONE', ( #5622, #91530, #62431, #209437 ) ) ;
#247046=EDGE_LOOP ( 'NONE', ( #82155, #166560, #127129, #28222 ) ) ;
#247050=CARTESIAN_POINT ( 'NONE',  ( 21.05000000000000071, 69.45934304831041572, -69.42310748452437963 ) ) ;
#247057=ORIENTED_EDGE ( 'NONE', *, *, #3237, .T. ) ;
#247072=DIRECTION ( 'NONE',  ( 0.000000000000000000, -8.267618268485210697E-15, 1.000000000000000000 ) ) ;
#247074=ORIENTED_EDGE ( 'NONE', *, *, #25258, .F. ) ;
#247097=AXIS2_PLACEMENT_3D ( 'NONE', #91562, #15906, #92833 ) ;
#247113=ORIENTED_EDGE ( 'NONE', *, *, #233097, .F. ) ;
#247134=AXIS2_PLACEMENT_3D ( 'NONE', #24811, #27387, #104290 ) ;
#247138=VERTEX_POINT ( 'NONE', #225697 ) ;
#247241=LINE ( 'NONE', #167748, #177102 ) ;
#247265=FACE_OUTER_BOUND ( 'NONE', #43280, .T. ) ;
#247323=CARTESIAN_POINT ( 'NONE',  ( 18.49999999999999289, 65.65621891165837098, -44.69466220664676115 ) ) ;
#247326=APPLICATION_CONTEXT ( 'automotive_design' ) ;
#247343=AXIS2_PLACEMENT_3D ( 'NONE', #144113, #42463, #201536 ) ;
#247359=ORIENTED_EDGE ( 'NONE', *, *, #103839, .F. ) ;
#247361=EDGE_LOOP ( 'NONE', ( #248322, #190970, #68485, #173710 ) ) ;
#247365=DIRECTION ( 'NONE',  ( 0.000000000000000000, -1.000000000000000000, -6.982962677686265922E-15 ) ) ;
#247375=ORIENTED_EDGE ( 'NONE', *, *, #64106, .F. ) ;
#247376=CIRCLE ( 'NONE', #118411, 0.1000000000000028644 ) ;
#247388=DIRECTION ( 'NONE',  ( 0.000000000000000000, 0.7397360091702792628, -0.6728971962616790981 ) ) ;
#247397=TOROIDAL_SURFACE ( 'NONE', #122334, 0.2000000000000000111, 0.1000000000000000056 ) ;
#247398=EDGE_LOOP ( 'NONE', ( #122236, #194504, #208201, #67780 ) ) ;
#247448=DIRECTION ( 'NONE',  ( 1.000000000000000000, 0.000000000000000000, 0.000000000000000000 ) ) ;
#247449=CARTESIAN_POINT ( 'NONE',  ( -23.15000000000000213, 84.66355140188063899, -45.54720860259156723 ) ) ;
#247491=ORIENTED_EDGE ( 'NONE', *, *, #4567, .T. ) ;
#247496=LINE ( 'NONE', #128844, #112796 ) ;
#247503=ORIENTED_EDGE ( 'NONE', *, *, #21057, .T. ) ;
#247523=ADVANCED_FACE ( 'NONE', ( #247558 ), #10242, .T. ) ;
#247529=CARTESIAN_POINT ( 'NONE',  ( 20.85000000000000142, 77.83585931145498193, -24.51866831572578320 ) ) ;
#247541=DIRECTION ( 'NONE',  ( -0.000000000000000000, 6.982962677686266711E-15, -1.000000000000000000 ) ) ;
#247558=FACE_OUTER_BOUND ( 'NONE', #216541, .T. ) ;
#247562=CARTESIAN_POINT ( 'NONE',  ( -18.59999999999999787, 65.66751761918619934, -30.42826094061123854 ) ) ;
#247591=CARTESIAN_POINT ( 'NONE',  ( -23.25000000000000000, 74.00000000001156764, -56.29848556176223440 ) ) ;
#247621=EDGE_LOOP ( 'NONE', ( #54730, #93100 ) ) ;
#247625=CARTESIAN_POINT ( 'NONE',  ( 22.47809213839789066, 75.96246293238321812, -81.17308081931213337 ) ) ;
#247627=CARTESIAN_POINT ( 'NONE',  ( -20.54999999999999716, 85.40000000001148805, -45.91707660717669626 ) ) ;
#247636=EDGE_LOOP ( 'NONE', ( #76295, #81216, #239379, #13035, #110107, #227546, #233557, #210471, #242877, #98669, #256601, #161967 ) ) ;
#247653=CARTESIAN_POINT ( 'NONE',  ( -20.64999999999999858, 73.50000000001156764, -56.29848556176223440 ) ) ;
#247655=CARTESIAN_POINT ( 'NONE',  ( 18.46082813848014226, 85.48074965091900879, -62.43873738180850097 ) ) ;
#247670=ORIENTED_EDGE ( 'NONE', *, *, #187557, .T. ) ;
#247693=VERTEX_POINT ( 'NONE', #235681 ) ;
#247715=CARTESIAN_POINT ( 'NONE',  ( 21.05000000000000071, 87.75000000001162448, -66.62310748452424036 ) ) ;
#247716=AXIS2_PLACEMENT_3D ( 'NONE', #238133, #236856, #97314 ) ;
#247776=CARTESIAN_POINT ( 'NONE',  ( 20.93284271247462414, 64.25000000001146816, -43.03791325517833855 ) ) ;
#247777=FACE_OUTER_BOUND ( 'NONE', #185957, .T. ) ;
#247798=FACE_OUTER_BOUND ( 'NONE', #6825, .T. ) ;
#247805=AXIS2_PLACEMENT_3D ( 'NONE', #169145, #232958, #150826 ) ;
#247861=CIRCLE ( 'NONE', #139513, 1.900000000000005906 ) ;
#247889=ORIENTED_EDGE ( 'NONE', *, *, #188236, .F. ) ;
#247894=DIRECTION ( 'NONE',  ( 0.000000000000000000, 1.000000000000000000, 6.982962677686267499E-15 ) ) ;
#247944=EDGE_CURVE ( 'NONE', #243532, #212207, #6050, .T. ) ;
#247959=ORIENTED_EDGE ( 'NONE', *, *, #25961, .F. ) ;
#247978=AXIS2_PLACEMENT_3D ( 'NONE', #5550, #205030, #121692 ) ;
#248000=FACE_OUTER_BOUND ( 'NONE', #195275, .T. ) ;
#248015=CIRCLE ( 'NONE', #131496, 0.09999999999999939493 ) ;
#248043=VERTEX_POINT ( 'NONE', #227670 ) ;
#248142=ADVANCED_FACE ( 'NONE', ( #112870 ), #252358, .F. ) ;
#248144=VERTEX_POINT ( 'NONE', #134968 ) ;
#248157=DIRECTION ( 'NONE',  ( 1.000000000000000000, 0.000000000000000000, 0.000000000000000000 ) ) ;
#248227=AXIS2_PLACEMENT_3D ( 'NONE', #83532, #66583, #183951 ) ;
#248245=CYLINDRICAL_SURFACE ( 'NONE', #3227, 2.000000000000001776 ) ;
#248251=EDGE_CURVE ( 'NONE', #244003, #165845, #213213, .T. ) ;
#248252=DIRECTION ( 'NONE',  ( 1.000000000000000000, -3.265361837132813093E-16, -2.280189983783949500E-30 ) ) ;
#248255=CIRCLE ( 'NONE', #6642, 0.09999999999999939493 ) ;
#248263=CARTESIAN_POINT ( 'NONE',  ( 20.94999999999999574, 62.00000000001161737, -64.09601495414187866 ) ) ;
#248275=ADVANCED_FACE ( 'NONE', ( #104818 ), #103552, .F. ) ;
#248306=CIRCLE ( 'NONE', #15087, 0.1000000000000028644 ) ;
#248310=EDGE_CURVE ( 'NONE', #46741, #241487, #171743, .T. ) ;
#248322=ORIENTED_EDGE ( 'NONE', *, *, #133598, .T. ) ;
#248332=ADVANCED_FACE ( 'NONE', ( #44891 ), #25347, .F. ) ;
#248343=DIRECTION ( 'NONE',  ( -1.000000000000000000, 0.000000000000000000, 0.000000000000000000 ) ) ;
#248344=CARTESIAN_POINT ( 'NONE',  ( 21.05000000000000071, 70.10000000001149090, -46.24220724918073699 ) ) ;
#248371=EDGE_CURVE ( 'NONE', #233233, #171475, #188283, .T. ) ;
#248372=DIRECTION ( 'NONE',  ( 0.000000000000000000, -7.147358527629762208E-15, 1.000000000000000000 ) ) ;
#248380=CARTESIAN_POINT ( 'NONE',  ( 23.24999999999999645, 71.00000000001158185, -57.11784146561126363 ) ) ;
#248381=CARTESIAN_POINT ( 'NONE',  ( 21.05000000000000071, 67.18454772081405224, -61.10271493191011416 ) ) ;
#248394=ORIENTED_EDGE ( 'NONE', *, *, #60810, .T. ) ;
#248404=DIRECTION ( 'NONE',  ( 0.000000000000000000, -1.387778780781454006E-13, -1.000000000000000000 ) ) ;
#248412=AXIS2_PLACEMENT_3D ( 'NONE', #119458, #257606, #138969 ) ;
#248413=EDGE_CURVE ( 'NONE', #218484, #97104, #25418, .T. ) ;
#248442=ORIENTED_EDGE ( 'NONE', *, *, #226704, .F. ) ;
#248450=VECTOR ( 'NONE', #3760, 1000.000000000000000 ) ;
#248531=CARTESIAN_POINT ( 'NONE',  ( -18.52139480978223318, 85.48135884507851756, -62.49855091740519697 ) ) ;
#248555=VECTOR ( 'NONE', #94369, 1000.000000000000000 ) ;
#248563=ORIENTED_EDGE ( 'NONE', *, *, #250248, .F. ) ;
#248565=DIRECTION ( 'NONE',  ( 1.000000000000000000, 0.000000000000000000, 0.000000000000000000 ) ) ;
#248574=CARTESIAN_POINT ( 'NONE',  ( -20.54999999999999716, 76.00000000001142553, -36.02310748452432421 ) ) ;
#248581=CARTESIAN_POINT ( 'NONE',  ( -23.15000000000000213, 76.00000000001139711, -32.12310748452431852 ) ) ;
#248601=LINE ( 'NONE', #109080, #122059 ) ;
#248608=AXIS2_PLACEMENT_3D ( 'NONE', #8253, #245576, #68215 ) ;
#248627=DIRECTION ( 'NONE',  ( 0.000000000000000000, 0.000000000000000000, 1.000000000000000000 ) ) ;
#248631=ORIENTED_EDGE ( 'NONE', *, *, #154483, .F. ) ;
#248632=ORIENTED_EDGE ( 'NONE', *, *, #172144, .T. ) ;
#248641=EDGE_CURVE ( 'NONE', #2421, #206022, #163351, .T. ) ;
#248644=ORIENTED_EDGE ( 'NONE', *, *, #253562, .T. ) ;
#248655=VERTEX_POINT ( 'NONE', #252710 ) ;
#248658=ADVANCED_FACE ( 'NONE', ( #57063 ), #230610, .F. ) ;
#248660=ORIENTED_EDGE ( 'NONE', *, *, #52032, .T. ) ;
#248690=CARTESIAN_POINT ( 'NONE',  ( -23.15000000000000213, 84.59626168225457832, -60.07297996737398194 ) ) ;
#248721=ORIENTED_EDGE ( 'NONE', *, *, #98698, .T. ) ;
#248728=CARTESIAN_POINT ( 'NONE',  ( 18.59999999999999076, 69.55000000001150795, -48.37310748452436826 ) ) ;
#248741=EDGE_LOOP ( 'NONE', ( #46108, #157516, #39722, #124551 ) ) ;
#248746=CYLINDRICAL_SURFACE ( 'NONE', #22411, 0.1000000000000028644 ) ;
#248758=DIRECTION ( 'NONE',  ( 0.000000000000000000, 7.026728003956683390E-15, -1.000000000000000000 ) ) ;
#248767=FILL_AREA_STYLE_COLOUR ( '', #127143 ) ;
#248776=FACE_OUTER_BOUND ( 'NONE', #116693, .T. ) ;
#248815=ADVANCED_FACE ( 'NONE', ( #157517 ), #225291, .T. ) ;
#248832=DIRECTION ( 'NONE',  ( 1.000000000000000000, -3.265361837132813093E-16, -2.280189983783949500E-30 ) ) ;
#248834=DIRECTION ( 'NONE',  ( 0.000000000000000000, 6.982962677686266711E-15, -1.000000000000000000 ) ) ;
#248848=CIRCLE ( 'NONE', #19909, 0.09999999999999939493 ) ;
#248857=CARTESIAN_POINT ( 'NONE',  ( 21.05000000000000071, 74.83729825007360148, -61.62310748452433273 ) ) ;
#248867=CIRCLE ( 'NONE', #32417, 0.1000000000000028644 ) ;
#248922=CARTESIAN_POINT ( 'NONE',  ( -21.65000000000000213, 68.29142135624881860, -48.37310748452437537 ) ) ;
#248935=ORIENTED_EDGE ( 'NONE', *, *, #169377, .T. ) ;
#248956=DIRECTION ( 'NONE',  ( 1.000000000000000000, 0.000000000000000000, 0.000000000000000000 ) ) ;
#248986=ADVANCED_FACE ( 'NONE', ( #247265 ), #30040, .T. ) ;
#248998=DIRECTION ( 'NONE',  ( 0.000000000000000000, -7.304098846218112382E-15, 1.000000000000000000 ) ) ;
#249044=EDGE_LOOP ( 'NONE', ( #46802, #29234 ) ) ;
#249047=ORIENTED_EDGE ( 'NONE', *, *, #159407, .T. ) ;
#249050=CARTESIAN_POINT ( 'NONE',  ( -18.59999999999999787, 77.68707439010330518, -82.33768045106596389 ) ) ;
#249063=VERTEX_POINT ( 'NONE', #55458 ) ;
#249065=CIRCLE ( 'NONE', #203255, 0.09999999999999739653 ) ;
#249076=FACE_OUTER_BOUND ( 'NONE', #182273, .T. ) ;
#249111=CYLINDRICAL_SURFACE ( 'NONE', #98176, 0.09999999999999939493 ) ;
#249114=ORIENTED_EDGE ( 'NONE', *, *, #76310, .F. ) ;
#249150=CARTESIAN_POINT ( 'NONE',  ( 20.94999999999999574, 74.75000000001159606, -61.62310748452433273 ) ) ;
#249176=CIRCLE ( 'NONE', #153927, 0.09999999999999939493 ) ;
#249192=CARTESIAN_POINT ( 'NONE',  ( 23.15000000000000213, 85.60000000001149090, -45.91707660717669626 ) ) ;
#249200=AXIS2_PLACEMENT_3D ( 'NONE', #224503, #109682, #249217 ) ;
#249209=ADVANCED_FACE ( 'NONE', ( #130747 ), #109886, .T. ) ;
#249217=DIRECTION ( 'NONE',  ( 1.000000000000000000, 0.000000000000000000, 0.000000000000000000 ) ) ;
#249227=CARTESIAN_POINT ( 'NONE',  ( -20.85000000000000142, 69.06610602788505560, -32.23746165015079868 ) ) ;
#249284=VECTOR ( 'NONE', #143623, 1000.000000000000000 ) ;
#249285=DIRECTION ( 'NONE',  ( 1.000000000000000000, 0.000000000000000000, 0.000000000000000000 ) ) ;
#249308=ORIENTED_EDGE ( 'NONE', *, *, #119104, .F. ) ;
#249322=EDGE_LOOP ( 'NONE', ( #9398, #8070, #206159, #47197, #237056, #133416, #228590, #254267, #150513 ) ) ;
#249369=DIRECTION ( 'NONE',  ( 0.000000000000000000, -1.000000000000000000, -7.272083257015735086E-15 ) ) ;
#249453=DIRECTION ( 'NONE',  ( 0.7071067811865127117, 0.7071067811865821007, 0.000000000000000000 ) ) ;
#249456=CARTESIAN_POINT ( 'NONE',  ( 20.95575313997065336, 65.38544669673677845, -61.90181678257957287 ) ) ;
#249477=DIRECTION ( 'NONE',  ( 1.000000000000000000, 0.000000000000000000, 0.000000000000000000 ) ) ;
#249528=CARTESIAN_POINT ( 'NONE',  ( 20.94999999999999574, 64.37928932189281284, -42.89152413686537102 ) ) ;
#249563=DIRECTION ( 'NONE',  ( 0.000000000000000000, -1.000000000000000000, -6.982962677686265922E-15 ) ) ;
#249578=CARTESIAN_POINT ( 'NONE',  ( 21.12769345151713196, 65.28071232307100047, -57.27562713832691799 ) ) ;
#249582=EDGE_CURVE ( 'NONE', #13982, #192458, #229969, .T. ) ;
#249585=FACE_OUTER_BOUND ( 'NONE', #216123, .T. ) ;
#249587=ADVANCED_FACE ( 'NONE', ( #138789 ), #116700, .F. ) ;
#249592=CIRCLE ( 'NONE', #191156, 11.89999999999999325 ) ;
#249664=FACE_OUTER_BOUND ( 'NONE', #120147, .T. ) ;
#249690=FACE_OUTER_BOUND ( 'NONE', #242998, .T. ) ;
#249702=DIRECTION ( 'NONE',  ( 0.000000000000000000, 7.086529944415894657E-15, -1.000000000000000000 ) ) ;
#249720=ORIENTED_EDGE ( 'NONE', *, *, #250248, .T. ) ;
#249735=AXIS2_PLACEMENT_3D ( 'NONE', #176966, #232117, #256400 ) ;
#249751=DIRECTION ( 'NONE',  ( 0.000000000000000000, -6.982962677686266711E-15, 1.000000000000000000 ) ) ;
#249752=EDGE_LOOP ( 'NONE', ( #254652, #24519, #73149, #203764 ) ) ;
#249757=EDGE_CURVE ( 'NONE', #255281, #89873, #34183, .T. ) ;
#249760=DIRECTION ( 'NONE',  ( 1.000000000000000000, 0.000000000000000000, 0.000000000000000000 ) ) ;
#249792=AXIS2_PLACEMENT_3D ( 'NONE', #227060, #30177, #10601 ) ;
#249832=AXIS2_PLACEMENT_3D ( 'NONE', #29603, #115206, #17395 ) ;
#249848=LINE ( 'NONE', #50335, #202329 ) ;
#249873=CARTESIAN_POINT ( 'NONE',  ( 18.59999999999999787, 76.00000000001165290, -69.52310748452431710 ) ) ;
#249896=ORIENTED_EDGE ( 'NONE', *, *, #233898, .T. ) ;
#249909=ORIENTED_EDGE ( 'NONE', *, *, #244181, .F. ) ;
#249922=EDGE_CURVE ( 'NONE', #126775, #90553, #236350, .T. ) ;
#249934=ORIENTED_EDGE ( 'NONE', *, *, #84324, .T. ) ;
#249964=VECTOR ( 'NONE', #116369, 1000.000000000000000 ) ;
#249986=ORIENTED_EDGE ( 'NONE', *, *, #80024, .F. ) ;
#249998=ORIENTED_EDGE ( 'NONE', *, *, #121264, .T. ) ;
#250074=CARTESIAN_POINT ( 'NONE',  ( -18.59999999999999787, 64.35000000001174669, -81.27310748452440237 ) ) ;
#250116=DIRECTION ( 'NONE',  ( 0.7071067811865474617, -0.7071067811865474617, -4.937700262164531476E-15 ) ) ;
#250119=VECTOR ( 'NONE', #138788, 1000.000000000000000 ) ;
#250174=CIRCLE ( 'NONE', #91938, 0.1000000000000028644 ) ;
#250184=LINE ( 'NONE', #170694, #150037 ) ;
#250192=ORIENTED_EDGE ( 'NONE', *, *, #94630, .T. ) ;
#250195=CARTESIAN_POINT ( 'NONE',  ( 22.42196299218230493, 75.99755832602443206, -81.17271918717379720 ) ) ;
#250226=DIRECTION ( 'NONE',  ( 1.000000000000000000, 0.000000000000000000, 0.000000000000000000 ) ) ;
#250248=EDGE_CURVE ( 'NONE', #151129, #203482, #55149, .T. ) ;
#250251=ORIENTED_EDGE ( 'NONE', *, *, #102947, .T. ) ;
#250259=CARTESIAN_POINT ( 'NONE',  ( 20.95000000000000284, 64.40000000001145963, -42.95131071479990936 ) ) ;
#250293=LINE ( 'NONE', #212468, #92431 ) ;
#250300=ORIENTED_EDGE ( 'NONE', *, *, #140788, .F. ) ;
#250305=VERTEX_POINT ( 'NONE', #53556 ) ;
#250315=CARTESIAN_POINT ( 'NONE',  ( 23.14999999999999858, 76.00000000001142553, -36.02310748452432421 ) ) ;
#250348=EDGE_CURVE ( 'NONE', #12040, #127785, #26338, .T. ) ;
#250355=AXIS2_PLACEMENT_3D ( 'NONE', #189800, #208097, #108960 ) ;
#250365=DIRECTION ( 'NONE',  ( -1.000000000000000000, 0.000000000000000000, 0.000000000000000000 ) ) ;
#250389=CARTESIAN_POINT ( 'NONE',  ( -18.59999999999999787, 77.25000000001136868, -28.22262673010923351 ) ) ;
#250434=DIRECTION ( 'NONE',  ( 1.000000000000000000, 0.000000000000000000, 0.000000000000000000 ) ) ;
#250436=EDGE_CURVE ( 'NONE', #230638, #211078, #142810, .T. ) ;
#250472=LINE ( 'NONE', #32760, #12091 ) ;
#250474=VECTOR ( 'NONE', #54743, 1000.000000000000000 ) ;
#250484=DIRECTION ( 'NONE',  ( 0.000000000000000000, 0.8777080977375072424, -0.4791956752371691608 ) ) ;
#250499=EDGE_CURVE ( 'NONE', #7765, #189565, #176190, .T. ) ;
#250547=CARTESIAN_POINT ( 'NONE',  ( 21.05000000000000071, 76.00000000001142553, -36.02310748452432421 ) ) ;
#250549=VERTEX_POINT ( 'NONE', #205892 ) ;
#250553=CARTESIAN_POINT ( 'NONE',  ( 20.94999999999999929, 76.00000000001142553, -36.02310748452432421 ) ) ;
#250555=EDGE_CURVE ( 'NONE', #20329, #124432, #28604, .T. ) ;
#250571=ADVANCED_FACE ( 'NONE', ( #235718 ), #154939, .T. ) ;
#250572=ORIENTED_EDGE ( 'NONE', *, *, #26803, .F. ) ;
#250596=CARTESIAN_POINT ( 'NONE',  ( -20.85000000000000142, 76.00000000001142553, -36.02310748452432421 ) ) ;
#250652=CARTESIAN_POINT ( 'NONE',  ( 20.95512820512820440, 67.12384868372345181, -57.37310748452438247 ) ) ;
#250670=PLANE ( 'NONE',  #227230 ) ;
#250680=DIRECTION ( 'NONE',  ( 1.000000000000000000, 0.000000000000000000, 0.000000000000000000 ) ) ;
#250722=ADVANCED_FACE ( 'NONE', ( #217424 ), #173242, .T. ) ;
#250733=FACE_OUTER_BOUND ( 'NONE', #16253, .T. ) ;
#250747=CARTESIAN_POINT ( 'NONE',  ( 22.39999999999999858, 68.20922040163827660, -69.62310748452438247 ) ) ;
#250794=DIRECTION ( 'NONE',  ( 0.000000000000000000, -6.982962677686266711E-15, 1.000000000000000000 ) ) ;
#250800=CARTESIAN_POINT ( 'NONE',  ( -22.50000000000088463, 75.95463834342392317, -81.17361631873501437 ) ) ;
#250819=AXIS2_PLACEMENT_3D ( 'NONE', #72840, #75407, #194060 ) ;
#250823=ORIENTED_EDGE ( 'NONE', *, *, #208917, .F. ) ;
#250832=CYLINDRICAL_SURFACE ( 'NONE', #118394, 0.09999999999999939493 ) ;
#250839=ORIENTED_EDGE ( 'NONE', *, *, #67135, .T. ) ;
#250844=DIRECTION ( 'NONE',  ( 0.000000000000000000, 1.000000000000000000, 6.982962677686266711E-15 ) ) ;
#250849=EDGE_CURVE ( 'NONE', #136730, #193535, #109699, .T. ) ;
#250851=PLANE ( 'NONE',  #235643 ) ;
#250874=EDGE_LOOP ( 'NONE', ( #164302, #60129, #71302, #120345 ) ) ;
#250891=CARTESIAN_POINT ( 'NONE',  ( -21.05000000000000071, 87.65000000001144542, -39.12310748452424747 ) ) ;
#250897=DIRECTION ( 'NONE',  ( 0.000000000000000000, 6.982962677686266711E-15, -1.000000000000000000 ) ) ;
#250929=CARTESIAN_POINT ( 'NONE',  ( -18.59999999999999787, 68.92903212821255465, -32.27654326265606954 ) ) ;
#250945=AXIS2_PLACEMENT_3D ( 'NONE', #52113, #181697, #149973 ) ;
#250991=ORIENTED_EDGE ( 'NONE', *, *, #187524, .T. ) ;
#250993=DIRECTION ( 'NONE',  ( 1.000000000000000000, 0.000000000000000000, 0.000000000000000000 ) ) ;
#251020=FACE_OUTER_BOUND ( 'NONE', #52171, .T. ) ;
#251021=ORIENTED_EDGE ( 'NONE', *, *, #96735, .T. ) ;
#251033=AXIS2_PLACEMENT_3D ( 'NONE', #225393, #143302, #222831 ) ;
#251046=ORIENTED_EDGE ( 'NONE', *, *, #9693, .T. ) ;
#251053=DIRECTION ( 'NONE',  ( -0.000000000000000000, 0.1298341882519668811, 0.9915357197604899309 ) ) ;
#251059=CARTESIAN_POINT ( 'NONE',  ( 23.14999999999998437, 76.00000000001168132, -73.57310748452432847 ) ) ;
#251080=VECTOR ( 'NONE', #133011, 1000.000000000000000 ) ;
#251113=AXIS2_PLACEMENT_3D ( 'NONE', #252741, #75436, #197906 ) ;
#251130=CARTESIAN_POINT ( 'NONE',  ( 22.39999999999999858, 75.90000000001170122, -77.31388708289770761 ) ) ;
#251171=CIRCLE ( 'NONE', #59626, 0.1000000000000028644 ) ;
#251193=CIRCLE ( 'NONE', #17971, 4.049999999999998046 ) ;
#251223=( BOUNDED_SURFACE ( )  B_SPLINE_SURFACE ( 3, 2, ( 
 ( #5611, #27812, #185564 ),
 ( #109864, #189428, #166030 ),
 ( #228559, #124314, #66899 ),
 ( #107305, #186870, #146414 ),
 ( #47313, #8226, #87729 ),
 ( #227252, #246812, #104699 ) ),
 .UNSPECIFIED., .F., .F., .F. ) 
 B_SPLINE_SURFACE_WITH_KNOTS ( ( 4, 2, 4 ),
 ( 3, 3 ),
 ( 6.719893378900507978E-05, 0.0002757154632485607666, 0.0004842319927081164535 ),
 ( 0.000000000000000000, 1.000000000000000000 ),
 .UNSPECIFIED. ) 
 GEOMETRIC_REPRESENTATION_ITEM ( )  RATIONAL_B_SPLINE_SURFACE ( (
 ( 1.000000000000000000, 0.7250110520819756932, 1.000000000000000000),
 ( 1.000000000000000000, 0.7277932058353090428, 1.000000000000000000),
 ( 1.000000000000000000, 0.7278452872625645886, 1.000000000000000000),
 ( 1.000000000000000000, 0.7221445671541159017, 1.000000000000000000),
 ( 1.000000000000000000, 0.7163662143785587411, 1.000000000000000000),
 ( 1.000000000000000000, 0.7071067811865475727, 1.000000000000000000) ) ) 
 REPRESENTATION_ITEM ( '' )  SURFACE ( )  );
#251238=CARTESIAN_POINT ( 'NONE',  ( 18.59999999999999787, 86.35479209693686187, -42.26656650145049099 ) ) ;
#251253=DIRECTION ( 'NONE',  ( -0.000000000000000000, 1.000000000000000000, 6.982962677686266711E-15 ) ) ;
#251263=ORIENTED_EDGE ( 'NONE', *, *, #135745, .T. ) ;
#251301=VERTEX_POINT ( 'NONE', #53597 ) ;
#251318=DIRECTION ( 'NONE',  ( 2.952720810173289112E-16, 1.000000000000000000, 6.982962677686266711E-15 ) ) ;
#251320=DIRECTION ( 'NONE',  ( 0.000000000000000000, -7.147358527629762208E-15, 1.000000000000000000 ) ) ;
#251339=VERTEX_POINT ( 'NONE', #109702 ) ;
#251342=EDGE_CURVE ( 'NONE', #26458, #106961, #218197, .T. ) ;
#251353=AXIS2_PLACEMENT_3D ( 'NONE', #59928, #140777, #96488 ) ;
#251361=LINE ( 'NONE', #210964, #62284 ) ;
#251384=EDGE_CURVE ( 'NONE', #35500, #139208, #147561, .T. ) ;
#251394=ORIENTED_EDGE ( 'NONE', *, *, #127198, .T. ) ;
#251435=AXIS2_PLACEMENT_3D ( 'NONE', #154589, #159700, #256150 ) ;
#251450=DIRECTION ( 'NONE',  ( 0.000000000000000000, -1.000000000000000000, 0.000000000000000000 ) ) ;
#251498=CARTESIAN_POINT ( 'NONE',  ( -23.15000000000000213, 85.60000000001150511, -45.91707660717669626 ) ) ;
#251546=CARTESIAN_POINT ( 'NONE',  ( -20.54999999999999716, 74.05981308412367525, -48.85222669557766295 ) ) ;
#251553=VECTOR ( 'NONE', #94017, 1000.000000000000000 ) ;
#251560=( BOUNDED_CURVE ( )  B_SPLINE_CURVE ( 3, ( #4279, #71981, #172402, #214049 ),
 .UNSPECIFIED., .F., .T. ) 
 B_SPLINE_CURVE_WITH_KNOTS ( ( 4, 4 ),
 ( 3.192897208853993085, 4.712388980384689674 ),
 .UNSPECIFIED. ) 
 CURVE ( )  GEOMETRIC_REPRESENTATION_ITEM ( )  RATIONAL_B_SPLINE_CURVE ( ( 1.000000000000000000, 0.8166740347213228279, 0.8166740347213228279, 1.000000000000000000 ) ) 
 REPRESENTATION_ITEM ( '' )  );
#251589=ORIENTED_EDGE ( 'NONE', *, *, #206244, .F. ) ;
#251609=DIRECTION ( 'NONE',  ( 1.000000000000000000, 0.000000000000000000, 0.000000000000000000 ) ) ;
#251642=VERTEX_POINT ( 'NONE', #208528 ) ;
#251666=LINE ( 'NONE', #152604, #209147 ) ;
#251681=CIRCLE ( 'NONE', #114296, 0.09999999999999939493 ) ;
#251699=ORIENTED_EDGE ( 'NONE', *, *, #84568, .F. ) ;
#251713=LINE ( 'NONE', #71810, #179818 ) ;
#251744=DIRECTION ( 'NONE',  ( 1.000000000000000000, 0.000000000000000000, 0.000000000000000000 ) ) ;
#251754=VERTEX_POINT ( 'NONE', #106823 ) ;
#251759=VECTOR ( 'NONE', #180771, 1000.000000000000000 ) ;
#251770=CARTESIAN_POINT ( 'NONE',  ( -20.64999999999999858, 68.85000000001156195, -57.17310748452437252 ) ) ;
#251786=CIRCLE ( 'NONE', #226839, 0.1000000000000028644 ) ;
#251837=EDGE_CURVE ( 'NONE', #6871, #119497, #154978, .T. ) ;
#251864=AXIS2_PLACEMENT_3D ( 'NONE', #157977, #134493, #99214 ) ;
#251904=ORIENTED_EDGE ( 'NONE', *, *, #1031, .T. ) ;
#251917=CARTESIAN_POINT ( 'NONE',  ( -21.05000000000000071, 64.25000000001146816, -43.03791325517834565 ) ) ;
#251938=ORIENTED_EDGE ( 'NONE', *, *, #146312, .T. ) ;
#252018=PLANE ( 'NONE',  #24244 ) ;
#252023=LINE ( 'NONE', #147805, #140153 ) ;
#252051=EDGE_CURVE ( 'NONE', #202854, #231849, #102641, .T. ) ;
#252114=VECTOR ( 'NONE', #123912, 1000.000000000000000 ) ;
#252124=CARTESIAN_POINT ( 'NONE',  ( 21.05000000000000071, 77.84908441863859707, -57.86709696307718787 ) ) ;
#252134=ADVANCED_FACE ( 'NONE', ( #50375 ), #129922, .T. ) ;
#252136=DIRECTION ( 'NONE',  ( -1.000000000000000000, -0.000000000000000000, -0.000000000000000000 ) ) ;
#252138=ORIENTED_EDGE ( 'NONE', *, *, #235202, .T. ) ;
#252144=VECTOR ( 'NONE', #198063, 1000.000000000000000 ) ;
#252171=CARTESIAN_POINT ( 'NONE',  ( 21.07928932188134397, 75.90110485435729970, -75.85162414091763594 ) ) ;
#252178=DIRECTION ( 'NONE',  ( -1.000000000000000000, 0.000000000000000000, 0.000000000000000000 ) ) ;
#252221=CARTESIAN_POINT ( 'NONE',  ( 18.49999999999999289, 69.55000000001173532, -81.27310748452437394 ) ) ;
#252299=TOROIDAL_SURFACE ( 'NONE', #102249, 0.4000000000000010214, 0.1000000000000000056 ) ;
#252312=CIRCLE ( 'NONE', #198160, 12.87499999999999822 ) ;
#252332=CARTESIAN_POINT ( 'NONE',  ( -23.25000000000000000, 77.73670573947892137, -24.50568489690058627 ) ) ;
#252334=DIRECTION ( 'NONE',  ( 1.000000000000000000, 0.000000000000000000, 0.000000000000000000 ) ) ;
#252358=PLANE ( 'NONE',  #50701 ) ;
#252377=FACE_OUTER_BOUND ( 'NONE', #190164, .T. ) ;
#252395=EDGE_CURVE ( 'NONE', #88477, #187198, #196792, .T. ) ;
#252403=EDGE_CURVE ( 'NONE', #33572, #67782, #178073, .T. ) ;
#252409=AXIS2_PLACEMENT_3D ( 'NONE', #148213, #227745, #166525 ) ;
#252412=AXIS2_PLACEMENT_3D ( 'NONE', #250315, #212489, #112111 ) ;
#252421=DIRECTION ( 'NONE',  ( -2.940209281316621016E-16, -1.000000000000000000, -4.704334850106593625E-15 ) ) ;
#252428=VECTOR ( 'NONE', #187145, 1000.000000000000000 ) ;
#252431=DIRECTION ( 'NONE',  ( 0.000000000000000000, 0.000000000000000000, 1.000000000000000000 ) ) ;
#252456=ADVANCED_FACE ( 'NONE', ( #7106, #166230, #67093 ), #106200, .F. ) ;
#252466=CARTESIAN_POINT ( 'NONE',  ( -20.87155475150660777, 64.25000000001148237, -42.92752095536695123 ) ) ;
#252474=CARTESIAN_POINT ( 'NONE',  ( 21.07928932188134397, 69.67148334361834827, -69.62200263017876978 ) ) ;
#252507=CIRCLE ( 'NONE', #52612, 0.1000000000000060146 ) ;
#252575=AXIS2_PLACEMENT_3D ( 'NONE', #16217, #137409, #193555 ) ;
#252590=ORIENTED_EDGE ( 'NONE', *, *, #82379, .F. ) ;
#252603=AXIS2_PLACEMENT_3D ( 'NONE', #85310, #157548, #204001 ) ;
#252656=EDGE_CURVE ( 'NONE', #201700, #239369, #238876, .T. ) ;
#252677=VERTEX_POINT ( 'NONE', #204863 ) ;
#252693=AXIS2_PLACEMENT_3D ( 'NONE', #12136, #72096, #91647 ) ;
#252710=CARTESIAN_POINT ( 'NONE',  ( 22.60000000000000142, 64.25043287652226809, -69.62396585362311896 ) ) ;
#252711=ADVANCED_FACE ( 'NONE', ( #31419 ), #19035, .F. ) ;
#252741=CARTESIAN_POINT ( 'NONE',  ( -20.64999999999999858, 85.00000000001149658, -45.91707660717669626 ) ) ;
#252752=CIRCLE ( 'NONE', #36121, 0.09999999999999939493 ) ;
#252757=PLANE ( 'NONE',  #255015 ) ;
#252777=CARTESIAN_POINT ( 'NONE',  ( -18.48179518609241612, 85.51832530050492664, -29.13340190776325400 ) ) ;
#252781=LINE ( 'NONE', #175847, #88002 ) ;
#252822=EDGE_CURVE ( 'NONE', #108916, #160136, #233460, .T. ) ;
#252824=DIRECTION ( 'NONE',  ( -0.000000000000000000, 1.000000000000000000, 6.982962677686266711E-15 ) ) ;
#252841=CIRCLE ( 'NONE', #107107, 0.09999999999999939493 ) ;
#252883=EDGE_CURVE ( 'NONE', #2960, #207654, #213868, .T. ) ;
#252910=CARTESIAN_POINT ( 'NONE',  ( -20.94999999999999929, 70.10000000001163301, -59.30400771986794695 ) ) ;
#252925=CARTESIAN_POINT ( 'NONE',  ( -21.13435531349822583, 69.50627893641943444, -69.52310748452437394 ) ) ;
#252949=AXIS2_PLACEMENT_3D ( 'NONE', #237051, #77960, #35041 ) ;
#252953=B_SPLINE_CURVE_WITH_KNOTS ( 'NONE', 3,
 ( #142460, #221974, #122922, #202449, #23837, #69374, #206305, #48503, #147606, #245438 ),
 .UNSPECIFIED., .F., .F.,
 ( 4, 2, 2, 2, 4 ),
 ( 0.000000000000000000, 4.221631689686969747E-05, 8.443263379373939495E-05, 0.0001688652675874697639, 0.0003377305351749538393 ),
 .UNSPECIFIED. ) ;
#252978=EDGE_LOOP ( 'NONE', ( #151993, #13777, #109814 ) ) ;
#252998=LINE ( 'NONE', #74411, #142329 ) ;
#253009=DIRECTION ( 'NONE',  ( 0.7071067811865127117, 0.7071067811865821007, 0.000000000000000000 ) ) ;
#253015=DIRECTION ( 'NONE',  ( 0.000000000000000000, -0.9274965247785323941, -0.3738317757009769760 ) ) ;
#253026=CIRCLE ( 'NONE', #198858, 0.1000000000000028644 ) ;
#253039=DIRECTION ( 'NONE',  ( -0.000000000000000000, -6.982962677686266711E-15, 1.000000000000000000 ) ) ;
#253087=ORIENTED_EDGE ( 'NONE', *, *, #57178, .F. ) ;
#253096=LINE ( 'NONE', #28976, #208395 ) ;
#253100=CARTESIAN_POINT ( 'NONE',  ( 21.05000000000000071, 76.00000000001139711, -32.02310748452432421 ) ) ;
#253154=CIRCLE ( 'NONE', #36720, 0.5000000000000004441 ) ;
#253184=CIRCLE ( 'NONE', #45082, 0.5000000000000004441 ) ;
#253203=DIRECTION ( 'NONE',  ( 1.000000000000000000, 0.000000000000000000, 0.000000000000000000 ) ) ;
#253214=VECTOR ( 'NONE', #220152, 1000.000000000000000 ) ;
#253234=ORIENTED_EDGE ( 'NONE', *, *, #161467, .T. ) ;
#253237=ORIENTED_EDGE ( 'NONE', *, *, #30240, .F. ) ;
#253244=DIRECTION ( 'NONE',  ( 0.000000000000000000, -0.1575844902526579161, -0.9875055080513779338 ) ) ;
#253264=VECTOR ( 'NONE', #9311, 1000.000000000000000 ) ;
#253281=CARTESIAN_POINT ( 'NONE',  ( 21.05000000000000071, 64.25000000001146816, -43.03791325517834565 ) ) ;
#253287=ADVANCED_FACE ( 'NONE', ( #39917, #17732 ), #62030, .T. ) ;
#253303=DIRECTION ( 'NONE',  ( 0.000000000000000000, 0.000000000000000000, 1.000000000000000000 ) ) ;
#253326=DIRECTION ( 'NONE',  ( 0.000000000000000000, 0.000000000000000000, 1.000000000000000000 ) ) ;
#253340=VERTEX_POINT ( 'NONE', #4595 ) ;
#253346=ADVANCED_FACE ( 'NONE', ( #24194 ), #103681, .F. ) ;
#253347=AXIS2_PLACEMENT_3D ( 'NONE', #121449, #180118, #183955 ) ;
#253352=CARTESIAN_POINT ( 'NONE',  ( -23.15000000000000213, 84.59626168225447884, -45.47323500167453858 ) ) ;
#253359=ORIENTED_EDGE ( 'NONE', *, *, #89643, .T. ) ;
#253364=ORIENTED_EDGE ( 'NONE', *, *, #228179, .T. ) ;
#253370=CARTESIAN_POINT ( 'NONE',  ( -20.64999999999999858, 74.07476635515169505, -48.75335101765046630 ) ) ;
#253373=VERTEX_POINT ( 'NONE', #46291 ) ;
#253377=CIRCLE ( 'NONE', #49372, 11.80000000000000426 ) ;
#253386=ORIENTED_EDGE ( 'NONE', *, *, #153010, .F. ) ;
#253401=VERTEX_POINT ( 'NONE', #73609 ) ;
#253420=CARTESIAN_POINT ( 'NONE',  ( 20.94999999999999929, 71.18691588786198565, -47.96462524104817504 ) ) ;
#253442=CIRCLE ( 'NONE', #32930, 0.1999999999999987899 ) ;
#253480=CYLINDRICAL_SURFACE ( 'NONE', #225031, 0.09999999999999939493 ) ;
#253489=EDGE_CURVE ( 'NONE', #201868, #34147, #89556, .T. ) ;
#253504=CARTESIAN_POINT ( 'NONE',  ( 21.09107601085543493, 75.96069283529440952, -75.88698545988413002 ) ) ;
#253537=AXIS2_PLACEMENT_3D ( 'NONE', #14063, #115716, #37476 ) ;
#253558=CARTESIAN_POINT ( 'NONE',  ( -21.05000000000000071, 74.83729825007360148, -61.62310748452433273 ) ) ;
#253562=EDGE_CURVE ( 'NONE', #88538, #148964, #194836, .T. ) ;
#253572=DIRECTION ( 'NONE',  ( 1.000000000000000000, 0.000000000000000000, 0.000000000000000000 ) ) ;
#253578=DIRECTION ( 'NONE',  ( 0.000000000000000000, 0.000000000000000000, 1.000000000000000000 ) ) ;
#253631=EDGE_LOOP ( 'NONE', ( #64573, #71427, #126667, #181595 ) ) ;
#253634=DIRECTION ( 'NONE',  ( 0.000000000000000000, -6.853228547068871147E-15, 1.000000000000000000 ) ) ;
#253635=EDGE_CURVE ( 'NONE', #172698, #147150, #64617, .T. ) ;
#253707=ORIENTED_EDGE ( 'NONE', *, *, #173646, .T. ) ;
#253708=ORIENTED_EDGE ( 'NONE', *, *, #36091, .T. ) ;
#253741=AXIS2_PLACEMENT_3D ( 'NONE', #119609, #101253, #242090 ) ;
#253751=CARTESIAN_POINT ( 'NONE',  ( -21.04386569057605527, 64.25000000001146816, -42.88027013274443533 ) ) ;
#253752=EDGE_LOOP ( 'NONE', ( #8506, #86261, #195702, #177930 ) ) ;
#253764=AXIS2_PLACEMENT_3D ( 'NONE', #240891, #222577, #103909 ) ;
#253767=ADVANCED_FACE ( 'NONE', ( #201221 ), #181675, .T. ) ;
#253773=CYLINDRICAL_SURFACE ( 'NONE', #60309, 0.1000000000000026007 ) ;
#253805=TOROIDAL_SURFACE ( 'NONE', #99678, 0.2000000000000000111, 0.1000000000000000056 ) ;
#253859=ORIENTED_EDGE ( 'NONE', *, *, #76582, .T. ) ;
#253878=ORIENTED_EDGE ( 'NONE', *, *, #130897, .T. ) ;
#253890=CARTESIAN_POINT ( 'NONE',  ( -23.25000000000000000, 76.00000000001165290, -69.52310748452431710 ) ) ;
#253897=ORIENTED_EDGE ( 'NONE', *, *, #63720, .T. ) ;
#253914=CARTESIAN_POINT ( 'NONE',  ( -22.49231231312463208, 64.35001509633437422, -69.58416037212577976 ) ) ;
#253948=ORIENTED_EDGE ( 'NONE', *, *, #234159, .F. ) ;
#253955=CIRCLE ( 'NONE', #62452, 0.1000000000000028783 ) ;
#253983=ADVANCED_FACE ( 'NONE', ( #214064 ), #100499, .T. ) ;
#254089=ORIENTED_EDGE ( 'NONE', *, *, #38099, .T. ) ;
#254094=AXIS2_PLACEMENT_3D ( 'NONE', #75509, #153793, #194172 ) ;
#254100=ORIENTED_EDGE ( 'NONE', *, *, #209231, .T. ) ;
#254117=CIRCLE ( 'NONE', #149924, 0.1000000000000028783 ) ;
#254142=CARTESIAN_POINT ( 'NONE',  ( -20.85000000000000142, 87.75000000001142553, -36.02310748452423894 ) ) ;
#254153=CARTESIAN_POINT ( 'NONE',  ( -21.64999999999999858, 68.65000000001157332, -57.27310748452437394 ) ) ;
#254221=FACE_OUTER_BOUND ( 'NONE', #210154, .T. ) ;
#254243=VECTOR ( 'NONE', #177288, 1000.000000000000000 ) ;
#254255=EDGE_CURVE ( 'NONE', #175346, #126775, #223203, .T. ) ;
#254267=ORIENTED_EDGE ( 'NONE', *, *, #28142, .T. ) ;
#254272=DIRECTION ( 'NONE',  ( -0.000000000000000000, 1.000000000000000000, 6.982962677686266711E-15 ) ) ;
#254277=CARTESIAN_POINT ( 'NONE',  ( 20.89192007715127986, 65.67101464000451472, -30.44043916224795510 ) ) ;
#254316=FACE_OUTER_BOUND ( 'NONE', #185046, .T. ) ;
#254342=LINE ( 'NONE', #18321, #43571 ) ;
#254343=ORIENTED_EDGE ( 'NONE', *, *, #86341, .F. ) ;
#254346=EDGE_LOOP ( 'NONE', ( #228890, #163103, #71428 ) ) ;
#254357=CARTESIAN_POINT ( 'NONE',  ( -22.50000000000000000, 76.00000000001165290, -69.52310748452431710 ) ) ;
#254364=DIRECTION ( 'NONE',  ( 0.000000000000000000, 7.116814260417668513E-15, -1.000000000000000000 ) ) ;
#254366=DIRECTION ( 'NONE',  ( 0.000000000000000000, -6.982962677686266711E-15, 1.000000000000000000 ) ) ;
#254392=AXIS2_PLACEMENT_3D ( 'NONE', #95601, #113886, #52620 ) ;
#254427=ORIENTED_EDGE ( 'NONE', *, *, #185727, .T. ) ;
#254450=DIRECTION ( 'NONE',  ( 0.000000000000000000, 0.000000000000000000, -1.000000000000000000 ) ) ;
#254458=ORIENTED_EDGE ( 'NONE', *, *, #21380, .F. ) ;
#254463=CARTESIAN_POINT ( 'NONE',  ( -23.25000000000000000, 77.83585931145498193, -24.51866831572578675 ) ) ;
#254505=DIRECTION ( 'NONE',  ( 0.000000000000000000, -6.982962677686267499E-15, 1.000000000000000000 ) ) ;
#254518=CARTESIAN_POINT ( 'NONE',  ( 21.05000000000000071, 85.00000000001149658, -45.91707660717670336 ) ) ;
#254532=DIRECTION ( 'NONE',  ( -1.000000000000000000, 0.000000000000000000, 0.000000000000000000 ) ) ;
#254542=CIRCLE ( 'NONE', #204490, 0.1000000000000028644 ) ;
#254561=ORIENTED_EDGE ( 'NONE', *, *, #139149, .T. ) ;
#254562=ORIENTED_EDGE ( 'NONE', *, *, #231527, .F. ) ;
#254596=VECTOR ( 'NONE', #21260, 1000.000000000000000 ) ;
#254599=FACE_OUTER_BOUND ( 'NONE', #184918, .T. ) ;
#254622=ORIENTED_EDGE ( 'NONE', *, *, #5172, .T. ) ;
#254632=ORIENTED_EDGE ( 'NONE', *, *, #69680, .F. ) ;
#254633=EDGE_CURVE ( 'NONE', #234345, #53002, #73586, .T. ) ;
#254635=VECTOR ( 'NONE', #222339, 1000.000000000000000 ) ;
#254652=ORIENTED_EDGE ( 'NONE', *, *, #60810, .F. ) ;
#254679=ORIENTED_EDGE ( 'NONE', *, *, #234061, .F. ) ;
#254682=EDGE_CURVE ( 'NONE', #34877, #85029, #196130, .T. ) ;
#254723=ADVANCED_FACE ( 'NONE', ( #3041 ), #182083, .T. ) ;
#254735=FACE_OUTER_BOUND ( 'NONE', #193498, .T. ) ;
#254740=ORIENTED_EDGE ( 'NONE', *, *, #81730, .T. ) ;
#254793=ORIENTED_EDGE ( 'NONE', *, *, #173284, .F. ) ;
#254797=ORIENTED_EDGE ( 'NONE', *, *, #138465, .T. ) ;
#254807=EDGE_CURVE ( 'NONE', #211829, #206022, #13343, .T. ) ;
#254817=CARTESIAN_POINT ( 'NONE',  ( 18.49999999999999645, 77.29973367124252093, -79.49497796165491081 ) ) ;
#254823=CARTESIAN_POINT ( 'NONE',  ( 23.15000000000000213, 87.75000000001143974, -39.12310748452424747 ) ) ;
#254842=AXIS2_PLACEMENT_3D ( 'NONE', #154289, #233787, #253326 ) ;
#254881=AXIS2_PLACEMENT_3D ( 'NONE', #198317, #197021, #217858 ) ;
#254923=AXIS2_PLACEMENT_3D ( 'NONE', #243762, #245046, #204619 ) ;
#254956=EDGE_LOOP ( 'NONE', ( #212667, #6443, #90625, #188864 ) ) ;
#254963=CIRCLE ( 'NONE', #109276, 0.09999999999999939493 ) ;
#254970=VERTEX_POINT ( 'NONE', #117571 ) ;
#254988=CARTESIAN_POINT ( 'NONE',  ( 21.05000000000000426, 69.69981666374535223, -69.57443491686539971 ) ) ;
#255015=AXIS2_PLACEMENT_3D ( 'NONE', #153733, #136659, #214928 ) ;
#255021=DIRECTION ( 'NONE',  ( 1.000000000000000000, 0.000000000000000000, 0.000000000000000000 ) ) ;
#255038=CARTESIAN_POINT ( 'NONE',  ( 18.50000000000000711, 85.41907808086091336, -29.19318213431596121 ) ) ;
#255051=ORIENTED_EDGE ( 'NONE', *, *, #6940, .F. ) ;
#255069=EDGE_CURVE ( 'NONE', #97864, #64945, #66019, .T. ) ;
#255089=DIRECTION ( 'NONE',  ( 1.301042606982683734E-14, 0.8660254037844367092, -0.5000000000000037748 ) ) ;
#255098=CARTESIAN_POINT ( 'NONE',  ( -20.94999999999999929, 69.15387683765879956, -32.28538121767450519 ) ) ;
#255115=DIRECTION ( 'NONE',  ( 0.000000000000000000, -7.086529944415893080E-15, 1.000000000000000000 ) ) ;
#255147=ORIENTED_EDGE ( 'NONE', *, *, #112142, .T. ) ;
#255178=EDGE_CURVE ( 'NONE', #17643, #92561, #178473, .T. ) ;
#255192=CARTESIAN_POINT ( 'NONE',  ( 23.24999999999999289, 69.35000000001151932, -48.17310748452437252 ) ) ;
#255209=CARTESIAN_POINT ( 'NONE',  ( -21.05000000000000071, 87.65000000001163016, -66.62310748452424036 ) ) ;
#255214=AXIS2_PLACEMENT_3D ( 'NONE', #255547, #174836, #75699 ) ;
#255262=DIRECTION ( 'NONE',  ( 0.000000000000000000, 6.982962677686266711E-15, -1.000000000000000000 ) ) ;
#255277=ORIENTED_EDGE ( 'NONE', *, *, #141336, .F. ) ;
#255281=VERTEX_POINT ( 'NONE', #229523 ) ;
#255293=ORIENTED_EDGE ( 'NONE', *, *, #23010, .F. ) ;
#255295=DIRECTION ( 'NONE',  ( -0.000000000000000000, -6.982962677686266711E-15, 1.000000000000000000 ) ) ;
#255297=CARTESIAN_POINT ( 'NONE',  ( -21.04999999999999716, 76.08574093704510233, -75.93693377333728733 ) ) ;
#255300=EDGE_LOOP ( 'NONE', ( #65636, #229484, #72707, #121981 ) ) ;
#255306=VERTEX_POINT ( 'NONE', #73046 ) ;
#255315=CYLINDRICAL_SURFACE ( 'NONE', #257035, 0.09999999999999520384 ) ;
#255337=ORIENTED_EDGE ( 'NONE', *, *, #76449, .T. ) ;
#255339=DIRECTION ( 'NONE',  ( 1.000000000000000000, 0.000000000000000000, 0.000000000000000000 ) ) ;
#255349=ORIENTED_EDGE ( 'NONE', *, *, #14867, .F. ) ;
#255356=DIRECTION ( 'NONE',  ( -1.000000000000000000, -0.000000000000000000, -0.000000000000000000 ) ) ;
#255359=TOROIDAL_SURFACE ( 'NONE', #201243, 7.800000000000000711, 0.1000000000000000056 ) ;
#255376=CIRCLE ( 'NONE', #113782, 0.1000000000000028644 ) ;
#255381=EDGE_CURVE ( 'NONE', #102074, #176779, #53555, .T. ) ;
#255431=VECTOR ( 'NONE', #60168, 1000.000000000000000 ) ;
#255449=ORIENTED_EDGE ( 'NONE', *, *, #235771, .F. ) ;
#255463=ORIENTED_EDGE ( 'NONE', *, *, #63762, .T. ) ;
#255499=DIRECTION ( 'NONE',  ( 0.000000000000000000, -6.938893903907222067E-15, 1.000000000000000000 ) ) ;
#255528=CARTESIAN_POINT ( 'NONE',  ( 18.54148534481893762, 65.67467670974366456, -30.45317318268843465 ) ) ;
#255537=CARTESIAN_POINT ( 'NONE',  ( 21.09316766718127667, 69.62984668753723838, -69.56237088683906222 ) ) ;
#255547=CARTESIAN_POINT ( 'NONE',  ( 23.14999999999999858, 76.00000000001142553, -36.02310748452432421 ) ) ;
#255554=FACE_OUTER_BOUND ( 'NONE', #62221, .T. ) ;
#255559=ORIENTED_EDGE ( 'NONE', *, *, #145568, .F. ) ;
#255564=CIRCLE ( 'NONE', #80622, 0.1000000000000052097 ) ;
#255576=ORIENTED_EDGE ( 'NONE', *, *, #185816, .T. ) ;
#255580=DIRECTION ( 'NONE',  ( -1.000000000000000000, 0.000000000000000000, 0.000000000000000000 ) ) ;
#255618=CARTESIAN_POINT ( 'NONE',  ( -18.50000000000000711, 85.41920341803825067, -62.27532167409560060 ) ) ;
#255664=VERTEX_POINT ( 'NONE', #190082 ) ;
#255676=FACE_OUTER_BOUND ( 'NONE', #63753, .T. ) ;
#255746=ORIENTED_EDGE ( 'NONE', *, *, #192555, .T. ) ;
#255777=CIRCLE ( 'NONE', #22802, 0.1000000000000028644 ) ;
#255804=FACE_OUTER_BOUND ( 'NONE', #247398, .T. ) ;
#255819=CARTESIAN_POINT ( 'NONE',  ( 23.25000000000000355, 98.45632476063454419, -62.72920903679256099 ) ) ;
#255870=AXIS2_PLACEMENT_3D ( 'NONE', #138182, #61235, #202035 ) ;
#255903=AXIS2_PLACEMENT_3D ( 'NONE', #232866, #212013, #34666 ) ;
#255909=DIRECTION ( 'NONE',  ( 0.000000000000000000, 6.982962677686266711E-15, -1.000000000000000000 ) ) ;
#255916=ORIENTED_EDGE ( 'NONE', *, *, #171910, .F. ) ;
#255918=AXIS2_PLACEMENT_3D ( 'NONE', #245174, #163087, #241332 ) ;
#255923=DIRECTION ( 'NONE',  ( -1.000000000000000000, 0.000000000000000000, 0.000000000000000000 ) ) ;
#255933=DIRECTION ( 'NONE',  ( 0.000000000000000000, 0.000000000000000000, 1.000000000000000000 ) ) ;
#255945=ADVANCED_FACE ( 'NONE', ( #45121 ), #242031, .T. ) ;
#256025=CARTESIAN_POINT ( 'NONE',  ( 21.14999999999999503, 76.00000000001169553, -76.06376443622556849 ) ) ;
#256050=VECTOR ( 'NONE', #86304, 1000.000000000000000 ) ;
#256062=DIRECTION ( 'NONE',  ( 0.000000000000000000, 0.000000000000000000, 1.000000000000000000 ) ) ;
#256089=DIRECTION ( 'NONE',  ( -1.000000000000000000, -0.000000000000000000, -0.000000000000000000 ) ) ;
#256150=DIRECTION ( 'NONE',  ( 0.000000000000000000, 0.000000000000000000, 1.000000000000000000 ) ) ;
#256181=CARTESIAN_POINT ( 'NONE',  ( 21.05000000000000071, 88.41227409416113403, -39.02310748452423894 ) ) ;
#256221=FACE_OUTER_BOUND ( 'NONE', #161421, .T. ) ;
#256276=CARTESIAN_POINT ( 'NONE',  ( 20.94999999999999574, 77.85102823015243700, -57.86919421510181394 ) ) ;
#256288=EDGE_CURVE ( 'NONE', #67154, #58501, #115890, .T. ) ;
#256290=DIRECTION ( 'NONE',  ( -0.000000000000000000, -1.000000000000000000, -6.982962677686266711E-15 ) ) ;
#256296=VERTEX_POINT ( 'NONE', #71640 ) ;
#256314=CARTESIAN_POINT ( 'NONE',  ( -20.54999999999999716, 73.50000000001151079, -49.24772940728643533 ) ) ;
#256323=EDGE_CURVE ( 'NONE', #147150, #111234, #76748, .T. ) ;
#256327=ORIENTED_EDGE ( 'NONE', *, *, #190658, .T. ) ;
#256340=LINE ( 'NONE', #157344, #128150 ) ;
#256359=DIRECTION ( 'NONE',  ( 1.000000000000000000, 0.000000000000000000, 0.000000000000000000 ) ) ;
#256360=CYLINDRICAL_SURFACE ( 'NONE', #247716, 0.09999999999999939493 ) ;
#256361=EDGE_LOOP ( 'NONE', ( #243820, #88958, #104021, #13760 ) ) ;
#256368=CARTESIAN_POINT ( 'NONE',  ( 18.49999999999999645, 76.00000000001165290, -69.52310748452431710 ) ) ;
#256389=CIRCLE ( 'NONE', #60619, 7.800000000000001599 ) ;
#256400=DIRECTION ( 'NONE',  ( 0.000000000000000000, 0.000000000000000000, -1.000000000000000000 ) ) ;
#256438=DIRECTION ( 'NONE',  ( 0.000000000000000000, -1.000000000000000000, -6.982962677686265922E-15 ) ) ;
#256451=CARTESIAN_POINT ( 'NONE',  ( 20.96937028524355284, 65.37553062838493645, -62.03168138335477977 ) ) ;
#256485=LINE ( 'NONE', #34980, #182248 ) ;
#256528=DIRECTION ( 'NONE',  ( -1.000000000000000000, 0.000000000000000000, 0.000000000000000000 ) ) ;
#256540=CARTESIAN_POINT ( 'NONE',  ( -21.14999999999999858, 64.25000000001161027, -62.73924182154625129 ) ) ;
#256544=ORIENTED_EDGE ( 'NONE', *, *, #190468, .F. ) ;
#256570=EDGE_CURVE ( 'NONE', #150942, #68194, #184865, .T. ) ;
#256587=CARTESIAN_POINT ( 'NONE',  ( -18.31331870001086060, 85.53629471919219895, -29.15452879353895099 ) ) ;
#256601=ORIENTED_EDGE ( 'NONE', *, *, #165020, .T. ) ;
#256620=DIRECTION ( 'NONE',  ( 0.000000000000000000, 0.000000000000000000, 1.000000000000000000 ) ) ;
#256654=TOROIDAL_SURFACE ( 'NONE', #144258, 0.2000000000000000111, 0.1000000000000000056 ) ;
#256660=CIRCLE ( 'NONE', #161046, 0.1000000000000009492 ) ;
#256679=AXIS2_PLACEMENT_3D ( 'NONE', #78690, #120445, #119130 ) ;
#256715=CIRCLE ( 'NONE', #181751, 0.09999999999999971412 ) ;
#256724=DIRECTION ( 'NONE',  ( -1.000000000000000000, 0.000000000000000000, -0.000000000000000000 ) ) ;
#256730=CARTESIAN_POINT ( 'NONE',  ( 21.00023020733438273, 69.60913075474394418, -69.52310748452435973 ) ) ;
#256792=CARTESIAN_POINT ( 'NONE',  ( 20.85000000000000142, 77.14957036958705316, -28.20719500002235236 ) ) ;
#256806=CARTESIAN_POINT ( 'NONE',  ( 20.86777300164945004, 65.66799936921481162, -30.42993998886010587 ) ) ;
#256808=CARTESIAN_POINT ( 'NONE',  ( 18.59117750673696179, 65.66751761918619934, -30.42826094061123854 ) ) ;
#256816=DIRECTION ( 'NONE',  ( 0.000000000000000000, 0.000000000000000000, -1.000000000000000000 ) ) ;
#256834=TOROIDAL_SURFACE ( 'NONE', #186166, 11.70000000000000462, 0.1000000000000000056 ) ;
#256845=CARTESIAN_POINT ( 'NONE',  ( -23.15000000000000213, 64.35000000001146248, -43.03791325517834565 ) ) ;
#256858=VERTEX_POINT ( 'NONE', #24508 ) ;
#256864=AXIS2_PLACEMENT_3D ( 'NONE', #226372, #28236, #228978 ) ;
#256880=EDGE_CURVE ( 'NONE', #7765, #144828, #14016, .T. ) ;
#256886=CARTESIAN_POINT ( 'NONE',  ( -18.39999999999999858, 85.50000000001161027, -62.52382180668540457 ) ) ;
#256932=LINE ( 'NONE', #78335, #237551 ) ;
#256989=CYLINDRICAL_SURFACE ( 'NONE', #190024, 7.900000000000000355 ) ;
#257003=CIRCLE ( 'NONE', #32221, 3.900000000000000799 ) ;
#257013=EDGE_CURVE ( 'NONE', #39027, #206635, #218353, .T. ) ;
#257035=AXIS2_PLACEMENT_3D ( 'NONE', #172029, #196667, #97545 ) ;
#257066=ADVANCED_FACE ( 'NONE', ( #70058 ), #149594, .F. ) ;
#257081=ORIENTED_EDGE ( 'NONE', *, *, #21133, .T. ) ;
#257110=EDGE_LOOP ( 'NONE', ( #34067, #145070, #132160, #226067, #107600 ) ) ;
#257154=CARTESIAN_POINT ( 'NONE',  ( -20.64999999999999858, 85.50000000001159606, -59.62913836187181005 ) ) ;
#257177=DIRECTION ( 'NONE',  ( 0.000000000000000000, -1.000000000000000000, -7.272083257015735086E-15 ) ) ;
#257202=CARTESIAN_POINT ( 'NONE',  ( 21.05000000000000071, 67.12872031401595052, -60.96447848938343128 ) ) ;
#257203=CIRCLE ( 'NONE', #119927, 0.5000000000000004441 ) ;
#257211=ORIENTED_EDGE ( 'NONE', *, *, #73878, .F. ) ;
#257216=CARTESIAN_POINT ( 'NONE',  ( -20.85000000000000142, 64.25000000001148237, -42.80697314750250371 ) ) ;
#257311=CARTESIAN_POINT ( 'NONE',  ( -20.85000000000000142, 65.66751761918618513, -30.42826094061123499 ) ) ;
#257320=EDGE_LOOP ( 'NONE', ( #156109, #176423, #172613, #185829 ) ) ;
#257381=LINE ( 'NONE', #35852, #237833 ) ;
#257389=ADVANCED_FACE ( 'NONE', ( #209232 ), #163702, .T. ) ;
#257395=AXIS2_PLACEMENT_3D ( 'NONE', #12948, #173332, #237104 ) ;
#257397=ORIENTED_EDGE ( 'NONE', *, *, #1373, .T. ) ;
#257400=EDGE_CURVE ( 'NONE', #95061, #212130, #168541, .T. ) ;
#257404=EDGE_CURVE ( 'NONE', #181531, #182718, #193451, .T. ) ;
#257436=EDGE_CURVE ( 'NONE', #127785, #187652, #56035, .T. ) ;
#257452=CARTESIAN_POINT ( 'NONE',  ( 21.05000000000000071, 85.00000000001149658, -45.91707660717670336 ) ) ;
#257456=LINE ( 'NONE', #118005, #15333 ) ;
#257509=ORIENTED_EDGE ( 'NONE', *, *, #238385, .T. ) ;
#257510=DIRECTION ( 'NONE',  ( 0.000000000000000000, -7.272083257015735086E-15, 1.000000000000000000 ) ) ;
#257539=EDGE_CURVE ( 'NONE', #150112, #37076, #114319, .T. ) ;
#257606=DIRECTION ( 'NONE',  ( -1.000000000000000000, -0.000000000000000000, -0.000000000000000000 ) ) ;
#257612=EDGE_CURVE ( 'NONE', #214318, #93424, #76902, .T. ) ;
#257623=CIRCLE ( 'NONE', #149395, 11.74999999999999645 ) ;
#257630=ORIENTED_EDGE ( 'NONE', *, *, #231597, .F. ) ;
#257685=DIRECTION ( 'NONE',  ( 1.000000000000000000, 0.000000000000000000, 0.000000000000000000 ) ) ;
#257701=EDGE_CURVE ( 'NONE', #189246, #25147, #13003, .T. ) ;
#257747=CARTESIAN_POINT ( 'NONE',  ( 20.97107704358301916, 67.12452184799030874, -60.96413425513512863 ) ) ;
#257781=DIRECTION ( 'NONE',  ( 0.000000000000000000, -0.9887567792719351711, 0.1495327102803594987 ) ) ;
#257796=DIRECTION ( 'NONE',  ( 0.000000000000000000, 0.000000000000000000, 1.000000000000000000 ) ) ;
#257859=EDGE_CURVE ( 'NONE', #156337, #253401, #177216, .T. ) ;
#257870=CARTESIAN_POINT ( 'NONE',  ( -18.59999999999999787, 74.83729825007360148, -61.42310748452432989 ) ) ;
#257872=CARTESIAN_POINT ( 'NONE',  ( -18.46919391072065153, 85.67072438828911629, -29.34930395272471415 ) ) ;
#257879=CARTESIAN_POINT ( 'NONE',  ( -22.50000000000000000, 64.35012909624745703, -69.60562737539738976 ) ) ;
#257901=CARTESIAN_POINT ( 'NONE',  ( -21.05000000000000071, 87.29603075034673054, -39.07100664418810965 ) ) ;
#257953=CARTESIAN_POINT ( 'NONE',  ( 21.05000000000000071, 76.00000000001145395, -40.02310748452431710 ) ) ;
#257957=VERTEX_POINT ( 'NONE', #143175 ) ;
#257962=CARTESIAN_POINT ( 'NONE',  ( 18.59999999999999076, 69.45000000001149942, -48.37310748452436826 ) ) ;
#258023=CIRCLE ( 'NONE', #70845, 0.1000000000000028644 ) ;
#258074=CARTESIAN_POINT ( 'NONE',  ( -20.85000000000000142, 77.16412189325258453, -28.10825939895270764 ) ) ;
#258079=SHAPE_DEFINITION_REPRESENTATION ( #191023, #135069 ) ;
#258090=AXIS2_PLACEMENT_3D ( 'NONE', #62262, #141786, #162657 ) ;
#258098=CYLINDRICAL_SURFACE ( 'NONE', #199583, 0.09999999999999939493 ) ;
#258100=EDGE_CURVE ( 'NONE', #134468, #178236, #64789, .T. ) ;
#258102=CARTESIAN_POINT ( 'NONE',  ( 18.49999999999998934, 65.70711192142313450, -30.56510546851223609 ) ) ;
#258103=FACE_OUTER_BOUND ( 'NONE', #121688, .T. ) ;
#258104=AXIS2_PLACEMENT_3D ( 'NONE', #205885, #42978, #83344 ) ;
#258106=DIRECTION ( 'NONE',  ( 0.000000000000000000, -0.1350103645451974088, 0.9908441862701587999 ) ) ;
ENDSEC;
END-ISO-10303-21;
